ISO-10303-21;
HEADER;
FILE_DESCRIPTION (('STEP AP214'),
    '1' );
FILE_NAME ('Top Pivot Bracket.step',
    '2026-10-12T23:53:07',
    ( '' ),
    ( '' ),
    'SwSTEP 2.0',
    'SolidWorks 2024',
    '' );
FILE_SCHEMA (( 'AUTOMOTIVE_DESIGN' ));
ENDSEC;

DATA;
#1=CARTESIAN_POINT ( 'NONE',  ( 0.4999436808859595294, -1.292550018364103881, 0.6106580130240608639 ) ) ;
#2=CARTESIAN_POINT ( 'NONE',  ( 0.6766858697071348461, -1.447219178500369852, 0.5182417262812423209 ) ) ;
#3=EDGE_LOOP ( 'NONE', ( #27545, #19145, #8078, #4181 ) ) ;
#4=CARTESIAN_POINT ( 'NONE',  ( 0.4897881687547872565, -1.080982661159355818, 0.5914788577480112330 ) ) ;
#10=CARTESIAN_POINT ( 'NONE',  ( 0.3847673884423530866, -1.587979917868051594, 0.7195363636215315051 ) ) ;
#11=CARTESIAN_POINT ( 'NONE',  ( 0.06449619071327084008, -0.8352737646558907603, 0.1359541117914142838 ) ) ;
#12=CARTESIAN_POINT ( 'NONE',  ( 0.1868532161955482884, -0.6181774020623623800, -0.006882278619014759076 ) ) ;
#13=CARTESIAN_POINT ( 'NONE',  ( 0.06860968454252140691, -0.5593946951873564055, 0.07183308462254860138 ) ) ;
#14=VERTEX_POINT ( 'NONE', #12483 ) ;
#16=CARTESIAN_POINT ( 'NONE',  ( 0.4409725506264777772, -1.045015864252073712, 0.6370139139982947674 ) ) ;
#17=CARTESIAN_POINT ( 'NONE',  ( 0.1277648457822606887, -0.6229659815690001823, 0.3707106540332985034 ) ) ;
#25=CARTESIAN_POINT ( 'NONE',  ( 0.3439459955960700865, -1.757593179262507466, 0.4441638180110000222 ) ) ;
#27=CARTESIAN_POINT ( 'NONE',  ( 0.1178002186443738025, -1.269485432265525793, 0.6202127893679206805 ) ) ;
#31=CARTESIAN_POINT ( 'NONE',  ( 0.1947294528115406376, -0.9190940877486376559, 0.2754987677893815934 ) ) ;
#33=CARTESIAN_POINT ( 'NONE',  ( 0.4569214742076340707, -1.218928684383336236, 0.5856983068965044836 ) ) ;
#34=CARTESIAN_POINT ( 'NONE',  ( 0.3193861777821562220, -1.171684894966655399, 0.5563056129421823925 ) ) ;
#35=CARTESIAN_POINT ( 'NONE',  ( 0.1851448419613674068, -1.516587896426844662, 0.7176110508928341680 ) ) ;
#38=CARTESIAN_POINT ( 'NONE',  ( 0.5966652623928320187, -1.460067201996130271, 0.6057417262805135927 ) ) ;
#44=CARTESIAN_POINT ( 'NONE',  ( 0.2625221014770238726, -1.677489247281143347, 0.5299707248247536029 ) ) ;
#46=CARTESIAN_POINT ( 'NONE',  ( 0.5765142360455419723, -1.424711725393718265, 0.6097170742772620722 ) ) ;
#47=CARTESIAN_POINT ( 'NONE',  ( 0.001926542279114920901, -0.5275834520082917090, 0.09413269016402606160 ) ) ;
#52=CARTESIAN_POINT ( 'NONE',  ( 0.2972168835034767476, -1.656689438746897558, 0.5739732049407664238 ) ) ;
#54=CARTESIAN_POINT ( 'NONE',  ( 0.08190433410803919789, -1.308169647316527184, 0.5665045013630258808 ) ) ;
#63=CARTESIAN_POINT ( 'NONE',  ( 0.2884976522880303706, -0.9761975876302364519, 0.7460397395601686688 ) ) ;
#64=CARTESIAN_POINT ( 'NONE',  ( 0.1828007326059407633, -0.8784064217732538982, 0.5457344770029756154 ) ) ;
#65=CARTESIAN_POINT ( 'NONE',  ( 0.2745644270868899950, -1.657411742223986018, 0.7254928767627549790 ) ) ;
#67=CARTESIAN_POINT ( 'NONE',  ( 0.3207235327959215287, -1.760688231293898953, 0.5959548780354907427 ) ) ;
#75=CARTESIAN_POINT ( 'NONE',  ( 0.07120675875603865723, -0.8149881486554784171, 0.8228864848196146831 ) ) ;
#76=CARTESIAN_POINT ( 'NONE',  ( 0.09717445250287677638, -1.337075187059802994, 0.7110840001749388906 ) ) ;
#78=CARTESIAN_POINT ( 'NONE',  ( 0.3560095073596968307, -0.8726986411092064744, 0.7484988241699506162 ) ) ;
#81=CARTESIAN_POINT ( 'NONE',  ( 0.6872956252228072938, -1.545186843986040115, 0.5945327379366810439 ) ) ;
#84=ORIENTED_EDGE ( 'NONE', *, *, #28072, .F. ) ;
#86=CARTESIAN_POINT ( 'NONE',  ( 0.1825910822803085698, -1.345967781949698239, 0.9412546887375772275 ) ) ;
#87=CARTESIAN_POINT ( 'NONE',  ( 0.5953442517954894431, -1.487188481951640773, 0.5814371352277787341 ) ) ;
#90=CARTESIAN_POINT ( 'NONE',  ( 0.1967848402874973202, -0.7048484731626001309, 0.3032743993732655574 ) ) ;
#91=ORIENTED_EDGE ( 'NONE', *, *, #5942, .F. ) ;
#99=CARTESIAN_POINT ( 'NONE',  ( 0.09103128088014370012, -0.7737444593052549280, 0.2676987870228014210 ) ) ;
#100=CARTESIAN_POINT ( 'NONE',  ( 0.3114310930860528792, -1.743835956959021161, 0.7216218591552465700 ) ) ;
#102=CARTESIAN_POINT ( 'NONE',  ( 0.5255678041659990196, -1.526919996939806623, 0.5791403307438186543 ) ) ;
#107=CARTESIAN_POINT ( 'NONE',  ( -0.01736481776669303659, -0.6872203660140440151, -0.01676916986599873496 ) ) ;
#108=CARTESIAN_POINT ( 'NONE',  ( 0.6985683150901143001, -1.438855895731389056, 0.5688516854839209547 ) ) ;
#109=CARTESIAN_POINT ( 'NONE',  ( 0.5745725605903601041, -1.619018034204693146, 0.5636810530413540743 ) ) ;
#110=CARTESIAN_POINT ( 'NONE',  ( -0.002236529766539807878, -0.8463514994925549484, 0.1275420592413386567 ) ) ;
#113=CARTESIAN_POINT ( 'NONE',  ( 0.01632176102313256591, -1.052923364454138255, 0.5995154855756178458 ) ) ;
#114=CARTESIAN_POINT ( 'NONE',  ( 0.5138184642618360831, -1.118801421376873551, 0.5693865086028936373 ) ) ;
#118=CARTESIAN_POINT ( 'NONE',  ( 0.6078054091579164764, -1.478899637288701996, 0.5472081702953829341 ) ) ;
#126=CARTESIAN_POINT ( 'NONE',  ( 0.08704502409080258629, -0.7188400997375623547, 0.02651060292151286024 ) ) ;
#130=CARTESIAN_POINT ( 'NONE',  ( -0.004104496411111036719, -0.9055868175180781243, 0.5348166647311645150 ) ) ;
#132=ORIENTED_EDGE ( 'NONE', *, *, #28235, .F. ) ;
#133=ADVANCED_FACE ( 'NONE', ( #4027 ), #10817, .T. ) ;
#134=DIRECTION ( 'NONE',  ( -1.000000000000000000, 0.000000000000000000, 0.000000000000000000 ) ) ;
#138=EDGE_CURVE ( 'NONE', #15118, #39770, #26750, .T. ) ;
#142=ORIENTED_EDGE ( 'NONE', *, *, #5731, .F. ) ;
#144=CARTESIAN_POINT ( 'NONE',  ( 0.1448932857592245271, -0.7256843399750660950, 0.5340175887863652937 ) ) ;
#147=CARTESIAN_POINT ( 'NONE',  ( 0.4408799025385287673, -1.573480893639235711, 0.5609592079540931531 ) ) ;
#149=CARTESIAN_POINT ( 'NONE',  ( 0.5621007238609228018, -1.618750287028627222, 0.5241914645917098436 ) ) ;
#151=CARTESIAN_POINT ( 'NONE',  ( 0.1406250000000003053, -0.9233928627580062498, 0.1457185332388702126 ) ) ;
#153=CARTESIAN_POINT ( 'NONE',  ( 0.2614565024141663474, -0.7584087153545726601, 0.1023043458361302949 ) ) ;
#155=CARTESIAN_POINT ( 'NONE',  ( 0.5811800998074035940, -1.495285155999573012, 0.5781461679035739820 ) ) ;
#158=( BOUNDED_SURFACE ( )  B_SPLINE_SURFACE ( 3, 2, ( 
 ( #37955, #25824, #4400 ),
 ( #1341, #3597, #16958 ),
 ( #29091, #25426, #31783 ),
 ( #29309, #38557, #10179 ),
 ( #16166, #7070, #22943 ),
 ( #35460, #3797, #13468 ),
 ( #22335, #22748, #16353 ),
 ( #28703, #19641, #16549 ),
 ( #567, #9766, #13063 ),
 ( #749, #35275, #26035 ),
 ( #23144, #13657, #1157 ),
 ( #25614, #32175, #3986 ),
 ( #9969, #38145, #28888 ),
 ( #35066, #26222, #4194 ),
 ( #6872, #19447, #10570 ),
 ( #35672, #7261, #19835 ),
 ( #31985, #32369, #7475 ),
 ( #16761, #20052, #32585 ),
 ( #8302, #7875, #1760 ),
 ( #23745, #5201, #39365 ),
 ( #10788, #32982, #35881 ),
 ( #33586, #30307, #14068 ),
 ( #30113, #14672, #23360 ),
 ( #7693, #30518, #11184 ),
 ( #21059, #4581, #20448 ),
 ( #39175, #20873, #26422 ),
 ( #5396, #17958, #13849 ),
 ( #38958, #20258, #17571 ),
 ( #32780, #14272, #17754 ),
 ( #36267, #17153, #29702 ),
 ( #27027, #1547, #39554 ),
 ( #4788, #26644, #2134 ),
 ( #33394, #17363, #11000 ),
 ( #23558, #23959, #20665 ),
 ( #36076, #26836, #29918 ),
 ( #8088, #33199, #27242 ),
 ( #11387, #5004, #1944 ),
 ( #39773, #14459, #36488 ),
 ( #11603, #24165, #36689 ),
 ( #8495, #40164, #36882 ),
 ( #5611, #8690, #39969 ),
 ( #18367, #37696, #18167 ),
 ( #12206, #18792, #21268 ),
 ( #33805, #40579, #11994 ),
 ( #100, #31343, #6225 ),
 ( #27841, #30721, #24953 ),
 ( #37289, #15080, #31131 ),
 ( #9103, #30913, #3148 ) ),
 .UNSPECIFIED., .F., .F., .T. ) 
 B_SPLINE_SURFACE_WITH_KNOTS ( ( 4, 2, 2, 2, 2, 2, 2, 2, 2, 2, 2, 2, 2, 2, 2, 2, 2, 2, 2, 2, 2, 2, 2, 4 ),
 ( 3, 3 ),
 ( 0.009784760482578789414, 0.01303178080197338849, 0.01465529096167068890, 0.01627880112136798757, 0.01952582144076258491, 0.02114933160045988358, 0.02277284176015718226, 0.02926688239894638041, 0.03251390271834098122, 0.03576092303773557857, 0.03900794335713017591, 0.04225496367652477325, 0.04387847383622207192, 0.04550198399591937060, 0.04712549415561667621, 0.04874900431531397488, 0.05037251447501127355, 0.05199602463470857916, 0.05361953479440587783, 0.05443128987425452370, 0.05524304495410317650, 0.05686655511380047517, 0.05849006527349777385, 0.06173708559289237119 ),
 ( 0.000000000000000000, 1.000000000000000000 ),
 .UNSPECIFIED. ) 
 GEOMETRIC_REPRESENTATION_ITEM ( )  RATIONAL_B_SPLINE_SURFACE ( (
 ( 1.000000000000000000, 0.6287678658096880202, 1.000000000000000000),
 ( 1.000000000000000000, 0.6288662671286704420, 1.000000000000000000),
 ( 1.000000000000000000, 0.6274741409696639183, 1.000000000000000000),
 ( 1.000000000000000000, 0.6287776757897947100, 1.000000000000000000),
 ( 1.000000000000000000, 0.6296837007773170569, 1.000000000000000000),
 ( 1.000000000000000000, 0.6313229865883394076, 1.000000000000000000),
 ( 1.000000000000000000, 0.6321460476172471310, 1.000000000000000000),
 ( 1.000000000000000000, 0.6347778756843863723, 1.000000000000000000),
 ( 1.000000000000000000, 0.6367158758108866223, 1.000000000000000000),
 ( 1.000000000000000000, 0.6398588341727308171, 1.000000000000000000),
 ( 1.000000000000000000, 0.6409477486316274009, 1.000000000000000000),
 ( 1.000000000000000000, 0.6432257032707729971, 1.000000000000000000),
 ( 1.000000000000000000, 0.6444106978184096501, 1.000000000000000000),
 ( 1.000000000000000000, 0.6505171573845394128, 1.000000000000000000),
 ( 1.000000000000000000, 0.6559831852215063375, 1.000000000000000000),
 ( 1.000000000000000000, 0.6631771220578878134, 1.000000000000000000),
 ( 1.000000000000000000, 0.6653492434363603714, 1.000000000000000000),
 ( 1.000000000000000000, 0.6687561138349609191, 1.000000000000000000),
 ( 1.000000000000000000, 0.6700066037122677232, 1.000000000000000000),
 ( 1.000000000000000000, 0.6713450054086019803, 1.000000000000000000),
 ( 1.000000000000000000, 0.6714450553368720431, 1.000000000000000000),
 ( 1.000000000000000000, 0.6706951819970428108, 1.000000000000000000),
 ( 1.000000000000000000, 0.6697953818427609951, 1.000000000000000000),
 ( 1.000000000000000000, 0.6680617541732161158, 1.000000000000000000),
 ( 1.000000000000000000, 0.6674309137187000029, 1.000000000000000000),
 ( 1.000000000000000000, 0.6661647704555568872, 1.000000000000000000),
 ( 1.000000000000000000, 0.6655247572274053391, 1.000000000000000000),
 ( 1.000000000000000000, 0.6643577078737322728, 1.000000000000000000),
 ( 1.000000000000000000, 0.6638299590325124067, 1.000000000000000000),
 ( 1.000000000000000000, 0.6631078123530266266, 1.000000000000000000),
 ( 1.000000000000000000, 0.6629281639512619728, 1.000000000000000000),
 ( 1.000000000000000000, 0.6631493259863866507, 1.000000000000000000),
 ( 1.000000000000000000, 0.6635445073558746687, 1.000000000000000000),
 ( 1.000000000000000000, 0.6652273697468563673, 1.000000000000000000),
 ( 1.000000000000000000, 0.6664745574001266215, 1.000000000000000000),
 ( 1.000000000000000000, 0.6697857743441212319, 1.000000000000000000),
 ( 1.000000000000000000, 0.6718404721287462023, 1.000000000000000000),
 ( 1.000000000000000000, 0.6753207313297656667, 1.000000000000000000),
 ( 1.000000000000000000, 0.6765490974884642572, 1.000000000000000000),
 ( 1.000000000000000000, 0.6790248312221631721, 1.000000000000000000),
 ( 1.000000000000000000, 0.6802787004308656904, 1.000000000000000000),
 ( 1.000000000000000000, 0.6840080678706492723, 1.000000000000000000),
 ( 1.000000000000000000, 0.6864616782751722379, 1.000000000000000000),
 ( 1.000000000000000000, 0.6908458362598728364, 1.000000000000000000),
 ( 1.000000000000000000, 0.6927390833103468371, 1.000000000000000000),
 ( 1.000000000000000000, 0.6973153832233414118, 1.000000000000000000),
 ( 1.000000000000000000, 0.6988858220003437705, 1.000000000000000000),
 ( 1.000000000000000000, 0.6986036234954329238, 1.000000000000000000) ) ) 
 REPRESENTATION_ITEM ( '' )  SURFACE ( )  );
#165=CARTESIAN_POINT ( 'NONE',  ( 0.3175065632424611817, -1.048436534473135895, 0.7840659024250604681 ) ) ;
#167=CARTESIAN_POINT ( 'NONE',  ( 0.5193158764790237747, -1.143105642405225053, 0.8514134314631569556 ) ) ;
#169=CARTESIAN_POINT ( 'NONE',  ( 0.04665094350991502714, -1.166787722506144265, 0.6642627002602656816 ) ) ;
#174=CARTESIAN_POINT ( 'NONE',  ( 0.1876874445810236824, -0.7927434498347614156, 0.2846742484563515863 ) ) ;
#182=CARTESIAN_POINT ( 'NONE',  ( 0.6604279980842809872, -1.474831068641988763, 0.4182417262808776348 ) ) ;
#185=CARTESIAN_POINT ( 'NONE',  ( 0.3311937503011831985, -1.162386653964609939, 0.5777461324143994270 ) ) ;
#191=CARTESIAN_POINT ( 'NONE',  ( 0.2591027371085388720, -1.332731507978919705, 0.5181001316254452149 ) ) ;
#195=CARTESIAN_POINT ( 'NONE',  ( 0.5122077321654537885, -1.314614967837785198, 0.5911197364003766275 ) ) ;
#198=CARTESIAN_POINT ( 'NONE',  ( 0.1892170003689550017, -0.8723299121346327345, 0.2416867767302488257 ) ) ;
#201=EDGE_CURVE ( 'NONE', #33071, #36154, #13038, .T. ) ;
#202=CARTESIAN_POINT ( 'NONE',  ( 0.04650976029988308780, -1.055486831112860902, 0.7228979986002838087 ) ) ;
#204=CARTESIAN_POINT ( 'NONE',  ( 0.04803016009707758438, -0.5362635619093905071, 0.1457185332388692967 ) ) ;
#206=CARTESIAN_POINT ( 'NONE',  ( 0.1846550159866843510, -0.8403219816448772583, 0.07989493322373726614 ) ) ;
#207=CARTESIAN_POINT ( 'NONE',  ( 0.06829125384024312129, -0.5762991475062954061, 0.04819365463926665594 ) ) ;
#210=CARTESIAN_POINT ( 'NONE',  ( 0.5379134690603978308, -1.159344755639895030, 0.5916774385555967353 ) ) ;
#211=CARTESIAN_POINT ( 'NONE',  ( 0.2895267596155666756, -1.012179684896779674, 0.7737674755748008559 ) ) ;
#213=CARTESIAN_POINT ( 'NONE',  ( 0.1867098991225878413, -0.7409322124881813076, 0.03654140106717494729 ) ) ;
#222=DIRECTION ( 'NONE',  ( 0.01455087615875037474, 0.9998941303973200023, 4.192763588336697022E-17 ) ) ;
#223=CIRCLE ( 'NONE', #16616, 0.009999999999999996739 ) ;
#230=LINE ( 'NONE', #12724, #21231 ) ;
#231=CARTESIAN_POINT ( 'NONE',  ( 0.1959177972118346378, -1.369282659305815386, 0.4807434598345527443 ) ) ;
#232=PLANE ( 'NONE',  #32346 ) ;
#235=CARTESIAN_POINT ( 'NONE',  ( 0.1623712441042921006, -1.412506991498796660, 0.8192480828659791658 ) ) ;
#236=CARTESIAN_POINT ( 'NONE',  ( 6.601686217279748340E-05, -0.6230491400307559546, -0.09540615510927821785 ) ) ;
#241=EDGE_CURVE ( 'NONE', #4902, #25362, #16461, .T. ) ;
#243=VERTEX_POINT ( 'NONE', #32631 ) ;
#246=VECTOR ( 'NONE', #25682, 39.37007874015748143 ) ;
#248=CARTESIAN_POINT ( 'NONE',  ( 0.5830587952300703147, -1.433043469348942667, 0.7044988243964402930 ) ) ;
#254=ORIENTED_EDGE ( 'NONE', *, *, #22555, .F. ) ;
#256=CARTESIAN_POINT ( 'NONE',  ( 0.01082074132985459333, -0.5320958912064523982, 0.1749010329950502485 ) ) ;
#260=EDGE_CURVE ( 'NONE', #19095, #7024, #37850, .T. ) ;
#261=CARTESIAN_POINT ( 'NONE',  ( 0.1896903302788489343, -0.9196856789278203825, -0.03797464539687132185 ) ) ;
#270=DIRECTION ( 'NONE',  ( 0.8660512985181133550, 0.4999551463232373982, 0.000000000000000000 ) ) ;
#272=CARTESIAN_POINT ( 'NONE',  ( 0.2940074227696489184, -1.028172634779288996, 0.7298538202148366905 ) ) ;
#273=CARTESIAN_POINT ( 'NONE',  ( 0.2184614013223490359, -1.436573476884752676, 0.9287958070571558089 ) ) ;
#275=B_SPLINE_CURVE_WITH_KNOTS ( 'NONE', 3,
 ( #22885, #22270, #22466, #4121, #25752, #3529, #19580, #35404, #26164, #7198, #13001, #13395, #38277, #34994, #25549, #32115, #16292, #38493 ),
 .UNSPECIFIED., .F., .F.,
 ( 4, 2, 2, 2, 2, 2, 2, 2, 4 ),
 ( 0.001290851923713245844, 0.001894763156073155964, 0.002498674388433065868, 0.003102585620792975771, 0.003706496853152886108, 0.004310408085512795577, 0.004914319317872705914, 0.005518230550232615383, 0.006122141782592525720 ),
 .UNSPECIFIED. ) ;
#276=CARTESIAN_POINT ( 'NONE',  ( 0.2650312354662574532, -1.481736570352484073, 1.013012391360898823 ) ) ;
#286=CARTESIAN_POINT ( 'NONE',  ( 0.05954370505521044965, -1.068900277825352907, 0.7381710695662248023 ) ) ;
#290=VECTOR ( 'NONE', #11669, 39.37007874015748143 ) ;
#295=CARTESIAN_POINT ( 'NONE',  ( 0.1145935282722230358, -1.416615153024734397, 0.5154658030382857081 ) ) ;
#296=CARTESIAN_POINT ( 'NONE',  ( 0.2587121583883757459, -1.613885124491862610, 0.8258352243388695779 ) ) ;
#298=CARTESIAN_POINT ( 'NONE',  ( 0.1324595997283633808, -0.5754775961032010390, 0.2510594539120258872 ) ) ;
#299=CARTESIAN_POINT ( 'NONE',  ( 0.3434800707737146741, -1.169184835483404905, 0.4282596159937968605 ) ) ;
#303=CARTESIAN_POINT ( 'NONE',  ( 0.6611732595943385915, -1.536511864384403125, 0.7149362408420358861 ) ) ;
#308=CARTESIAN_POINT ( 'NONE',  ( 0.3098923999789689465, -1.765709567672198554, 0.5653262919047477020 ) ) ;
#310=CARTESIAN_POINT ( 'NONE',  ( 0.08557407651291307205, -0.7673689209508794962, 0.1706946678738483492 ) ) ;
#313=CARTESIAN_POINT ( 'NONE',  ( 0.4632380810071169974, -1.418384998081447357, 0.8128757890859310553 ) ) ;
#316=ORIENTED_EDGE ( 'NONE', *, *, #23007, .T. ) ;
#317=CARTESIAN_POINT ( 'NONE',  ( 0.4382936615902019439, -1.691409853567093613, 0.6111383081645538340 ) ) ;
#318=CARTESIAN_POINT ( 'NONE',  ( 0.6861498661271836497, -1.412370093654202963, 0.8150029156550121501 ) ) ;
#321=CARTESIAN_POINT ( 'NONE',  ( 0.6089727181761853680, -1.479025121845506385, 0.5718834518386042287 ) ) ;
#325=EDGE_CURVE ( 'NONE', #12308, #507, #36520, .T. ) ;
#326=CARTESIAN_POINT ( 'NONE',  ( 0.05583995664670776682, -1.335624775257321817, 0.3157417262808777658 ) ) ;
#328=DIRECTION ( 'NONE',  ( 0.000000000000000000, 0.8660477418057301868, -0.4999613074160793036 ) ) ;
#329=CARTESIAN_POINT ( 'NONE',  ( 0.1932042024315755446, -0.7994606748157702114, 0.2910003379690608294 ) ) ;
#334=CARTESIAN_POINT ( 'NONE',  ( 0.5142508901037518010, -1.533077155716542572, 0.5735235060962670106 ) ) ;
#337=ORIENTED_EDGE ( 'NONE', *, *, #31529, .T. ) ;
#340=CARTESIAN_POINT ( 'NONE',  ( 0.1860255769997808117, -0.8548752387040396972, 0.1809200802102173822 ) ) ;
#342=CARTESIAN_POINT ( 'NONE',  ( 0.4091335057472371695, -1.131547141905885789, 0.4177417262808780229 ) ) ;
#344=CARTESIAN_POINT ( 'NONE',  ( -0.009649777317831131213, -0.8763596202099832588, 0.4395725020134745309 ) ) ;
#346=ORIENTED_EDGE ( 'NONE', *, *, #34113, .T. ) ;
#348=AXIS2_PLACEMENT_3D ( 'NONE', #34589, #18959, #3519 ) ;
#356=VERTEX_POINT ( 'NONE', #17196 ) ;
#358=CARTESIAN_POINT ( 'NONE',  ( 0.1233651857933633078, -0.6859638927695101973, 0.4603130361914588020 ) ) ;
#360=ORIENTED_EDGE ( 'NONE', *, *, #18286, .F. ) ;
#362=CARTESIAN_POINT ( 'NONE',  ( 0.1767352294523506506, -0.9049482756361506564, 0.7300595450672812126 ) ) ;
#363=CARTESIAN_POINT ( 'NONE',  ( 0.002296835029420831766, -0.5198933010532058585, 0.1654604498185965056 ) ) ;
#366=CARTESIAN_POINT ( 'NONE',  ( 0.4548150350199453018, -1.105354657904178861, 0.5682417262808776570 ) ) ;
#368=AXIS2_PLACEMENT_3D ( 'NONE', #20608, #11332, #1490 ) ;
#372=CARTESIAN_POINT ( 'NONE',  ( 0.1936977043547155886, -0.7769779101379276076, 0.5892091259747814780 ) ) ;
#377=CYLINDRICAL_SURFACE ( 'NONE', #1513, 0.08749999999977554899 ) ;
#380=CARTESIAN_POINT ( 'NONE',  ( 0.4446247626930326380, -1.240635375613917901, 0.8187945045632878394 ) ) ;
#381=CARTESIAN_POINT ( 'NONE',  ( -0.002282498291095993656, -0.8555267327002353817, 0.1457185332388701293 ) ) ;
#382=EDGE_CURVE ( 'NONE', #8839, #6763, #10547, .T. ) ;
#384=CARTESIAN_POINT ( 'NONE',  ( 0.2254586261693722060, -0.6723955984770768612, 0.4589204916406527945 ) ) ;
#385=CARTESIAN_POINT ( 'NONE',  ( 0.5383058276557359800, -1.161081979360616190, 0.5534299176528929554 ) ) ;
#386=CARTESIAN_POINT ( 'NONE',  ( 0.02977708404944962722, -1.115570236398492066, 0.6630177360434016398 ) ) ;
#390=B_SPLINE_CURVE_WITH_KNOTS ( 'NONE', 3,
 ( #34289, #36761, #25033, #40256, #31227, #40473, #12295, #18058, #9393, #6095 ),
 .UNSPECIFIED., .F., .F.,
 ( 4, 2, 2, 2, 4 ),
 ( 0.0003323657284514935093, 0.0008074047817991935900, 0.001282443835146893779, 0.001757482888494593751, 0.002232521941842293724 ),
 .UNSPECIFIED. ) ;
#393=CARTESIAN_POINT ( 'NONE',  ( 0.6298776228253546439, -1.586001970545553252, 0.4270054416526937735 ) ) ;
#395=DIRECTION ( 'NONE',  ( -0.8660512985181134660, -0.4999551463232372872, 0.000000000000000000 ) ) ;
#396=CARTESIAN_POINT ( 'NONE',  ( 0.2698036132048247104, -0.9625005881386677897, 0.7146062034794288254 ) ) ;
#405=CARTESIAN_POINT ( 'NONE',  ( 0.1873756208929918121, -1.374400995849163198, 0.4173619172664751464 ) ) ;
#410=CARTESIAN_POINT ( 'NONE',  ( 0.5095436923513168015, -1.308647369734698085, 0.6228639752712391564 ) ) ;
#413=CARTESIAN_POINT ( 'NONE',  ( 0.4929465528686915454, -1.082715557938388029, 0.5653634300333020279 ) ) ;
#418=( BOUNDED_SURFACE ( )  B_SPLINE_SURFACE ( 3, 2, ( 
 ( #38846, #4085, #28600 ),
 ( #35565, #1253, #6769 ),
 ( #34961, #10292, #22857 ),
 ( #35775, #4301, #13147 ),
 ( #7364, #19941, #16866 ),
 ( #3495, #19138, #19347 ),
 ( #25936, #31677, #16055 ),
 ( #3704, #25711, #38242 ),
 ( #10073, #19552, #4493 ),
 ( #39066, #10892, #23650 ),
 ( #2246, #24251, #26526 ),
 ( #5099, #33483, #26737 ),
 ( #17055, #20556, #36171 ),
 ( #17464, #39663, #33090 ),
 ( #29601, #39459, #26926 ),
 ( #14785, #11284, #4686 ),
 ( #13956, #29809, #23464 ),
 ( #17256, #32688, #23851 ),
 ( #1443, #35980, #4898 ),
 ( #30203, #7585, #1847 ),
 ( #36376, #11500, #8195 ),
 ( #7786, #27132, #11696 ),
 ( #36590, #17853, #20355 ),
 ( #20767, #32876, #1650 ),
 ( #8392, #7980, #39877 ),
 ( #33290, #30017, #2034 ),
 ( #14362, #14169, #17657 ),
 ( #14565, #39267, #11090 ),
 ( #24064, #20963, #5289 ),
 ( #27346, #30415, #20160 ) ),
 .UNSPECIFIED., .F., .F., .F. ) 
 B_SPLINE_SURFACE_WITH_KNOTS ( ( 4, 2, 2, 2, 2, 2, 2, 2, 2, 2, 2, 2, 2, 2, 4 ),
 ( 3, 3 ),
 ( 1.192622389734054877E-18, 0.0008889885672519496837, 0.001333482850877924092, 0.001777977134503898283, 0.002222471418129872475, 0.002666965701755846883, 0.003111459985381820857, 0.003555954269007795265, 0.004000448552633769674, 0.004444942836259744082, 0.004889437119885718490, 0.005333931403511692898, 0.005778425687137667306, 0.006222919970763641714, 0.007111908538015589663 ),
 ( 0.000000000000000000, 1.000000000000000000 ),
 .UNSPECIFIED. ) 
 GEOMETRIC_REPRESENTATION_ITEM ( )  RATIONAL_B_SPLINE_SURFACE ( (
 ( 1.000000000000000000, 0.7087966873486397645, 1.000000000000000000),
 ( 1.000000000000000000, 0.7254043283289703936, 1.000000000000000000),
 ( 1.000000000000000000, 0.7477302227775445287, 1.000000000000000000),
 ( 1.000000000000000000, 0.7823973320993324876, 1.000000000000000000),
 ( 1.000000000000000000, 0.7940349421475684233, 1.000000000000000000),
 ( 1.000000000000000000, 0.8170648074608825029, 1.000000000000000000),
 ( 1.000000000000000000, 0.8285120912207648569, 1.000000000000000000),
 ( 1.000000000000000000, 0.8502521819941248893, 1.000000000000000000),
 ( 1.000000000000000000, 0.8606365733870987578, 1.000000000000000000),
 ( 1.000000000000000000, 0.8803670527789597688, 1.000000000000000000),
 ( 1.000000000000000000, 0.8897136316908171860, 1.000000000000000000),
 ( 1.000000000000000000, 0.9068004400909128737, 1.000000000000000000),
 ( 1.000000000000000000, 0.9146221070091428151, 1.000000000000000000),
 ( 1.000000000000000000, 0.9288284161271825878, 1.000000000000000000),
 ( 1.000000000000000000, 0.9352460323245295193, 1.000000000000000000),
 ( 1.000000000000000000, 0.9462102292809775328, 1.000000000000000000),
 ( 1.000000000000000000, 0.9508087505105436987, 1.000000000000000000),
 ( 1.000000000000000000, 0.9581430234375604149, 1.000000000000000000),
 ( 1.000000000000000000, 0.9608521639589725494, 1.000000000000000000),
 ( 1.000000000000000000, 0.9639951171735293700, 1.000000000000000000),
 ( 1.000000000000000000, 0.9644675829175349824, 1.000000000000000000),
 ( 1.000000000000000000, 0.9630894221799249921, 1.000000000000000000),
 ( 1.000000000000000000, 0.9612789446135701077, 1.000000000000000000),
 ( 1.000000000000000000, 0.9555297994135374395, 1.000000000000000000),
 ( 1.000000000000000000, 0.9515877792135777336, 1.000000000000000000),
 ( 1.000000000000000000, 0.9419945274880047181, 1.000000000000000000),
 ( 1.000000000000000000, 0.9363124543101019048, 1.000000000000000000),
 ( 1.000000000000000000, 0.9165938519170033771, 1.000000000000000000),
 ( 1.000000000000000000, 0.9002247319857109575, 1.000000000000000000),
 ( 1.000000000000000000, 0.8810606863760693797, 1.000000000000000000) ) ) 
 REPRESENTATION_ITEM ( '' )  SURFACE ( )  );
#419=CARTESIAN_POINT ( 'NONE',  ( 0.04148277367085517059, -0.5962918094959076543, 0.3490695081863538496 ) ) ;
#420=CARTESIAN_POINT ( 'NONE',  ( 0.08668618681611810206, -0.7427351849914437532, 0.03552623599536654242 ) ) ;
#424=ORIENTED_EDGE ( 'NONE', *, *, #40222, .F. ) ;
#426=CARTESIAN_POINT ( 'NONE',  ( 0.5604574556245232042, -1.488111770035372983, 0.6880931705970741996 ) ) ;
#428=CARTESIAN_POINT ( 'NONE',  ( 0.06747690200236802771, -1.330070943150462925, 0.5060650602545776477 ) ) ;
#440=EDGE_CURVE ( 'NONE', #15736, #13839, #35714, .T. ) ;
#446=EDGE_CURVE ( 'NONE', #15271, #15727, #25800, .T. ) ;
#447=EDGE_CURVE ( 'NONE', #8445, #7904, #17904, .T. ) ;
#448=CARTESIAN_POINT ( 'NONE',  ( 0.4885592119991905014, -1.080308374838712782, 0.5952236481819053182 ) ) ;
#449=CARTESIAN_POINT ( 'NONE',  ( 0.1676694287369189240, -1.385544946528693089, 0.5182417262812420988 ) ) ;
#450=EDGE_CURVE ( 'NONE', #9282, #2281, #5151, .T. ) ;
#451=CARTESIAN_POINT ( 'NONE',  ( 0.5494247343383880100, -1.165528289934207429, 0.5856983068965392336 ) ) ;
#452=CARTESIAN_POINT ( 'NONE',  ( 0.2633622372885912610, -1.685028111793015926, 0.5636491875944877883 ) ) ;
#453=CARTESIAN_POINT ( 'NONE',  ( 0.1861033513463754285, -1.549633035783825497, 0.5860151309145639198 ) ) ;
#456=CARTESIAN_POINT ( 'NONE',  ( 0.3377018382744822467, -1.172509963254503518, 0.4282583286688060875 ) ) ;
#461=CARTESIAN_POINT ( 'NONE',  ( 0.7053289366243524761, -1.513890837374202158, 0.5668602961216192559 ) ) ;
#463=CARTESIAN_POINT ( 'NONE',  ( 0.3843292633124594238, -1.119501845244787130, 0.8107229143054137666 ) ) ;
#465=ORIENTED_EDGE ( 'NONE', *, *, #25908, .T. ) ;
#468=CARTESIAN_POINT ( 'NONE',  ( 0.5641757645307916569, -1.616462539050035785, 0.4683090780955098120 ) ) ;
#469=ORIENTED_EDGE ( 'NONE', *, *, #4281, .F. ) ;
#470=CARTESIAN_POINT ( 'NONE',  ( 0.3010413997904062278, -1.655300281042359600, 0.6398421476192419632 ) ) ;
#475=CARTESIAN_POINT ( 'NONE',  ( 0.01173648626945268322, -0.6872203660140956405, -0.1131804859792006068 ) ) ;
#481=CARTESIAN_POINT ( 'NONE',  ( 0.1854061228264040906, -0.8389673959738600528, 0.1645307725974398116 ) ) ;
#483=CARTESIAN_POINT ( 'NONE',  ( 0.5876954366397778573, -1.441089883205937117, 0.7245674945195832439 ) ) ;
#484=CARTESIAN_POINT ( 'NONE',  ( 0.2595046455490389592, -0.9774713019456258145, 0.6992928735491890091 ) ) ;
#486=CARTESIAN_POINT ( 'NONE',  ( 0.4848298080272115396, -1.171730077801051539, 0.4182417262808777458 ) ) ;
#488=EDGE_CURVE ( 'NONE', #27736, #11923, #6051, .T. ) ;
#489=CARTESIAN_POINT ( 'NONE',  ( 0.7476847780466161497, -1.513986987551942498, 0.3667417262808780887 ) ) ;
#490=CARTESIAN_POINT ( 'NONE',  ( 0.4237998664792062553, -1.180002069003335929, 0.7229979235705997764 ) ) ;
#495=EDGE_CURVE ( 'NONE', #990, #7711, #37493, .T. ) ;
#496=CARTESIAN_POINT ( 'NONE',  ( 0.09580854502948936424, -0.9100554415251292939, 0.8942175666832257175 ) ) ;
#497=CARTESIAN_POINT ( 'NONE',  ( 0.1189259589201130257, -1.413964385820541736, 0.5805317459970470440 ) ) ;
#505=ORIENTED_EDGE ( 'NONE', *, *, #13643, .T. ) ;
#506=CARTESIAN_POINT ( 'NONE',  ( 0.1962654359417508876, -0.5719901442833904559, 0.2972479173850666734 ) ) ;
#507=VERTEX_POINT ( 'NONE', #18837 ) ;
#508=CARTESIAN_POINT ( 'NONE',  ( 0.1070125746715546999, -1.413633491471445458, 0.5553720351514388476 ) ) ;
#510=EDGE_CURVE ( 'NONE', #1876, #18789, #14721, .T. ) ;
#511=CARTESIAN_POINT ( 'NONE',  ( 0.1313907764345140505, -0.5643515122363669256, 0.2179657342365748374 ) ) ;
#514=EDGE_CURVE ( 'NONE', #10550, #11729, #5072, .T. ) ;
#517=CARTESIAN_POINT ( 'NONE',  ( 0.6572694620505376006, -1.525419925066909155, 0.7402068353553745705 ) ) ;
#521=DIRECTION ( 'NONE',  ( 1.000000000000000000, 0.000000000000000000, 0.000000000000000000 ) ) ;
#523=CARTESIAN_POINT ( 'NONE',  ( 0.1213365863176824183, -0.8079515073422893767, 0.4383441164392827272 ) ) ;
#525=CARTESIAN_POINT ( 'NONE',  ( 0.5391969560877111212, -1.519063423995081097, 0.5750070075651220192 ) ) ;
#528=VERTEX_POINT ( 'NONE', #1489 ) ;
#529=CARTESIAN_POINT ( 'NONE',  ( 0.4741118015397497998, -1.670572742253769727, 0.5762195691663208885 ) ) ;
#530=CARTESIAN_POINT ( 'NONE',  ( 0.6665471296844990290, -1.561491147660964307, 0.5827599307756513580 ) ) ;
#531=ORIENTED_EDGE ( 'NONE', *, *, #39085, .F. ) ;
#533=CARTESIAN_POINT ( 'NONE',  ( 0.6089456720007967450, -1.479017793199127073, 0.5713140754762677798 ) ) ;
#536=CARTESIAN_POINT ( 'NONE',  ( 0.1437340355044557927, -1.283861693981850349, 0.4177417262808780229 ) ) ;
#539=CARTESIAN_POINT ( 'NONE',  ( 1.365923996832131609E-16, -0.9481888444201341803, 0.1298224387748352637 ) ) ;
#540=CARTESIAN_POINT ( 'NONE',  ( 0.5133443775832216005, -1.117606250044787863, 0.5819851345710455037 ) ) ;
#548=CARTESIAN_POINT ( 'NONE',  ( 0.08873715221104290507, -0.6057874258154822833, 0.05339092507093272377 ) ) ;
#549=ORIENTED_EDGE ( 'NONE', *, *, #6752, .T. ) ;
#550=CARTESIAN_POINT ( 'NONE',  ( 0.05560027925352286488, -1.335209592177159843, 0.5707417262808780478 ) ) ;
#552=CARTESIAN_POINT ( 'NONE',  ( 0.08948292566159925243, -1.134162181311695550, 0.7575026790715814196 ) ) ;
#555=DIRECTION ( 'NONE',  ( -0.4999551463232372317, 0.8660512985181134660, 0.000000000000000000 ) ) ;
#563=CARTESIAN_POINT ( 'NONE',  ( 0.008263909818985001182, -0.6872203660130532521, -0.01225013371141639093 ) ) ;
#565=CARTESIAN_POINT ( 'NONE',  ( 0.09048026637970207897, -0.6074845422973050857, 0.1898228571399218079 ) ) ;
#566=ORIENTED_EDGE ( 'NONE', *, *, #18209, .T. ) ;
#567=CARTESIAN_POINT ( 'NONE',  ( 0.01057740630157828245, -0.5480095452971527337, 0.4707834600657733182 ) ) ;
#568=CARTESIAN_POINT ( 'NONE',  ( 0.4695802469098975807, -1.548054174230837576, 0.6821400120564988789 ) ) ;
#569=CARTESIAN_POINT ( 'NONE',  ( 0.05836881057500214326, -0.8816445732772075772, 0.7596868123788362848 ) ) ;
#571=CARTESIAN_POINT ( 'NONE',  ( 0.007603976726586691992, -0.8548043520540634654, 0.3312797348522363849 ) ) ;
#572=CARTESIAN_POINT ( 'NONE',  ( 0.1428380884784982152, -0.9251932626566119477, 0.2341808872370881034 ) ) ;
#575=CARTESIAN_POINT ( 'NONE',  ( 0.1887412855916204002, -0.4595320686313496550, 0.1406012133455269986 ) ) ;
#576=CARTESIAN_POINT ( 'NONE',  ( 0.1264400783069879464, -0.5746782940434723708, 0.2522357024984944740 ) ) ;
#581=AXIS2_PLACEMENT_3D ( 'NONE', #9769, #38747, #35070 ) ;
#583=CARTESIAN_POINT ( 'NONE',  ( 0.1989132775362471572, -0.6135140644431382739, 0.3133236772439795259 ) ) ;
#585=CARTESIAN_POINT ( 'NONE',  ( 0.03820476523828830046, -1.111795898603934907, 0.6475194386861253815 ) ) ;
#587=CARTESIAN_POINT ( 'NONE',  ( 0.1962011474396041510, -0.6975759447675977665, 0.3321746956187077715 ) ) ;
#588=CARTESIAN_POINT ( 'NONE',  ( 0.2113308451705910584, -0.9022860825909653215, 0.6394510361928067432 ) ) ;
#598=CARTESIAN_POINT ( 'NONE',  ( 0.1514479621444425883, -1.394758587859710852, 0.5685195609790014704 ) ) ;
#601=CARTESIAN_POINT ( 'NONE',  ( 0.4500029371338000184, -1.216587125310998552, 0.7147167669989350491 ) ) ;
#603=CARTESIAN_POINT ( 'NONE',  ( 0.2664054812813116402, -1.675250450210487241, 0.5049835301735086102 ) ) ;
#604=CARTESIAN_POINT ( 'NONE',  ( 0.4929286275565831765, -1.082705722935900727, 0.5701913825460898089 ) ) ;
#606=SHAPE_DEFINITION_REPRESENTATION ( #16679, #25967 ) ;
#607=CARTESIAN_POINT ( 'NONE',  ( 0.07366741488480997579, -1.208427444596519740, 0.7550469801918410218 ) ) ;
#609=CARTESIAN_POINT ( 'NONE',  ( 0.3400902099693209890, -1.481225204631317904, 0.8578335710567297490 ) ) ;
#610=CARTESIAN_POINT ( 'NONE',  ( 0.08694964513190821254, -0.7344668046902962377, 0.009253963018792546111 ) ) ;
#613=ORIENTED_EDGE ( 'NONE', *, *, #446, .T. ) ;
#616=CARTESIAN_POINT ( 'NONE',  ( 0.5675435908986786737, -1.503183644517305906, 0.5857270473429870838 ) ) ;
#626=CARTESIAN_POINT ( 'NONE',  ( 0.5012199843439465452, -1.111650260509063681, 0.8688705274730272876 ) ) ;
#629=CARTESIAN_POINT ( 'NONE',  ( 0.3499317094845083576, -1.754137739073151847, 0.4513909310129906038 ) ) ;
#634=CARTESIAN_POINT ( 'NONE',  ( 0.3445792654416063305, -1.157027493435655918, 0.4460452011843933917 ) ) ;
#635=DIRECTION ( 'NONE',  ( -0.8660512985181135770, -0.4999551463232370097, 0.000000000000000000 ) ) ;
#637=CARTESIAN_POINT ( 'NONE',  ( 0.2520126056674420467, -1.649747432069603059, 0.6712725404530499596 ) ) ;
#638=CARTESIAN_POINT ( 'NONE',  ( 0.0002505691696624545153, -0.4999728502647474704, -0.01895684034646696187 ) ) ;
#646=ORIENTED_EDGE ( 'NONE', *, *, #34266, .F. ) ;
#648=CARTESIAN_POINT ( 'NONE',  ( 0.1876053338355621880, -0.6785855078148245179, 0.1477569985384105666 ) ) ;
#649=CARTESIAN_POINT ( 'NONE',  ( 0.4721946110347202130, -1.256212455760594038, 0.8113655170462841237 ) ) ;
#650=DIRECTION ( 'NONE',  ( 0.8660512985181135770, 0.4999551463232372317, 0.000000000000000000 ) ) ;
#653=CARTESIAN_POINT ( 'NONE',  ( 0.5670603610380426929, -1.614819920947217824, 0.4627456299544086549 ) ) ;
#656=CARTESIAN_POINT ( 'NONE',  ( 0.2973196733566817462, -1.656726351290948918, 0.5753164574205285042 ) ) ;
#658=CARTESIAN_POINT ( 'NONE',  ( 0.1120274473155025569, -0.8465630035012994270, -0.03607198864310506847 ) ) ;
#667=CARTESIAN_POINT ( 'NONE',  ( 0.3211423535335589663, -1.297371328969667337, 0.4638875385414486519 ) ) ;
#668=CARTESIAN_POINT ( 'NONE',  ( 0.2544129889468665917, -0.8811365994555702130, 0.5079734207411469304 ) ) ;
#669=LINE ( 'NONE', #6570, #17377 ) ;
#670=CARTESIAN_POINT ( 'NONE',  ( 0.6077710551370157921, -1.479885162639095642, 0.5931706700332087800 ) ) ;
#671=CARTESIAN_POINT ( 'NONE',  ( 0.1556509205458345979, -0.8505966782751922528, 0.4456406740063399430 ) ) ;
#672=CARTESIAN_POINT ( 'NONE',  ( 0.3187641638634987618, -1.760284878867080183, 0.5597302103697527897 ) ) ;
#675=CARTESIAN_POINT ( 'NONE',  ( 0.6163017222665648776, -1.575337489768728449, 0.4182417262808778013 ) ) ;
#677=CARTESIAN_POINT ( 'NONE',  ( 0.3176952829412639789, -1.763573368804407293, 0.5240040142934835332 ) ) ;
#681=CARTESIAN_POINT ( 'NONE',  ( 0.1088350085164224712, -1.405274509034461161, 0.6288405113567394622 ) ) ;
#691=CARTESIAN_POINT ( 'NONE',  ( 0.1082355115415229163, -1.414758509789771024, 0.5473920290540288391 ) ) ;
#693=CARTESIAN_POINT ( 'NONE',  ( 0.5957873154750314981, -1.486690956665239760, 0.5986609531166485754 ) ) ;
#704=CARTESIAN_POINT ( 'NONE',  ( 0.002121429450436813045, -0.9534082139883235385, -0.06462206035643694446 ) ) ;
#707=CARTESIAN_POINT ( 'NONE',  ( 0.08602377501804453486, -0.7462434654154141978, 0.1699095607782871165 ) ) ;
#709=CARTESIAN_POINT ( 'NONE',  ( 0.5385507356656885625, -1.518881873005200722, 0.5634855329511206934 ) ) ;
#713=CIRCLE ( 'NONE', #2666, 0.01000000000000002970 ) ;
#714=CARTESIAN_POINT ( 'NONE',  ( 0.3524912763923935266, -1.753296592790281716, 0.5876423733645496084 ) ) ;
#715=CARTESIAN_POINT ( 'NONE',  ( 0.6988690859294481861, -1.438864552056196455, 0.5752383414672479489 ) ) ;
#717=CARTESIAN_POINT ( 'NONE',  ( 0.5001471755736989211, -1.324671238001419171, 0.8078733825486025255 ) ) ;
#720=CARTESIAN_POINT ( 'NONE',  ( 0.05573493074139709846, -1.335442843293342063, 0.4177417262808780229 ) ) ;
#723=CARTESIAN_POINT ( 'NONE',  ( 0.05217694232180475344, -1.283001185023028068, 0.6381678350426021051 ) ) ;
#724=CARTESIAN_POINT ( 'NONE',  ( 0.5135987199389938640, -1.118799288056715691, 0.5631670202300380623 ) ) ;
#727=CARTESIAN_POINT ( 'NONE',  ( 0.3832962518680279596, -1.721467521351945917, 0.4207717472948147019 ) ) ;
#728=CARTESIAN_POINT ( 'NONE',  ( 0.4470380544993052263, -1.155950011936287547, 0.4182417262808778013 ) ) ;
#730=CARTESIAN_POINT ( 'NONE',  ( 0.4676789493019616883, -1.559177855287317005, 0.5735223705611400824 ) ) ;
#735=CARTESIAN_POINT ( 'NONE',  ( 0.3207919832889619127, -1.182535135427784878, 0.4177417262808780229 ) ) ;
#736=CARTESIAN_POINT ( 'NONE',  ( 0.6778058174389349766, -1.398346805643282620, 0.6444391890521875554 ) ) ;
#737=ORIENTED_EDGE ( 'NONE', *, *, #19321, .T. ) ;
#744=ADVANCED_FACE ( 'NONE', ( #32924 ), #24766, .F. ) ;
#747=CARTESIAN_POINT ( 'NONE',  ( 0.5264113014007821834, -1.640729993778253126, 0.5682417262808786562 ) ) ;
#748=CARTESIAN_POINT ( 'NONE',  ( 0.1407641140263237722, -0.7425519615811172480, 0.5154596140880725041 ) ) ;
#749=CARTESIAN_POINT ( 'NONE',  ( 0.01618926723855275418, -0.5805349003106968775, 0.5268594266229615908 ) ) ;
#750=CARTESIAN_POINT ( 'NONE',  ( 0.08568842022380158963, -0.5512911918770847519, 0.2017856240869609075 ) ) ;
#753=CARTESIAN_POINT ( 'NONE',  ( 0.6217057667416072686, -1.470137463580756476, 0.4986251887174529829 ) ) ;
#754=CARTESIAN_POINT ( 'NONE',  ( 0.1903653584895528827, -0.9166996592303769953, 0.2311698029113070929 ) ) ;
#755=VERTEX_POINT ( 'NONE', #9061 ) ;
#756=ORIENTED_EDGE ( 'NONE', *, *, #8755, .T. ) ;
#759=CARTESIAN_POINT ( 'NONE',  ( 0.1897115188215528769, -0.5340561384918134369, 0.1468274819697357736 ) ) ;
#765=DIRECTION ( 'NONE',  ( -0.8660512985181134660, -0.4999551463232372872, 0.000000000000000000 ) ) ;
#767=CARTESIAN_POINT ( 'NONE',  ( 0.2674444507101633728, -0.7485333398656358606, 0.5795413912256205391 ) ) ;
#770=CARTESIAN_POINT ( 'NONE',  ( 0.5313858342244102140, -1.164972183933710825, 0.5039547296423043665 ) ) ;
#771=CARTESIAN_POINT ( 'NONE',  ( 0.04540579952787707901, -1.158556396592530513, 0.6631049105669120092 ) ) ;
#775=CARTESIAN_POINT ( 'NONE',  ( 0.2569662571990922184, -0.9629747482851543916, 0.6869665874150546747 ) ) ;
#777=CARTESIAN_POINT ( 'NONE',  ( 0.6940617502335346689, -1.499911880483144166, 0.4737457937229823668 ) ) ;
#778=ORIENTED_EDGE ( 'NONE', *, *, #15008, .T. ) ;
#780=CARTESIAN_POINT ( 'NONE',  ( 0.5265030742546764619, -1.341057478605462316, 0.7770388537806591778 ) ) ;
#786=CARTESIAN_POINT ( 'NONE',  ( 0.1891450095147329813, -0.5717505337550861100, 0.2886938745194108646 ) ) ;
#788=CARTESIAN_POINT ( 'NONE',  ( 0.1859432605888821921, -0.7573098151843028480, 0.1022962920937455361 ) ) ;
#789=CARTESIAN_POINT ( 'NONE',  ( 0.4906812380651594530, -1.277603856553843897, 0.5875273083986286560 ) ) ;
#794=CARTESIAN_POINT ( 'NONE',  ( 0.3384799338905536970, -0.9979650346196410338, 0.5984318192120324786 ) ) ;
#795=ORIENTED_EDGE ( 'NONE', *, *, #11536, .F. ) ;
#799=VERTEX_POINT ( 'NONE', #28189 ) ;
#800=CARTESIAN_POINT ( 'NONE',  ( 0.1226422125323946705, -0.8479982503710601360, 0.6959758587416453590 ) ) ;
#801=CARTESIAN_POINT ( 'NONE',  ( 0.06475727327243140097, -0.8283951214762328430, 0.1002009769046496579 ) ) ;
#806=CARTESIAN_POINT ( 'NONE',  ( 0.5662983945365519522, -1.503052247576714961, 0.5610676162927376032 ) ) ;
#813=CARTESIAN_POINT ( 'NONE',  ( 0.1169788285577439829, -1.415237608940837388, 0.5049415650359101448 ) ) ;
#814=LINE ( 'NONE', #16615, #246 ) ;
#820=EDGE_CURVE ( 'NONE', #1211, #35870, #12969, .T. ) ;
#823=CARTESIAN_POINT ( 'NONE',  ( 0.1841393808565141010, -0.5721394145837870315, 0.006895157961417135856 ) ) ;
#824=CARTESIAN_POINT ( 'NONE',  ( 0.4103533436992015671, -1.245885857446504374, 0.5182417262812503145 ) ) ;
#828=CARTESIAN_POINT ( 'NONE',  ( 0.003142067210302413628, -0.5716151664902620055, 0.1991251360516817781 ) ) ;
#835=B_SPLINE_CURVE_WITH_KNOTS ( 'NONE', 3,
 ( #23386, #4599, #19860, #4219, #29333, #11019, #38762, #1179, #10594, #17174 ),
 .UNSPECIFIED., .F., .F.,
 ( 4, 2, 2, 2, 4 ),
 ( 4.793059745592843663E-05, 0.001006021979757477577, 0.001964113362059026827, 0.002922204744360576076, 0.003880296126662125325 ),
 .UNSPECIFIED. ) ;
#836=B_SPLINE_SURFACE_WITH_KNOTS ( 'NONE', 5, 5, ( 
 ( #31533, #22111, #19202, #720, #25171, #326 ),
 ( #12829, #25391, #16517, #536, #13032, #13220 ),
 ( #7045, #37492, #21896, #16324, #34422, #22714 ),
 ( #38111, #6237, #38311, #31744, #9930, #35246 ),
 ( #19614, #37922, #37709, #9533, #4755, #29277 ),
 ( #1514, #35847, #20228, #38720, #10541, #32549 ) ),
 .UNSPECIFIED., .F., .F., .F.,
 ( 6, 6 ),
 ( 6, 6 ),
 ( -6.477000000001651436, 6.477000000001639002 ),
 ( -2.080605796196421498, 4.396394203803585476 ),
 .UNSPECIFIED. ) ;
#837=ORIENTED_EDGE ( 'NONE', *, *, #8785, .F. ) ;
#842=CARTESIAN_POINT ( 'NONE',  ( 0.4354831391633621207, -1.199087596169247094, 0.7698817195160777560 ) ) ;
#844=ORIENTED_EDGE ( 'NONE', *, *, #14510, .F. ) ;
#845=CARTESIAN_POINT ( 'NONE',  ( 0.5544279432241370209, -1.187676084274785548, 0.5985052393047670671 ) ) ;
#849=VERTEX_POINT ( 'NONE', #9460 ) ;
#850=CARTESIAN_POINT ( 'NONE',  ( 0.2997655131913015136, -1.638171704166688558, 0.7345980899167104949 ) ) ;
#854=CARTESIAN_POINT ( 'NONE',  ( 0.1867780286631144093, -0.7337134285967986669, -0.08446770797961487831 ) ) ;
#860=CARTESIAN_POINT ( 'NONE',  ( 0.1109053458322742519, -0.9286334977625223530, 0.1468672030441772469 ) ) ;
#862=CARTESIAN_POINT ( 'NONE',  ( 0.5864976212241491682, -1.491712091267360263, 0.6107045218380184881 ) ) ;
#865=CARTESIAN_POINT ( 'NONE',  ( 0.4248423436954585908, -1.212122267013820753, 0.6558017523709199770 ) ) ;
#866=CARTESIAN_POINT ( 'NONE',  ( 0.01056671636551369080, -0.5306646670528684107, 0.1647702481118153983 ) ) ;
#868=FACE_OUTER_BOUND ( 'NONE', #23037, .T. ) ;
#875=EDGE_CURVE ( 'NONE', #7023, #10339, #36997, .T. ) ;
#877=CARTESIAN_POINT ( 'NONE',  ( 0.1788174026987448817, -0.4928320601422241931, 0.1325682524468290158 ) ) ;
#879=EDGE_CURVE ( 'NONE', #19095, #17240, #22904, .T. ) ;
#887=EDGE_CURVE ( 'NONE', #19917, #25255, #28631, .T. ) ;
#891=CARTESIAN_POINT ( 'NONE',  ( 0.1905436384893607615, -0.5945559727383887827, 0.3046096357648226949 ) ) ;
#893=DIRECTION ( 'NONE',  ( 1.000000000000000000, 0.000000000000000000, 0.000000000000000000 ) ) ;
#896=CARTESIAN_POINT ( 'NONE',  ( 0.1315527212125843504, -0.5529222810202329974, 0.1699692310456895061 ) ) ;
#904=EDGE_CURVE ( 'NONE', #20709, #39668, #32268, .T. ) ;
#911=CARTESIAN_POINT ( 'NONE',  ( 0.1954888443903809170, -0.9019706710010376716, 0.6101278593650538706 ) ) ;
#912=CARTESIAN_POINT ( 'NONE',  ( 0.06924657340765723312, -0.5400045880099078044, 0.1460913089649399643 ) ) ;
#913=CARTESIAN_POINT ( 'NONE',  ( 0.5403952185064613278, -1.517255356709687808, 0.6224652973508716380 ) ) ;
#916=CARTESIAN_POINT ( 'NONE',  ( 0.6987898065016509008, -1.520117587203002607, 0.5151143090318311968 ) ) ;
#918=CARTESIAN_POINT ( 'NONE',  ( 0.3061809949057166524, -1.759155323846213204, 0.5693298920811382668 ) ) ;
#920=CARTESIAN_POINT ( 'NONE',  ( 0.4284865639878338017, -1.682583770571502990, 0.4182417262808776903 ) ) ;
#921=B_SPLINE_CURVE_WITH_KNOTS ( 'NONE', 3,
 ( #12992, #9882, #6791, #3728, #35998, #1865, #32499, #7606, #4323, #23667, #23271, #10493, #23877, #14379, #30040, #13777, #10914, #19964, #8006, #26157, #20374, #26341, #4512, #16886, #32705, #38675, #26945, #30219, #2051, #23060, #39477, #36401, #11308, #1674, #36192, #10701, #29427, #35590, #8216, #1465 ),
 .UNSPECIFIED., .F., .F.,
 ( 4, 2, 2, 2, 2, 2, 2, 2, 2, 2, 2, 2, 2, 2, 2, 2, 2, 2, 2, 4 ),
 ( 0.000000000000000000, 0.002694941689597518588, 0.005389883379195037176, 0.008084825068792557065, 0.009432295913591315709, 0.01077976675839007435, 0.01212723760318883647, 0.01347470844798758990, 0.01414844387038696923, 0.01482217929278635028, 0.01549591471518572787, 0.01616965013758510719, 0.01684338555998448825, 0.01751712098238386930, 0.01886459182718262795, 0.02021206267198139006, 0.02088579809438077459, 0.02122266580558046858, 0.02139109966118031905, 0.02155953351678016952 ),
 .UNSPECIFIED. ) ;
#923=CARTESIAN_POINT ( 'NONE',  ( 0.3158858043796832216, -1.003067975662501832, 0.7589385492876046246 ) ) ;
#924=CARTESIAN_POINT ( 'NONE',  ( -3.231615316776240918E-05, -0.7201627993511090509, -0.1017344997239397197 ) ) ;
#926=CARTESIAN_POINT ( 'NONE',  ( 0.006276500232904156859, -0.8404987286125837898, 0.1047677167647131508 ) ) ;
#928=CARTESIAN_POINT ( 'NONE',  ( -0.002023118427450016753, -0.8974731051190899533, 0.1948784381876195460 ) ) ;
#929=CARTESIAN_POINT ( 'NONE',  ( 0.3302065591133839240, -0.9317669992161012882, 0.6252562391197076241 ) ) ;
#932=CARTESIAN_POINT ( 'NONE',  ( 0.3740960844805631957, -1.108072201694596526, 0.5182417262812423209 ) ) ;
#934=CARTESIAN_POINT ( 'NONE',  ( 0.1835961851041346959, -0.5126270562563732813, 0.08826789480522242992 ) ) ;
#936=CARTESIAN_POINT ( 'NONE',  ( 0.4861084675450336734, -1.181744968368830584, 0.4182417262808778569 ) ) ;
#939=CARTESIAN_POINT ( 'NONE',  ( 0.01055999354153808190, -0.5296565605740091165, 0.1443450864220710561 ) ) ;
#941=CARTESIAN_POINT ( 'NONE',  ( 0.08738337528432148227, -0.6948978725876520102, 0.02266917563589926354 ) ) ;
#942=ORIENTED_EDGE ( 'NONE', *, *, #39899, .F. ) ;
#943=DIRECTION ( 'NONE',  ( 0.000000000000000000, 0.000000000000000000, -1.000000000000000000 ) ) ;
#944=CARTESIAN_POINT ( 'NONE',  ( 0.4504239474101026652, -1.039103266886249655, 0.7909361398939754872 ) ) ;
#948=ORIENTED_EDGE ( 'NONE', *, *, #21075, .T. ) ;
#954=ORIENTED_EDGE ( 'NONE', *, *, #21625, .F. ) ;
#955=CARTESIAN_POINT ( 'NONE',  ( 0.04687500000000000694, -0.4345172148286636782, 0.1921395889696510262 ) ) ;
#956=CARTESIAN_POINT ( 'NONE',  ( 0.09733160485405090157, -0.6654810868242956312, 0.3090395299204725110 ) ) ;
#959=CARTESIAN_POINT ( 'NONE',  ( 0.4692883835019161509, -1.557836661473111395, 0.5661479686463081196 ) ) ;
#961=CARTESIAN_POINT ( 'NONE',  ( 0.08034914622429441267, -0.9725984063009643910, 0.8263393459352617043 ) ) ;
#963=CARTESIAN_POINT ( 'NONE',  ( 0.1967796840110664081, -0.9202189791215042991, 0.2910963043859624566 ) ) ;
#966=CARTESIAN_POINT ( 'NONE',  ( 0.1961146565040154666, -0.5779037128980665239, 0.3019974763434182807 ) ) ;
#970=CARTESIAN_POINT ( 'NONE',  ( 0.6742391038958878147, -1.391540648348956966, 0.6661449684938977045 ) ) ;
#972=ADVANCED_FACE ( 'NONE', ( #11697 ), #23462, .T. ) ;
#979=CARTESIAN_POINT ( 'NONE',  ( 0.2640953184584151625, -0.9556158622373929212, 0.7086077991120209862 ) ) ;
#985=DIRECTION ( 'NONE',  ( -0.4999551463232371762, 0.8660512985181134660, -0.000000000000000000 ) ) ;
#987=CARTESIAN_POINT ( 'NONE',  ( 0.3051773648903314817, -1.756515850768020304, 0.5493070528972983091 ) ) ;
#989=CARTESIAN_POINT ( 'NONE',  ( 0.06595730239831418262, -0.8537221610436072083, 0.3900050273732788564 ) ) ;
#990=VERTEX_POINT ( 'NONE', #22805 ) ;
#998=CARTESIAN_POINT ( 'NONE',  ( 0.4104893297753217096, -1.161006097983400709, 0.7058587609593679479 ) ) ;
#999=LINE ( 'NONE', #9610, #37082 ) ;
#1001=CARTESIAN_POINT ( 'NONE',  ( 0.1875000000000002498, -0.9151275355372966436, 0.1457185332388701016 ) ) ;
#1003=ADVANCED_FACE ( 'NONE', ( #28935 ), #31589, .T. ) ;
#1010=CARTESIAN_POINT ( 'NONE',  ( 0.3934995777983899545, -1.530652811628217425, 0.7930223495936653544 ) ) ;
#1012=CARTESIAN_POINT ( 'NONE',  ( 0.1905436384893574309, -0.5945559727383904480, 0.3046096357648198638 ) ) ;
#1015=ORIENTED_EDGE ( 'NONE', *, *, #2225, .F. ) ;
#1017=CARTESIAN_POINT ( 'NONE',  ( 0.4137411116391392918, -1.124414850558264733, 0.5933932595712226865 ) ) ;
#1018=CARTESIAN_POINT ( 'NONE',  ( 0.1199036801841761174, -0.5680492792121983880, 0.2364068004411575830 ) ) ;
#1023=DIRECTION ( 'NONE',  ( -0.8660512985181139101, -0.4999551463232362325, 5.802457945118985070E-16 ) ) ;
#1027=CARTESIAN_POINT ( 'NONE',  ( 0.6791199086483500347, -1.400839286187941957, 0.8214794356666539343 ) ) ;
#1029=CARTESIAN_POINT ( 'NONE',  ( 0.07556315841227354002, -1.331191507351498160, 0.4849083929475443422 ) ) ;
#1037=CARTESIAN_POINT ( 'NONE',  ( 0.1848741932763747764, -0.8057379068672942957, 0.02534018588883596781 ) ) ;
#1043=CARTESIAN_POINT ( 'NONE',  ( 0.03132541776874769868, -0.7585458590990268313, 0.6287131927338691639 ) ) ;
#1048=ORIENTED_EDGE ( 'NONE', *, *, #13178, .F. ) ;
#1054=CARTESIAN_POINT ( 'NONE',  ( 0.5536405708538106873, -1.384481591576937509, 0.6244451514967195305 ) ) ;
#1057=CARTESIAN_POINT ( 'NONE',  ( 0.2043709925794569282, -0.7174950807506157435, 0.3538749514786183048 ) ) ;
#1062=CARTESIAN_POINT ( 'NONE',  ( 0.3133035272563549078, -1.575440432857677431, 0.8162228474935855349 ) ) ;
#1069=TOROIDAL_SURFACE ( 'NONE', #16131, 0.04749999999977547877, 0.01000000000000000021 ) ;
#1070=CARTESIAN_POINT ( 'NONE',  ( 0.3211452305271019769, -1.297376312664729081, 0.5471643355025310740 ) ) ;
#1071=CARTESIAN_POINT ( 'NONE',  ( 0.1862185816537504646, -0.9153565697885686081, 0.1497573156717260934 ) ) ;
#1072=DIRECTION ( 'NONE',  ( -0.4999551463232372317, 0.8660512985181134660, -0.000000000000000000 ) ) ;
#1073=CARTESIAN_POINT ( 'NONE',  ( 0.5931681649608109286, -1.450353124920298331, 0.7100355140729243120 ) ) ;
#1074=CARTESIAN_POINT ( 'NONE',  ( 0.1687818703766520989, -0.9104748073852155787, 0.6043791483695026834 ) ) ;
#1076=CARTESIAN_POINT ( 'NONE',  ( 0.1487034783640427960, -1.203069224257576897, 0.9182092241904131757 ) ) ;
#1077=CARTESIAN_POINT ( 'NONE',  ( 0.4232662408345057026, -1.152421473039004995, 0.4182417262808778013 ) ) ;
#1078=CARTESIAN_POINT ( 'NONE',  ( 0.4385112828469532875, -1.229609716458687441, 0.5557375479387191008 ) ) ;
#1084=LINE ( 'NONE', #23272, #31039 ) ;
#1086=CARTESIAN_POINT ( 'NONE',  ( 0.3453377680719361131, -1.749458763706787545, 0.4498113177181523037 ) ) ;
#1088=CARTESIAN_POINT ( 'NONE',  ( 0.3059973874268072103, -1.701798401340633982, 0.8340740219765057084 ) ) ;
#1095=CARTESIAN_POINT ( 'NONE',  ( 0.2675603648060154716, -1.673609121357023666, 0.5605535550759273011 ) ) ;
#1096=CARTESIAN_POINT ( 'NONE',  ( 0.5888117849411206306, -1.461768036186659847, 0.6982214778808412126 ) ) ;
#1102=CARTESIAN_POINT ( 'NONE',  ( 0.6672755688376807992, -1.557826434319784514, 0.6345042746411464485 ) ) ;
#1108=EDGE_LOOP ( 'NONE', ( #15223, #30868, #10948, #31753 ) ) ;
#1109=CARTESIAN_POINT ( 'NONE',  ( 0.09149069872302392770, -0.8181431826323624090, 0.2735856555635383103 ) ) ;
#1110=CARTESIAN_POINT ( 'NONE',  ( 0.3336325236675090067, -1.050835064020409160, 0.7593003920438236021 ) ) ;
#1111=CARTESIAN_POINT ( 'NONE',  ( 0.5388828585122440451, -1.518987218245586135, 0.5695592972482714789 ) ) ;
#1113=CARTESIAN_POINT ( 'NONE',  ( 0.1765406453986485269, -0.4888679620873611631, 0.1632814624852850782 ) ) ;
#1116=CARTESIAN_POINT ( 'NONE',  ( 0.3915481144911456268, -1.718409356248215447, 0.6204489441750801193 ) ) ;
#1121=DIRECTION ( 'NONE',  ( -0.4999551463232371762, 0.8660512985181134660, -0.000000000000000000 ) ) ;
#1123=CARTESIAN_POINT ( 'NONE',  ( 3.244074353476664772E-08, -0.6526340382750903668, -0.1135225766990422963 ) ) ;
#1124=CARTESIAN_POINT ( 'NONE',  ( 0.3515944374025173902, -1.098270542177856912, 0.7997119400958316859 ) ) ;
#1126=( CONVERSION_BASED_UNIT ( 'INCH', #10967 ) LENGTH_UNIT ( ) NAMED_UNIT ( #23398 ) );
#1127=CARTESIAN_POINT ( 'NONE',  ( 0.2225889308918536924, -1.238345268919997855, 0.5682417262808776570 ) ) ;
#1130=CARTESIAN_POINT ( 'NONE',  ( 0.1227332031174801358, -1.426450801877330088, 0.6430247681006037164 ) ) ;
#1131=CARTESIAN_POINT ( 'NONE',  ( 0.4929433234940127639, -1.082713786091526353, 0.5692160337251114255 ) ) ;
#1135=FACE_OUTER_BOUND ( 'NONE', #11630, .T. ) ;
#1144=CARTESIAN_POINT ( 'NONE',  ( 0.6387812025505826830, -1.332167957021822557, 0.7527387398627037873 ) ) ;
#1150=CARTESIAN_POINT ( 'NONE',  ( 0.3048570497350418518, -1.756853555320991189, 0.5694442476137144826 ) ) ;
#1153=CARTESIAN_POINT ( 'NONE',  ( 0.7175296490783633629, -1.539929330036125421, 0.8144692937752638917 ) ) ;
#1154=EDGE_CURVE ( 'NONE', #1703, #17938, #16900, .T. ) ;
#1155=CARTESIAN_POINT ( 'NONE',  ( 0.08811120843107830836, -0.6855307903982026385, 0.1873295917847169478 ) ) ;
#1157=CARTESIAN_POINT ( 'NONE',  ( 0.03015888383791201846, -0.5831136045742685292, 0.5494185303259956354 ) ) ;
#1158=CARTESIAN_POINT ( 'NONE',  ( 0.4645154715899988407, -1.476824984445624711, 0.7857104932153542443 ) ) ;
#1159=CARTESIAN_POINT ( 'NONE',  ( 0.1460326451217981436, -1.211929559011373891, 0.9332704621650906862 ) ) ;
#1161=CARTESIAN_POINT ( 'NONE',  ( 0.1073778561850880914, -0.9490620967497181981, 0.3854551792646946917 ) ) ;
#1165=CARTESIAN_POINT ( 'NONE',  ( 0.2082119840840267744, -0.7174231593591114953, 0.6726620554019909770 ) ) ;
#1167=LINE ( 'NONE', #26048, #3608 ) ;
#1172=CARTESIAN_POINT ( 'NONE',  ( 0.3628146410451159598, -0.9034970372909253422, 0.7254628211502860413 ) ) ;
#1174=CARTESIAN_POINT ( 'NONE',  ( 0.5001593862222446507, -1.120530468926300927, 0.4879659633826187171 ) ) ;
#1176=CARTESIAN_POINT ( 'NONE',  ( 0.01334304990240413324, -0.9205301472758444792, 0.5571205034865969186 ) ) ;
#1179=CARTESIAN_POINT ( 'NONE',  ( 0.3264027515311576644, -1.294324649726913634, 0.4430263674525740658 ) ) ;
#1180=CARTESIAN_POINT ( 'NONE',  ( 0.3700259886275120702, -1.148283099900891058, 0.7265771563811994627 ) ) ;
#1185=CARTESIAN_POINT ( 'NONE',  ( 0.09360223597190081568, -0.5959407479578081590, 0.2661619178395356333 ) ) ;
#1187=CARTESIAN_POINT ( 'NONE',  ( 0.1169788285577439829, -1.415237608940837388, 0.5049415650359101448 ) ) ;
#1188=CARTESIAN_POINT ( 'NONE',  ( 0.2764376405909636514, -1.316227483431351875, 0.6113284502048742519 ) ) ;
#1193=CARTESIAN_POINT ( 'NONE',  ( 0.4806401579603196139, -1.259507117968132528, 0.6434039063252821045 ) ) ;
#1196=CARTESIAN_POINT ( 'NONE',  ( 0.2734279889346977188, -0.9622732688880970553, 0.5233991146725487376 ) ) ;
#1201=CARTESIAN_POINT ( 'NONE',  ( 0.04900772023046805204, -0.5599104050450269821, 0.2516739294092621426 ) ) ;
#1203=CARTESIAN_POINT ( 'NONE',  ( 0.1954949921222078613, -0.7168102854172049287, 0.3287466980362075963 ) ) ;
#1208=ADVANCED_FACE ( 'NONE', ( #24612 ), #5032, .F. ) ;
#1209=CARTESIAN_POINT ( 'NONE',  ( 0.1191842311548099581, -0.5541223904023430125, 0.1890049277065241062 ) ) ;
#1211=VERTEX_POINT ( 'NONE', #15552 ) ;
#1215=DIRECTION ( 'NONE',  ( 1.000000000000000000, 0.000000000000000000, 0.000000000000000000 ) ) ;
#1216=CARTESIAN_POINT ( 'NONE',  ( 0.3693619091536758936, -1.731651576748437948, 0.6146617367520950115 ) ) ;
#1218=CARTESIAN_POINT ( 'NONE',  ( 0.7412791958894395794, -1.507305061506947430, 0.6536223584324379887 ) ) ;
#1224=EDGE_CURVE ( 'NONE', #9524, #13839, #31428, .T. ) ;
#1232=CARTESIAN_POINT ( 'NONE',  ( -8.537024980200822558E-17, -0.6872203660140405734, 0.09557912180100291977 ) ) ;
#1240=CARTESIAN_POINT ( 'NONE',  ( 0.1436225252650951412, -1.283668529478381393, 0.4687417262808780127 ) ) ;
#1244=CARTESIAN_POINT ( 'NONE',  ( 0.5446150423827782472, -1.368799154680095942, 0.7286756449045225237 ) ) ;
#1245=CARTESIAN_POINT ( 'NONE',  ( 0.3484677573834994435, -1.177852168535778565, 0.4182417262808778013 ) ) ;
#1246=VERTEX_POINT ( 'NONE', #13258 ) ;
#1247=CARTESIAN_POINT ( 'NONE',  ( 0.4661750196922136991, -1.070732324447800421, 0.6917658376937553255 ) ) ;
#1252=CARTESIAN_POINT ( 'NONE',  ( 0.02322307456033121872, -0.5318894034165193574, 0.1546977929980313804 ) ) ;
#1253=CARTESIAN_POINT ( 'NONE',  ( 0.6071598558232448317, -1.592990773492276357, 0.4345894283230820609 ) ) ;
#1254=DIRECTION ( 'NONE',  ( 1.060606950627616897E-16, 6.122684696619992497E-17, 1.000000000000000000 ) ) ;
#1261=CARTESIAN_POINT ( 'NONE',  ( 0.1872878105913098612, -0.8400613882515264308, 0.2180701053272094680 ) ) ;
#1262=CARTESIAN_POINT ( 'NONE',  ( 0.1734397871105309574, -1.266755107815962678, 0.4263792231164484359 ) ) ;
#1264=CARTESIAN_POINT ( 'NONE',  ( 0.1026041305702724421, -0.8285543066798866096, 0.1791339961852569385 ) ) ;
#1266=CARTESIAN_POINT ( 'NONE',  ( 0.4864384408240609581, -1.181579935974320650, 0.4182417262808778013 ) ) ;
#1271=FACE_OUTER_BOUND ( 'NONE', #28939, .T. ) ;
#1273=CARTESIAN_POINT ( 'NONE',  ( 0.3504057387187117234, -1.153664717295437070, 0.4422128889498894710 ) ) ;
#1278=CARTESIAN_POINT ( 'NONE',  ( 0.3204139389452037023, -1.755336229099433654, 0.4849083929475442867 ) ) ;
#1279=CARTESIAN_POINT ( 'NONE',  ( 0.7053080889764471451, -1.513942001867420339, 0.5667347313869608438 ) ) ;
#1281=CARTESIAN_POINT ( 'NONE',  ( 0.5429359209136535025, -1.169310040315109545, 0.5682417262808779901 ) ) ;
#1283=CARTESIAN_POINT ( 'NONE',  ( 0.2679398507666006513, -1.673757272405929752, 0.5655069686649734084 ) ) ;
#1284=CARTESIAN_POINT ( 'NONE',  ( 0.6018252865098940863, -1.483102701789519973, 0.5702406811564502132 ) ) ;
#1289=CARTESIAN_POINT ( 'NONE',  ( 0.2400030092520472336, -0.7789576557571062931, 0.7291493276161450376 ) ) ;
#1292=CARTESIAN_POINT ( 'NONE',  ( -0.01256779751711274359, -0.5607309962333324460, 0.2869151978856656626 ) ) ;
#1294=CARTESIAN_POINT ( 'NONE',  ( 0.1915833156076485189, -1.371527921740720135, 0.5547766577986595893 ) ) ;
#1295=CARTESIAN_POINT ( 'NONE',  ( 0.3740960844805631957, -1.108072201694596526, 0.5182417262812423209 ) ) ;
#1298=CARTESIAN_POINT ( 'NONE',  ( 0.0006246259811798426324, -0.9534082139883233165, 0.04185307883324813905 ) ) ;
#1299=ORIENTED_EDGE ( 'NONE', *, *, #9495, .T. ) ;
#1301=B_SPLINE_CURVE_WITH_KNOTS ( 'NONE', 3,
 ( #24995, #18845, #33861, #21712 ),
 .UNSPECIFIED., .F., .F.,
 ( 4, 4 ),
 ( 0.000000000000000000, 0.0002458494465879629775 ),
 .UNSPECIFIED. ) ;
#1302=CARTESIAN_POINT ( 'NONE',  ( 0.1576472890307486219, -0.8786603732910064357, 0.5360059036955113765 ) ) ;
#1303=CARTESIAN_POINT ( 'NONE',  ( 0.1291963080521598140, -0.7094397666660188229, 0.4795944692163690570 ) ) ;
#1304=CARTESIAN_POINT ( 'NONE',  ( 0.1108305878322193849, -0.5649205625374638107, 0.2321049223534430439 ) ) ;
#1305=CARTESIAN_POINT ( 'NONE',  ( 0.03052449867241842710, -1.064021556079522535, 0.6116746401987742665 ) ) ;
#1308=LINE ( 'NONE', #35428, #6856 ) ;
#1313=CARTESIAN_POINT ( 'NONE',  ( 0.01148915324952597475, -0.8840235622257791581, -0.02343339859393702568 ) ) ;
#1314=CARTESIAN_POINT ( 'NONE',  ( 0.06942125022148733227, -0.5427962089461003670, 0.1770506202226188042 ) ) ;
#1317=CARTESIAN_POINT ( 'NONE',  ( 0.1849096901904442591, -1.549205955729530793, 0.5682417262808778791 ) ) ;
#1318=CARTESIAN_POINT ( 'NONE',  ( 0.3318484986314376162, -0.9704704429389122700, 0.6048456486855374736 ) ) ;
#1320=CARTESIAN_POINT ( 'NONE',  ( 0.7255563027409094312, -1.477976514587821422, 0.7347025679090390948 ) ) ;
#1323=CARTESIAN_POINT ( 'NONE',  ( 0.3061892459480512474, -1.759162422899352318, 0.5694323708298315578 ) ) ;
#1330=CARTESIAN_POINT ( 'NONE',  ( 0.4381829047093346863, -1.020301330954181518, 0.7847444992166355826 ) ) ;
#1335=CARTESIAN_POINT ( 'NONE',  ( 0.3351195522891313172, -1.762354232558481337, 0.5631496603913015431 ) ) ;
#1336=FACE_OUTER_BOUND ( 'NONE', #15794, .T. ) ;
#1339=CARTESIAN_POINT ( 'NONE',  ( 0.7541811597904449771, -1.515850492646690473, 0.8047797755351335791 ) ) ;
#1340=CARTESIAN_POINT ( 'NONE',  ( 0.08947262244426219813, -0.6461490780200273010, 0.1933266256753762846 ) ) ;
#1341=CARTESIAN_POINT ( 'NONE',  ( 0.0004750029074822290955, -0.4386152177297633070, 0.1882660082133467416 ) ) ;
#1342=VECTOR ( 'NONE', #22126, 39.37007874015748854 ) ;
#1343=CARTESIAN_POINT ( 'NONE',  ( 0.3025071352787032652, -1.151881836541575721, 0.8404721679195121808 ) ) ;
#1344=CARTESIAN_POINT ( 'NONE',  ( 0.2172267109180897882, -1.451647963948341058, 0.9382086856453861756 ) ) ;
#1345=CARTESIAN_POINT ( 'NONE',  ( 0.3163996966746501771, -1.646713064435177731, 0.5991727703659502913 ) ) ;
#1346=CARTESIAN_POINT ( 'NONE',  ( 0.1020516685261761286, -0.9421306251871297555, 0.3381412032200973861 ) ) ;
#1349=CARTESIAN_POINT ( 'NONE',  ( 0.2248552728485077867, -0.5917194789810457101, 0.4907616766386495022 ) ) ;
#1353=CARTESIAN_POINT ( 'NONE',  ( 0.1180487212903242045, -1.414513468998023660, 0.5470211090928080999 ) ) ;
#1354=CARTESIAN_POINT ( 'NONE',  ( 0.6117231882494743589, -1.284912631992666254, 0.6460020013211499323 ) ) ;
#1356=CARTESIAN_POINT ( 'NONE',  ( 0.01797837544738539739, -0.9279355173420600345, 0.5914959875658215571 ) ) ;
#1361=CARTESIAN_POINT ( 'NONE',  ( 0.4171940613675130805, -1.169327234610036292, 0.7033695205199608225 ) ) ;
#1364=EDGE_CURVE ( 'NONE', #36154, #36726, #4129, .T. ) ;
#1367=CARTESIAN_POINT ( 'NONE',  ( 0.5241818771854670489, -1.140424305731243981, 0.6527584601043535661 ) ) ;
#1368=CARTESIAN_POINT ( 'NONE',  ( 0.09129909826610711765, -0.5802035170451905755, 0.2220056307398889928 ) ) ;
#1369=ADVANCED_FACE ( 'NONE', ( #23561 ), #26823, .T. ) ;
#1373=CARTESIAN_POINT ( 'NONE',  ( 0.07923844099270259400, -0.8780064891624800305, 0.4970579955510663339 ) ) ;
#1379=CARTESIAN_POINT ( 'NONE',  ( 0.4799067833796559768, -1.259349870180440867, 0.5814271704687581366 ) ) ;
#1381=CARTESIAN_POINT ( 'NONE',  ( 0.5303494909463689622, -1.149217331578959334, 0.5682610892518529244 ) ) ;
#1382=CARTESIAN_POINT ( 'NONE',  ( 0.1897171943901793389, -0.9163440338727294465, 0.2193954077252403545 ) ) ;
#1386=CARTESIAN_POINT ( 'NONE',  ( 0.4137368557930669044, -1.589575952096031308, 0.5753881675367246151 ) ) ;
#1388=CARTESIAN_POINT ( 'NONE',  ( 0.08870872266905797943, -0.5912816985501267997, 0.03819782855198166488 ) ) ;
#1394=VERTEX_POINT ( 'NONE', #39178 ) ;
#1396=CARTESIAN_POINT ( 'NONE',  ( 0.1208409751158145834, -0.5758948413296848257, 0.2589058236990056661 ) ) ;
#1400=TOROIDAL_SURFACE ( 'NONE', #35517, 0.07749999999977555398, 0.01000000000000000021 ) ;
#1401=CARTESIAN_POINT ( 'NONE',  ( 0.6059136413949802735, -1.592571915802247329, 0.4262670158568807044 ) ) ;
#1403=CARTESIAN_POINT ( 'NONE',  ( 0.2311145781227797180, -1.233632278668805649, 0.4896568257691081283 ) ) ;
#1407=B_SPLINE_CURVE_WITH_KNOTS ( 'NONE', 3,
 ( #22209, #21787, #3859, #15614 ),
 .UNSPECIFIED., .F., .F.,
 ( 4, 4 ),
 ( 0.000000000000000000, 0.0005595226744648492193 ),
 .UNSPECIFIED. ) ;
#1408=CARTESIAN_POINT ( 'NONE',  ( 0.3390826044135689665, -0.8321809361840178942, 0.7462327844847882474 ) ) ;
#1415=CARTESIAN_POINT ( 'NONE',  ( 0.4591673992659657810, -1.217701019417315456, 0.4854672771262538711 ) ) ;
#1416=CARTESIAN_POINT ( 'NONE',  ( 0.09075966053248608889, -1.322849613925215939, 0.4537811506657316030 ) ) ;
#1418=CARTESIAN_POINT ( 'NONE',  ( 0.008416785622808892545, -0.6338120178247520498, 0.4051738709354697487 ) ) ;
#1420=EDGE_CURVE ( 'NONE', #23564, #13401, #8503, .T. ) ;
#1423=CARTESIAN_POINT ( 'NONE',  ( 0.5860257985473380504, -1.592810714289444762, 0.4182417262808776903 ) ) ;
#1425=AXIS2_PLACEMENT_3D ( 'NONE', #15329, #2990, #3751 ) ;
#1426=ADVANCED_FACE ( 'NONE', ( #7879 ), #20945, .T. ) ;
#1434=CARTESIAN_POINT ( 'NONE',  ( 0.5120527146466833379, -1.317106629872495160, 0.7639365440521486139 ) ) ;
#1436=ORIENTED_EDGE ( 'NONE', *, *, #36419, .T. ) ;
#1437=CARTESIAN_POINT ( 'NONE',  ( 0.2182827306251404198, -0.8246641648518335810, 0.4150641157079975052 ) ) ;
#1439=EDGE_LOOP ( 'NONE', ( #38172, #28947, #24871, #22597 ) ) ;
#1441=CARTESIAN_POINT ( 'NONE',  ( 0.2654007536097648390, -1.440376723817250237, 0.9058617339288995707 ) ) ;
#1442=EDGE_CURVE ( 'NONE', #32978, #17370, #29921, .T. ) ;
#1443=CARTESIAN_POINT ( 'NONE',  ( 0.6929203575076985366, -1.501108135639614094, 0.4708622924348231931 ) ) ;
#1445=CARTESIAN_POINT ( 'NONE',  ( 0.4092450614235220163, -1.131740385117829817, 0.4687417262808780127 ) ) ;
#1448=ORIENTED_EDGE ( 'NONE', *, *, #33089, .F. ) ;
#1450=CARTESIAN_POINT ( 'NONE',  ( 0.1679539120650488104, -1.280520828024429125, 0.4182417262808778013 ) ) ;
#1452=CARTESIAN_POINT ( 'NONE',  ( 0.3364536680357681497, -1.190071269297861889, 0.7177689078920298504 ) ) ;
#1453=CARTESIAN_POINT ( 'NONE',  ( 0.3204139389452037023, -1.755336229099433654, 0.4849083929475442867 ) ) ;
#1458=CARTESIAN_POINT ( 'NONE',  ( 0.6568730927750874304, -1.460570608776338597, 0.4224083929475443977 ) ) ;
#1460=CIRCLE ( 'NONE', #9981, 0.08749999999977554899 ) ;
#1465=CARTESIAN_POINT ( 'NONE',  ( 0.06486042810549992599, -1.341249661891149803, 0.5682417262808776570 ) ) ;
#1474=ORIENTED_EDGE ( 'NONE', *, *, #36700, .F. ) ;
#1475=CARTESIAN_POINT ( 'NONE',  ( 0.1725857835740884083, -0.5195664690050083578, 0.1686779206399890985 ) ) ;
#1476=EDGE_LOOP ( 'NONE', ( #31834, #27847, #31710, #25511 ) ) ;
#1479=CARTESIAN_POINT ( 'NONE',  ( 0.2518471669880268937, -0.8867173105660602905, 0.6889547098528300273 ) ) ;
#1480=CARTESIAN_POINT ( 'NONE',  ( -0.002007161383423167276, -0.8507966130668344062, 0.1047852373880929638 ) ) ;
#1483=CARTESIAN_POINT ( 'NONE',  ( 0.3565602430104690135, -0.9764240072966976491, 0.8491718633188657384 ) ) ;
#1487=CARTESIAN_POINT ( 'NONE',  ( 0.1626312629268945875, -1.287482680162472359, 0.9420587295005244943 ) ) ;
#1489=CARTESIAN_POINT ( 'NONE',  ( 0.4380553862277722921, -1.229819722584721164, 0.5856983068965045947 ) ) ;
#1490=DIRECTION ( 'NONE',  ( 0.8660512985181126888, 0.4999551463232384529, 0.000000000000000000 ) ) ;
#1495=CARTESIAN_POINT ( 'NONE',  ( -0.0006767624898369264692, -0.7404579356088998310, -0.1178596299512801177 ) ) ;
#1496=VERTEX_POINT ( 'NONE', #30310 ) ;
#1497=ORIENTED_EDGE ( 'NONE', *, *, #8121, .T. ) ;
#1499=CARTESIAN_POINT ( 'NONE',  ( 0.1025463942476791679, -0.8285650497785959079, 0.3528706793080363946 ) ) ;
#1501=CARTESIAN_POINT ( 'NONE',  ( 0.09522050325736274023, -0.5826464688574188866, 0.2907231271288692187 ) ) ;
#1502=CARTESIAN_POINT ( 'NONE',  ( 0.5304122745878165901, -1.471811735070700511, 0.7419010974003765746 ) ) ;
#1504=CARTESIAN_POINT ( 'NONE',  ( 0.5919322900404796473, -1.484735096275495048, 0.6354748705596902081 ) ) ;
#1505=CARTESIAN_POINT ( 'NONE',  ( 0.6114488815859958626, -1.589096688252098266, 0.4246483893745142679 ) ) ;
#1507=CARTESIAN_POINT ( 'NONE',  ( 0.7427087848590744334, -1.516420150208810380, 0.5553993000885846243 ) ) ;
#1508=CARTESIAN_POINT ( 'NONE',  ( 0.06805528675573245534, -1.337523170998923927, 0.5185299294045161433 ) ) ;
#1511=CARTESIAN_POINT ( 'NONE',  ( -3.183539100166564637E-08, -0.6701325942983367145, -0.1152599293596888730 ) ) ;
#1513=AXIS2_PLACEMENT_3D ( 'NONE', #20014, #1121, #12878 ) ;
#1514=CARTESIAN_POINT ( 'NONE',  ( 0.4972671625857253974, -1.080199071502573771, 0.5707417262808780478 ) ) ;
#1516=CARTESIAN_POINT ( 'NONE',  ( 0.09565263806948612335, -1.148840486724431953, 0.8358535653919648700 ) ) ;
#1517=CARTESIAN_POINT ( 'NONE',  ( 0.4302506758624459748, -1.041368148273517313, 0.6535113357015974733 ) ) ;
#1519=CARTESIAN_POINT ( 'NONE',  ( 0.6872158423035881203, -1.414036026188038031, 0.8114895833460221697 ) ) ;
#1524=EDGE_CURVE ( 'NONE', #4497, #13794, #9031, .T. ) ;
#1525=CARTESIAN_POINT ( 'NONE',  ( 0.3164773456298530796, -1.761773283766707499, 0.5681507431435155464 ) ) ;
#1528=CARTESIAN_POINT ( 'NONE',  ( 0.3187641638634987618, -1.760284878867080183, 0.5597302103697527897 ) ) ;
#1532=CARTESIAN_POINT ( 'NONE',  ( 0.3247324306351094814, -1.759421949583082956, 0.4854534786567449300 ) ) ;
#1533=CARTESIAN_POINT ( 'NONE',  ( 0.3740232550247291066, -0.9210422728154799010, 0.7367171417286558777 ) ) ;
#1540=CARTESIAN_POINT ( 'NONE',  ( 0.4471227077962564578, -1.226789242222319443, 0.5945616820347162657 ) ) ;
#1545=CARTESIAN_POINT ( 'NONE',  ( 0.1008403764883030462, -0.6728090870223089048, 0.3368761478404066478 ) ) ;
#1547=CARTESIAN_POINT ( 'NONE',  ( 0.2596705996059036070, -1.501196151453698668, 1.012645528602832856 ) ) ;
#1549=CARTESIAN_POINT ( 'NONE',  ( 0.4477263009981874986, -1.446915290368048224, 0.8103176498262139038 ) ) ;
#1550=CARTESIAN_POINT ( 'NONE',  ( 0.2327167355993654541, -1.504842320349070173, 0.9206877750890873902 ) ) ;
#1552=CARTESIAN_POINT ( 'NONE',  ( 0.06016085808641227078, -0.9698831199938917624, 0.4410261798063859207 ) ) ;
#1554=EDGE_CURVE ( 'NONE', #32680, #3626, #26230, .T. ) ;
#1555=CARTESIAN_POINT ( 'NONE',  ( 0.3702380742285729109, -1.615333040638610385, 0.5482224031604636671 ) ) ;
#1556=CARTESIAN_POINT ( 'NONE',  ( 0.1894921497020525258, -0.4689065141878340226, 0.2178402233697973867 ) ) ;
#1561=CARTESIAN_POINT ( 'NONE',  ( 0.4444209036527600465, -1.039833579653637319, 0.7404771872114588316 ) ) ;
#1567=CARTESIAN_POINT ( 'NONE',  ( 0.4358230120647305084, -1.191225622903871351, 0.6736421652573473251 ) ) ;
#1573=CARTESIAN_POINT ( 'NONE',  ( 0.4856540751714051862, -1.094772563176381830, 0.7053893588296803463 ) ) ;
#1576=VECTOR ( 'NONE', #24035, 39.37007874015748143 ) ;
#1577=CARTESIAN_POINT ( 'NONE',  ( 0.04904889558162006669, -0.8792800190827789741, 0.4846422760073311187 ) ) ;
#1584=CARTESIAN_POINT ( 'NONE',  ( 0.4366927577353089118, -1.195111805554035289, 0.6938221743858382640 ) ) ;
#1588=VERTEX_POINT ( 'NONE', #2741 ) ;
#1590=ORIENTED_EDGE ( 'NONE', *, *, #28286, .F. ) ;
#1591=CARTESIAN_POINT ( 'NONE',  ( 0.1879010291930788001, -0.5477411782657776174, -0.08446770797961487831 ) ) ;
#1592=CARTESIAN_POINT ( 'NONE',  ( 0.3562885538576506250, -1.448602233765710956, 0.8591113950276315636 ) ) ;
#1593=CARTESIAN_POINT ( 'NONE',  ( 0.08794147700442006554, -0.6552000505539613551, 0.02671434475884571294 ) ) ;
#1595=CARTESIAN_POINT ( 'NONE',  ( 0.1338345669307856312, -1.289664158897918078, 0.4854672773588690204 ) ) ;
#1600=CARTESIAN_POINT ( 'NONE',  ( 0.1211351843104187254, -0.5779263820291693499, 0.2644342070444274939 ) ) ;
#1606=CARTESIAN_POINT ( 'NONE',  ( 0.6257246952511709148, -1.577931829754174009, 0.4224971546942883904 ) ) ;
#1608=CARTESIAN_POINT ( 'NONE',  ( 0.1322978751951766341, -1.279211731145868169, 0.4318426636282766129 ) ) ;
#1609=CARTESIAN_POINT ( 'NONE',  ( 0.1889603646001475068, -0.5843802352234823694, 0.2966845687057266812 ) ) ;
#1613=CARTESIAN_POINT ( 'NONE',  ( 0.6712941330769894854, -1.387165532388958678, 0.7909734157804186871 ) ) ;
#1619=CARTESIAN_POINT ( 'NONE',  ( 0.1840595033465176056, -0.8547675690073376353, 0.1457166466292989515 ) ) ;
#1620=CARTESIAN_POINT ( 'NONE',  ( 0.6839214307796153136, -1.445693534907656508, 0.4790777032679445213 ) ) ;
#1633=EDGE_LOOP ( 'NONE', ( #22929, #38455, #14161, #25594 ) ) ;
#1640=CARTESIAN_POINT ( 'NONE',  ( 0.3828956050899013919, -1.120133131850320263, 0.7911315793847942812 ) ) ;
#1643=CARTESIAN_POINT ( 'NONE',  ( 0.4820398931871337500, -1.088803207145679242, 0.6894399345265510570 ) ) ;
#1649=CARTESIAN_POINT ( 'NONE',  ( 0.05844364294462878889, -0.7327107322325441263, 0.5805734399641627741 ) ) ;
#1650=CARTESIAN_POINT ( 'NONE',  ( 0.7040907193196406233, -1.491292208824496424, 0.5118938265934908083 ) ) ;
#1651=CARTESIAN_POINT ( 'NONE',  ( 0.1153571302060458353, -0.4466443244026027659, 0.1507141667401463714 ) ) ;
#1656=CARTESIAN_POINT ( 'NONE',  ( 0.1581650021276241880, -1.285700486175305857, 0.4182417262808778013 ) ) ;
#1659=CARTESIAN_POINT ( 'NONE',  ( 0.4375190507963158115, -1.228364410370137660, 0.5956955845658383764 ) ) ;
#1661=AXIS2_PLACEMENT_3D ( 'NONE', #1295, #17698, #1893 ) ;
#1664=EDGE_CURVE ( 'NONE', #32520, #27730, #38877, .T. ) ;
#1667=CARTESIAN_POINT ( 'NONE',  ( 0.2876584704904820433, -1.030801853274127655, 0.6172218215535044683 ) ) ;
#1669=CARTESIAN_POINT ( 'NONE',  ( 0.3484900513549475942, -1.166308394724161479, 0.4314524459101332643 ) ) ;
#1674=CARTESIAN_POINT ( 'NONE',  ( 0.06449607379900242077, -1.337176272736496419, 0.5902663767274672901 ) ) ;
#1679=CARTESIAN_POINT ( 'NONE',  ( 0.01204616690667267322, -0.4657357789976088180, 0.01148779890123117695 ) ) ;
#1680=CARTESIAN_POINT ( 'NONE',  ( 0.4051926429175483624, -1.104840550354867279, 0.6011831493249744085 ) ) ;
#1681=CARTESIAN_POINT ( 'NONE',  ( 0.3112618463733268781, -1.738655945234965916, 0.7427334498521994677 ) ) ;
#1685=CARTESIAN_POINT ( 'NONE',  ( 0.1764830872386634331, -0.4886048756821292915, 0.1725546913697795504 ) ) ;
#1689=CARTESIAN_POINT ( 'NONE',  ( 0.1347597814052855225, -0.5521900656507784388, 0.1611950669615822840 ) ) ;
#1690=CARTESIAN_POINT ( 'NONE',  ( -0.001169249310984843589, -0.7938970875308333230, 0.02649849479796821672 ) ) ;
#1694=CARTESIAN_POINT ( 'NONE',  ( 0.1787515287242018858, -0.6558014035218070470, 0.6057541867068507724 ) ) ;
#1695=EDGE_LOOP ( 'NONE', ( #23782, #30098, #37718, #33340 ) ) ;
#1698=CARTESIAN_POINT ( 'NONE',  ( 0.1897596718690655326, -1.237814093943444993, 0.5863089767353449888 ) ) ;
#1703=VERTEX_POINT ( 'NONE', #12916 ) ;
#1705=CARTESIAN_POINT ( 'NONE',  ( 0.1744008153849919973, -0.8797694432983949042, 0.5730610230391658400 ) ) ;
#1707=EDGE_CURVE ( 'NONE', #755, #34098, #23755, .T. ) ;
#1708=CARTESIAN_POINT ( 'NONE',  ( 0.1350056248402534687, -0.6996330933666771168, 0.5045168804572850441 ) ) ;
#1710=CARTESIAN_POINT ( 'NONE',  ( 0.5529922410844849701, -1.511190678568866241, 0.5733929733483635882 ) ) ;
#1711=CARTESIAN_POINT ( 'NONE',  ( 0.05177553688007868748, -1.201125113761218666, 0.6644015224960638788 ) ) ;
#1712=CARTESIAN_POINT ( 'NONE',  ( 0.6068955179909718556, -1.480486077813617962, 0.5781976481189164963 ) ) ;
#1721=CARTESIAN_POINT ( 'NONE',  ( -0.0003523642967645715515, -0.9220156720689431928, 0.06121834490154719893 ) ) ;
#1728=CARTESIAN_POINT ( 'NONE',  ( 0.02199361096923483153, -0.8343928545013460374, 0.5934276300867008525 ) ) ;
#1729=CARTESIAN_POINT ( 'NONE',  ( 0.4556897805969272741, -1.061013212638954206, 0.6517789979982376858 ) ) ;
#1731=CARTESIAN_POINT ( 'NONE',  ( 0.6221473432577675489, -1.308691071842436493, 0.8644659521288400317 ) ) ;
#1735=EDGE_CURVE ( 'NONE', #36909, #24607, #37427, .T. ) ;
#1738=CARTESIAN_POINT ( 'NONE',  ( 0.3110797536664995366, -1.761551355401022700, 0.5692323052624194135 ) ) ;
#1740=VERTEX_POINT ( 'NONE', #4250 ) ;
#1742=CARTESIAN_POINT ( 'NONE',  ( 0.1259012050209226963, -1.123654620964547934, 0.8919649897266007654 ) ) ;
#1746=CARTESIAN_POINT ( 'NONE',  ( 0.06450940144326640369, -1.331203771656425561, 0.5682439549991663563 ) ) ;
#1747=B_SPLINE_CURVE_WITH_KNOTS ( 'NONE', 3,
 ( #30685, #33971, #27192, #26977, #39513, #20618 ),
 .UNSPECIFIED., .F., .F.,
 ( 4, 2, 4 ),
 ( 0.000000000000000000, 0.5000000000000000000, 1.000000000000000000 ),
 .UNSPECIFIED. ) ;
#1748=CARTESIAN_POINT ( 'NONE',  ( 0.6179353394495007423, -1.299228382567916285, 0.5682417262808777680 ) ) ;
#1750=EDGE_LOOP ( 'NONE', ( #8435, #16528, #28992, #34357 ) ) ;
#1753=FACE_BOUND ( 'NONE', #18113, .T. ) ;
#1754=CARTESIAN_POINT ( 'NONE',  ( 0.5660458073529762713, -1.502436908615445210, 0.5399521221014897954 ) ) ;
#1758=CARTESIAN_POINT ( 'NONE',  ( 0.1831772843670138040, -1.238081160791867585, 0.5906532873403225192 ) ) ;
#1759=CARTESIAN_POINT ( 'NONE',  ( 0.1200222707058349603, -0.7080646023026895275, 0.4423028072555330592 ) ) ;
#1760=CARTESIAN_POINT ( 'NONE',  ( 0.1261966868762690042, -0.9842092163644554637, 0.9331960565778399941 ) ) ;
#1761=CARTESIAN_POINT ( 'NONE',  ( 0.09811070749329325880, -0.5560036527972357367, 0.2112130360183118449 ) ) ;
#1762=CARTESIAN_POINT ( 'NONE',  ( 0.2276870189180398851, -1.487426405742815261, 0.9274550246884837312 ) ) ;
#1763=CARTESIAN_POINT ( 'NONE',  ( 0.1614670899430008522, -0.7569536277469717245, 0.1022936816274460647 ) ) ;
#1764=CARTESIAN_POINT ( 'NONE',  ( 0.09375000000000006939, -0.9316581899787153009, 0.1457185332388701571 ) ) ;
#1770=CARTESIAN_POINT ( 'NONE',  ( 0.1207008425007928681, -0.4921100478383975685, 0.3258471659695452161 ) ) ;
#1771=EDGE_CURVE ( 'NONE', #6171, #3151, #4037, .T. ) ;
#1773=CARTESIAN_POINT ( 'NONE',  ( 0.3690965330173307524, -1.099411688709415413, 0.5182417262812423209 ) ) ;
#1778=CARTESIAN_POINT ( 'NONE',  ( 0.5633629393321837320, -1.208205391268785567, 0.7270432621192387534 ) ) ;
#1787=CARTESIAN_POINT ( 'NONE',  ( 0.3880044884704604846, -0.9770951376028897961, 0.6894504840255317735 ) ) ;
#1790=CARTESIAN_POINT ( 'NONE',  ( 0.1759864516496214559, -1.107502683655886555, 0.7499173190827560509 ) ) ;
#1794=CARTESIAN_POINT ( 'NONE',  ( 0.1949582633045185420, -1.370042541011457837, 0.4186407401730019018 ) ) ;
#1796=CARTESIAN_POINT ( 'NONE',  ( 0.4667596051884817521, -1.235694863872689897, 0.6085114794545928296 ) ) ;
#1804=CARTESIAN_POINT ( 'NONE',  ( 0.06137814430738681298, -0.5595901097020826720, 0.2438590846621483677 ) ) ;
#1805=CARTESIAN_POINT ( 'NONE',  ( 0.08985841505820577058, -0.5644647999051150000, 0.1403608567123640904 ) ) ;
#1811=CARTESIAN_POINT ( 'NONE',  ( 0.5739652476806176296, -1.499266104267773736, 0.5740897328662426524 ) ) ;
#1816=CARTESIAN_POINT ( 'NONE',  ( 0.1931523484426772019, -1.244006994361245511, 0.4502174690324191042 ) ) ;
#1817=CARTESIAN_POINT ( 'NONE',  ( 0.07550925375975386933, -1.312278240014781661, 0.4838115075940697118 ) ) ;
#1819=CARTESIAN_POINT ( 'NONE',  ( 0.2114022633412600827, -0.5658596150412534831, 0.4491712673773823883 ) ) ;
#1825=FACE_OUTER_BOUND ( 'NONE', #35829, .T. ) ;
#1827=CARTESIAN_POINT ( 'NONE',  ( 0.3053298862878815467, -1.679825167650452089, 0.8905181393053133165 ) ) ;
#1830=CARTESIAN_POINT ( 'NONE',  ( 0.4677164644732115795, -1.686000531315665407, 0.5767158751130112559 ) ) ;
#1832=ORIENTED_EDGE ( 'NONE', *, *, #38175, .F. ) ;
#1835=CARTESIAN_POINT ( 'NONE',  ( 0.05579155178881651383, -1.335540925555324332, 0.3667417262808778111 ) ) ;
#1836=EDGE_LOOP ( 'NONE', ( #37686, #13941, #13062, #14876, #26572, #22028 ) ) ;
#1838=CARTESIAN_POINT ( 'NONE',  ( 0.5092908111800726889, -1.308897765795846713, 0.6930370963245210403 ) ) ;
#1841=CARTESIAN_POINT ( 'NONE',  ( 0.4299297405268334149, -1.031605064505895619, 0.6882246241152528698 ) ) ;
#1844=CARTESIAN_POINT ( 'NONE',  ( 0.3224042817241155601, -1.181557111677860705, 0.5668948776571440806 ) ) ;
#1845=ORIENTED_EDGE ( 'NONE', *, *, #8517, .F. ) ;
#1846=CARTESIAN_POINT ( 'NONE',  ( 0.3083011426979856973, -1.561450148453558118, 0.8343410752513801265 ) ) ;
#1847=CARTESIAN_POINT ( 'NONE',  ( 0.6949609426117219213, -1.492559866762042331, 0.4793319850971706209 ) ) ;
#1849=CARTESIAN_POINT ( 'NONE',  ( 0.3208715077212234701, -1.182672892261233732, 0.4687417262808780127 ) ) ;
#1855=CARTESIAN_POINT ( 'NONE',  ( 0.1552519097254527192, -0.9561661948719739623, 0.6628835997166871996 ) ) ;
#1862=CARTESIAN_POINT ( 'NONE',  ( 0.4199258674957010995, -1.127834923126881606, 0.4949619196504369545 ) ) ;
#1865=CARTESIAN_POINT ( 'NONE',  ( 0.002683297570301478637, -0.9564051229508913066, 0.3926252623119886875 ) ) ;
#1866=CARTESIAN_POINT ( 'NONE',  ( 0.4475625759263253678, -1.247751609582666843, 0.6057417262809817737 ) ) ;
#1867=VECTOR ( 'NONE', #4494, 39.37007874015748854 ) ;
#1872=CARTESIAN_POINT ( 'NONE',  ( 0.0004750074233420679450, -0.4386152179651120475, 0.1512205247030782573 ) ) ;
#1874=VERTEX_POINT ( 'NONE', #4841 ) ;
#1875=EDGE_CURVE ( 'NONE', #24616, #4342, #9961, .T. ) ;
#1876=VERTEX_POINT ( 'NONE', #17413 ) ;
#1877=CARTESIAN_POINT ( 'NONE',  ( 0.1903419785339184878, -0.5326379394093359032, 0.2481619417568516339 ) ) ;
#1880=EDGE_CURVE ( 'NONE', #2643, #40111, #16828, .T. ) ;
#1881=CARTESIAN_POINT ( 'NONE',  ( 0.3434118854289890943, -1.064821506014568708, 0.7872763406766211114 ) ) ;
#1884=CARTESIAN_POINT ( 'NONE',  ( 0.007864899693521575086, -0.7290558150142686378, -0.007045877879649726193 ) ) ;
#1888=CARTESIAN_POINT ( 'NONE',  ( 0.3175383896200173472, -1.184309477189361415, 0.5626414999152751228 ) ) ;
#1890=CARTESIAN_POINT ( 'NONE',  ( 0.2711658269972071489, -1.669704017044846278, 0.6768845942166327179 ) ) ;
#1892=CARTESIAN_POINT ( 'NONE',  ( 0.1507440847924569616, -1.242487625469949952, 0.6036539243957432799 ) ) ;
#1893=DIRECTION ( 'NONE',  ( 0.8660512985181134660, 0.4999551463232372872, 0.000000000000000000 ) ) ;
#1898=CARTESIAN_POINT ( 'NONE',  ( 0.01147012505024846800, -0.8931644348827614266, -0.01216302941885656977 ) ) ;
#1899=CARTESIAN_POINT ( 'NONE',  ( 0.1186103394390872201, -1.414144848331978510, 0.5683298932114988489 ) ) ;
#1900=CARTESIAN_POINT ( 'NONE',  ( 0.07548269292739374914, -0.5857035475933982660, 0.3081389644222882196 ) ) ;
#1904=CARTESIAN_POINT ( 'NONE',  ( 0.05990572404004890911, -1.332677842034995397, 0.5606126620464084720 ) ) ;
#1906=LINE ( 'NONE', #32944, #29878 ) ;
#1911=CARTESIAN_POINT ( 'NONE',  ( 0.4183850207828535006, -1.104805702410075030, 0.5963159008084065738 ) ) ;
#1914=CARTESIAN_POINT ( 'NONE',  ( 0.1180550382625277506, -1.031362315377588157, 0.9291368297579983837 ) ) ;
#1915=CARTESIAN_POINT ( 'NONE',  ( 0.3170172301852910435, -0.9601440561661597206, 0.5902234374070133294 ) ) ;
#1917=CARTESIAN_POINT ( 'NONE',  ( 0.4045891740076953402, -0.9484829520717948936, 0.8148132024759134895 ) ) ;
#1920=EDGE_CURVE ( 'NONE', #38229, #35870, #10603, .T. ) ;
#1923=CARTESIAN_POINT ( 'NONE',  ( 0.05974118262646924138, -0.8876447553630215648, 0.7647173577216134222 ) ) ;
#1924=EDGE_CURVE ( 'NONE', #18554, #15872, #4049, .T. ) ;
#1925=CARTESIAN_POINT ( 'NONE',  ( 0.2006210498355077976, -1.239694361563377534, 0.4577691556116682547 ) ) ;
#1931=CARTESIAN_POINT ( 'NONE',  ( 0.5718426945711908571, -1.221126421150759755, 0.7198242229513793777 ) ) ;
#1935=( BOUNDED_SURFACE ( )  B_SPLINE_SURFACE ( 2, 3, ( 
 ( #1866, #24474, #30441, #21183, #20794, #21407, #36613, #40293, #26946, #30220, #2268, #14809, #27372, #33942, #33315 ),
 ( #5121, #39478, #30838, #5742, #14588, #27156, #11523, #11718, #24275, #15201, #27760, #36798, #8608, #23668, #5531 ),
 ( #25292, #31653, #28775, #6745, #24691, #3078, #18492, #25077, #12125, #37222, #28574, #37832, #21795, #40509, #37611 ),
 ( #34329, #18919, #6140, #2865, #15413, #28169, #27970, #34940, #19115, #3474, #15621, #9648, #9435, #6347, #28365 ),
 ( #9040, #31861, #21602, #12332, #16029, #31263, #5927, #33, #22013, #6539, #19323, #34125, #24889, #451, #34538 ) ),
 .UNSPECIFIED., .F., .F., .F. ) 
 B_SPLINE_SURFACE_WITH_KNOTS ( ( 3, 2, 3 ),
 ( 4, 3, 2, 2, 2, 2, 4 ),
 ( -0.01000000000000000021, 0.000000000000000000, 1.000000000000000000 ),
 ( -0.2248845959520953119, -0.1024158528858618994, -0.002066484013594062884, 0.001425941394020094344, 0.9981093185551406233, 1.001427204709084418, 1.101776573581352281 ),
 .UNSPECIFIED. ) 
 GEOMETRIC_REPRESENTATION_ITEM ( )  RATIONAL_B_SPLINE_SURFACE ( (
 ( 1.000000000000000000, 1.000000000000000000, 1.000000000000000000, 1.000000000000000000, 1.000000000000000000, 1.000000000000000000, 1.000000000000000000, 1.000000000000000000, 1.000000000000000000, 1.000000000000000000, 1.000000000000000000, 1.000000000000000000, 1.000000000000000000, 1.000000000000000000, 1.000000000000000000),
 ( 1.000000000000000000, 1.000000000000000000, 1.000000000000000000, 1.000000000000000000, 1.000000000000000000, 1.000000000000000000, 1.000000000000000000, 1.000000000000000000, 1.000000000000000000, 1.000000000000000000, 1.000000000000000000, 1.000000000000000000, 1.000000000000000000, 1.000000000000000000, 1.000000000000000000),
 ( 1.000000000000000000, 1.000000000000000000, 1.000000000000000000, 1.000000000000000000, 1.000000000000000000, 1.000000000000000000, 1.000000000000000000, 1.000000000000000000, 1.000000000000000000, 1.000000000000000000, 1.000000000000000000, 1.000000000000000000, 1.000000000000000000, 1.000000000000000000, 1.000000000000000000),
 ( 0.7063388106193552174, 0.7063388106193552174, 0.7063388106193552174, 0.7063388106193552174, 0.7063388106193552174, 0.7063388106193546623, 0.7063388106193546623, 0.7063388106193546623, 0.7063388106193546623, 0.7063388106193546623, 0.7063388106193546623, 0.7063388106193552174, 0.7063388106193552174, 0.7063388106193552174, 0.7063388106193552174),
 ( 1.000000000000000000, 1.000000000000000000, 1.000000000000000000, 1.000000000000000000, 1.000000000000000000, 1.000000000000000000, 1.000000000000000000, 1.000000000000000000, 1.000000000000000000, 1.000000000000000000, 1.000000000000000000, 1.000000000000000000, 1.000000000000000000, 1.000000000000000000, 1.000000000000000000) ) ) 
 REPRESENTATION_ITEM ( '' )  SURFACE ( )  );
#1938=CARTESIAN_POINT ( 'NONE',  ( 0.5640895105453352931, -1.503407492374277510, 0.5358556994421860287 ) ) ;
#1941=ORIENTED_EDGE ( 'NONE', *, *, #6752, .F. ) ;
#1942=CARTESIAN_POINT ( 'NONE',  ( 0.1091017126209868487, -1.269603009439766339, 0.6006954958647061638 ) ) ;
#1943=CARTESIAN_POINT ( 'NONE',  ( 0.1981269588659515801, -0.8717101755341865044, 0.6257585543226611424 ) ) ;
#1944=CARTESIAN_POINT ( 'NONE',  ( 0.3109746253762922796, -1.659824283146108748, 0.9017776097172691685 ) ) ;
#1945=CARTESIAN_POINT ( 'NONE',  ( 0.1509521914015893862, -0.7534614311450832380, 0.5756042479487297747 ) ) ;
#1946=CARTESIAN_POINT ( 'NONE',  ( 0.5923833459584677552, -1.600710257484702970, 0.4291951338990673825 ) ) ;
#1949=CARTESIAN_POINT ( 'NONE',  ( 0.06950777349364366253, -1.183310629122789503, 0.6632153050984169740 ) ) ;
#1953=CARTESIAN_POINT ( 'NONE',  ( 0.3545037818611191383, -0.8523828408883230567, 0.7589984277719855621 ) ) ;
#1957=CARTESIAN_POINT ( 'NONE',  ( 0.08352889633857743523, -1.314305457479380879, 0.4727645997108643749 ) ) ;
#1958=B_SPLINE_CURVE_WITH_KNOTS ( 'NONE', 3,
 ( #24339, #9293, #9509, #15073, #6000, #27438, #8900, #36868, #21662, #30713, #21258, #12587, #34608, #24946, #40155, #18782, #27830, #6411, #33996, #2729, #31335, #34400, #6214, #5801, #8683, #21872, #33795, #37688, #30906, #34189, #30507, #18359, #3139, #18567, #5602, #2338, #15680, #15276, #14877, #39962, #31121, #2535, #15492, #25149, #2935, #12198, #28043, #11985 ),
 .UNSPECIFIED., .F., .F.,
 ( 4, 2, 2, 2, 2, 2, 2, 2, 2, 2, 2, 2, 2, 2, 2, 2, 2, 2, 2, 2, 2, 2, 2, 4 ),
 ( 0.004590105785999735490, 0.006718271026485181721, 0.008846436266970628820, 0.01097460150745607765, 0.01310276674794152649, 0.01523093198842697185, 0.01735909722891242069, 0.01948726246939787299, 0.02161542770988332182, 0.02374359295036877066, 0.02587175819085422296, 0.02693584081109693870, 0.02799992343133965791, 0.03012808867182510675, 0.03119217129206782249, 0.03225625391231053823, 0.03332033653255325745, 0.03385237784267460665, 0.03438441915279595584, 0.03544850177303865424, 0.03651258439328135263, 0.03757666701352405797, 0.03810870832364541411, 0.03864074963376676330 ),
 .UNSPECIFIED. ) ;
#1960=CARTESIAN_POINT ( 'NONE',  ( 0.1087663190456345796, -1.420020949109092934, 0.5260726173889570534 ) ) ;
#1961=CARTESIAN_POINT ( 'NONE',  ( 0.2980752164830456907, -0.8471807121723260448, 0.6106271213134966125 ) ) ;
#1965=ORIENTED_EDGE ( 'NONE', *, *, #30859, .T. ) ;
#1966=CARTESIAN_POINT ( 'NONE',  ( 0.4257416900749242394, -1.216787901257387228, 0.6459620410871801388 ) ) ;
#1970=CARTESIAN_POINT ( 'NONE',  ( 0.3826582672041143329, -0.9717923329141301414, 0.6844662983072338225 ) ) ;
#1973=CARTESIAN_POINT ( 'NONE',  ( 0.2085758075447457227, -1.314883828705479152, 0.6759879400794416293 ) ) ;
#1975=CARTESIAN_POINT ( 'NONE',  ( 0.1904911882605962448, -1.371587248428298045, 0.5682417262808803216 ) ) ;
#1979=CARTESIAN_POINT ( 'NONE',  ( 0.4441119490203502829, -1.203454984316005616, 0.6735005572665853091 ) ) ;
#1981=CARTESIAN_POINT ( 'NONE',  ( 0.6540709664215760277, -1.593060928864740156, 0.5182417262812423209 ) ) ;
#1988=CARTESIAN_POINT ( 'NONE',  ( 0.2106021162434502936, -1.038359553320539419, 0.8169558973072331698 ) ) ;
#1989=CARTESIAN_POINT ( 'NONE',  ( 0.7011468811679719693, -1.538227936001232088, 0.5810316690295218578 ) ) ;
#1991=CARTESIAN_POINT ( 'NONE',  ( 0.5667833376006989887, -1.501841640556043744, 0.4952036213288417144 ) ) ;
#1994=ORIENTED_EDGE ( 'NONE', *, *, #1707, .F. ) ;
#1995=EDGE_CURVE ( 'NONE', #21929, #1211, #18798, .T. ) ;
#1997=CARTESIAN_POINT ( 'NONE',  ( 0.1230184117381799835, -0.5703923235244722223, 0.2416267668379052103 ) ) ;
#1998=ORIENTED_EDGE ( 'NONE', *, *, #30675, .F. ) ;
#1999=CARTESIAN_POINT ( 'NONE',  ( 0.3304338600317479613, -1.765066422999553186, 0.5534862069867115819 ) ) ;
#2001=CARTESIAN_POINT ( 'NONE',  ( 0.6008383320827431762, -1.595119844626816885, 0.4182417262808776903 ) ) ;
#2002=CARTESIAN_POINT ( 'NONE',  ( 0.09068171474054860515, -1.314855571806884615, 0.4630352297835350073 ) ) ;
#2004=CARTESIAN_POINT ( 'NONE',  ( 0.07070506769835151195, -1.314942671243113814, 0.5018317509599571347 ) ) ;
#2006=CARTESIAN_POINT ( 'NONE',  ( 0.1927581100858387075, -0.5042345029781482024, 0.3213135115051561908 ) ) ;
#2009=CARTESIAN_POINT ( 'NONE',  ( 0.01128729522873549510, -0.9461985897320858152, 0.1457185332388702959 ) ) ;
#2012=FACE_OUTER_BOUND ( 'NONE', #1439, .T. ) ;
#2014=CARTESIAN_POINT ( 'NONE',  ( 0.1536596445529301580, -1.277574755431481135, 0.4245438548657214928 ) ) ;
#2015=CARTESIAN_POINT ( 'NONE',  ( -3.414809992080329023E-17, -0.4300901116921415634, 0.2008512132480425316 ) ) ;
#2021=CARTESIAN_POINT ( 'NONE',  ( 0.4089992519647981384, -1.131314579718122992, 0.3157417262808777658 ) ) ;
#2022=CARTESIAN_POINT ( 'NONE',  ( 0.1316017208954911588, -1.248059642665102942, 0.5182417262812423209 ) ) ;
#2024=CARTESIAN_POINT ( 'NONE',  ( 0.5185792659196485355, -1.323880597841234241, 0.6352211934613883892 ) ) ;
#2028=CARTESIAN_POINT ( 'NONE',  ( 0.4978751173634345939, -1.107738205778658669, 0.6841874689585324409 ) ) ;
#2031=CARTESIAN_POINT ( 'NONE',  ( 0.01041333297898627656, -0.5306758790526455716, 0.1248763267698726892 ) ) ;
#2032=AXIS2_PLACEMENT_3D ( 'NONE', #7969, #14551, #4482 ) ;
#2033=CARTESIAN_POINT ( 'NONE',  ( 0.3500362837767272972, -1.585416944253276172, 0.7709133781444270639 ) ) ;
#2034=CARTESIAN_POINT ( 'NONE',  ( 0.7066443439621657996, -1.495287734631166598, 0.5281105036456856805 ) ) ;
#2035=CARTESIAN_POINT ( 'NONE',  ( 0.1870390274204316861, -0.5985361199501452178, 0.003541061305677496631 ) ) ;
#2041=CARTESIAN_POINT ( 'NONE',  ( 0.1142242363313231979, -0.8822466011666808550, 0.5261702761697892861 ) ) ;
#2045=CARTESIAN_POINT ( 'NONE',  ( 0.3865105166509632539, -1.105244162432096999, 0.6295132537179397580 ) ) ;
#2046=CARTESIAN_POINT ( 'NONE',  ( 0.3067120372624415614, -1.770199942203851240, 0.4177417262808785781 ) ) ;
#2047=CARTESIAN_POINT ( 'NONE',  ( 0.3433891623868345344, -1.169237029733195543, 0.4282016284639145742 ) ) ;
#2051=CARTESIAN_POINT ( 'NONE',  ( 0.05360726000536972929, -1.265335673192477639, 0.6608739414109141563 ) ) ;
#2066=CARTESIAN_POINT ( 'NONE',  ( 0.009065448934498832739, -0.6074849142585841966, 0.009116045154335344555 ) ) ;
#2070=EDGE_LOOP ( 'NONE', ( #34144, #33477, #18552, #6853, #4350, #3277, #10660 ) ) ;
#2071=CARTESIAN_POINT ( 'NONE',  ( -0.001578457898017553238, -0.5340257668161403348, 0.1971401768889480544 ) ) ;
#2072=CARTESIAN_POINT ( 'NONE',  ( 0.5908512823694407334, -1.601569576941602957, 0.4282615004916613399 ) ) ;
#2073=CARTESIAN_POINT ( 'NONE',  ( 0.1470252489180754740, -1.243555166057507932, 0.6044257298140193191 ) ) ;
#2078=ORIENTED_EDGE ( 'NONE', *, *, #26556, .T. ) ;
#2080=CARTESIAN_POINT ( 'NONE',  ( 0.3431906593882065315, -1.156341550885930491, 0.6074911006494660981 ) ) ;
#2081=CARTESIAN_POINT ( 'NONE',  ( 0.2137282995058389923, -1.231963470009917128, 0.5563255107610510786 ) ) ;
#2082=CARTESIAN_POINT ( 'NONE',  ( 0.1924812274689710334, -0.8175909794505628048, 0.6368276176361362673 ) ) ;
#2085=CARTESIAN_POINT ( 'NONE',  ( 0.1871597835675367083, -0.7100598730055870389, 0.03076398055866989140 ) ) ;
#2087=CARTESIAN_POINT ( 'NONE',  ( 0.3211374802916291959, -1.297362887257381026, 0.4402873239467990918 ) ) ;
#2090=CARTESIAN_POINT ( 'NONE',  ( 0.3837046737290842335, -1.723330870051356767, 0.4227126563901177358 ) ) ;
#2094=CARTESIAN_POINT ( 'NONE',  ( 0.4314229567236929630, -1.111443131039648868, 0.6061934567595625989 ) ) ;
#2099=CARTESIAN_POINT ( 'NONE',  ( 0.2190338188766751681, -1.487106827364948147, 0.9008211596871106286 ) ) ;
#2100=CARTESIAN_POINT ( 'NONE',  ( 0.4790383449168201802, -1.075084602395082634, 0.6124719440393814329 ) ) ;
#2101=CARTESIAN_POINT ( 'NONE',  ( 0.02769007923577383040, -0.9640067030880757892, 0.6504839076559877364 ) ) ;
#2103=CARTESIAN_POINT ( 'NONE',  ( 0.4504805333218593333, -1.026900667268108469, 0.8467065612799143937 ) ) ;
#2109=AXIS2_PLACEMENT_3D ( 'NONE', #5302, #24081, #30642 ) ;
#2115=CARTESIAN_POINT ( 'NONE',  ( 0.004217272053185415481, -0.5691354127735893664, 0.3239988763902699742 ) ) ;
#2117=CARTESIAN_POINT ( 'NONE',  ( 0.5553811761775682143, -1.443364489385942306, 0.7462368593144907969 ) ) ;
#2119=CARTESIAN_POINT ( 'NONE',  ( 0.3204479958614548929, -1.182666560659948907, 0.5682417262808776570 ) ) ;
#2122=CARTESIAN_POINT ( 'NONE',  ( 0.1963745812722482442, -0.6060194383687296238, 0.2878283022669332891 ) ) ;
#2124=EDGE_LOOP ( 'NONE', ( #13708, #37503, #35908, #38126 ) ) ;
#2126=ORIENTED_EDGE ( 'NONE', *, *, #15191, .T. ) ;
#2133=CARTESIAN_POINT ( 'NONE',  ( 0.1125212918553140234, -0.7619884966536627502, 0.4061142703594107228 ) ) ;
#2134=CARTESIAN_POINT ( 'NONE',  ( 0.2800970862558492813, -1.537244030595081856, 0.9925064799805612958 ) ) ;
#2135=CARTESIAN_POINT ( 'NONE',  ( 0.4968737439736803374, -1.542313245617131345, 0.5635433591466190162 ) ) ;
#2138=CARTESIAN_POINT ( 'NONE',  ( 0.01879405481382893928, -0.9579227845311485412, 0.3482156429045401569 ) ) ;
#2144=CARTESIAN_POINT ( 'NONE',  ( 0.3038869664936152959, -0.7554869697991318800, 0.6839101067327857386 ) ) ;
#2155=EDGE_CURVE ( 'NONE', #39497, #33041, #35155, .T. ) ;
#2156=CARTESIAN_POINT ( 'NONE',  ( 0.3085271267949294960, -1.189394089994698867, 0.5261560657346352476 ) ) ;
#2157=CARTESIAN_POINT ( 'NONE',  ( 0.5231597928089396499, -1.148848539795074508, 0.7464108937515090414 ) ) ;
#2169=CARTESIAN_POINT ( 'NONE',  ( 0.2080690969106096522, -0.8521148724087993509, 0.3830115466634239074 ) ) ;
#2170=AXIS2_PLACEMENT_3D ( 'NONE', #14577, #11708, #27149 ) ;
#2171=CARTESIAN_POINT ( 'NONE',  ( 0.08509462338391231284, -0.8106601328590971045, 0.1993838098214128496 ) ) ;
#2172=CARTESIAN_POINT ( 'NONE',  ( 0.2220010284085898178, -1.342657189645787064, 0.6229336649678032245 ) ) ;
#2181=CARTESIAN_POINT ( 'NONE',  ( 0.4436287470858775728, -1.200807317510819372, 0.6564808803850732399 ) ) ;
#2186=CARTESIAN_POINT ( 'NONE',  ( 0.07298619815556110779, -1.313484934506050417, 0.5462077094077502082 ) ) ;
#2190=CARTESIAN_POINT ( 'NONE',  ( 0.06121954705759836968, -0.5575974508628280812, 0.2378852839864381008 ) ) ;
#2194=CARTESIAN_POINT ( 'NONE',  ( 0.5602799925893692246, -1.505597493397644149, 0.5182417262812344383 ) ) ;
#2198=CARTESIAN_POINT ( 'NONE',  ( 0.2691130962247216263, -0.9494530259878606326, 0.7322442259066408443 ) ) ;
#2199=CARTESIAN_POINT ( 'NONE',  ( 0.5779297624755960205, -1.623152544610868109, 0.5629341535590222101 ) ) ;
#2201=EDGE_CURVE ( 'NONE', #35465, #5749, #6210, .T. ) ;
#2209=CARTESIAN_POINT ( 'NONE',  ( 0.3073438066573006555, -0.7730596496961650299, 0.7003458109913517360 ) ) ;
#2213=CARTESIAN_POINT ( 'NONE',  ( -2.194512287980899339E-05, -0.9481927139106636204, 0.1806018079512390906 ) ) ;
#2216=DIRECTION ( 'NONE',  ( -0.8593916653663324912, 0.5113178712883813537, 0.000000000000000000 ) ) ;
#2217=CARTESIAN_POINT ( 'NONE',  ( 0.5775767250843619749, -1.612202439891691652, 0.5714792215281596643 ) ) ;
#2223=CARTESIAN_POINT ( 'NONE',  ( 0.01054327228848483088, -0.5372198261166355460, 0.4758561573974433023 ) ) ;
#2225=EDGE_CURVE ( 'NONE', #3536, #15736, #37612, .T. ) ;
#2226=CARTESIAN_POINT ( 'NONE',  ( 0.1415875073431126230, -1.284922281152920398, 0.5547766581037201217 ) ) ;
#2227=CARTESIAN_POINT ( 'NONE',  ( 0.6008383320827377361, -1.595119844626803562, 0.4182417262808777458 ) ) ;
#2231=CARTESIAN_POINT ( 'NONE',  ( 0.3611552640280384363, -1.125445538258061928, 0.6035644152996554324 ) ) ;
#2234=CARTESIAN_POINT ( 'NONE',  ( 0.4557618173848551058, -1.227332695086565506, 0.7391538672619316630 ) ) ;
#2237=CARTESIAN_POINT ( 'NONE',  ( 0.4302506758624459748, -1.041368148273517313, 0.6535113357015974733 ) ) ;
#2238=ORIENTED_EDGE ( 'NONE', *, *, #1554, .F. ) ;
#2239=B_SPLINE_CURVE_WITH_KNOTS ( 'NONE', 3,
 ( #30247, #33529, #24504, #5339 ),
 .UNSPECIFIED., .F., .F.,
 ( 4, 4 ),
 ( 5.011996131622145663E-14, 7.281930351775003953E-08 ),
 .UNSPECIFIED. ) ;
#2242=DIRECTION ( 'NONE',  ( 0.8660512985181135770, 0.4999551463232369541, 0.000000000000000000 ) ) ;
#2245=CARTESIAN_POINT ( 'NONE',  ( 0.03562778247724820296, -0.5379013666131609028, 0.1838651273310172585 ) ) ;
#2246=CARTESIAN_POINT ( 'NONE',  ( 0.6651013997919192899, -1.542812421080071550, 0.4323470902494797041 ) ) ;
#2250=CARTESIAN_POINT ( 'NONE',  ( 0.4893086098151709362, -1.099159724303276020, 0.7026458958596925042 ) ) ;
#2251=VERTEX_POINT ( 'NONE', #27589 ) ;
#2255=CARTESIAN_POINT ( 'NONE',  ( 0.1107380495411959126, -0.8768048433569302080, 0.5086585179081277719 ) ) ;
#2260=CARTESIAN_POINT ( 'NONE',  ( 0.2467884284475332646, -1.005975727473770398, 0.5856700373633461076 ) ) ;
#2261=CARTESIAN_POINT ( 'NONE',  ( 0.3077938761450154104, -1.772073966255670596, 0.3667417262808779777 ) ) ;
#2263=CARTESIAN_POINT ( 'NONE',  ( 0.1852697686925744991, -0.8388888312570772499, 0.1465813977937011903 ) ) ;
#2264=CARTESIAN_POINT ( 'NONE',  ( 0.03259135683726806926, -1.157323147438684030, 0.6652026314908382476 ) ) ;
#2267=CARTESIAN_POINT ( 'NONE',  ( 0.4403554762574504733, -1.137327559350066242, 0.4417353236092321778 ) ) ;
#2268=CARTESIAN_POINT ( 'NONE',  ( 0.5535797480692251638, -1.186549887580578444, 0.6057417262809811076 ) ) ;
#2272=CARTESIAN_POINT ( 'NONE',  ( 2.161549057781019548E-05, -0.4383321693235875394, 0.06536088093990558012 ) ) ;
#2274=LINE ( 'NONE', #33946, #25825 ) ;
#2275=CARTESIAN_POINT ( 'NONE',  ( 0.3587298685345038929, -1.621939747702046297, 0.4817067625245350371 ) ) ;
#2278=ORIENTED_EDGE ( 'NONE', *, *, #20859, .T. ) ;
#2281=VERTEX_POINT ( 'NONE', #37252 ) ;
#2285=CARTESIAN_POINT ( 'NONE',  ( 0.007248405253956994622, -0.7849820093401896903, 0.02096406129000137619 ) ) ;
#2286=ORIENTED_EDGE ( 'NONE', *, *, #37409, .T. ) ;
#2289=ORIENTED_EDGE ( 'NONE', *, *, #18541, .F. ) ;
#2290=CARTESIAN_POINT ( 'NONE',  ( -0.001589221141236483482, -0.5299580663956803273, 0.1754197759787374244 ) ) ;
#2300=CARTESIAN_POINT ( 'NONE',  ( 0.2209893336501091432, -1.227886349168061386, 0.5261107291778043260 ) ) ;
#2301=AXIS2_PLACEMENT_3D ( 'NONE', #35795, #26548, #32703 ) ;
#2302=CARTESIAN_POINT ( 'NONE',  ( 0.2002263348979474444, -0.8551021424006158833, 0.6387041187184567814 ) ) ;
#2303=CARTESIAN_POINT ( 'NONE',  ( 0.1856764667174918837, -0.8115940886088498507, 0.08463465656060843723 ) ) ;
#2304=FACE_OUTER_BOUND ( 'NONE', #14277, .T. ) ;
#2311=CARTESIAN_POINT ( 'NONE',  ( 0.3077938761450154104, -1.772073966255670596, 0.3667417262808779777 ) ) ;
#2312=CARTESIAN_POINT ( 'NONE',  ( -1.316612518408581027E-05, -0.9424504616873518037, 0.09060630441213164687 ) ) ;
#2316=CARTESIAN_POINT ( 'NONE',  ( 0.07933644511000853550, -0.9611106349790075054, 0.8249633512138372371 ) ) ;
#2317=CARTESIAN_POINT ( 'NONE',  ( 0.03393842632515668700, -0.9998690014380283708, 0.6797094769501190736 ) ) ;
#2319=CARTESIAN_POINT ( 'NONE',  ( 0.5091714098097919194, -1.126742604313814677, 0.8493738626068785269 ) ) ;
#2322=CARTESIAN_POINT ( 'NONE',  ( 0.4115766028365042128, -1.733048369835246794, 0.5182417262812423209 ) ) ;
#2325=CARTESIAN_POINT ( 'NONE',  ( 0.5264113014007820723, -1.640729993778254014, 0.5682417262808777680 ) ) ;
#2329=CARTESIAN_POINT ( 'NONE',  ( 0.07864456654739519770, -0.9658104792752110201, 0.8218898466748431053 ) ) ;
#2330=CARTESIAN_POINT ( 'NONE',  ( 0.5385340078061969793, -1.420402263057676695, 0.7715738128166309551 ) ) ;
#2335=CARTESIAN_POINT ( 'NONE',  ( 0.2889710164712426255, -0.7847915145120791802, 0.6224945701162477585 ) ) ;
#2338=CARTESIAN_POINT ( 'NONE',  ( 0.6738503551975361106, -1.390429358051159081, 0.7373033579730302600 ) ) ;
#2343=ORIENTED_EDGE ( 'NONE', *, *, #10360, .T. ) ;
#2344=CARTESIAN_POINT ( 'NONE',  ( 0.2214974906291148626, -0.9030582019982653641, 0.6599196580771191645 ) ) ;
#2346=CARTESIAN_POINT ( 'NONE',  ( 0.4988733860125649788, -1.542123411666028732, 0.6032420550392955105 ) ) ;
#2347=CARTESIAN_POINT ( 'NONE',  ( -0.001106909109950914580, -0.7985540816996060665, 0.01933639101178150771 ) ) ;
#2348=CARTESIAN_POINT ( 'NONE',  ( 0.0007702871825654963910, -0.9531316724789442585, 0.2767708779485607562 ) ) ;
#2352=CARTESIAN_POINT ( 'NONE',  ( 0.3612790108085988106, -0.8653713489192644825, 0.7675946798073856048 ) ) ;
#2362=CARTESIAN_POINT ( 'NONE',  ( 0.3119755472902833726, -1.175847033624922489, 0.5195546043588886720 ) ) ;
#2363=CARTESIAN_POINT ( 'NONE',  ( 0.5544279432241370209, -1.187676084274785548, 0.5985052393047670671 ) ) ;
#2365=CARTESIAN_POINT ( 'NONE',  ( 0.1889603646001475068, -0.5843802352234823694, 0.2966845687057266812 ) ) ;
#2367=CARTESIAN_POINT ( 'NONE',  ( 0.6590705178848084156, -1.601721441849921268, 0.5182417262812423209 ) ) ;
#2375=CARTESIAN_POINT ( 'NONE',  ( 0.02141150205530418724, -0.8856259524795232485, 0.4902799836155304347 ) ) ;
#2384=CARTESIAN_POINT ( 'NONE',  ( 0.4203373861789014843, -1.172197600499562009, 0.6891193374043744768 ) ) ;
#2387=EDGE_CURVE ( 'NONE', #35372, #36916, #669, .T. ) ;
#2388=FACE_BOUND ( 'NONE', #23456, .T. ) ;
#2393=CARTESIAN_POINT ( 'NONE',  ( 0.1568341744305939145, -0.7257825074155194178, 0.5774065548309712526 ) ) ;
#2396=CARTESIAN_POINT ( 'NONE',  ( 0.4424104223302582906, -1.573875977550938110, 0.5848388507199695496 ) ) ;
#2398=CARTESIAN_POINT ( 'NONE',  ( 0.6047538891612447287, -1.605163873594933843, 0.4396382108053983884 ) ) ;
#2404=CARTESIAN_POINT ( 'NONE',  ( 0.4219977553732560116, -1.241953814191006256, 0.8304148750200471829 ) ) ;
#2405=CARTESIAN_POINT ( 'NONE',  ( 0.4746252454845096280, -1.666917666310047119, 0.4878717617910002802 ) ) ;
#2412=AXIS2_PLACEMENT_3D ( 'NONE', #17855, #33693, #24453 ) ;
#2413=CARTESIAN_POINT ( 'NONE',  ( 0.3805742881279173817, -0.9147748976205605231, 0.7744170315737640697 ) ) ;
#2415=CARTESIAN_POINT ( 'NONE',  ( 0.006178162761485163183, -0.9774033419544895240, 0.4753174591059177168 ) ) ;
#2420=CARTESIAN_POINT ( 'NONE',  ( 0.6011193747858227798, -1.595581932925101976, 0.4276689662439276396 ) ) ;
#2424=VERTEX_POINT ( 'NONE', #4093 ) ;
#2436=CARTESIAN_POINT ( 'NONE',  ( 0.4037390063638767734, -1.153315448710456881, 0.7518491778188490793 ) ) ;
#2438=ORIENTED_EDGE ( 'NONE', *, *, #25908, .F. ) ;
#2439=CARTESIAN_POINT ( 'NONE',  ( 0.4975638555224211612, -1.097967759515461550, 0.6244301767862630026 ) ) ;
#2446=CARTESIAN_POINT ( 'NONE',  ( 0.2700198664771301660, -1.375350736655498229, 0.9052646506941134374 ) ) ;
#2448=CARTESIAN_POINT ( 'NONE',  ( 0.1766268836841131673, -0.5128407814923380270, -0.004769247607836917847 ) ) ;
#2453=CARTESIAN_POINT ( 'NONE',  ( 0.4110504371346864194, -1.121748555647557266, 0.6019148399695160023 ) ) ;
#2454=CARTESIAN_POINT ( 'NONE',  ( 0.5526746308725590806, -1.505849688569114608, 0.6462697217425257268 ) ) ;
#2458=ADVANCED_FACE ( 'NONE', ( #17471 ), #3732, .T. ) ;
#2459=CARTESIAN_POINT ( 'NONE',  ( 0.09153058604599668968, -0.8486693615597448170, 0.3862177764867652519 ) ) ;
#2464=CARTESIAN_POINT ( 'NONE',  ( 0.7472913949145145729, -1.513305546476923613, 0.4177417262808786336 ) ) ;
#2468=CARTESIAN_POINT ( 'NONE',  ( 0.01226155556033644428, -1.026869578359442370, 0.5617476425356938696 ) ) ;
#2470=CARTESIAN_POINT ( 'NONE',  ( 0.4302259848396451369, -1.133463226324729733, 0.4383158576218293967 ) ) ;
#2473=CARTESIAN_POINT ( 'NONE',  ( 0.01186068252828692722, -0.5714573607336731476, -0.08599319573038584352 ) ) ;
#2480=ORIENTED_EDGE ( 'NONE', *, *, #2387, .T. ) ;
#2485=VERTEX_POINT ( 'NONE', #20775 ) ;
#2486=VERTEX_POINT ( 'NONE', #8399 ) ;
#2489=CARTESIAN_POINT ( 'NONE',  ( -0.0002190029760103817690, -0.5598929387007183234, 0.2782029251743489140 ) ) ;
#2490=CARTESIAN_POINT ( 'NONE',  ( 0.1465179088820477704, -0.8893166351135021186, 0.5570520123011054592 ) ) ;
#2491=CARTESIAN_POINT ( 'NONE',  ( 0.2055039781776641650, -1.247779362046685714, 0.5783501873904609569 ) ) ;
#2492=CARTESIAN_POINT ( 'NONE',  ( 0.3605386037194296400, -1.159593875931560714, 0.5133706147585744839 ) ) ;
#2499=B_SPLINE_SURFACE_WITH_KNOTS ( 'NONE', 3, 3, ( 
 ( #22822, #19517, #38213, #4051, #7132, #7327, #13721, #32232, #1218, #22401, #38020, #35739, #29377, #10038, #34930, #19904, #29165, #32442, #12937, #1027, #3671, #13538, #6736, #38620, #3460, #25484, #16833, #10440, #23001, #26287, #38810, #10640, #7549, #19312, #16229, #28768, #626, #7945, #5069, #27313, #8555, #10858, #20519, #11663, #32654, #8159, #5261, #39842, #17630, #1408, #13916, #30177, #2209, #20321, #26488, #33052, #29985, #27095, #4858, #24222, #35949, #33455, #1819, #8364, #39025, #14136, #23432, #2006, #29768, #17024, #30379, #20933, #36556, #32842, #17431, #7755, #14532, #4460 ),
 ( #24029, #26898, #14335, #17820, #20733, #4649, #33260, #14749, #36745, #29565, #26707, #39628, #39427, #36135, #39238, #11465, #11250, #17221, #1613, #11060, #23619, #23819, #36341, #3204, #21729, #8767, #2806, #34068, #37355, #15353, #21344, #33655, #12460, #21949, #167, #37547, #33882, #8978, #9168, #34478, #30589, #28297, #25220, #24834, #12657, #37766, #2413, #5684, #40451, #21548, #5466, #15749, #5868, #37164, #34265, #30983, #25014, #18427, #27913, #14951, #12276, #6074, #6289, #21128, #18643, #18240, #27503, #40029, #24419, #11852, #18033, #36950, #30784, #31204, #28113, #3021, #15566, #2603 ),
 ( #15140, #40644, #27702, #9369, #18861, #31402, #40233, #12069, #24634, #22352, #38361, #970, #4212, #26051, #31800, #32189, #31998, #13076, #3616, #10200, #35084, #4001, #13488, #25841, #38571, #9782, #35290, #32390, #22768, #37972, #3810, #22556, #7084, #16365, #34871, #22164, #10392, #22954, #29328, #35473, #6684, #38161, #19654, #7277, #19051, #16778, #13674, #13275, #1172, #26236, #31587, #19258, #28903, #9985, #34678, #9585, #19856, #6483, #767, #3405, #15961, #28506, #384, #12882, #16180, #25441, #28720, #16566, #583, #25630, #29110, #6891, #19464, #4416, #11016, #14693, #23162, #39574 ),
 ( #7705, #23572, #5023, #35898, #36092, #17380, #20274, #13863, #7892, #8319, #32794, #29717, #1354, #14475, #20465, #32998, #20073, #11407, #7492, #39192, #29939, #17770, #26440, #4804, #1778, #14290, #23382, #38975, #17168, #29517, #2157, #27046, #17588, #10805, #38757, #10587, #23975, #20889, #4595, #32601, #26852, #1561, #16974, #35691, #36508, #14083, #30323, #26660, #39379, #11202, #33217, #23766, #36286, #8104, #20682, #30133, #1961, #33411, #5220, #5631, #8512, #18381, #5821, #12017, #34426, #30929, #21077, #18595, #27460, #2755, #17979, #36704, #3160, #24576, #24179, #6241, #30538, #21286 ),
 ( #39790, #15093, #18814, #31357, #27261, #5413, #11622, #33602, #15304, #2363, #14901, #27651, #31150, #39984, #12415, #24965, #21899, #11805, #24363, #40180, #6025, #18186, #2558, #37496, #36900, #37110, #34213, #8710, #8927, #27860, #33828, #30736, #21501, #9318, #34019, #40398, #12224, #2968, #24787, #37305, #9118, #28068, #21683, #15517, #40597, #16328, #25587, #7049, #28671, #13035, #25175, #6839, #35030, #929, #10358, #19422, #12833, #9538, #22115, #19005, #34636, #12611, #7236, #6433, #22505, #22718, #22921, #31537, #9738, #31956, #329, #10145, #28250, #3565, #35436, #19805, #32343, #3349 ),
 ( #15908, #19617, #724, #32152, #114, #3773, #28454, #34820, #25396, #540, #15704, #37712, #16520, #6630, #38114, #3958, #35250, #38318, #26006, #37925, #22305, #19205, #31748, #16134, #28864, #9933, #13223, #25792, #29060, #13437, #38528, #20420, #17540, #39525, #17331, #13633, #26199, #1729, #14429, #32556, #38723, #20232, #1517, #39335, #32752, #11357, #7449, #4974, #14036, #20634, #10544, #26395, #23119, #14245, #1318, #29282, #1915, #33169, #8055, #4375, #29675, #35642, #26808, #4165, #39146, #16931, #32954, #36241, #10973, #4556, #30087, #4758, #29474, #29889, #26997, #23927, #36457, #38926 ),
 ( #20022, #8269, #20842, #17125, #16731, #1131, #7848, #26610, #11157, #10757, #23530, #13825, #36049, #23329, #23714, #35852, #7665, #12330, #14637, #25075, #12520, #18701, #448, #37609, #27208, #25288, #34123, #9432, #24137, #2100, #9836, #31261, #30270, #33362, #11575, #9221, #12943, #5170, #22010, #6537, #28571, #6345, #39741, #36659, #31453, #3471, #21029, #8465, #21793, #3076, #28362, #34326, #25492, #5925, #34732, #15619, #9646, #18489, #15410, #31044, #3261, #2863, #17722, #31651, #22214, #37830, #27968, #28167, #40507, #15811, #24887, #31, #37410, #34536, #19112, #18917, #6137, #16027 ) ),
 .UNSPECIFIED., .F., .F., .F.,
 ( 4, 1, 1, 1, 4 ),
 ( 4, 3, 1, 1, 1, 1, 1, 1, 1, 1, 1, 1, 1, 1, 1, 1, 1, 1, 1, 1, 1, 1, 1, 1, 1, 1, 1, 1, 1, 1, 1, 1, 1, 1, 1, 1, 1, 1, 1, 1, 1, 1, 1, 1, 1, 1, 1, 1, 1, 1, 1, 1, 1, 1, 1, 1, 1, 1, 1, 1, 1, 1, 1, 1, 1, 1, 1, 1, 1, 1, 1, 1, 1, 4 ),
 ( 0.000000000000000000, 0.2500000000000000000, 0.5000000000000000000, 0.7500000000000000000, 1.000000000000000000 ),
 ( -0.01000000000000000021, 0.000000000000000000, 0.002255859375000000052, 0.004511718750000000104, 0.006767578124999999722, 0.009023437500000000208, 0.01127929687499999896, 0.01353515624999999944, 0.01579101562499999820, 0.01804687500000000042, 0.02255859374999999792, 0.02707031249999999889, 0.03158203124999999639, 0.03609375000000000083, 0.04060546874999999833, 0.04511718749999999584, 0.04962890625000000028, 0.05414062499999999778, 0.05865234375000000222, 0.06316406249999999278, 0.06767578124999999722, 0.07218750000000000167, 0.07669921874999999223, 0.08121093749999999667, 0.09023437499999999167, 0.09925781250000000056, 0.1082812499999999956, 0.1173046875000000044, 0.1263281249999999856, 0.1353515624999999944, 0.1443750000000000033, 0.1533984374999999845, 0.1624218749999999933, 0.1714453125000000022, 0.1804687499999999833, 0.1894921874999999922, 0.1985156250000000011, 0.2075390624999999822, 0.2165624999999999911, 0.2346093750000000089, 0.2526562499999999711, 0.2707031249999999889, 0.2887500000000000067, 0.3067968749999999689, 0.3248437499999999867, 0.3428906250000000044, 0.3609374999999999667, 0.3789843749999999845, 0.3970312500000000022, 0.4150781249999999645, 0.4331249999999999822, 0.4511718750000000000, 0.4692187500000000178, 0.4872656250000000355, 0.5053124999999999423, 0.5414062499999999778, 0.5775000000000000133, 0.6303124999999999423, 0.6567187500000000178, 0.6831249999999999822, 0.7095312499999999467, 0.7359375000000000222, 0.7623437499999999867, 0.7887500000000000622, 0.8151562500000000266, 0.8415624999999999911, 0.8679687499999999556, 0.8943750000000001421, 0.9207812499999998845, 0.9471875000000000711, 0.9603906250000000533, 0.9735937500000000355, 0.9867968750000000178, 1.000000000000000000 ),
 .UNSPECIFIED. ) ;
#2500=CARTESIAN_POINT ( 'NONE',  ( 0.2625882174288838855, -0.9523961353426481091, 0.7085637651928656799 ) ) ;
#2501=CARTESIAN_POINT ( 'NONE',  ( 0.1871311130424547498, -0.7120295780690556464, 0.03084641936662753381 ) ) ;
#2503=CARTESIAN_POINT ( 'NONE',  ( 0.2711450911080737769, -1.632422954829337636, 0.7869752074672371478 ) ) ;
#2507=CARTESIAN_POINT ( 'NONE',  ( 0.4130427319115463902, -1.705619880099039198, 0.4224177903210530882 ) ) ;
#2512=CARTESIAN_POINT ( 'NONE',  ( 0.4815360835401190087, -1.665003689908300277, 0.5707417262808793801 ) ) ;
#2516=CARTESIAN_POINT ( 'NONE',  ( 0.7022701326239239039, -1.539209993927390219, 0.4224083929475443977 ) ) ;
#2517=CARTESIAN_POINT ( 'NONE',  ( 0.01618294926847982027, -0.6819691077562005654, 0.5071040197741758515 ) ) ;
#2518=CARTESIAN_POINT ( 'NONE',  ( 0.08705077985668224771, -1.275137320191813917, 0.7451449987256821839 ) ) ;
#2520=CARTESIAN_POINT ( 'NONE',  ( 0.5297859054048726923, -1.159963375372088823, 0.8529160106009885389 ) ) ;
#2521=CARTESIAN_POINT ( 'NONE',  ( 0.6988007311651551756, -1.542424956370897160, 0.5852637934084858884 ) ) ;
#2523=( BOUNDED_SURFACE ( )  B_SPLINE_SURFACE ( 3, 2, ( 
 ( #4046, #2001, #13910 ),
 ( #36549, #14331, #1401 ),
 ( #26702, #29980, #36129 ),
 ( #26283, #5065, #14525 ),
 ( #30173, #26482, #1606 ),
 ( #27089, #23208, #20929 ),
 ( #17425, #33450, #5256 ),
 ( #39019, #33047, #14132 ),
 ( #8360, #17626, #24025 ),
 ( #11459, #20120, #7545 ) ),
 .UNSPECIFIED., .F., .F., .T. ) 
 B_SPLINE_SURFACE_WITH_KNOTS ( ( 4, 2, 2, 2, 4 ),
 ( 3, 3 ),
 ( -2.042636892962690354E-16, 0.0004458836822742874139, 0.0008917673645487790915, 0.001337651046823270769, 0.001783534729097762447 ),
 ( 0.000000000000000000, 1.000000000000000000 ),
 .UNSPECIFIED. ) 
 GEOMETRIC_REPRESENTATION_ITEM ( )  RATIONAL_B_SPLINE_SURFACE ( (
 ( 1.000000000000000000, 0.7270749630177930634, 1.000000000000000000),
 ( 1.000000000000000000, 0.7753295258064453188, 1.000000000000000000),
 ( 1.000000000000000000, 0.8134500463251533864, 1.000000000000000000),
 ( 1.000000000000000000, 0.8693879047592659726, 1.000000000000000000),
 ( 1.000000000000000000, 0.8872992176887145588, 1.000000000000000000),
 ( 1.000000000000000000, 0.9041895492973218706, 1.000000000000000000),
 ( 1.000000000000000000, 0.9028865482022944144, 1.000000000000000000),
 ( 1.000000000000000000, 0.8835743685064011421, 1.000000000000000000),
 ( 1.000000000000000000, 0.8656690658353223267, 1.000000000000000000),
 ( 1.000000000000000000, 0.8407181564551341468, 1.000000000000000000) ) ) 
 REPRESENTATION_ITEM ( '' )  SURFACE ( )  );
#2525=ORIENTED_EDGE ( 'NONE', *, *, #1880, .T. ) ;
#2526=CARTESIAN_POINT ( 'NONE',  ( 0.6522089892707538805, -1.452491178199303956, 0.4224083929475448973 ) ) ;
#2527=CARTESIAN_POINT ( 'NONE',  ( 0.004846577187571122179, -0.5767503433068859042, 0.3422196348096480656 ) ) ;
#2529=CARTESIAN_POINT ( 'NONE',  ( 0.5874265235786473305, -1.491095056082657466, 0.5633939987125622384 ) ) ;
#2532=CARTESIAN_POINT ( 'NONE',  ( 0.6150013826522254812, -1.299199899150926374, 0.5044333340123036136 ) ) ;
#2533=ORIENTED_EDGE ( 'NONE', *, *, #10248, .T. ) ;
#2534=ORIENTED_EDGE ( 'NONE', *, *, #23489, .F. ) ;
#2535=CARTESIAN_POINT ( 'NONE',  ( 0.6980568480161586375, -1.433467586945206929, 0.6380938078099552824 ) ) ;
#2541=CARTESIAN_POINT ( 'NONE',  ( 0.1323007547259467120, -0.7872386167069682639, 0.4801189427118005004 ) ) ;
#2543=CARTESIAN_POINT ( 'NONE',  ( 0.4973151438122045964, -1.542462661965338766, 0.5710983407029659453 ) ) ;
#2545=CARTESIAN_POINT ( 'NONE',  ( 0.07403655305110988516, -1.312857837003576833, 0.5491095645124061120 ) ) ;
#2546=CARTESIAN_POINT ( 'NONE',  ( 0.03174232663013761002, -1.011915959827874190, 0.5403155396012611078 ) ) ;
#2550=CARTESIAN_POINT ( 'NONE',  ( 0.4448084983678752269, -1.018341691379531344, 0.8445668428770941594 ) ) ;
#2556=CARTESIAN_POINT ( 'NONE',  ( 0.2610261613789442992, -1.678452829011149561, 0.5218982752881765608 ) ) ;
#2557=CARTESIAN_POINT ( 'NONE',  ( 0.3082562917470283437, -1.189540619778174380, 0.5196934755922930638 ) ) ;
#2558=CARTESIAN_POINT ( 'NONE',  ( 0.5291583206849711507, -1.148825028536799131, 0.6606389499358795714 ) ) ;
#2565=CARTESIAN_POINT ( 'NONE',  ( 0.4679778500672936992, -1.237826332153874942, 0.6057417262809768888 ) ) ;
#2567=CARTESIAN_POINT ( 'NONE',  ( 0.1642982928013839161, -0.8629055878361323595, 0.5584950140652098494 ) ) ;
#2570=CARTESIAN_POINT ( 'NONE',  ( 0.02700589308869108529, -0.9048577289495857157, 0.5464201800401247144 ) ) ;
#2577=CARTESIAN_POINT ( 'NONE',  ( 0.4567016086251121654, -1.219691737450557145, 0.6383600239578398616 ) ) ;
#2579=CARTESIAN_POINT ( 'NONE',  ( 0.2043566422458189535, -1.364136262758315121, 0.5557375579486671935 ) ) ;
#2582=CARTESIAN_POINT ( 'NONE',  ( 0.06588517883490634108, -1.329221574522195137, 0.5283365633529514271 ) ) ;
#2583=VERTEX_POINT ( 'NONE', #31026 ) ;
#2585=CARTESIAN_POINT ( 'NONE',  ( 0.3978516996529349870, -1.472654256470057987, 0.8275371935563656800 ) ) ;
#2587=CARTESIAN_POINT ( 'NONE',  ( 0.5883754668686869138, -1.614204823230756203, 0.4538795894651435625 ) ) ;
#2588=CARTESIAN_POINT ( 'NONE',  ( 0.4952488905928924545, -1.196841907270136174, 0.4182417262808778013 ) ) ;
#2593=CARTESIAN_POINT ( 'NONE',  ( 0.2399483944973402061, -0.8897145941320553364, 0.6956011753531377018 ) ) ;
#2594=CARTESIAN_POINT ( 'NONE',  ( 0.4640654899589395921, -1.684528450414659817, 0.4570323128730537365 ) ) ;
#2597=CARTESIAN_POINT ( 'NONE',  ( 0.1614573949321077284, -0.7569534866611321577, 0.1932149833450299559 ) ) ;
#2600=CARTESIAN_POINT ( 'NONE',  ( 0.1881571720199402276, -1.258443498167182817, 0.4308778177761442563 ) ) ;
#2601=ADVANCED_FACE ( 'NONE', ( #36781 ), #37596, .T. ) ;
#2603=CARTESIAN_POINT ( 'NONE',  ( 0.1895831464430141056, -0.5047047246472137205, 0.1457185332388698518 ) ) ;
#2606=CARTESIAN_POINT ( 'NONE',  ( 0.009301758140802687466, -0.9958182297342890177, 0.5251311197228717420 ) ) ;
#2608=B_SPLINE_CURVE_WITH_KNOTS ( 'NONE', 3,
 ( #27469, #27873, #40411, #12236, #22316, #26019, #34437, #12844, #34833, #548, #19016, #6644, #28262, #31547, #16144, #31965, #22517, #941, #19217, #126, #32160, #9330, #3970, #35042, #6852, #35258, #28466, #18823, #3173, #29073, #9746, #13452, #19432, #12621 ),
 .UNSPECIFIED., .F., .F.,
 ( 4, 2, 2, 2, 2, 2, 2, 2, 2, 2, 2, 2, 2, 2, 2, 2, 4 ),
 ( 0.000000000000000000, 0.0006192929267342644345, 0.001238585853468528869, 0.001857878780202793303, 0.002477171706937057738, 0.003096464633671321739, 0.003715757560405590944, 0.004335050487139859715, 0.004954343413874128486, 0.005573636340608397258, 0.006192929267342666029, 0.006812222194076935668, 0.007431515120811204439, 0.008050808047545472343, 0.008670100974279741982, 0.009289393901014011620, 0.009908686827748279524 ),
 .UNSPECIFIED. ) ;
#2624=CARTESIAN_POINT ( 'NONE',  ( 0.3249540854508322085, -1.179364160644205128, 0.5783250968866978647 ) ) ;
#2628=CARTESIAN_POINT ( 'NONE',  ( 0.4423174438215108362, -1.206761583220333778, 0.7319083686835440306 ) ) ;
#2631=CARTESIAN_POINT ( 'NONE',  ( 0.4756538103953397711, -1.077424610118791648, 0.6442006390088441670 ) ) ;
#2635=ORIENTED_EDGE ( 'NONE', *, *, #1995, .T. ) ;
#2636=CARTESIAN_POINT ( 'NONE',  ( 0.009578720288114734097, -0.5684218271147216672, 0.04142997145147423593 ) ) ;
#2638=CARTESIAN_POINT ( 'NONE',  ( 0.3561794159690685468, -1.622419985511465823, 0.5747848533733730392 ) ) ;
#2639=CARTESIAN_POINT ( 'NONE',  ( 0.06495584141124570443, -0.8202245329731961965, 0.08014687577841178578 ) ) ;
#2640=CARTESIAN_POINT ( 'NONE',  ( 0.1761160692862425159, -0.6130882321663837509, -0.07245465855189868465 ) ) ;
#2641=DIRECTION ( 'NONE',  ( 0.8660512985181126888, 0.4999551463232384529, 0.000000000000000000 ) ) ;
#2643=VERTEX_POINT ( 'NONE', #6728 ) ;
#2644=CARTESIAN_POINT ( 'NONE',  ( 0.4530449344480740881, -1.054480797917887180, 0.7183760019440903477 ) ) ;
#2645=CARTESIAN_POINT ( 'NONE',  ( 0.1164452680309506771, -0.5621043433723575955, 0.2200809357625567453 ) ) ;
#2648=DIRECTION ( 'NONE',  ( -0.4999551463232372317, 0.8660512985181135770, -0.000000000000000000 ) ) ;
#2651=CARTESIAN_POINT ( 'NONE',  ( 0.4420022301528255815, -1.686445855772801705, 0.4182417262808776903 ) ) ;
#2653=CARTESIAN_POINT ( 'NONE',  ( 0.3091361241754520539, -1.774399086135407533, 0.3157417262808776548 ) ) ;
#2654=DIRECTION ( 'NONE',  ( 0.8660512985181135770, 0.4999551463232371762, 0.000000000000000000 ) ) ;
#2658=EDGE_CURVE ( 'NONE', #6212, #23907, #37109, .T. ) ;
#2659=CARTESIAN_POINT ( 'NONE',  ( 0.4792622942854181112, -1.127254429899091637, 0.4859857865428779400 ) ) ;
#2663=CARTESIAN_POINT ( 'NONE',  ( 0.08897272204609851798, -1.263855944153051469, 0.7613784839713820807 ) ) ;
#2664=CARTESIAN_POINT ( 'NONE',  ( 0.3268505546336938905, -1.758215942194889969, 0.4787252747007004205 ) ) ;
#2665=CARTESIAN_POINT ( 'NONE',  ( 0.0005306896791119474367, -0.4438826107187291981, 0.2002152464016503652 ) ) ;
#2666=AXIS2_PLACEMENT_3D ( 'NONE', #25305, #28786, #25503 ) ;
#2681=ORIENTED_EDGE ( 'NONE', *, *, #2886, .F. ) ;
#2682=CARTESIAN_POINT ( 'NONE',  ( -0.001068161708947345471, -0.5484958227261149677, 0.2458947828252880385 ) ) ;
#2685=CARTESIAN_POINT ( 'NONE',  ( 0.3669101237188617803, -1.155878863020100011, 0.4953911018533934674 ) ) ;
#2687=ORIENTED_EDGE ( 'NONE', *, *, #15745, .T. ) ;
#2689=CARTESIAN_POINT ( 'NONE',  ( 0.08565325978148723152, -0.8127617527064519010, 0.1840195686883785431 ) ) ;
#2690=CARTESIAN_POINT ( 'NONE',  ( 0.3655313958116495621, -1.732873032179087058, 0.4268294808601417190 ) ) ;
#2692=CARTESIAN_POINT ( 'NONE',  ( 0.4796062271711729608, -1.296889239581610731, 0.8144315461438738080 ) ) ;
#2693=CARTESIAN_POINT ( 'NONE',  ( 0.5965761245944036784, -1.493465029535157029, 0.5182417262812423209 ) ) ;
#2694=CARTESIAN_POINT ( 'NONE',  ( 0.2741618706575962294, -1.669228526676626245, 0.6701936342721495077 ) ) ;
#2696=CARTESIAN_POINT ( 'NONE',  ( 0.3203399455593453071, -1.760717822755525797, 0.5904099678045555688 ) ) ;
#2697=CARTESIAN_POINT ( 'NONE',  ( 0.4139549699696334351, -1.708531266749635069, 0.4267841496025627790 ) ) ;
#2698=CARTESIAN_POINT ( 'NONE',  ( 0.3965728918691002192, -1.716106284337745702, 0.4221472374420881524 ) ) ;
#2701=CARTESIAN_POINT ( 'NONE',  ( 0.2906430027847833331, -0.9902279025455028583, 0.7333702739393529457 ) ) ;
#2702=CARTESIAN_POINT ( 'NONE',  ( 0.4650638207231214127, -1.115967253294534167, 0.5748459061576319806 ) ) ;
#2708=CARTESIAN_POINT ( 'NONE',  ( 0.008416785622808892545, -0.6338120178247520498, 0.4051738709354697487 ) ) ;
#2709=CARTESIAN_POINT ( 'NONE',  ( 0.07627944499376293486, -1.206878283085004444, 0.7625613511206872364 ) ) ;
#2711=CARTESIAN_POINT ( 'NONE',  ( 0.4514527476588715560, -1.032880248282614266, 0.8272311760340308462 ) ) ;
#2719=CARTESIAN_POINT ( 'NONE',  ( 0.2424357324133526170, -1.539388940635932457, 0.9028508052754699031 ) ) ;
#2722=CARTESIAN_POINT ( 'NONE',  ( 0.5284083360280649178, -1.405426350308686345, 0.7820653062704271408 ) ) ;
#2723=CARTESIAN_POINT ( 'NONE',  ( 0.3546403334084172743, -1.742554324808940347, 0.4373760386089020624 ) ) ;
#2726=CARTESIAN_POINT ( 'NONE',  ( 0.5556047631917466756, -1.190343314783628870, 0.5823040822259395455 ) ) ;
#2729=CARTESIAN_POINT ( 'NONE',  ( 0.4837496661226462491, -1.089885176164768765, 0.8053770729510393300 ) ) ;
#2734=CARTESIAN_POINT ( 'NONE',  ( 0.5536297569049346556, -1.186194075236972179, 0.6057417262809815517 ) ) ;
#2737=CARTESIAN_POINT ( 'NONE',  ( 0.1116805044116661316, -0.7434698432209100316, 0.4023817199705208569 ) ) ;
#2739=CARTESIAN_POINT ( 'NONE',  ( 0.1049838256438099249, -0.5659121791580637995, 0.2385271282840315255 ) ) ;
#2740=CARTESIAN_POINT ( 'NONE',  ( 0.3172915166155709232, -1.763408040713600577, 0.5249560652895838286 ) ) ;
#2741=CARTESIAN_POINT ( 'NONE',  ( 0.06581764578086118922, -1.340728352476674212, 0.5449258910593480776 ) ) ;
#2743=ORIENTED_EDGE ( 'NONE', *, *, #22017, .F. ) ;
#2744=CARTESIAN_POINT ( 'NONE',  ( 0.4694680599816452027, -1.673450296079499466, 0.5834365554883687022 ) ) ;
#2745=CARTESIAN_POINT ( 'NONE',  ( 0.2329990834885074247, -0.7658510446276335371, 0.7180707385985112268 ) ) ;
#2751=DIRECTION ( 'NONE',  ( -0.4999551463232372317, 0.8660512985181135770, -0.000000000000000000 ) ) ;
#2755=CARTESIAN_POINT ( 'NONE',  ( 0.1967848402874973202, -0.7048484731626001309, 0.3032743993732655574 ) ) ;
#2758=( BOUNDED_SURFACE ( )  B_SPLINE_SURFACE ( 3, 2, ( 
 ( #19857, #25632, #16366 ),
 ( #385, #22557, #28904 ),
 ( #4003, #37973, #10393 ),
 ( #770, #22956, #9783 ),
 ( #38758, #1174, #13276 ),
 ( #29329, #32391, #13675 ),
 ( #38163, #15962, #28722 ),
 ( #10589, #25844, #22353 ),
 ( #9987, #19053, #23163 ),
 ( #6484, #31590, #3406 ) ),
 .UNSPECIFIED., .F., .F., .T. ) 
 B_SPLINE_SURFACE_WITH_KNOTS ( ( 4, 2, 2, 2, 4 ),
 ( 3, 3 ),
 ( 0.01180411870105455355, 0.01260860704157424489, 0.01341309538209393623, 0.01421758372261362757, 0.01502207206313332065 ),
 ( 0.000000000000000000, 0.6794541557782065588 ),
 .UNSPECIFIED. ) 
 GEOMETRIC_REPRESENTATION_ITEM ( )  RATIONAL_B_SPLINE_SURFACE ( (
 ( 1.000000000000000000, 0.8005432181983026529, 0.8721299149832257847),
 ( 1.000000000000000000, 0.8005023781569950980, 0.8721037327721876675),
 ( 1.000000000000000000, 0.8004856833031734897, 0.8720930298401630143),
 ( 1.000000000000000000, 0.8004816785315187477, 0.8720904624143410722),
 ( 1.000000000000000000, 0.8004939698596951203, 0.8720983422826746878),
 ( 1.000000000000000000, 0.8005299687168438982, 0.8721214208507863663),
 ( 1.000000000000000000, 0.8005535718565474079, 0.8721365526274713620),
 ( 1.000000000000000000, 0.8006044241474448153, 0.8721691536085041108),
 ( 1.000000000000000000, 0.8006320503125461396, 0.8721868645133341591),
 ( 1.000000000000000000, 0.8006591322813667588, 0.8722042265384517545) ) ) 
 REPRESENTATION_ITEM ( '' )  SURFACE ( )  );
#2761=AXIS2_PLACEMENT_3D ( 'NONE', #8730, #15720, #134 ) ;
#2763=CARTESIAN_POINT ( 'NONE',  ( 0.5846118587689395074, -1.493149640613376627, 0.5722307761754854560 ) ) ;
#2768=CARTESIAN_POINT ( 'NONE',  ( 0.1948208630905133021, -0.8880093436342747504, 0.6128872966510791054 ) ) ;
#2771=CARTESIAN_POINT ( 'NONE',  ( 0.06357782896711253184, -1.038394445277960987, 0.7229233463101174539 ) ) ;
#2777=CARTESIAN_POINT ( 'NONE',  ( 0.7409681548321257472, -1.515722218252784748, 0.5271419462256154986 ) ) ;
#2790=CARTESIAN_POINT ( 'NONE',  ( 0.07310625969965998949, -0.5492403936048265711, 0.2026465080310040634 ) ) ;
#2792=CARTESIAN_POINT ( 'NONE',  ( 0.5998866944813456836, -1.596483326503712163, 0.4395608873836986397 ) ) ;
#2793=CARTESIAN_POINT ( 'NONE',  ( 0.4661714095618022524, -1.154128127646582458, 0.4228544605197694373 ) ) ;
#2798=CARTESIAN_POINT ( 'NONE',  ( 0.1427444512807377885, -0.6541520024106974862, 0.4271693757410587322 ) ) ;
#2799=CARTESIAN_POINT ( 'NONE',  ( 0.4778399605452497423, -1.666371875539310432, 0.5376480933357082881 ) ) ;
#2800=DIRECTION ( 'NONE',  ( -0.4999551463232372317, 0.8660512985181135770, -0.000000000000000000 ) ) ;
#2806=CARTESIAN_POINT ( 'NONE',  ( 0.6116693357450743163, -1.291191393066782211, 0.8405059385265429839 ) ) ;
#2808=CARTESIAN_POINT ( 'NONE',  ( 0.02620755023972913891, -1.037821530677986992, 0.5805157883271023778 ) ) ;
#2811=LINE ( 'NONE', #18038, #1576 ) ;
#2812=CARTESIAN_POINT ( 'NONE',  ( 0.08740683213217560754, -0.8118925016582974052, 0.2366527497468325636 ) ) ;
#2822=ORIENTED_EDGE ( 'NONE', *, *, #15988, .T. ) ;
#2824=AXIS2_PLACEMENT_3D ( 'NONE', #26102, #6528, #1215 ) ;
#2828=CARTESIAN_POINT ( 'NONE',  ( 0.5105415332760498970, -1.310647974363944090, 0.6145840706319117830 ) ) ;
#2831=CARTESIAN_POINT ( 'NONE',  ( 0.3550881284155063544, -0.9867921891001451007, 0.6236314015414725631 ) ) ;
#2834=CARTESIAN_POINT ( 'NONE',  ( 0.1052201234866705776, -1.408655232269138358, 0.5916332308596470302 ) ) ;
#2837=CARTESIAN_POINT ( 'NONE',  ( 0.07484919615358114064, -0.7926208454270931014, 0.6479314650129559539 ) ) ;
#2839=CARTESIAN_POINT ( 'NONE',  ( 0.1136133567237439662, -0.6088964843684741002, -0.08269403125744159699 ) ) ;
#2843=ORIENTED_EDGE ( 'NONE', *, *, #1771, .F. ) ;
#2844=CARTESIAN_POINT ( 'NONE',  ( 0.4773881915714036639, -1.084785724581697863, 0.7107894162981950315 ) ) ;
#2846=CARTESIAN_POINT ( 'NONE',  ( 0.2807752934945104695, -1.015156109853498023, 0.7786345481072077801 ) ) ;
#2848=CARTESIAN_POINT ( 'NONE',  ( 0.4015936175283410514, -1.155705023113092533, 0.5182417262812423209 ) ) ;
#2856=CARTESIAN_POINT ( 'NONE',  ( 0.7483483892508734359, -1.515136533364971339, 0.3157417262808776548 ) ) ;
#2858=EDGE_CURVE ( 'NONE', #30450, #23564, #11102, .T. ) ;
#2859=LINE ( 'NONE', #34728, #29966 ) ;
#2863=CARTESIAN_POINT ( 'NONE',  ( 0.2615876942762666579, -0.9557769062746830357, 0.5027841231788432452 ) ) ;
#2864=CARTESIAN_POINT ( 'NONE',  ( 0.4673658794513684822, -1.111510721115457123, 0.5568865556175225384 ) ) ;
#2865=CARTESIAN_POINT ( 'NONE',  ( 0.4480069854757587899, -1.224024607427070199, 0.6057417262810179670 ) ) ;
#2867=CARTESIAN_POINT ( 'NONE',  ( 0.007928552535923857544, -0.8847668029847218785, 0.5082548692313750838 ) ) ;
#2868=CARTESIAN_POINT ( 'NONE',  ( 0.2722331219925429036, -1.671874623808670135, 0.4849083929475441201 ) ) ;
#2871=CARTESIAN_POINT ( 'NONE',  ( 0.3666095998147628765, -1.617393197634767299, 0.4854686549615687685 ) ) ;
#2876=CARTESIAN_POINT ( 'NONE',  ( 0.4102339696967467475, -1.075663819259173870, 0.5182417262812423209 ) ) ;
#2880=CARTESIAN_POINT ( 'NONE',  ( 0.5884947987833728522, -1.442678314496853131, 0.6829111437943111707 ) ) ;
#2881=CARTESIAN_POINT ( 'NONE',  ( 0.01000299637147959199, -0.5446455199555007010, 0.07760565969044912193 ) ) ;
#2886=EDGE_CURVE ( 'NONE', #40221, #36916, #16735, .T. ) ;
#2889=CARTESIAN_POINT ( 'NONE',  ( 0.1635760886199158770, -1.208793886606414070, 0.9133870697123913640 ) ) ;
#2890=CARTESIAN_POINT ( 'NONE',  ( 0.09659820559305749843, -0.8547292609823787801, 0.4202044640824337818 ) ) ;
#2891=CARTESIAN_POINT ( 'NONE',  ( 0.2277821696528544160, -1.351061424029422309, 0.4182417262808770797 ) ) ;
#2900=CARTESIAN_POINT ( 'NONE',  ( 0.1852697703518006722, -0.8388889655799379730, 0.1397141703224135112 ) ) ;
#2902=CARTESIAN_POINT ( 'NONE',  ( 0.2730111487096660294, -0.9521603032302338177, 0.7332358461412977757 ) ) ;
#2903=CARTESIAN_POINT ( 'NONE',  ( 0.2398899415561628889, -0.9495379235619473279, 0.6725648971787069330 ) ) ;
#2906=CARTESIAN_POINT ( 'NONE',  ( 0.01258354067333375750, -0.4467589052256379922, 0.2540486221606858552 ) ) ;
#2908=CARTESIAN_POINT ( 'NONE',  ( 0.3854584602151780448, -1.723663440349962439, 0.4240230717917121694 ) ) ;
#2909=CARTESIAN_POINT ( 'NONE',  ( 0.6601361389616772213, -1.566348459635070522, 0.5707417262808793801 ) ) ;
#2915=CARTESIAN_POINT ( 'NONE',  ( 0.003300039066125767893, -0.4845961630426517952, 0.3648084845760091732 ) ) ;
#2917=CARTESIAN_POINT ( 'NONE',  ( 0.09023307471144903502, -1.313753669190550255, 0.7175206707109292870 ) ) ;
#2919=CARTESIAN_POINT ( 'NONE',  ( 0.6207796129641102167, -1.305782781463471265, 0.8357864796646383709 ) ) ;
#2920=AXIS2_PLACEMENT_3D ( 'NONE', #16021, #22613, #12513 ) ;
#2923=CYLINDRICAL_SURFACE ( 'NONE', #10746, 0.1762268159172277748 ) ;
#2927=CARTESIAN_POINT ( 'NONE',  ( 0.2326053079067355867, -1.504550822924993536, 0.9203436614353645018 ) ) ;
#2929=CARTESIAN_POINT ( 'NONE',  ( 0.1568487634955791910, -0.6765984673290891260, 0.4608420472205499996 ) ) ;
#2932=CARTESIAN_POINT ( 'NONE',  ( 0.3304381985390301701, -0.8896417797241282788, 0.6549085351719812209 ) ) ;
#2933=ORIENTED_EDGE ( 'NONE', *, *, #10901, .F. ) ;
#2935=CARTESIAN_POINT ( 'NONE',  ( 0.6993744165018669356, -1.438184434374068399, 0.5964060907162921366 ) ) ;
#2937=EDGE_CURVE ( 'NONE', #24566, #36154, #4243, .T. ) ;
#2943=ADVANCED_FACE ( 'NONE', ( #24217 ), #6070, .T. ) ;
#2947=CARTESIAN_POINT ( 'NONE',  ( 0.08630297934288916339, -0.7465732544923662228, 0.1807232860058308743 ) ) ;
#2949=CARTESIAN_POINT ( 'NONE',  ( 0.5152864262115902649, -1.503242855671597766, 0.7141587765705896818 ) ) ;
#2951=CARTESIAN_POINT ( 'NONE',  ( -0.002143816844750521915, -0.8544176354026742359, 0.1237328532832608491 ) ) ;
#2954=ORIENTED_EDGE ( 'NONE', *, *, #3469, .T. ) ;
#2955=CARTESIAN_POINT ( 'NONE',  ( 0.4518928892634598293, -1.683692191370343538, 0.6017796442898305509 ) ) ;
#2956=CARTESIAN_POINT ( 'NONE',  ( 0.6977729861270942635, -1.432737804912566082, 0.6428259928577456650 ) ) ;
#2961=DIRECTION ( 'NONE',  ( 0.000000000000000000, 0.000000000000000000, 1.000000000000000000 ) ) ;
#2963=CARTESIAN_POINT ( 'NONE',  ( 0.3730815298380146805, -1.156738423958018291, 0.4182417262809047243 ) ) ;
#2966=CARTESIAN_POINT ( 'NONE',  ( 0.2675581168115488961, -1.674785173045962194, 0.4888193750310237395 ) ) ;
#2967=DIRECTION ( 'NONE',  ( -0.007183093100618591353, -0.4999484090412826265, -0.8660253988599863062 ) ) ;
#2968=CARTESIAN_POINT ( 'NONE',  ( 0.4609105641225965111, -1.064890115380353386, 0.6919706562625183022 ) ) ;
#2969=AXIS2_PLACEMENT_3D ( 'NONE', #10212, #6695, #19272 ) ;
#2973=CARTESIAN_POINT ( 'NONE',  ( 0.5139471409257055923, -1.531975829649279808, 0.5486243274997595343 ) ) ;
#2982=CARTESIAN_POINT ( 'NONE',  ( 0.1325631505235937146, -1.280238184107190369, 0.7308764952167086104 ) ) ;
#2987=CARTESIAN_POINT ( 'NONE',  ( 0.1253884927449593900, -1.293580113097495765, 0.4291439200971798318 ) ) ;
#2990=DIRECTION ( 'NONE',  ( 0.000000000000000000, 7.931692224083225994E-17, -1.000000000000000000 ) ) ;
#2991=EDGE_CURVE ( 'NONE', #23093, #40221, #7526, .T. ) ;
#2994=DIRECTION ( 'NONE',  ( 0.8660512985181129109, 0.4999551463232380089, 0.000000000000000000 ) ) ;
#2997=EDGE_CURVE ( 'NONE', #19917, #21274, #39374, .T. ) ;
#2998=CARTESIAN_POINT ( 'NONE',  ( 0.07502636376510861405, -1.323892984169241949, 0.5081013553160158569 ) ) ;
#3001=CARTESIAN_POINT ( 'NONE',  ( 0.4412115301948774104, -1.573601263554865293, 0.5662306361009304956 ) ) ;
#3002=DIRECTION ( 'NONE',  ( -0.08131595302302933870, -0.04568309556551754247, 0.9956408843370728734 ) ) ;
#3003=CARTESIAN_POINT ( 'NONE',  ( 0.5779288858437423571, -1.623150939738223109, 0.5629342317618580838 ) ) ;
#3010=CARTESIAN_POINT ( 'NONE',  ( 0.1253102310817552911, -0.5531591968941835802, 0.1790963605822581683 ) ) ;
#3012=CARTESIAN_POINT ( 'NONE',  ( 0.4788046145333532677, -1.665542548548383905, 0.5304359953099284652 ) ) ;
#3015=( BOUNDED_SURFACE ( )  B_SPLINE_SURFACE ( 3, 2, ( 
 ( #7936, #36331, #20511 ),
 ( #33045, #20725, #33253 ),
 ( #30171, #39621, #1999 ),
 ( #14521, #5255, #8358 ) ),
 .UNSPECIFIED., .F., .F., .T. ) 
 B_SPLINE_SURFACE_WITH_KNOTS ( ( 4, 4 ),
 ( 3, 3 ),
 ( 0.001944782987540475327, 0.002901087691608646765 ),
 ( 0.000000000000000000, 1.000000000000000000 ),
 .UNSPECIFIED. ) 
 GEOMETRIC_REPRESENTATION_ITEM ( )  RATIONAL_B_SPLINE_SURFACE ( (
 ( 1.000000000000000000, 0.6942579658572588519, 1.000000000000000000),
 ( 1.000000000000000000, 0.6962136974480453988, 1.000000000000000000),
 ( 1.000000000000000000, 0.6983443629434031852, 1.000000000000000000),
 ( 1.000000000000000000, 0.6992614111707954327, 1.000000000000000000) ) ) 
 REPRESENTATION_ITEM ( '' )  SURFACE ( )  );
#3016=CARTESIAN_POINT ( 'NONE',  ( 0.4753071910876713324, -1.208389221472485398, 0.5182417262812494263 ) ) ;
#3017=CARTESIAN_POINT ( 'NONE',  ( 0.2217501959041398851, -1.238826317744727623, 0.5698378396483744224 ) ) ;
#3019=CARTESIAN_POINT ( 'NONE',  ( 0.1826134026666640375, -1.261648033191452578, 0.4282186462236585722 ) ) ;
#3021=CARTESIAN_POINT ( 'NONE',  ( 0.1896045607153576118, -0.5049209053381719103, 0.1595777137938904078 ) ) ;
#3023=CARTESIAN_POINT ( 'NONE',  ( 0.05281413292478839838, -1.208094164924696123, 0.6641569417577480872 ) ) ;
#3028=CARTESIAN_POINT ( 'NONE',  ( 0.1654684907951354811, -0.8644978747596554491, 0.5573653326411247555 ) ) ;
#3040=DIRECTION ( 'NONE',  ( -1.000000000000000000, 0.000000000000000000, 0.000000000000000000 ) ) ;
#3041=CARTESIAN_POINT ( 'NONE',  ( 0.6540709664215760277, -1.593060928864740156, 0.5182417262812423209 ) ) ;
#3042=CARTESIAN_POINT ( 'NONE',  ( 0.06936654275873489761, -1.327133429011184917, 0.5458395137742713121 ) ) ;
#3044=CARTESIAN_POINT ( 'NONE',  ( 0.4746656776394587163, -1.252825698842344959, 0.6966861032914614116 ) ) ;
#3048=CARTESIAN_POINT ( 'NONE',  ( 0.3394669778924194747, -0.9758008820872865474, 0.6115353432225060226 ) ) ;
#3054=CARTESIAN_POINT ( 'NONE',  ( 0.3868601653778248051, -1.605681501165217906, 0.5994997544633362541 ) ) ;
#3056=CARTESIAN_POINT ( 'NONE',  ( 0.1847888282947060534, -0.8330427479178647010, 0.06499907415858525994 ) ) ;
#3058=EDGE_LOOP ( 'NONE', ( #16851, #25467, #39490, #5246 ) ) ;
#3062=CARTESIAN_POINT ( 'NONE',  ( 0.3558122948646044725, -0.9979958203889786050, 0.6057407852365402912 ) ) ;
#3063=CARTESIAN_POINT ( 'NONE',  ( 0.1173840559349740853, -0.5715400563125977440, 0.2482123610220977605 ) ) ;
#3066=CARTESIAN_POINT ( 'NONE',  ( 0.07014435923142441076, -1.325199841737237261, 0.5075297796642793680 ) ) ;
#3068=DIRECTION ( 'NONE',  ( 0.8660512985181134660, 0.4999551463232372317, 0.000000000000000000 ) ) ;
#3076=CARTESIAN_POINT ( 'NONE',  ( 0.3767165169986340101, -1.018944133209149783, 0.6225985890371608100 ) ) ;
#3078=CARTESIAN_POINT ( 'NONE',  ( 0.4638218765581886838, -1.238038477568070839, 0.6057417262809816627 ) ) ;
#3079=CARTESIAN_POINT ( 'NONE',  ( 0.3130702568482664483, -1.175243511012216580, 0.5339619868235715439 ) ) ;
#3080=CARTESIAN_POINT ( 'NONE',  ( 0.03359830163007831300, -1.106472467758128353, 0.6807021762515294006 ) ) ;
#3084=CARTESIAN_POINT ( 'NONE',  ( 0.3186359832558304794, -1.645093617292038957, 0.5084158906598844618 ) ) ;
#3097=CARTESIAN_POINT ( 'NONE',  ( 0.3014137048403158770, -1.651046165962986478, 0.6735612096716837582 ) ) ;
#3102=ORIENTED_EDGE ( 'NONE', *, *, #36554, .T. ) ;
#3107=CARTESIAN_POINT ( 'NONE',  ( 0.5473844695833234297, -1.374494293802986711, 0.7608074972636496014 ) ) ;
#3108=CARTESIAN_POINT ( 'NONE',  ( 0.2821105676325378897, -1.010667300530192936, 0.7205108277189851140 ) ) ;
#3110=CARTESIAN_POINT ( 'NONE',  ( 0.3254365784322334476, -1.747317980671322157, 0.7218611321553708438 ) ) ;
#3111=CARTESIAN_POINT ( 'NONE',  ( 0.07217859744021073998, -1.325427469710779738, 0.5682417262808779901 ) ) ;
#3112=CARTESIAN_POINT ( 'NONE',  ( 0.3259879919982042185, -1.767950897709266611, 0.5312986935552648227 ) ) ;
#3113=CARTESIAN_POINT ( 'NONE',  ( 0.4040419229627993936, -1.153899704180549879, 0.7428076885917280769 ) ) ;
#3114=DIRECTION ( 'NONE',  ( -0.4999551463232372317, 0.8660512985181134660, -0.000000000000000000 ) ) ;
#3117=EDGE_CURVE ( 'NONE', #27710, #20709, #1167, .T. ) ;
#3119=CARTESIAN_POINT ( 'NONE',  ( 0.08371583302770695123, -1.272799487215662495, 0.7379929360799946103 ) ) ;
#3122=CARTESIAN_POINT ( 'NONE',  ( 0.2575330336140166931, -0.6922558787343077169, 0.5832620184353838333 ) ) ;
#3128=B_SPLINE_CURVE_WITH_KNOTS ( 'NONE', 3,
 ( #26103, #28950, #9827, #34722, #13535, #22998, #1216, #10438, #22399, #22609, #38414, #35523, #3458, #29375, #26285, #25895, #13719, #38807 ),
 .UNSPECIFIED., .F., .F.,
 ( 4, 2, 2, 2, 2, 2, 2, 2, 4 ),
 ( 0.000000000000000000, 0.0006978799593375504704, 0.001395759918675100941, 0.002093639878012653905, 0.002791519837350207953, 0.003489399796687762435, 0.004187279756025318218, 0.004885159715362874001, 0.005583039674700429784 ),
 .UNSPECIFIED. ) ;
#3130=ORIENTED_EDGE ( 'NONE', *, *, #7231, .F. ) ;
#3132=CARTESIAN_POINT ( 'NONE',  ( 0.2689337271815545605, -1.650725020051581504, 0.7800499242891761886 ) ) ;
#3133=CARTESIAN_POINT ( 'NONE',  ( 0.5346679333427164504, -1.402191149477463261, 0.7798264699775933062 ) ) ;
#3136=CARTESIAN_POINT ( 'NONE',  ( 0.5554409461590971153, -1.190971970253151824, 0.5682417262808781011 ) ) ;
#3139=CARTESIAN_POINT ( 'NONE',  ( 0.6575415210681188061, -1.363599502042151190, 0.7651167678683458151 ) ) ;
#3143=CARTESIAN_POINT ( 'NONE',  ( 0.4517177305807006937, -1.568671020668126914, 0.6057417262804751790 ) ) ;
#3147=CARTESIAN_POINT ( 'NONE',  ( 0.09865219997896333692, -0.7828559995779595937, 0.3308637533635402361 ) ) ;
#3148=CARTESIAN_POINT ( 'NONE',  ( 0.3186686258432176455, -1.760399750288523357, 0.5682417262808792113 ) ) ;
#3149=CARTESIAN_POINT ( 'NONE',  ( 0.5262759607219161806, -1.526737561883647398, 0.5945435633807139020 ) ) ;
#3151=VERTEX_POINT ( 'NONE', #35687 ) ;
#3153=CARTESIAN_POINT ( 'NONE',  ( 0.6633289903567118895, -1.542975281133564636, 0.6975821153327242952 ) ) ;
#3154=CARTESIAN_POINT ( 'NONE',  ( 0.5699439007204750718, -1.617412408666830448, 0.5656496617915443004 ) ) ;
#3158=CARTESIAN_POINT ( 'NONE',  ( 0.2676785629568417257, -1.674416124214124446, 0.5054568562724600644 ) ) ;
#3159=CARTESIAN_POINT ( 'NONE',  ( 1.365923996832131609E-16, -0.9481888444201339583, 0.1457185332388703791 ) ) ;
#3160=CARTESIAN_POINT ( 'NONE',  ( 0.1896483993057378192, -0.6911749089203499397, 0.2228938739458891649 ) ) ;
#3163=CARTESIAN_POINT ( 'NONE',  ( 0.5709043678375559372, -1.616165998060699049, 0.5779678008732025418 ) ) ;
#3167=CARTESIAN_POINT ( 'NONE',  ( 0.5845226641748834107, -1.491917136578684744, 0.5353822420918034064 ) ) ;
#3170=EDGE_LOOP ( 'NONE', ( #38504, #646, #4565, #254 ) ) ;
#3173=CARTESIAN_POINT ( 'NONE',  ( 0.08562216985915493961, -0.7978384895209408301, 0.09062995534711226764 ) ) ;
#3174=VERTEX_POINT ( 'NONE', #18375 ) ;
#3176=CARTESIAN_POINT ( 'NONE',  ( -0.005479581593941192964, -0.8983412709979351485, 0.5156674170252182332 ) ) ;
#3180=CARTESIAN_POINT ( 'NONE',  ( 0.3351195522891313172, -1.762354232558481337, 0.5631496603913015431 ) ) ;
#3181=EDGE_CURVE ( 'NONE', #37440, #24067, #10836, .T. ) ;
#3187=CARTESIAN_POINT ( 'NONE',  ( 0.1124437242459924158, -0.6641345740908473072, 0.4088893035250216190 ) ) ;
#3190=CARTESIAN_POINT ( 'NONE',  ( 0.6964952729471024506, -1.533352077435225391, 0.5923684272575838738 ) ) ;
#3191=CARTESIAN_POINT ( 'NONE',  ( 0.07283724563382373840, -0.5406377204022615457, 0.1540664544690148741 ) ) ;
#3193=CARTESIAN_POINT ( 'NONE',  ( 0.5574362741858098769, -1.620420278163815286, 0.4861798668042197069 ) ) ;
#3195=CARTESIAN_POINT ( 'NONE',  ( 0.2634247196158754356, -0.9771240080834830977, 0.5484523488112167389 ) ) ;
#3196=CARTESIAN_POINT ( 'NONE',  ( 0.1186103394390872201, -1.414144848331978510, 0.5683298932114988489 ) ) ;
#3198=CARTESIAN_POINT ( 'NONE',  ( 0.1259887422558554904, -0.5708039110117676396, 0.2411005981708249368 ) ) ;
#3204=CARTESIAN_POINT ( 'NONE',  ( 0.6347819612394876021, -1.328236395719069263, 0.8269854195084552773 ) ) ;
#3206=CARTESIAN_POINT ( 'NONE',  ( 0.01932545507967057402, -1.072689427073633128, 0.6194964679467892532 ) ) ;
#3209=CARTESIAN_POINT ( 'NONE',  ( 0.1961333673497456243, -0.6677565227190264130, 0.3323178443805968052 ) ) ;
#3210=FACE_OUTER_BOUND ( 'NONE', #27052, .T. ) ;
#3211=CARTESIAN_POINT ( 'NONE',  ( 0.07006815180908280982, -1.315301596572416631, 0.5080907171456734428 ) ) ;
#3217=CARTESIAN_POINT ( 'NONE',  ( 0.08509557923809639435, -0.8164785559594017750, 0.1457185332388710730 ) ) ;
#3219=ORIENTED_EDGE ( 'NONE', *, *, #26053, .F. ) ;
#3221=CARTESIAN_POINT ( 'NONE',  ( 0.1871240791749231025, -1.373980404802405353, 0.5685824782455963788 ) ) ;
#3225=CARTESIAN_POINT ( 'NONE',  ( 0.3342347797450085922, -1.058365783522508208, 0.7408787376446750450 ) ) ;
#3228=CARTESIAN_POINT ( 'NONE',  ( 0.4765072543226545609, -1.073695880004174930, 0.6154142099768207252 ) ) ;
#3233=CARTESIAN_POINT ( 'NONE',  ( 0.02691720668820642148, -0.9716517312894669134, 0.6480984491125419966 ) ) ;
#3237=CARTESIAN_POINT ( 'NONE',  ( 0.07236692127650729001, -0.7316196773536807196, 0.5741060721534142486 ) ) ;
#3239=CARTESIAN_POINT ( 'NONE',  ( 0.1747797283729930762, -0.8954128581900229200, 0.04731367366808376940 ) ) ;
#3240=CARTESIAN_POINT ( 'NONE',  ( 0.06761598059943987882, -0.6219880238673772821, 0.01307546307162734019 ) ) ;
#3246=CARTESIAN_POINT ( 'NONE',  ( 0.5359002092464226763, -1.453873471191388544, 0.7520340848835496139 ) ) ;
#3247=EDGE_LOOP ( 'NONE', ( #34094, #337, #32721, #15715, #14050 ) ) ;
#3248=CARTESIAN_POINT ( 'NONE',  ( 0.1869154501082920528, -0.7268340247273499255, 0.03292103754823103717 ) ) ;
#3254=DIRECTION ( 'NONE',  ( 0.6185154643211973058, 0.3739688674182602979, -0.6910759050910669776 ) ) ;
#3256=CARTESIAN_POINT ( 'NONE',  ( 0.1319437676963613748, -1.258139845592547434, 0.6230237721763144387 ) ) ;
#3261=CARTESIAN_POINT ( 'NONE',  ( 0.2734279889346977188, -0.9622732688880970553, 0.5233991146725487376 ) ) ;
#3263=DIRECTION ( 'NONE',  ( 0.4999551463232372317, -0.8660512985181134660, 0.000000000000000000 ) ) ;
#3265=CARTESIAN_POINT ( 'NONE',  ( 0.1721302213443809126, -1.453494483496651890, 0.7931418093652549128 ) ) ;
#3268=CARTESIAN_POINT ( 'NONE',  ( 0.3587090678007808231, -1.161727987938869555, 0.4182417262808778013 ) ) ;
#3270=ORIENTED_EDGE ( 'NONE', *, *, #3938, .T. ) ;
#3275=CARTESIAN_POINT ( 'NONE',  ( 0.5983201278204041129, -1.462679505942070080, 0.6053214617447383317 ) ) ;
#3277=ORIENTED_EDGE ( 'NONE', *, *, #12815, .T. ) ;
#3278=EDGE_LOOP ( 'NONE', ( #19123, #8535, #12577, #1048 ) ) ;
#3279=CARTESIAN_POINT ( 'NONE',  ( 0.2018730987858452508, -0.7302160269438148221, 0.3392082505062085640 ) ) ;
#3281=CARTESIAN_POINT ( 'NONE',  ( 0.02614423585516349388, -0.6518502750570457360, 0.4684854799394865821 ) ) ;
#3282=CARTESIAN_POINT ( 'NONE',  ( 0.2680263476856213911, -1.006194344260251006, 0.7179568291910547462 ) ) ;
#3283=CARTESIAN_POINT ( 'NONE',  ( 0.2038749045098602886, -1.364881829950852721, 0.4182417262808790226 ) ) ;
#3285=CARTESIAN_POINT ( 'NONE',  ( 0.01217390823686615060, -0.4283984760907826872, 0.1286254401998236097 ) ) ;
#3291=CARTESIAN_POINT ( 'NONE',  ( 0.1852697703518008665, -0.8388889655799581790, 0.1410250186500984493 ) ) ;
#3293=CARTESIAN_POINT ( 'NONE',  ( 0.5861427556958135332, -1.492383513481604362, 0.5940502790402875100 ) ) ;
#3294=CARTESIAN_POINT ( 'NONE',  ( 0.2009823985145610392, -0.8991965598532170034, 0.5949443444603982334 ) ) ;
#3295=CARTESIAN_POINT ( 'NONE',  ( 0.2682897491456118222, -1.618043430020381646, 0.8112229545981489709 ) ) ;
#3296=CARTESIAN_POINT ( 'NONE',  ( 0.02257819890113409514, -0.5399740301406672494, 0.4766629420431791608 ) ) ;
#3305=CARTESIAN_POINT ( 'NONE',  ( 0.09388211606716308222, -1.317406247416022858, 0.7243147876381810235 ) ) ;
#3308=CARTESIAN_POINT ( 'NONE',  ( 0.7044564683220037038, -1.517225624775331072, 0.5721507375637494563 ) ) ;
#3313=CARTESIAN_POINT ( 'NONE',  ( 0.2709798375537315063, -1.666113143576919642, 0.7428107703390531835 ) ) ;
#3314=CARTESIAN_POINT ( 'NONE',  ( 0.5947316391157766446, -1.487148168449749619, 0.5691497089179062829 ) ) ;
#3315=CARTESIAN_POINT ( 'NONE',  ( 0.5436011381715165625, -1.169374965638590558, 0.5906050259210040565 ) ) ;
#3322=CARTESIAN_POINT ( 'NONE',  ( 0.4860430332212200000, -1.937050167757587760, 0.5182417262812423209 ) ) ;
#3329=CARTESIAN_POINT ( 'NONE',  ( 0.08809811930380141709, -0.7701783715479050274, 0.2329054462128774816 ) ) ;
#3330=CARTESIAN_POINT ( 'NONE',  ( 0.08990936761271779709, -0.5436479961250808568, 0.1446695161202876112 ) ) ;
#3332=CARTESIAN_POINT ( 'NONE',  ( 0.5250712364136614907, -1.526826414575088053, 0.5708821469565591444 ) ) ;
#3339=CARTESIAN_POINT ( 'NONE',  ( 0.4117959629386627185, -1.718119050787106250, 0.6105174604612256806 ) ) ;
#3340=CARTESIAN_POINT ( 'NONE',  ( 0.6726913636366114169, -1.388499336029741515, 0.7397682110044472292 ) ) ;
#3342=CARTESIAN_POINT ( 'NONE',  ( 0.5674346215910480717, -1.617636063460796025, 0.5669677346690390474 ) ) ;
#3343=B_SPLINE_CURVE_WITH_KNOTS ( 'NONE', 3,
 ( #5754, #38040, #28790, #9661, #28380, #13138 ),
 .UNSPECIFIED., .F., .F.,
 ( 4, 2, 4 ),
 ( 0.000000000000000000, 0.0005522092370844346697, 0.001104418474168869339 ),
 .UNSPECIFIED. ) ;
#3344=CARTESIAN_POINT ( 'NONE',  ( 0.5127413057567625776, -1.344192398881990602, 0.8010895931681089044 ) ) ;
#3348=CARTESIAN_POINT ( 'NONE',  ( 0.05651694441833610832, -1.310850388052192894, 0.6148622741790434887 ) ) ;
#3349=CARTESIAN_POINT ( 'NONE',  ( 0.1843752803354802849, -0.7900634509218503743, 0.1457185332388700461 ) ) ;
#3356=AXIS2_PLACEMENT_3D ( 'NONE', #27355, #15187, #5915 ) ;
#3366=CARTESIAN_POINT ( 'NONE',  ( 0.4089992519647981384, -1.131314579718122992, 0.3157417262808777658 ) ) ;
#3367=CARTESIAN_POINT ( 'NONE',  ( 0.1711433029897516944, -1.377856651617054062, 0.6045512896720135476 ) ) ;
#3368=ORIENTED_EDGE ( 'NONE', *, *, #38043, .F. ) ;
#3371=ORIENTED_EDGE ( 'NONE', *, *, #24745, .T. ) ;
#3372=CARTESIAN_POINT ( 'NONE',  ( 0.3273012371184206293, -1.767032042405956904, 0.5424971694272759937 ) ) ;
#3374=FACE_OUTER_BOUND ( 'NONE', #22473, .T. ) ;
#3382=CARTESIAN_POINT ( 'NONE',  ( 0.09071780102537924106, -0.6083146503190497434, 0.1978526169899092468 ) ) ;
#3387=CARTESIAN_POINT ( 'NONE',  ( 0.4410457167306740534, -1.573541075230501241, 0.5635949220671795379 ) ) ;
#3390=CARTESIAN_POINT ( 'NONE',  ( 0.2803729568343131806, -0.9884757496409375399, 0.5728653952958084883 ) ) ;
#3392=VECTOR ( 'NONE', #28196, 39.37007874015748143 ) ;
#3395=CARTESIAN_POINT ( 'NONE',  ( 0.1887530776919918163, -0.4596756685375818496, 0.1557014379196421383 ) ) ;
#3397=CARTESIAN_POINT ( 'NONE',  ( 0.5818399341603623931, -1.494769269184020866, 0.5993433759778750147 ) ) ;
#3403=CARTESIAN_POINT ( 'NONE',  ( 0.1127117262141932863, -0.6977186850741163848, 0.5101031591922252639 ) ) ;
#3405=CARTESIAN_POINT ( 'NONE',  ( 0.2529714763052502979, -0.7233805682233873657, 0.5452257223911994855 ) ) ;
#3406=CARTESIAN_POINT ( 'NONE',  ( 0.4051896412206086873, -1.145861017645314783, 0.4245813808998249450 ) ) ;
#3408=CARTESIAN_POINT ( 'NONE',  ( 0.05758214410466930278, -1.240647563727545144, 0.6561832231837511076 ) ) ;
#3412=CARTESIAN_POINT ( 'NONE',  ( 0.2637479789745994507, -0.6009450727723176788, 0.1023043458361303365 ) ) ;
#3416=CARTESIAN_POINT ( 'NONE',  ( 0.4614790457781012822, -1.239149285203732687, 0.7960982376345531186 ) ) ;
#3422=ORIENTED_EDGE ( 'NONE', *, *, #12408, .F. ) ;
#3425=TOROIDAL_SURFACE ( 'NONE', #26435, 0.04749999999977547877, 0.01000000000000000021 ) ;
#3426=CARTESIAN_POINT ( 'NONE',  ( 0.1872855758231053713, -1.374285790641261329, 0.4677874389472473915 ) ) ;
#3430=CARTESIAN_POINT ( 'NONE',  ( 0.5010253830127560093, -1.294911479982484348, 0.5984545886549959004 ) ) ;
#3431=DIRECTION ( 'NONE',  ( 0.0001066307966871704452, -1.551735798909009237E-06, -0.9999999943137325431 ) ) ;
#3433=CARTESIAN_POINT ( 'NONE',  ( 0.4383612739836618144, -1.052766492039166391, 0.6342478131430038246 ) ) ;
#3436=CARTESIAN_POINT ( 'NONE',  ( 0.05062930621939953219, -1.075691773360101466, 0.7334325894009673386 ) ) ;
#3437=ORIENTED_EDGE ( 'NONE', *, *, #7884, .F. ) ;
#3439=CARTESIAN_POINT ( 'NONE',  ( 0.3847140583749202869, -1.605421369524298703, 0.5663922353625259198 ) ) ;
#3441=CARTESIAN_POINT ( 'NONE',  ( 0.1127291481688585117, -0.7509215673570545091, -0.08735086836678220001 ) ) ;
#3442=CARTESIAN_POINT ( 'NONE',  ( 0.06918013971839866161, -0.5399928739580638348, 0.1359763300881502157 ) ) ;
#3443=EDGE_LOOP ( 'NONE', ( #40262, #19545 ) ) ;
#3444=EDGE_CURVE ( 'NONE', #4902, #34794, #8533, .T. ) ;
#3449=CARTESIAN_POINT ( 'NONE',  ( 0.1830018851694050763, -0.7784347268374490758, 0.5945923564955621909 ) ) ;
#3458=CARTESIAN_POINT ( 'NONE',  ( 0.4384682549770916871, -1.691311010828499883, 0.6110381959906349136 ) ) ;
#3460=CARTESIAN_POINT ( 'NONE',  ( 0.6396239940202712582, -1.336901993116134779, 0.8551876651762376769 ) ) ;
#3461=TOROIDAL_SURFACE ( 'NONE', #28419, 0.04749999999977547877, 0.01000000000000000021 ) ;
#3469=EDGE_CURVE ( 'NONE', #5749, #36473, #18838, .T. ) ;
#3471=CARTESIAN_POINT ( 'NONE',  ( 0.4083208966368579995, -1.036284369767852764, 0.6331064141399478373 ) ) ;
#3472=ADVANCED_FACE ( 'NONE', ( #28857 ), #18584, .F. ) ;
#3473=FACE_OUTER_BOUND ( 'NONE', #20117, .T. ) ;
#3474=CARTESIAN_POINT ( 'NONE',  ( 0.5145478920242605447, -1.185611792012001509, 0.6057417262811334302 ) ) ;
#3476=CARTESIAN_POINT ( 'NONE',  ( 0.02760435326350026836, -0.9850525496912549972, 0.6581503728771671557 ) ) ;
#3478=CARTESIAN_POINT ( 'NONE',  ( 0.3704697912810945848, -1.166474544107110267, 0.4182417262808778013 ) ) ;
#3480=ORIENTED_EDGE ( 'NONE', *, *, #16792, .F. ) ;
#3485=VECTOR ( 'NONE', #22618, 39.37007874015748143 ) ;
#3486=CARTESIAN_POINT ( 'NONE',  ( 0.5760521384482631957, -1.423519085382992433, 0.6171703776866719338 ) ) ;
#3489=ORIENTED_EDGE ( 'NONE', *, *, #39169, .F. ) ;
#3490=CARTESIAN_POINT ( 'NONE',  ( 0.5904407432689540158, -1.601769558089914502, 0.4345720983630151357 ) ) ;
#3494=CARTESIAN_POINT ( 'NONE',  ( 0.01170032160320996946, -0.5546732792797903766, 0.2570475303832205349 ) ) ;
#3495=CARTESIAN_POINT ( 'NONE',  ( 0.6427111490925289106, -1.572123239621654900, 0.4256043397410034790 ) ) ;
#3498=CARTESIAN_POINT ( 'NONE',  ( 0.01198570820082700897, -0.4922037379152022218, -0.02535380372549751390 ) ) ;
#3506=CARTESIAN_POINT ( 'NONE',  ( 0.1852697703518018935, -0.8388889655799397493, 0.1449575636331411899 ) ) ;
#3507=CONICAL_SURFACE ( 'NONE', #10082, 0.1624877031048690135, 0.1745329251994329756 ) ;
#3511=CARTESIAN_POINT ( 'NONE',  ( 0.1723377558215138383, -0.8672015974434073016, 0.5125204039364767983 ) ) ;
#3512=CARTESIAN_POINT ( 'NONE',  ( 0.01058981954642434879, -0.5333385045931418045, 0.1834384537311664620 ) ) ;
#3513=CARTESIAN_POINT ( 'NONE',  ( 0.2812803162299816750, -1.541674682308305844, 0.9904418111512126588 ) ) ;
#3519=DIRECTION ( 'NONE',  ( 0.8660512985181126888, 0.4999551463232384529, 0.000000000000000000 ) ) ;
#3529=CARTESIAN_POINT ( 'NONE',  ( 0.4689530283559364410, -1.130095828402380764, 0.4666897101730458353 ) ) ;
#3531=CARTESIAN_POINT ( 'NONE',  ( 0.09046428421607514980, -1.271807512115344485, 0.5182417262812423209 ) ) ;
#3532=CARTESIAN_POINT ( 'NONE',  ( 0.2595980677342931142, -1.678828727236759244, 0.5659945771154371030 ) ) ;
#3533=CARTESIAN_POINT ( 'NONE',  ( 0.2774676337662247971, -0.9469401346137602538, 0.7275640284046342998 ) ) ;
#3536=VERTEX_POINT ( 'NONE', #6426 ) ;
#3539=ORIENTED_EDGE ( 'NONE', *, *, #27037, .F. ) ;
#3543=CARTESIAN_POINT ( 'NONE',  ( 0.6590705178848084156, -1.601721441849921268, 0.5182417262812423209 ) ) ;
#3545=CARTESIAN_POINT ( 'NONE',  ( 0.2276060635785035757, -0.9284834125224814549, 0.6579476060701295870 ) ) ;
#3549=CARTESIAN_POINT ( 'NONE',  ( 0.1156421456406209886, -0.6222233367372450585, 0.3743582360812274246 ) ) ;
#3554=CARTESIAN_POINT ( 'NONE',  ( 0.6405997180189585416, -1.336161063724098597, 0.7844527642137872903 ) ) ;
#3558=CARTESIAN_POINT ( 'NONE',  ( 0.6090448915793870155, -1.479032872888494499, 0.5731864665443510143 ) ) ;
#3560=CARTESIAN_POINT ( 'NONE',  ( 0.1892549258828873926, -0.8411929458066104148, 0.2428197129412378030 ) ) ;
#3564=CARTESIAN_POINT ( 'NONE',  ( 0.03359830163007831300, -1.106472467758128353, 0.6807021762515294006 ) ) ;
#3565=CARTESIAN_POINT ( 'NONE',  ( 0.1860214731903934160, -0.7916887388224913558, 0.2098883466634208494 ) ) ;
#3577=CARTESIAN_POINT ( 'NONE',  ( 0.1861044033398533692, -0.8581774586871301347, 0.1812730634833334131 ) ) ;
#3579=CARTESIAN_POINT ( 'NONE',  ( 0.05563540667800927902, -1.335270441939011121, 0.5197417262808780025 ) ) ;
#3581=CARTESIAN_POINT ( 'NONE',  ( 0.1034500356823820494, -1.184998414006736223, 0.7606213861980615221 ) ) ;
#3584=CARTESIAN_POINT ( 'NONE',  ( 0.4340705412225758231, -1.136956705126083378, 0.5182417262812423209 ) ) ;
#3586=CARTESIAN_POINT ( 'NONE',  ( 0.08888686490980646226, -1.314157010769999578, 0.4560913452963717973 ) ) ;
#3587=DIRECTION ( 'NONE',  ( -0.4999551463232371762, 0.8660512985181134660, -0.000000000000000000 ) ) ;
#3588=CARTESIAN_POINT ( 'NONE',  ( 0.5972966887670781988, -1.597972273499876250, 0.4286416649299261694 ) ) ;
#3591=VERTEX_POINT ( 'NONE', #38106 ) ;
#3592=FACE_OUTER_BOUND ( 'NONE', #35599, .T. ) ;
#3594=CARTESIAN_POINT ( 'NONE',  ( 0.2372193036104026098, -0.8972535433454568166, 0.6983280862938940903 ) ) ;
#3596=ORIENTED_EDGE ( 'NONE', *, *, #2858, .T. ) ;
#3597=CARTESIAN_POINT ( 'NONE',  ( 2.583431119901448829E-05, -0.4262564435357387160, 0.1903957133491850640 ) ) ;
#3598=CARTESIAN_POINT ( 'NONE',  ( 0.4621341988872929574, -1.532972198998491242, 0.7252595559952519366 ) ) ;
#3603=CARTESIAN_POINT ( 'NONE',  ( 0.3082980917340821247, -1.007433431510620592, 0.6024509563116612343 ) ) ;
#3608=VECTOR ( 'NONE', #10580, 39.37007874015748143 ) ;
#3609=CARTESIAN_POINT ( 'NONE',  ( 0.3653257479037889111, -1.126353351805138070, 0.8077794159112313688 ) ) ;
#3615=AXIS2_PLACEMENT_3D ( 'NONE', #34066, #33653, #15138 ) ;
#3616=CARTESIAN_POINT ( 'NONE',  ( 0.6387812025505826830, -1.332167957021822557, 0.7527387398627037873 ) ) ;
#3618=CARTESIAN_POINT ( 'NONE',  ( 0.05061809761307144856, -1.246180169307136154, 0.6688036225518566580 ) ) ;
#3620=CARTESIAN_POINT ( 'NONE',  ( 0.08146015332400738385, -1.318321297778865864, 0.4704503523288164346 ) ) ;
#3622=CARTESIAN_POINT ( 'NONE',  ( 0.2046378645136894270, -0.9147060450658054398, 0.6214472678333320399 ) ) ;
#3624=CARTESIAN_POINT ( 'NONE',  ( 0.6982506810322021140, -1.496459467441635827, 0.4853452239463521556 ) ) ;
#3626=VERTEX_POINT ( 'NONE', #9728 ) ;
#3631=ADVANCED_FACE ( 'NONE', ( #29267 ), #29665, .F. ) ;
#3632=CARTESIAN_POINT ( 'NONE',  ( 0.3629635513856721563, -1.169857187001789534, 0.4182417262808778013 ) ) ;
#3633=B_SPLINE_CURVE_WITH_KNOTS ( 'NONE', 3,
 ( #20055, #32372, #33201, #5006, #39556, #17573, #16960, #32782, #36490, #23146, #35883, #27029, #23962, #23560, #11390, #26646, #19837, #29311, #29504, #4791, #17366, #39367 ),
 .UNSPECIFIED., .F., .F.,
 ( 4, 2, 2, 2, 2, 2, 2, 2, 2, 2, 4 ),
 ( 0.000000000000000000, 0.001208936138749878856, 0.002417872277499757711, 0.003022340346874696597, 0.003626808416249635483, 0.004835744554999510218, 0.006044680693749383653, 0.006649148763124320370, 0.007253616832499257955, 0.008462552971249126185, 0.009671489109998996150 ),
 .UNSPECIFIED. ) ;
#3635=EDGE_CURVE ( 'NONE', #13015, #38131, #34571, .T. ) ;
#3638=CARTESIAN_POINT ( 'NONE',  ( 0.1156620092545082995, -1.416098910045857862, 0.4676871692938218694 ) ) ;
#3642=CARTESIAN_POINT ( 'NONE',  ( 0.5007618516461782576, -1.294244025654331498, 0.6028626338283670227 ) ) ;
#3644=CARTESIAN_POINT ( 'NONE',  ( 0.3224045394708089374, -1.760747393242730219, 0.4928480064586597265 ) ) ;
#3645=CARTESIAN_POINT ( 'NONE',  ( 0.4928690250500026293, -1.082673021089655574, 0.5721439028494731405 ) ) ;
#3648=CARTESIAN_POINT ( 'NONE',  ( 0.05865460281497637818, -1.118264395791441101, 0.7485648030501707018 ) ) ;
#3650=CARTESIAN_POINT ( 'NONE',  ( 0.1751718594852775535, -1.050137195076516816, 0.8364126339080514283 ) ) ;
#3652=CARTESIAN_POINT ( 'NONE',  ( 0.06557244994597240251, -0.7859005477308489418, 0.03515882536214479798 ) ) ;
#3653=CARTESIAN_POINT ( 'NONE',  ( 0.1845297650884798746, -0.8463068900015028317, 0.09522967538727487857 ) ) ;
#3657=ORIENTED_EDGE ( 'NONE', *, *, #325, .F. ) ;
#3658=CARTESIAN_POINT ( 'NONE',  ( 0.4154885538802266520, -1.127358870322865858, 0.5795187171650935110 ) ) ;
#3659=CARTESIAN_POINT ( 'NONE',  ( 0.1171479976344189378, -0.5695749914720167340, 0.2425808011265505881 ) ) ;
#3662=CARTESIAN_POINT ( 'NONE',  ( 0.5429359209136535025, -1.169310040315109545, 0.5682417262808779901 ) ) ;
#3669=ADVANCED_FACE ( 'NONE', ( #17322 ), #33173, .T. ) ;
#3670=B_SPLINE_CURVE_WITH_KNOTS ( 'NONE', 3,
 ( #38488, #16892, #19762, #10708, #35401, #4114, #1681, #26560, #23069, #1088, #35803, #16683, #35596, #20185, #19971, #13600, #26162, #7615, #38682, #4928, #4716, #32507, #39097, #10919, #39293, #32711, #13986, #23487, #7810, #14198, #11115, #23672, #33320, #8422, #39903, #11313, #33723, #21187, #20989, #14592, #30844, #11723, #18304, #8224, #24091, #20798, #40088, #39695, #26950, #36619, #5538, #2665, #18499, #27377, #36410, #24478, #1872, #36802 ),
 .UNSPECIFIED., .F., .F.,
 ( 4, 2, 2, 2, 2, 2, 2, 2, 2, 2, 2, 2, 2, 2, 2, 2, 2, 2, 2, 2, 2, 2, 2, 2, 2, 2, 2, 2, 4 ),
 ( 3.058345997481036509E-05, 0.001707590458248171112, 0.003384597456521531555, 0.005061604454794892648, 0.006738611453068253307, 0.007577114952204934070, 0.008415618451341613099, 0.01009262544961496422, 0.01176963244788831707, 0.01344663944616166992, 0.01512364644443502278, 0.01680065344270836869, 0.01847766044098172328, 0.02015466743925507440, 0.02350868143580178010, 0.02686269543234847887, 0.03021670942889519151, 0.03189371642716854610, 0.03357072342544189375, 0.04027875141853529128, 0.04195575841680863893, 0.04363276541508198658, 0.04698677941162868882, 0.04866378640990204341, 0.05034079340817539105, 0.05201780040644875258, 0.05285630390558542641, 0.05327555565515376679, 0.05369480740472210023 ),
 .UNSPECIFIED. ) ;
#3671=CARTESIAN_POINT ( 'NONE',  ( 0.6710503155864784297, -1.387729643236325083, 0.8301965501372990941 ) ) ;
#3673=CARTESIAN_POINT ( 'NONE',  ( 0.4175441604896325543, -1.126814933402447760, 0.5435073546807187572 ) ) ;
#3682=CARTESIAN_POINT ( 'NONE',  ( 0.1492358308521446464, -1.145521527551625951, 0.9752184947445524665 ) ) ;
#3683=CARTESIAN_POINT ( 'NONE',  ( 0.0003189345953180242532, -0.4719140995912783354, 0.02086241239832067884 ) ) ;
#3686=ADVANCED_FACE ( 'NONE', ( #10535 ), #37356, .T. ) ;
#3688=ADVANCED_FACE ( 'NONE', ( #36037 ), #1069, .T. ) ;
#3692=EDGE_LOOP ( 'NONE', ( #31840, #15078 ) ) ;
#3700=CARTESIAN_POINT ( 'NONE',  ( 0.1936486515345767767, -0.8111868380948229484, 0.2874045417164454164 ) ) ;
#3701=ORIENTED_EDGE ( 'NONE', *, *, #30119, .F. ) ;
#3702=CARTESIAN_POINT ( 'NONE',  ( 0.01084281108554383498, -0.5360844055732374436, 0.1962519228010750350 ) ) ;
#3704=CARTESIAN_POINT ( 'NONE',  ( 0.6528690609575362735, -1.559671037451765274, 0.4269390887829667136 ) ) ;
#3711=EDGE_LOOP ( 'NONE', ( #21390, #10679, #29640, #22225, #3539 ) ) ;
#3715=CARTESIAN_POINT ( 'NONE',  ( 0.1116628760231743317, -0.9290305928360726995, 0.1898406166415877172 ) ) ;
#3717=CARTESIAN_POINT ( 'NONE',  ( 0.5745168371614193248, -1.419270820774067854, 0.7497674921010183402 ) ) ;
#3718=CARTESIAN_POINT ( 'NONE',  ( 0.3777855516927814961, -1.148309276396616729, 0.7252356322318088688 ) ) ;
#3719=CARTESIAN_POINT ( 'NONE',  ( 0.07072154735683021387, -0.9109290280001659523, 0.7683321812563286279 ) ) ;
#3720=CARTESIAN_POINT ( 'NONE',  ( 0.4809147765755076853, -1.118094034716835994, 0.5264152588799988486 ) ) ;
#3721=B_SPLINE_CURVE_WITH_KNOTS ( 'NONE', 3,
 ( #32617, #4817, #17391, #19867, #32404, #29949, #16794, #29341 ),
 .UNSPECIFIED., .F., .F.,
 ( 4, 2, 2, 4 ),
 ( 0.0001297999473408272800, 0.002093273211076724771, 0.003075009842944673340, 0.004056746474812622343 ),
 .UNSPECIFIED. ) ;
#3725=CARTESIAN_POINT ( 'NONE',  ( 0.3247324306352935563, -1.759421949583405365, 0.4854534786567430427 ) ) ;
#3728=CARTESIAN_POINT ( 'NONE',  ( 0.0003933147203880468725, -0.9422125792237651121, 0.2874793698223738203 ) ) ;
#3729=CARTESIAN_POINT ( 'NONE',  ( 0.06448274526053174305, -1.286806166505041427, 0.5182417262812423209 ) ) ;
#3732=( BOUNDED_SURFACE ( )  B_SPLINE_SURFACE ( 3, 2, ( 
 ( #36178, #39273, #1656 ),
 ( #32694, #11096, #4692 ),
 ( #4904, #20970, #1450 ),
 ( #1262, #32884, #4309 ),
 ( #7792, #7987, #27139 ),
 ( #36597, #38853, #29415 ) ),
 .UNSPECIFIED., .F., .F., .F. ) 
 B_SPLINE_SURFACE_WITH_KNOTS ( ( 4, 2, 4 ),
 ( 3, 3 ),
 ( 3.035766082959412415E-18, 0.0004219452060208952896, 0.0008438904120417875434 ),
 ( 0.000000000000000000, 1.000000000000000000 ),
 .UNSPECIFIED. ) 
 GEOMETRIC_REPRESENTATION_ITEM ( )  RATIONAL_B_SPLINE_SURFACE ( (
 ( 1.000000000000000000, 0.8275829691081225681, 1.000000000000000000),
 ( 1.000000000000000000, 0.8234190626268043101, 1.000000000000000000),
 ( 1.000000000000000000, 0.8108491116769944718, 1.000000000000000000),
 ( 1.000000000000000000, 0.7704115495969776628, 1.000000000000000000),
 ( 1.000000000000000000, 0.7425865172308375728, 1.000000000000000000),
 ( 1.000000000000000000, 0.7079223141425768917, 1.000000000000000000) ) ) 
 REPRESENTATION_ITEM ( '' )  SURFACE ( )  );
#3741=CARTESIAN_POINT ( 'NONE',  ( 0.1066313631270083273, -1.413218563028875829, 0.5580310067598821533 ) ) ;
#3742=CARTESIAN_POINT ( 'NONE',  ( 0.2744681798667284456, -1.667287544441652614, 0.6824681254658000462 ) ) ;
#3743=CARTESIAN_POINT ( 'NONE',  ( 0.5951897655464796211, -1.487216002287215622, 0.5778840690689636128 ) ) ;
#3747=ORIENTED_EDGE ( 'NONE', *, *, #8109, .T. ) ;
#3750=ORIENTED_EDGE ( 'NONE', *, *, #9731, .T. ) ;
#3751=DIRECTION ( 'NONE',  ( 0.000000000000000000, 1.000000000000000000, 7.931692224083225994E-17 ) ) ;
#3759=CARTESIAN_POINT ( 'NONE',  ( 0.09447558850840712119, -0.7779443503602000431, 0.3004461803567781142 ) ) ;
#3761=CARTESIAN_POINT ( 'NONE',  ( 0.5396210408343224962, -1.519077833686574230, 0.5827304004285395189 ) ) ;
#3765=CARTESIAN_POINT ( 'NONE',  ( 0.3766692548637607940, -1.738998721234757738, 0.6049789936288398895 ) ) ;
#3766=CARTESIAN_POINT ( 'NONE',  ( 0.7250766506443707682, -1.477170034539755594, 0.7383090895715118673 ) ) ;
#3767=CARTESIAN_POINT ( 'NONE',  ( 0.5779297624755960205, -1.623152544610868109, 0.5629341535590222101 ) ) ;
#3768=CARTESIAN_POINT ( 'NONE',  ( 0.5473208382521128623, -1.395613029667247318, 0.7752695405470998447 ) ) ;
#3772=CARTESIAN_POINT ( 'NONE',  ( 0.001484713323275439105, -0.9577160478316373293, 0.3237126889746802516 ) ) ;
#3773=CARTESIAN_POINT ( 'NONE',  ( 0.5138550893713603740, -1.118750960246259307, 0.5715134594416469982 ) ) ;
#3775=FACE_OUTER_BOUND ( 'NONE', #22812, .T. ) ;
#3778=CARTESIAN_POINT ( 'NONE',  ( 0.4393112170097341340, -1.154367431024637236, 0.4182417262808776903 ) ) ;
#3779=ORIENTED_EDGE ( 'NONE', *, *, #20222, .T. ) ;
#3780=CARTESIAN_POINT ( 'NONE',  ( 0.4426157458868572037, -1.573711800953075279, 0.5837462811315755618 ) ) ;
#3781=CARTESIAN_POINT ( 'NONE',  ( 0.002367394983755363291, -0.5282119844061586855, 0.1345257393686825342 ) ) ;
#3782=CARTESIAN_POINT ( 'NONE',  ( 0.1864731436350384464, -0.8522398885375680466, 0.1983945186742870626 ) ) ;
#3786=CARTESIAN_POINT ( 'NONE',  ( 0.1522219036447276519, -1.333917548074724957, 0.6890782258552490269 ) ) ;
#3787=VERTEX_POINT ( 'NONE', #5161 ) ;
#3795=CARTESIAN_POINT ( 'NONE',  ( 0.03411772795726943780, -0.6984928504873072486, 0.8050285864669745051 ) ) ;
#3796=CARTESIAN_POINT ( 'NONE',  ( 0.1724172692436113929, -0.7740579048028638498, 0.6032149419744345931 ) ) ;
#3797=CARTESIAN_POINT ( 'NONE',  ( 0.003107293377653203969, -0.4819238241330969785, 0.3575383394813408389 ) ) ;
#3798=CARTESIAN_POINT ( 'NONE',  ( 0.4691319308531145538, -1.557781732288214815, 0.5635712613440997387 ) ) ;
#3801=CARTESIAN_POINT ( 'NONE',  ( 0.5970079706708396605, -1.484385675791830561, 0.4807375746916206505 ) ) ;
#3802=CARTESIAN_POINT ( 'NONE',  ( 0.4659064572791866143, -1.067879587118542695, 0.6257723985471262962 ) ) ;
#3810=CARTESIAN_POINT ( 'NONE',  ( 0.5484444682544461491, -1.189958873811490347, 0.8086343185444866410 ) ) ;
#3811=CARTESIAN_POINT ( 'NONE',  ( 0.04175646742902282271, -1.134690233913784096, 0.6571772246382447946 ) ) ;
#3814=CARTESIAN_POINT ( 'NONE',  ( 0.3135409431748647502, -1.021031066816359578, 0.7509690875494603457 ) ) ;
#3815=DIRECTION ( 'NONE',  ( 0.4999551463232372317, -0.8660512985181134660, 0.000000000000000000 ) ) ;
#3819=CARTESIAN_POINT ( 'NONE',  ( 0.5859993564695399337, -1.438286673147110450, 0.6889924778701744801 ) ) ;
#3822=VERTEX_POINT ( 'NONE', #24130 ) ;
#3824=( BOUNDED_SURFACE ( )  B_SPLINE_SURFACE ( 3, 2, ( 
 ( #891, #12792, #34785 ),
 ( #6588, #31711, #16092 ),
 ( #28635, #506, #9896 ),
 ( #6803, #19383, #31919 ),
 ( #16895, #11532, #38881 ),
 ( #29437, #13993, #14203 ),
 ( #13786, #1877, #19979 ),
 ( #32715, #8016, #11317 ),
 ( #36204, #26354, #17683 ),
 ( #20592, #23888, #14596 ),
 ( #1475, #14390, #1685 ),
 ( #24097, #20804, #36008 ),
 ( #4333, #23677, #26770 ),
 ( #26566, #7814, #10714 ),
 ( #36416, #4720, #23286 ),
 ( #39102, #7622, #10926 ),
 ( #23492, #20385, #32912 ),
 ( #36624, #32511, #8228 ) ),
 .UNSPECIFIED., .F., .F., .T. ) 
 B_SPLINE_SURFACE_WITH_KNOTS ( ( 4, 2, 2, 2, 2, 2, 2, 2, 4 ),
 ( 3, 3 ),
 ( 5.421010862427522170E-20, 0.0008416854974228110600, 0.001683370994845622120, 0.002525056492268432963, 0.003366741989691244240, 0.005050112984536865926, 0.005470955733248271564, 0.005891798481959677203, 0.006733483979382488480 ),
 ( 0.000000000000000000, 1.000000000000000000 ),
 .UNSPECIFIED. ) 
 GEOMETRIC_REPRESENTATION_ITEM ( )  RATIONAL_B_SPLINE_SURFACE ( (
 ( 1.000000000000000000, 0.9337218516597644014, 1.000000000000000000),
 ( 1.000000000000000000, 0.9180632194023589099, 1.000000000000000000),
 ( 1.000000000000000000, 0.9017816102666014189, 1.000000000000000000),
 ( 1.000000000000000000, 0.8702833930568698584, 1.000000000000000000),
 ( 1.000000000000000000, 0.8550524697729792178, 1.000000000000000000),
 ( 1.000000000000000000, 0.8283366390151297720, 1.000000000000000000),
 ( 1.000000000000000000, 0.8166982876196974273, 1.000000000000000000),
 ( 1.000000000000000000, 0.7986721614753765630, 1.000000000000000000),
 ( 1.000000000000000000, 0.7922423667821044679, 1.000000000000000000),
 ( 1.000000000000000000, 0.7799115254237425354, 1.000000000000000000),
 ( 1.000000000000000000, 0.7807892787035727311, 1.000000000000000000),
 ( 1.000000000000000000, 0.7819697445861952811, 1.000000000000000000),
 ( 1.000000000000000000, 0.7826749973298559038, 1.000000000000000000),
 ( 1.000000000000000000, 0.7867376866317696837, 1.000000000000000000),
 ( 1.000000000000000000, 0.7898188915124169096, 1.000000000000000000),
 ( 1.000000000000000000, 0.8019006071314157547, 1.000000000000000000),
 ( 1.000000000000000000, 0.8137456928813621149, 1.000000000000000000),
 ( 1.000000000000000000, 0.8282401589944672349, 1.000000000000000000) ) ) 
 REPRESENTATION_ITEM ( '' )  SURFACE ( )  );
#3825=CARTESIAN_POINT ( 'NONE',  ( 0.2233893057605496613, -1.353603863650753469, 0.4173121127524894169 ) ) ;
#3828=CARTESIAN_POINT ( 'NONE',  ( 0.4269689327050869565, -1.183341550326573177, 0.7120333345843747885 ) ) ;
#3830=CARTESIAN_POINT ( 'NONE',  ( 0.3219857165489931061, -1.758039968903889250, 0.4848815471996625326 ) ) ;
#3831=CARTESIAN_POINT ( 'NONE',  ( 0.1856290495283919040, -0.8698730627085041744, 0.1722928722954065184 ) ) ;
#3833=CARTESIAN_POINT ( 'NONE',  ( 0.01482441653333900489, -0.9260584756313956500, 0.5696548266057109844 ) ) ;
#3835=CARTESIAN_POINT ( 'NONE',  ( 0.3872640377415917934, -1.605414403979557925, 0.6082151896501704069 ) ) ;
#3836=CARTESIAN_POINT ( 'NONE',  ( 0.08543706580305507337, -0.8249828158407566114, 0.1015297857590274355 ) ) ;
#3837=CARTESIAN_POINT ( 'NONE',  ( 0.1843176191431192545, -0.8530889732836612893, 0.1272869310077573146 ) ) ;
#3842=CARTESIAN_POINT ( 'NONE',  ( 0.5384555088268765388, -1.160728211852388947, 0.5797400768281307792 ) ) ;
#3844=CARTESIAN_POINT ( 'NONE',  ( 0.5668525377163954326, -1.503218863262137939, 0.5717302897758860247 ) ) ;
#3845=ORIENTED_EDGE ( 'NONE', *, *, #30859, .F. ) ;
#3850=CARTESIAN_POINT ( 'NONE',  ( 0.4567198261210261845, -1.219045092035883293, 0.5856983068965102568 ) ) ;
#3859=CARTESIAN_POINT ( 'NONE',  ( 0.07115259279998498165, -1.324306246913844021, 0.5002830441458163691 ) ) ;
#3860=CARTESIAN_POINT ( 'NONE',  ( 0.3186320389496528627, -1.760431904683431359, 0.5682417262808792113 ) ) ;
#3863=DIRECTION ( 'NONE',  ( 0.9931241558664195557, 5.463695987328507662E-14, -0.1170658405966981674 ) ) ;
#3865=CARTESIAN_POINT ( 'NONE',  ( 0.1845357796896161806, -0.8398727082387180687, 0.07607969940124001407 ) ) ;
#3870=CARTESIAN_POINT ( 'NONE',  ( 0.2491647336858476003, -1.658092311124387708, 0.5917354811442696594 ) ) ;
#3871=CARTESIAN_POINT ( 'NONE',  ( -0.0001404195193253628224, -0.8121462962669929730, -0.07004528601953871614 ) ) ;
#3881=CARTESIAN_POINT ( 'NONE',  ( 0.4655342829600510046, -1.243759628728527966, 0.7615958905844258942 ) ) ;
#3884=CARTESIAN_POINT ( 'NONE',  ( 0.2882448896600493526, -0.8342145444298804113, 0.5948296420995525802 ) ) ;
#3887=CARTESIAN_POINT ( 'NONE',  ( 0.5953197980378833742, -1.599064723402610300, 0.4311035055375501135 ) ) ;
#3889=CARTESIAN_POINT ( 'NONE',  ( 0.01207517534499727083, -0.5592029808840295324, 0.2697748480126794801 ) ) ;
#3893=CARTESIAN_POINT ( 'NONE',  ( 0.01204206997202984797, -0.4674074136848835326, 0.008773000355436783720 ) ) ;
#3895=ORIENTED_EDGE ( 'NONE', *, *, #28545, .T. ) ;
#3898=CARTESIAN_POINT ( 'NONE',  ( 0.2516264960652024874, -0.9499261728892368639, 0.4858447589484862217 ) ) ;
#3902=CARTESIAN_POINT ( 'NONE',  ( 0.3705277829417951141, -1.241127117052787554, 0.6578903985100409413 ) ) ;
#3905=CARTESIAN_POINT ( 'NONE',  ( 0.4716011037672954709, -1.161152322290847971, 0.4182417262808811320 ) ) ;
#3912=FACE_OUTER_BOUND ( 'NONE', #31874, .T. ) ;
#3913=CARTESIAN_POINT ( 'NONE',  ( 0.1797611301157409636, -0.4952674041179104814, 0.1258321121258487441 ) ) ;
#3916=CARTESIAN_POINT ( 'NONE',  ( 0.4394396372989468613, -1.699335966064649206, 0.4346836767675715252 ) ) ;
#3922=CARTESIAN_POINT ( 'NONE',  ( 0.1048591973540500683, -1.410537849644770025, 0.5682417262808777680 ) ) ;
#3923=CARTESIAN_POINT ( 'NONE',  ( 0.2629078703310521736, -1.686706023028639478, 0.5455699756094425368 ) ) ;
#3924=CARTESIAN_POINT ( 'NONE',  ( 0.1314486695871137090, -0.5541963170049430953, 0.1786156050719973354 ) ) ;
#3925=CARTESIAN_POINT ( 'NONE',  ( 0.5536297569049346556, -1.186194075236972179, 0.6057417262809815517 ) ) ;
#3930=CARTESIAN_POINT ( 'NONE',  ( 0.6296519982359254364, -1.458631199707426385, 0.8241730067046653119 ) ) ;
#3935=CARTESIAN_POINT ( 'NONE',  ( -0.002922341574000678326, -0.8469330747986107966, 0.04185307883324775047 ) ) ;
#3937=CARTESIAN_POINT ( 'NONE',  ( 0.1157690968366767853, -0.8206980902245742948, 0.4173617279069409824 ) ) ;
#3938=EDGE_CURVE ( 'NONE', #13059, #29074, #36012, .T. ) ;
#3940=CARTESIAN_POINT ( 'NONE',  ( 0.1903510223940173829, -0.8354967341176428031, 0.6604265076868101048 ) ) ;
#3945=ADVANCED_FACE ( 'NONE', ( #4050 ), #25775, .F. ) ;
#3947=CARTESIAN_POINT ( 'NONE',  ( 0.4191100986681001173, -1.701672718972385701, 0.4233639548768205474 ) ) ;
#3952=CARTESIAN_POINT ( 'NONE',  ( 0.6090209075241541647, -1.479030249925110008, 0.5727419068642127797 ) ) ;
#3953=CARTESIAN_POINT ( 'NONE',  ( -6.803815825995611946E-06, -0.7962170029740717192, -0.09155518444196047989 ) ) ;
#3957=CARTESIAN_POINT ( 'NONE',  ( 0.05796715499547382133, -1.320156192035571774, 0.6033327867956804758 ) ) ;
#3958=CARTESIAN_POINT ( 'NONE',  ( 0.5099336548069899333, -1.112575729146672243, 0.5993070616419141627 ) ) ;
#3961=FACE_OUTER_BOUND ( 'NONE', #6511, .T. ) ;
#3965=CARTESIAN_POINT ( 'NONE',  ( 0.3164584772848521577, -1.761781577301324786, 0.5677477157759467374 ) ) ;
#3968=CARTESIAN_POINT ( 'NONE',  ( 0.002296835029421141847, -0.5198933010532248433, 0.1369805761320314896 ) ) ;
#3970=CARTESIAN_POINT ( 'NONE',  ( 0.08659183687672357410, -0.7486551410394269856, 0.03870967331810245410 ) ) ;
#3972=CARTESIAN_POINT ( 'NONE',  ( 0.4972671625857253974, -1.080199071502573771, 0.5707417262808780478 ) ) ;
#3973=CARTESIAN_POINT ( 'NONE',  ( 0.1927903040881008279, -0.5292341811144671837, 0.2767179517167643321 ) ) ;
#3976=PLANE ( 'NONE',  #26437 ) ;
#3984=CARTESIAN_POINT ( 'NONE',  ( 0.3022532383517997912, -1.314739514998899850, 1.137766315222363822 ) ) ;
#3985=CARTESIAN_POINT ( 'NONE',  ( 0.09335318867712337487, -0.5801916173533016030, 0.2651423415210660273 ) ) ;
#3986=CARTESIAN_POINT ( 'NONE',  ( 0.03472485495275277889, -0.6070042031976854435, 0.5858001736030246098 ) ) ;
#3987=CARTESIAN_POINT ( 'NONE',  ( 0.08585723802341010957, -0.5540659370326329602, 0.2123023186766486992 ) ) ;
#3989=CARTESIAN_POINT ( 'NONE',  ( 0.3699448142092459091, -1.724996014291202195, 0.4246285625532579822 ) ) ;
#3990=CARTESIAN_POINT ( 'NONE',  ( 0.1406250000000002220, -0.9233928627580063608, 0.1613420322700153120 ) ) ;
#3991=ORIENTED_EDGE ( 'NONE', *, *, #24482, .F. ) ;
#3992=VERTEX_POINT ( 'NONE', #35737 ) ;
#4001=CARTESIAN_POINT ( 'NONE',  ( 0.6205349385892930947, -1.302967389835202772, 0.7736340727560927499 ) ) ;
#4002=B_SPLINE_CURVE_WITH_KNOTS ( 'NONE', 3,
 ( #26798, #23520, #7225, #7436, #23317, #7839 ),
 .UNSPECIFIED., .F., .F.,
 ( 4, 2, 4 ),
 ( 0.000000000000000000, 0.0004017397477019867208, 0.0008034794954039734417 ),
 .UNSPECIFIED. ) ;
#4003=CARTESIAN_POINT ( 'NONE',  ( 0.5369453289148307107, -1.161830891981910030, 0.5366278456428995591 ) ) ;
#4004=CARTESIAN_POINT ( 'NONE',  ( 0.05992504362659526601, -1.332686182584564838, 0.5764222388007066433 ) ) ;
#4010=CARTESIAN_POINT ( 'NONE',  ( 0.3662562376110679030, -1.103567295189709974, 0.7374271453170119228 ) ) ;
#4015=CARTESIAN_POINT ( 'NONE',  ( 0.5753973661769585801, -1.420263886208666282, 0.7195733474900496418 ) ) ;
#4018=CARTESIAN_POINT ( 'NONE',  ( 0.05610887725588498132, -0.8376633732021888656, 0.2147192758300057736 ) ) ;
#4022=CARTESIAN_POINT ( 'NONE',  ( 0.4803259847655330095, -1.663598153568734528, 0.4773340106711829733 ) ) ;
#4024=CARTESIAN_POINT ( 'NONE',  ( 0.4128242711560994871, -1.164714445187265524, 0.7168935161660692224 ) ) ;
#4027=FACE_OUTER_BOUND ( 'NONE', #4029, .T. ) ;
#4028=CARTESIAN_POINT ( 'NONE',  ( 0.1854168535569867549, -0.8697360073808747538, 0.1457185332388700738 ) ) ;
#4029=EDGE_LOOP ( 'NONE', ( #8678, #29260, #25409, #23135 ) ) ;
#4034=CARTESIAN_POINT ( 'NONE',  ( 0.2186375681070903965, -1.111317829052481443, 0.8545239218465585651 ) ) ;
#4035=CARTESIAN_POINT ( 'NONE',  ( 0.08727560228832158262, -0.7066680270200008662, 0.002681738102100845057 ) ) ;
#4036=CARTESIAN_POINT ( 'NONE',  ( 0.2033340932986389682, -0.6878354212131936318, 0.3466422550156073035 ) ) ;
#4037=LINE ( 'NONE', #32427, #11255 ) ;
#4041=DIRECTION ( 'NONE',  ( 0.8660512985181129109, 0.4999551463232380089, 0.000000000000000000 ) ) ;
#4042=CARTESIAN_POINT ( 'NONE',  ( 0.1192597013057371258, -0.5508091639576637721, 0.1706685560853501427 ) ) ;
#4043=ORIENTED_EDGE ( 'NONE', *, *, #20338, .F. ) ;
#4044=CARTESIAN_POINT ( 'NONE',  ( 0.1874553688902439730, -0.6895457488572201976, 0.05837238906507073027 ) ) ;
#4046=CARTESIAN_POINT ( 'NONE',  ( 0.5959315179729322010, -1.587052097778462789, 0.4182417262808776903 ) ) ;
#4049=B_SPLINE_CURVE_WITH_KNOTS ( 'NONE', 3,
 ( #2588, #15341, #27080, #12262 ),
 .UNSPECIFIED., .F., .F.,
 ( 4, 4 ),
 ( 2.201117333616983429E-17, 0.0002394164967011357874 ),
 .UNSPECIFIED. ) ;
#4050=FACE_OUTER_BOUND ( 'NONE', #3692, .T. ) ;
#4051=CARTESIAN_POINT ( 'NONE',  ( 0.7429241260303105499, -1.515741207197444762, 0.5682417262808782121 ) ) ;
#4053=CARTESIAN_POINT ( 'NONE',  ( 0.06581764578086118922, -1.340728352476674212, 0.5449258910593480776 ) ) ;
#4054=CARTESIAN_POINT ( 'NONE',  ( 0.1166065821415038645, -1.415338206367126039, 0.5682417262808805436 ) ) ;
#4056=AXIS2_PLACEMENT_3D ( 'NONE', #23864, #39888, #24262 ) ;
#4058=CARTESIAN_POINT ( 'NONE',  ( 0.2317652421976991728, -1.348504658504371179, 0.5084384545799764954 ) ) ;
#4065=CARTESIAN_POINT ( 'NONE',  ( 0.003124719664520401140, -0.5686731593868927792, 0.1286173008190011902 ) ) ;
#4066=CARTESIAN_POINT ( 'NONE',  ( 0.0002050826195777198982, -0.5232135321910946768, -0.04216937712956515816 ) ) ;
#4069=CARTESIAN_POINT ( 'NONE',  ( 0.3245308759113119113, -1.295391163961464365, 0.5682442948123348492 ) ) ;
#4070=LINE ( 'NONE', #14150, #19062 ) ;
#4076=CARTESIAN_POINT ( 'NONE',  ( 0.4114930829410045621, -1.163324819952073153, 0.7935316178056401881 ) ) ;
#4079=CARTESIAN_POINT ( 'NONE',  ( 0.5539006188405288800, -1.190957016459229800, 0.5326915342634773731 ) ) ;
#4084=CARTESIAN_POINT ( 'NONE',  ( 0.2735842598402163928, -1.463806052640699074, 0.8970317457453208521 ) ) ;
#4085=CARTESIAN_POINT ( 'NONE',  ( 0.5998866944813460167, -1.596483326503711719, 0.4395608873836979180 ) ) ;
#4087=CARTESIAN_POINT ( 'NONE',  ( 0.3048982267989291395, -1.756746414302343240, 0.5594309555313042859 ) ) ;
#4090=ORIENTED_EDGE ( 'NONE', *, *, #8343, .F. ) ;
#4092=CARTESIAN_POINT ( 'NONE',  ( 0.2942177235634530486, -0.9707437518647973329, 0.5507622206958932010 ) ) ;
#4093=CARTESIAN_POINT ( 'NONE',  ( 0.4076976354719489271, -1.154888438488554270, 0.4182417262808778013 ) ) ;
#4095=AXIS2_PLACEMENT_3D ( 'NONE', #28568, #19317, #16233 ) ;
#4098=CARTESIAN_POINT ( 'NONE',  ( 0.1475391676095154925, -0.8805552411648984723, 0.5367235207948595210 ) ) ;
#4102=CARTESIAN_POINT ( 'NONE',  ( 0.4929769546720680351, -1.176658441934731458, 0.4224096261816105979 ) ) ;
#4104=CARTESIAN_POINT ( 'NONE',  ( 0.6666114888622571844, -1.509927429286209044, 0.4229734475664606586 ) ) ;
#4109=CARTESIAN_POINT ( 'NONE',  ( 0.1781059945513061293, -0.4912486924221262652, 0.1372122367638805851 ) ) ;
#4110=CARTESIAN_POINT ( 'NONE',  ( 0.1100897290998920502, -1.360766454520437874, 0.6863977214180455588 ) ) ;
#4111=CARTESIAN_POINT ( 'NONE',  ( 0.3748597602280495655, -1.730449573624088577, 0.4273137188976714462 ) ) ;
#4114=CARTESIAN_POINT ( 'NONE',  ( 0.3114308091870697237, -1.743858490366296810, 0.7215154734554626303 ) ) ;
#4121=CARTESIAN_POINT ( 'NONE',  ( 0.4800914148601737041, -1.127024615723082102, 0.4875502256570667381 ) ) ;
#4126=CARTESIAN_POINT ( 'NONE',  ( 0.5832970171292772843, -1.454869700092910501, 0.7147772481381597931 ) ) ;
#4129=B_SPLINE_CURVE_WITH_KNOTS ( 'NONE', 3,
 ( #32178, #3989, #10383, #22946, #35463, #32985 ),
 .UNSPECIFIED., .F., .F.,
 ( 4, 2, 4 ),
 ( 0.000000000000000000, 0.0006518578806776564958, 0.001303715761355312992 ),
 .UNSPECIFIED. ) ;
#4133=ORIENTED_EDGE ( 'NONE', *, *, #25582, .T. ) ;
#4136=CARTESIAN_POINT ( 'NONE',  ( -0.01391884973526399255, -0.5383837722425610650, 0.2220458723941181878 ) ) ;
#4139=CARTESIAN_POINT ( 'NONE',  ( -0.001424324173367915976, -0.4210325180397652134, -0.01138449076159632478 ) ) ;
#4141=CARTESIAN_POINT ( 'NONE',  ( 0.08528037396856456842, -0.7892970555466644056, 0.1714812305220828614 ) ) ;
#4142=CARTESIAN_POINT ( 'NONE',  ( 0.08991044991096724948, -0.5436620188964982336, 0.1477941536733499428 ) ) ;
#4143=CARTESIAN_POINT ( 'NONE',  ( 0.4295717892363857815, -1.330470044908041549, 0.8374933259477883585 ) ) ;
#4145=CARTESIAN_POINT ( 'NONE',  ( 0.1765658034078008420, -0.4883776638658609004, 0.1544953457633272131 ) ) ;
#4147=CARTESIAN_POINT ( 'NONE',  ( 0.1876053338355621880, -0.6785855078148245179, 0.1477569985384105666 ) ) ;
#4148=CARTESIAN_POINT ( 'NONE',  ( 0.7033168319441670535, -1.517879297504465264, 0.5416718245419247513 ) ) ;
#4151=CARTESIAN_POINT ( 'NONE',  ( 0.3612474431891336546, -1.736522368699831231, 0.6106949725924829542 ) ) ;
#4155=CARTESIAN_POINT ( 'NONE',  ( 0.08146015332400738385, -1.318321297778865864, 0.4704503523288164346 ) ) ;
#4156=CARTESIAN_POINT ( 'NONE',  ( 0.6095253909009431537, -1.478947137852041571, 0.5845166421031070536 ) ) ;
#4158=CARTESIAN_POINT ( 'NONE',  ( -2.078131108109570059E-05, -0.9329081451665184321, 0.05729297375900673644 ) ) ;
#4159=CARTESIAN_POINT ( 'NONE',  ( 0.2056584174081136918, -0.8821123478198787948, 0.6984915149204232732 ) ) ;
#4160=CARTESIAN_POINT ( 'NONE',  ( 0.007872950027890082692, -0.7282374440040403352, -0.007258173132335108725 ) ) ;
#4163=CARTESIAN_POINT ( 'NONE',  ( 0.04935217837593552231, -1.087446678362770758, 0.7326706496891072229 ) ) ;
#4165=CARTESIAN_POINT ( 'NONE',  ( 0.2392493758066867593, -0.9067917679836680067, 0.4646394045636887959 ) ) ;
#4172=CARTESIAN_POINT ( 'NONE',  ( 0.4322324054394098281, -1.579800052727432513, 0.5947161825314808414 ) ) ;
#4173=CARTESIAN_POINT ( 'NONE',  ( 0.002410463536293692022, -0.5295147390142669330, 0.2118009195250746268 ) ) ;
#4178=CARTESIAN_POINT ( 'NONE',  ( 0.3424415908863561175, -1.747937484235674965, 0.4483338674950549940 ) ) ;
#4180=CARTESIAN_POINT ( 'NONE',  ( 0.1900797982425219412, -0.5100199057060679220, 0.2041009711615301980 ) ) ;
#4181=ORIENTED_EDGE ( 'NONE', *, *, #35299, .F. ) ;
#4191=CARTESIAN_POINT ( 'NONE',  ( 0.008753005055724370764, -0.6364574594817896669, -0.004136954017640373515 ) ) ;
#4192=CARTESIAN_POINT ( 'NONE',  ( 0.1716834812988722314, -0.8138579001414996128, 0.5861123461217216946 ) ) ;
#4194=CARTESIAN_POINT ( 'NONE',  ( 0.05060316692271353556, -0.6842963399715571438, 0.6915224596933228218 ) ) ;
#4195=CARTESIAN_POINT ( 'NONE',  ( 0.4698952129795286314, -1.558024368996808517, 0.5758555327645124011 ) ) ;
#4200=CARTESIAN_POINT ( 'NONE',  ( 0.2598333277624153004, -1.180520155007462435, 0.6285950746444651793 ) ) ;
#4203=ORIENTED_EDGE ( 'NONE', *, *, #36386, .F. ) ;
#4204=CARTESIAN_POINT ( 'NONE',  ( 0.3417996877168656411, -1.631766885285335533, 0.5547720684252442913 ) ) ;
#4206=CARTESIAN_POINT ( 'NONE',  ( 0.1756091917461258811, -0.6487560037695216941, 0.5970464724471860052 ) ) ;
#4212=CARTESIAN_POINT ( 'NONE',  ( 0.6714320665202346827, -1.386459733509071368, 0.6790741990638067271 ) ) ;
#4219=CARTESIAN_POINT ( 'NONE',  ( 0.3300652619718623670, -1.292236477103671621, 0.5183498055548371175 ) ) ;
#4220=CARTESIAN_POINT ( 'NONE',  ( 0.3469326936793421523, -1.116650062515026853, 0.7379221599654642860 ) ) ;
#4228=EDGE_CURVE ( 'NONE', #30976, #3992, #7943, .T. ) ;
#4231=CARTESIAN_POINT ( 'NONE',  ( 0.2733626960385290849, -1.310524412086364388, 0.6293287939193288327 ) ) ;
#4235=CARTESIAN_POINT ( 'NONE',  ( 0.1692576441742112137, -1.384930168205611656, 0.4264492190452435771 ) ) ;
#4238=CARTESIAN_POINT ( 'NONE',  ( 0.4874659257962786763, -1.270923258226311470, 0.6194086313868705229 ) ) ;
#4240=CARTESIAN_POINT ( 'NONE',  ( 0.3128440348530873716, -1.762786819375506964, 0.5229383029344989442 ) ) ;
#4243=CIRCLE ( 'NONE', #10151, 0.009999999999999913472 ) ;
#4246=VERTEX_POINT ( 'NONE', #11662 ) ;
#4247=CARTESIAN_POINT ( 'NONE',  ( 0.4133098505097531628, -1.589431319560335121, 0.5690080242323289905 ) ) ;
#4248=CARTESIAN_POINT ( 'NONE',  ( 0.08559278432067010667, -0.7989444401597723955, 0.09288191320694452746 ) ) ;
#4249=CARTESIAN_POINT ( 'NONE',  ( 0.1962081386259882654, -0.6973007354887533760, 0.3322094209430815903 ) ) ;
#4250=CARTESIAN_POINT ( 'NONE',  ( 0.4685502202651029569, -1.116536938686066183, 0.5688043585934901003 ) ) ;
#4252=ORIENTED_EDGE ( 'NONE', *, *, #22017, .T. ) ;
#4254=EDGE_CURVE ( 'NONE', #13571, #31015, #19263, .T. ) ;
#4256=CARTESIAN_POINT ( 'NONE',  ( 0.5732312758898047145, -1.493991244289733400, 0.6439092248849844768 ) ) ;
#4258=CONICAL_SURFACE ( 'NONE', #27270, 0.2609684784060898322, 0.1745329251994329756 ) ;
#4259=CARTESIAN_POINT ( 'NONE',  ( 0.1874424658970250124, -0.6905203129132115869, 0.04637705369058030269 ) ) ;
#4262=CARTESIAN_POINT ( 'NONE',  ( 0.4190734387097265756, -1.701429136684833976, 0.4229605459736927586 ) ) ;
#4264=B_SPLINE_CURVE_WITH_KNOTS ( 'NONE', 3,
 ( #15756, #40459, #27708, #12283, #34484, #25447 ),
 .UNSPECIFIED., .F., .F.,
 ( 4, 2, 4 ),
 ( 9.341771812940338307E-18, 0.0005303069012029996239, 0.001060613802405989924 ),
 .UNSPECIFIED. ) ;
#4267=CARTESIAN_POINT ( 'NONE',  ( 0.6699292074404794572, -1.569526485364059143, 0.6071573546319902759 ) ) ;
#4271=AXIS2_PLACEMENT_3D ( 'NONE', #11398, #8313, #23969 ) ;
#4273=CARTESIAN_POINT ( 'NONE',  ( 0.1847812854686134709, -0.6668630515069209341, -0.02837765232073623592 ) ) ;
#4274=FACE_BOUND ( 'NONE', #22324, .T. ) ;
#4275=CARTESIAN_POINT ( 'NONE',  ( 0.08146015332400816100, -1.318321297778866086, 0.4704503523288147138 ) ) ;
#4278=CARTESIAN_POINT ( 'NONE',  ( 0.2385638199407473237, -1.468035130309864655, 0.9857930272948494110 ) ) ;
#4281=EDGE_CURVE ( 'NONE', #15271, #5090, #8462, .T. ) ;
#4287=CARTESIAN_POINT ( 'NONE',  ( 0.4972320539234349468, -1.080138254241686413, 0.5197417262808780025 ) ) ;
#4291=CARTESIAN_POINT ( 'NONE',  ( 0.4869258355362139912, -1.276216671384446943, 0.7509782588010058824 ) ) ;
#4294=CARTESIAN_POINT ( 'NONE',  ( 0.1932042024315755446, -0.7994606748157702114, 0.2910003379690608294 ) ) ;
#4295=CARTESIAN_POINT ( 'NONE',  ( 0.1610229998878659197, -0.4681091962081970759, 0.1457315164630837434 ) ) ;
#4300=CARTESIAN_POINT ( 'NONE',  ( 0.02332224506199178857, -0.5411761724791561701, 0.2067749293666701627 ) ) ;
#4301=CARTESIAN_POINT ( 'NONE',  ( 0.6263553037110800581, -1.578101984896422616, 0.4270759148754849632 ) ) ;
#4303=CARTESIAN_POINT ( 'NONE',  ( 0.2318589737339854795, -1.232498520698479982, 0.5197417262808780025 ) ) ;
#4308=CARTESIAN_POINT ( 'NONE',  ( 0.2281093225164023686, -0.8646107249477655854, 0.4403547256474249494 ) ) ;
#4309=CARTESIAN_POINT ( 'NONE',  ( 0.1778554964483612943, -1.275556741434257679, 0.4182417262808778013 ) ) ;
#4311=CARTESIAN_POINT ( 'NONE',  ( 0.3213554034218941147, -1.166633905577155739, 0.7304078056503604532 ) ) ;
#4314=CARTESIAN_POINT ( 'NONE',  ( 0.4230904536261725912, -1.143177874484793577, 0.4241467574966739096 ) ) ;
#4316=CARTESIAN_POINT ( 'NONE',  ( 0.003668565761957516980, -0.8459993161072223433, 0.1457185332388710730 ) ) ;
#4319=CARTESIAN_POINT ( 'NONE',  ( 0.6435666744728262278, -1.544684321070708188, 0.4182417262808778013 ) ) ;
#4321=CARTESIAN_POINT ( 'NONE',  ( 0.2797581386905990675, -1.667519014922642873, 0.4662658620133214304 ) ) ;
#4323=CARTESIAN_POINT ( 'NONE',  ( 0.007337869580115062226, -0.9842806402802338761, 0.4958900936016981120 ) ) ;
#4326=CARTESIAN_POINT ( 'NONE',  ( 0.1097570854172637417, -1.412022420605677953, 0.6115137485124468864 ) ) ;
#4330=AXIS2_PLACEMENT_3D ( 'NONE', #15747, #13485, #765 ) ;
#4331=CARTESIAN_POINT ( 'NONE',  ( 0.7066102454780193165, -1.509906364535708923, 0.5603690879523279822 ) ) ;
#4333=CARTESIAN_POINT ( 'NONE',  ( 0.1727484476632766552, -0.5194822410394417389, 0.1386055728184389102 ) ) ;
#4337=CARTESIAN_POINT ( 'NONE',  ( 0.1402024954270775225, -0.6142130989947057751, 0.3459447826026630368 ) ) ;
#4342=VERTEX_POINT ( 'NONE', #12881 ) ;
#4344=ORIENTED_EDGE ( 'NONE', *, *, #33135, .T. ) ;
#4345=CARTESIAN_POINT ( 'NONE',  ( 0.03052257359372401863, -0.7992890816565190182, 0.6712346997200854259 ) ) ;
#4350=ORIENTED_EDGE ( 'NONE', *, *, #450, .T. ) ;
#4352=CARTESIAN_POINT ( 'NONE',  ( 0.1991609519065172529, -0.9184688065175017346, 0.6111039586238895538 ) ) ;
#4353=CARTESIAN_POINT ( 'NONE',  ( 0.09335350967634557795, -0.5942487015407079687, 0.2614486645500827544 ) ) ;
#4354=CARTESIAN_POINT ( 'NONE',  ( 0.5391681719232660486, -1.519059681939239903, 0.5745203956527785705 ) ) ;
#4356=CARTESIAN_POINT ( 'NONE',  ( 0.05545227241544782582, -1.226087868501680056, 0.6599560881964448011 ) ) ;
#4357=CARTESIAN_POINT ( 'NONE',  ( 0.6045036416640916510, -1.481621646331015008, 0.5979483913144312268 ) ) ;
#4366=CARTESIAN_POINT ( 'NONE',  ( 0.01165121832836692878, -0.7716130889810013382, -0.09920548477954149735 ) ) ;
#4367=CARTESIAN_POINT ( 'NONE',  ( 0.5454855820205488648, -1.408499188346827857, 0.7723196400189406008 ) ) ;
#4370=DIRECTION ( 'NONE',  ( -0.8315239468457111816, -0.5057278275750267671, -0.2297983686590817365 ) ) ;
#4371=CARTESIAN_POINT ( 'NONE',  ( 0.5433433239293584682, -1.169038973927291503, 0.5856983068965047057 ) ) ;
#4374=CARTESIAN_POINT ( 'NONE',  ( 0.1877024697326355740, -1.541847387273544756, 0.6461194557730155497 ) ) ;
#4375=CARTESIAN_POINT ( 'NONE',  ( 0.2803482358567763177, -0.9348470554797825294, 0.5439829518127811125 ) ) ;
#4377=CARTESIAN_POINT ( 'NONE',  ( 0.5433433239293584682, -1.169038973927291503, 0.5856983068965047057 ) ) ;
#4383=CARTESIAN_POINT ( 'NONE',  ( 0.01056251376256645870, -0.5300776972628027384, 0.1582814761548828608 ) ) ;
#4384=CARTESIAN_POINT ( 'NONE',  ( 0.09963077645664282500, -1.298161551546404890, 0.4482597153589827910 ) ) ;
#4388=CARTESIAN_POINT ( 'NONE',  ( 0.4929832608774247782, -1.104425667152665991, 0.8058332650092189242 ) ) ;
#4398=CARTESIAN_POINT ( 'NONE',  ( 0.1875000000000003608, -0.4593131964907913312, 0.1856949347217509150 ) ) ;
#4399=CARTESIAN_POINT ( 'NONE',  ( 0.08753440268785935008, -0.6845692626716123330, 0.1571571781002649437 ) ) ;
#4400=CARTESIAN_POINT ( 'NONE',  ( 0.01220488673141941274, -0.4284039384351941426, 0.1457185332388690469 ) ) ;
#4401=CARTESIAN_POINT ( 'NONE',  ( 0.09266747603540267941, -0.6010366268050462146, 0.3369889307053728911 ) ) ;
#4402=CARTESIAN_POINT ( 'NONE',  ( 0.09285203301658104258, -1.021206517960446369, 0.8557725610849984399 ) ) ;
#4404=CARTESIAN_POINT ( 'NONE',  ( 0.1443024366174217588, -1.195940908848212691, 0.6505907527369143573 ) ) ;
#4408=CARTESIAN_POINT ( 'NONE',  ( 0.1912291182594794137, -0.6824372825164394252, 0.6358572396827846251 ) ) ;
#4416=CARTESIAN_POINT ( 'NONE',  ( 0.1912376716460947867, -0.5867422834582064484, 0.1926850933134615362 ) ) ;
#4418=CARTESIAN_POINT ( 'NONE',  ( 0.01456394726322781524, -0.9250865771959065897, 0.5675178823144181317 ) ) ;
#4421=CARTESIAN_POINT ( 'NONE',  ( 0.3869860216863779678, -1.170324191591702867, 0.7132054132965995885 ) ) ;
#4426=ORIENTED_EDGE ( 'NONE', *, *, #34617, .F. ) ;
#4427=CARTESIAN_POINT ( 'NONE',  ( 0.09014181593920955748, -0.5678796035371341810, 0.1769828697681403995 ) ) ;
#4429=CARTESIAN_POINT ( 'NONE',  ( 0.4091244934080342510, -1.134466909110688482, 0.4685100012138834202 ) ) ;
#4431=CARTESIAN_POINT ( 'NONE',  ( 0.03202889392918712580, -0.8409986250695938859, 0.1457185332388704624 ) ) ;
#4435=CARTESIAN_POINT ( 'NONE',  ( 0.1466125325700726734, -1.398062017178772098, 0.4425755552918825830 ) ) ;
#4436=CARTESIAN_POINT ( 'NONE',  ( 0.4862264814005418656, -1.268791747036731365, 0.6246861129760243880 ) ) ;
#4438=DIRECTION ( 'NONE',  ( -0.4999551463232372317, 0.8660512985181135770, -0.000000000000000000 ) ) ;
#4443=CARTESIAN_POINT ( 'NONE',  ( 0.3467465376597937410, -1.426445918686239489, 0.8672919671349224036 ) ) ;
#4444=CARTESIAN_POINT ( 'NONE',  ( 0.06705560988554902513, -0.6676997200371664887, -0.0009185627879479015250 ) ) ;
#4446=CARTESIAN_POINT ( 'NONE',  ( 0.1586456724622636871, -1.275316570454761322, 0.4817113887073902756 ) ) ;
#4450=CARTESIAN_POINT ( 'NONE',  ( 0.1307689245043377746, -0.6231473675091006026, 0.3697794014886608416 ) ) ;
#4451=ORIENTED_EDGE ( 'NONE', *, *, #10258, .T. ) ;
#4454=EDGE_CURVE ( 'NONE', #31881, #36413, #17470, .T. ) ;
#4456=CARTESIAN_POINT ( 'NONE',  ( 0.1579832900275356389, -1.275892853358665979, 0.4209669457040660645 ) ) ;
#4457=ADVANCED_FACE ( 'NONE', ( #19050 ), #19653, .T. ) ;
#4458=CARTESIAN_POINT ( 'NONE',  ( 0.07197331016010956317, -1.314323866689726339, 0.4956685533872550176 ) ) ;
#4460=CARTESIAN_POINT ( 'NONE',  ( 0.1875000000000001943, -0.4593131964907913312, 0.1457185332388694909 ) ) ;
#4466=CARTESIAN_POINT ( 'NONE',  ( 0.1837736376643801794, -0.5304624996123088465, 0.05163021866974163571 ) ) ;
#4467=CARTESIAN_POINT ( 'NONE',  ( 0.4687869482605488969, -1.212150898723653114, 0.4951799515542131269 ) ) ;
#4468=CARTESIAN_POINT ( 'NONE',  ( 0.1398272630092362578, -1.288459453437826419, 0.4193546253734958817 ) ) ;
#4469=CARTESIAN_POINT ( 'NONE',  ( 3.304294434668030104E-05, -0.6893515101347650331, 0.1975634471597359221 ) ) ;
#4474=CARTESIAN_POINT ( 'NONE',  ( 0.5959315179729189893, -1.587052097778458348, 0.4182417262808776903 ) ) ;
#4478=ORIENTED_EDGE ( 'NONE', *, *, #30346, .T. ) ;
#4482=DIRECTION ( 'NONE',  ( 0.8660512985181136880, 0.4999551463232367876, 0.000000000000000000 ) ) ;
#4484=CARTESIAN_POINT ( 'NONE',  ( 0.5037817747200005192, -1.302264079412044362, 0.7382972978228007355 ) ) ;
#4487=CARTESIAN_POINT ( 'NONE',  ( 0.2974794542262550467, -0.9002722561939086043, 0.5860092920552725237 ) ) ;
#4492=CARTESIAN_POINT ( 'NONE',  ( 0.03244836639777012866, -0.6168844639952264508, 0.3981205770845226977 ) ) ;
#4493=CARTESIAN_POINT ( 'NONE',  ( 0.6503292821894245401, -1.549301679588444891, 0.4221565037074623827 ) ) ;
#4494=DIRECTION ( 'NONE',  ( -0.01254811300245605755, -0.8659344938869285579, -0.4999999971568663826 ) ) ;
#4495=CARTESIAN_POINT ( 'NONE',  ( 0.2316917763911649497, -1.232208891764917880, 0.5707417262808780478 ) ) ;
#4497=VERTEX_POINT ( 'NONE', #381 ) ;
#4501=CARTESIAN_POINT ( 'NONE',  ( 0.2792484994315600488, -1.098230303849151657, 0.7437165765675377571 ) ) ;
#4502=CARTESIAN_POINT ( 'NONE',  ( 0.5968691484058664676, -1.478977895573694079, 0.6175733170218915546 ) ) ;
#4503=EDGE_CURVE ( 'NONE', #15872, #23907, #10969, .T. ) ;
#4512=CARTESIAN_POINT ( 'NONE',  ( 0.03871195898642652844, -1.170490907799284219, 0.6777665691625279765 ) ) ;
#4513=CARTESIAN_POINT ( 'NONE',  ( 0.1829983673741292505, -0.5078818111421493642, 0.09707803729949140981 ) ) ;
#4514=CARTESIAN_POINT ( 'NONE',  ( 0.1729876862315062602, -0.5859491089648112272, 0.3201888025045112607 ) ) ;
#4521=CARTESIAN_POINT ( 'NONE',  ( 0.3862110256088818194, -1.731934476144515900, 0.4282538419479027247 ) ) ;
#4524=CARTESIAN_POINT ( 'NONE',  ( 0.1521802402523282638, -0.6543157544505630030, 0.4235539958437135599 ) ) ;
#4526=CARTESIAN_POINT ( 'NONE',  ( -0.0004984919465477205157, -0.7422635077827434147, -0.01332428955721734649 ) ) ;
#4530=CARTESIAN_POINT ( 'NONE',  ( 0.4127911607195844379, -1.067806736826314218, 0.8805981392688931875 ) ) ;
#4532=CARTESIAN_POINT ( 'NONE',  ( 0.2075111833072861844, -1.439991211493228285, 0.9346039839131908833 ) ) ;
#4536=CARTESIAN_POINT ( 'NONE',  ( 0.002842240357859183043, -0.6339827964191877552, 0.04185307883324698719 ) ) ;
#4538=EDGE_LOOP ( 'NONE', ( #10066, #20400, #34300, #25096, #3219 ) ) ;
#4539=CARTESIAN_POINT ( 'NONE',  ( 0.1173537979040395057, -0.8419870544700812642, 0.4212373387996306007 ) ) ;
#4542=CARTESIAN_POINT ( 'NONE',  ( 0.09200891480963520330, -0.5638355028864769913, 0.2394803638925667999 ) ) ;
#4543=( BOUNDED_SURFACE ( )  B_SPLINE_SURFACE ( 3, 2, ( 
 ( #15259, #30701, #9084 ),
 ( #28214, #21650, #34384 ),
 ( #27816, #9279, #12574 ),
 ( #18346, #40351, #18767 ),
 ( #36852, #81, #37673 ),
 ( #21243, #31498, #2521 ),
 ( #22072, #28418, #34595 ),
 ( #6398, #15061, #18966 ),
 ( #3308, #15871, #40141 ),
 ( #11969, #8884, #21460 ) ),
 .UNSPECIFIED., .F., .F., .F. ) 
 B_SPLINE_SURFACE_WITH_KNOTS ( ( 4, 2, 2, 2, 4 ),
 ( 3, 3 ),
 ( 0.01609622701100840714, 0.01664468962834504337, 0.01719315224568167960, 0.01774161486301831236, 0.01829007748035494860 ),
 ( 0.000000000000000000, 1.000000000000000000 ),
 .UNSPECIFIED. ) 
 GEOMETRIC_REPRESENTATION_ITEM ( )  RATIONAL_B_SPLINE_SURFACE ( (
 ( 1.000000000000000000, 0.7348357107202583283, 1.000000000000000000),
 ( 1.000000000000000000, 0.7390003998219781822, 1.000000000000000000),
 ( 1.000000000000000000, 0.7469310527984605041, 1.000000000000000000),
 ( 1.000000000000000000, 0.7680671187860059757, 1.000000000000000000),
 ( 1.000000000000000000, 0.7813269647889241609, 1.000000000000000000),
 ( 1.000000000000000000, 0.8093722468179129770, 1.000000000000000000),
 ( 1.000000000000000000, 0.8244642440797537164, 1.000000000000000000),
 ( 1.000000000000000000, 0.8536748302854195725, 1.000000000000000000),
 ( 1.000000000000000000, 0.8677611553907019770, 1.000000000000000000),
 ( 1.000000000000000000, 0.8808937523906948952, 1.000000000000000000) ) ) 
 REPRESENTATION_ITEM ( '' )  SURFACE ( )  );
#4544=CARTESIAN_POINT ( 'NONE',  ( 0.5391088926460998465, -1.519050063081437418, 0.5735442466919873361 ) ) ;
#4547=CARTESIAN_POINT ( 'NONE',  ( 0.6633872118601743528, -1.508244317614790386, 0.3999406418104182737 ) ) ;
#4548=CARTESIAN_POINT ( 'NONE',  ( 0.3304297980271364010, -1.754259251785285301, 0.5825477521894050215 ) ) ;
#4551=CARTESIAN_POINT ( 'NONE',  ( 0.01161354615076396445, -0.8030843809549637058, -0.08599057514136099201 ) ) ;
#4552=CARTESIAN_POINT ( 'NONE',  ( 0.5848508152300195828, -1.486263022089187036, 0.6467108361231791447 ) ) ;
#4555=CARTESIAN_POINT ( 'NONE',  ( -0.001215370517532385992, -0.9049306443239834019, 0.2850616817831099770 ) ) ;
#4556=CARTESIAN_POINT ( 'NONE',  ( 0.2007793764868952557, -0.8804627652107338553, 0.3298308470297674488 ) ) ;
#4558=CARTESIAN_POINT ( 'NONE',  ( 0.2170862770790429608, -0.5809856703168675418, 0.4747658466717744608 ) ) ;
#4560=CARTESIAN_POINT ( 'NONE',  ( 0.3084490738248236719, -1.760918681657249518, 0.5685408905292573811 ) ) ;
#4561=ORIENTED_EDGE ( 'NONE', *, *, #27044, .T. ) ;
#4562=CARTESIAN_POINT ( 'NONE',  ( 0.3222894045021684195, -1.758215778056678724, 0.5682417262808792113 ) ) ;
#4563=CARTESIAN_POINT ( 'NONE',  ( 0.004162127911717961384, -0.5769282519883277560, 0.3208275921695811217 ) ) ;
#4565=ORIENTED_EDGE ( 'NONE', *, *, #495, .F. ) ;
#4567=CARTESIAN_POINT ( 'NONE',  ( 0.2073655362268157221, -0.5791461380176760043, 0.4026997059449013427 ) ) ;
#4580=CARTESIAN_POINT ( 'NONE',  ( 0.09767013716984308813, -0.7037575184182598420, 0.3163885053921727808 ) ) ;
#4581=CARTESIAN_POINT ( 'NONE',  ( 0.2062639539987025650, -1.309334957533395016, 1.035302674386483712 ) ) ;
#4582=CARTESIAN_POINT ( 'NONE',  ( 0.2191569312961403060, -0.9640130920718992247, 0.7596813669479296482 ) ) ;
#4583=CARTESIAN_POINT ( 'NONE',  ( 0.2486902987866957404, -1.562349929515986613, 0.8878345574556952835 ) ) ;
#4584=CARTESIAN_POINT ( 'NONE',  ( 0.6540709664215760277, -1.593060928864740156, 0.5182417262812423209 ) ) ;
#4585=CARTESIAN_POINT ( 'NONE',  ( 0.1283426906650361188, -1.153757123153984487, 0.6565515665500586406 ) ) ;
#4588=CARTESIAN_POINT ( 'NONE',  ( 0.1899592773905523502, -0.4742143251099648626, 0.2358144428592672259 ) ) ;
#4589=CARTESIAN_POINT ( 'NONE',  ( 0.000000000000000000, -0.6872203660140440151, -0.1152499451672195641 ) ) ;
#4595=CARTESIAN_POINT ( 'NONE',  ( 0.4660228360541302517, -1.069033551699853479, 0.7465831672886248382 ) ) ;
#4599=CARTESIAN_POINT ( 'NONE',  ( 0.3267512268740185855, -1.294129692828816847, 0.5558767983972462412 ) ) ;
#4601=CARTESIAN_POINT ( 'NONE',  ( 0.2396306281060514576, -0.9727409984848369717, 0.6921125950347779554 ) ) ;
#4609=CARTESIAN_POINT ( 'NONE',  ( 0.4218330423680932695, -1.124294433920346670, 0.5332777205563549172 ) ) ;
#4611=CARTESIAN_POINT ( 'NONE',  ( 0.03596510069126712672, -0.8490400747553025207, 0.3220406306505974592 ) ) ;
#4616=DIRECTION ( 'NONE',  ( 0.000000000000000000, 0.000000000000000000, -1.000000000000000000 ) ) ;
#4618=EDGE_CURVE ( 'NONE', #7904, #13794, #27136, .T. ) ;
#4619=CARTESIAN_POINT ( 'NONE',  ( 0.4791019448734263886, -1.257055108044207170, 0.5997288661970070489 ) ) ;
#4620=DIRECTION ( 'NONE',  ( 0.4999551463232372317, -0.8660512985181134660, 0.000000000000000000 ) ) ;
#4621=CARTESIAN_POINT ( 'NONE',  ( 0.5148961277138980330, -1.134264126613404366, 0.5683444520426285118 ) ) ;
#4623=CARTESIAN_POINT ( 'NONE',  ( 0.1877336102437491272, -0.9152557094465934018, 0.1737200839639440053 ) ) ;
#4628=CARTESIAN_POINT ( 'NONE',  ( 0.1846367493580330643, -0.4547550531002670371, -0.08446770797961487831 ) ) ;
#4629=CARTESIAN_POINT ( 'NONE',  ( 0.06534675320629550199, -0.6525200402172089964, 0.4542822255817380306 ) ) ;
#4630=CARTESIAN_POINT ( 'NONE',  ( 0.08979932128046543005, -0.5650858933015915353, 0.1321911050941584620 ) ) ;
#4631=CARTESIAN_POINT ( 'NONE',  ( 0.08632066630984121247, -0.7257482948602275163, 0.1454106388476009426 ) ) ;
#4637=CARTESIAN_POINT ( 'NONE',  ( 0.4578914926014877040, -1.316819426484251876, 0.8252663181933341807 ) ) ;
#4645=CARTESIAN_POINT ( 'NONE',  ( 0.2178456820578618947, -1.229745583036154111, 0.4925753654759648659 ) ) ;
#4647=DIRECTION ( 'NONE',  ( 0.5209632322108713742, -0.8535791179992641142, 0.000000000000000000 ) ) ;
#4649=CARTESIAN_POINT ( 'NONE',  ( 0.7228851465660607323, -1.479175389011975428, 0.5919814340071456460 ) ) ;
#4655=DIRECTION ( 'NONE',  ( -0.4999551463232372317, 0.8660512985181135770, -0.000000000000000000 ) ) ;
#4657=CARTESIAN_POINT ( 'NONE',  ( 0.002391669266185704034, -0.4944279760261894308, 0.2539263035736906149 ) ) ;
#4667=CARTESIAN_POINT ( 'NONE',  ( 0.4598690013600978954, -1.115092733745942422, 0.5813559894972742947 ) ) ;
#4674=ADVANCED_FACE ( 'NONE', ( #20070 ), #30263, .F. ) ;
#4675=CARTESIAN_POINT ( 'NONE',  ( 0.3921016979062637575, -1.134099238832534162, 0.7924938403547856502 ) ) ;
#4677=ORIENTED_EDGE ( 'NONE', *, *, #36554, .F. ) ;
#4678=CARTESIAN_POINT ( 'NONE',  ( 0.1851443459949622949, -0.7907988577364570837, 0.1906562862421710969 ) ) ;
#4681=CARTESIAN_POINT ( 'NONE',  ( 0.1766140053765036799, -0.4884607529735562892, 0.1457336358543773192 ) ) ;
#4684=EDGE_LOOP ( 'NONE', ( #4344, #37175, #16696, #20191, #9025 ) ) ;
#4685=CARTESIAN_POINT ( 'NONE',  ( 0.03470550179739362306, -0.6286058976697491696, 0.4199817593366443336 ) ) ;
#4686=CARTESIAN_POINT ( 'NONE',  ( 0.6822549037112248804, -1.506992060536815448, 0.4516695578178590020 ) ) ;
#4688=CARTESIAN_POINT ( 'NONE',  ( 0.4972320539234349468, -1.080138254241686413, 0.5197417262808780025 ) ) ;
#4692=CARTESIAN_POINT ( 'NONE',  ( 0.1630093775333145978, -1.283014495054401793, 0.4182417262808778013 ) ) ;
#4694=EDGE_CURVE ( 'NONE', #13346, #28462, #7511, .T. ) ;
#4695=CARTESIAN_POINT ( 'NONE',  ( 0.4384185415325656532, -1.229513547616574609, 0.5866921512824373464 ) ) ;
#4697=EDGE_CURVE ( 'NONE', #3787, #24651, #10897, .T. ) ;
#4701=CARTESIAN_POINT ( 'NONE',  ( 0.2565305817069650218, -1.011710961920390339, 0.5944358237650989585 ) ) ;
#4702=CIRCLE ( 'NONE', #11948, 0.01000000000000002970 ) ;
#4710=CARTESIAN_POINT ( 'NONE',  ( 0.3959476892382831625, -1.138264379635865353, 0.4306935340366444542 ) ) ;
#4714=CARTESIAN_POINT ( 'NONE',  ( 0.0003960311365576736739, -0.4455394904127599198, 0.08489233873622216431 ) ) ;
#4716=CARTESIAN_POINT ( 'NONE',  ( 0.2503797518491029939, -1.479909065722671002, 1.008170915534915446 ) ) ;
#4720=CARTESIAN_POINT ( 'NONE',  ( 0.1872789457748890163, -0.5068293638037115745, 0.1231878790029107551 ) ) ;
#4724=ADVANCED_FACE ( 'NONE', ( #8509 ), #37122, .T. ) ;
#4725=CARTESIAN_POINT ( 'NONE',  ( 0.1348549594756915104, -0.5515731166344398639, 0.1532284265886467711 ) ) ;
#4726=CARTESIAN_POINT ( 'NONE',  ( 0.006625058703027312222, -0.8256683006665239688, 0.06834504167984893630 ) ) ;
#4728=EDGE_CURVE ( 'NONE', #13190, #17955, #27351, .T. ) ;
#4729=ORIENTED_EDGE ( 'NONE', *, *, #35628, .T. ) ;
#4730=CARTESIAN_POINT ( 'NONE',  ( 0.3097869260829022031, -1.188640176377027791, 0.4996798932217296763 ) ) ;
#4732=CARTESIAN_POINT ( 'NONE',  ( 0.08271634070018635265, -1.004823404736711501, 0.8361326721138350182 ) ) ;
#4734=CARTESIAN_POINT ( 'NONE',  ( 0.1922398268636369700, -1.242606702096344051, 0.6043157665294947023 ) ) ;
#4739=ORIENTED_EDGE ( 'NONE', *, *, #35065, .T. ) ;
#4740=CARTESIAN_POINT ( 'NONE',  ( 0.08647094942830720055, -0.8134528749729150743, 0.2066784198371740267 ) ) ;
#4742=CARTESIAN_POINT ( 'NONE',  ( 0.09091041988698707332, -0.5766203509326254251, 0.2109086659841546418 ) ) ;
#4743=CARTESIAN_POINT ( 'NONE',  ( 0.1978543033782794447, -0.8340884217837519765, 0.6564551516366390338 ) ) ;
#4752=CARTESIAN_POINT ( 'NONE',  ( -7.828841584765314999E-06, -0.8039854292597425900, -0.08783247702100009657 ) ) ;
#4753=CARTESIAN_POINT ( 'NONE',  ( 0.06995977277154606655, -0.5495845434848062316, 0.2074071626960130033 ) ) ;
#4754=CIRCLE ( 'NONE', #34342, 0.009999999999999995004 ) ;
#4755=CARTESIAN_POINT ( 'NONE',  ( 0.4090604450045443596, -1.131420581850358653, 0.3667417262808778666 ) ) ;
#4757=CARTESIAN_POINT ( 'NONE',  ( 0.1872829031602858685, -1.532932250049839906, 0.6789365607098191147 ) ) ;
#4758=CARTESIAN_POINT ( 'NONE',  ( 0.1920143701880955289, -0.8743002769911518701, 0.2704752137325454608 ) ) ;
#4761=CARTESIAN_POINT ( 'NONE',  ( 0.1927581100858387075, -0.5042345029781482024, 0.3213135115051561908 ) ) ;
#4769=CARTESIAN_POINT ( 'NONE',  ( 0.1098459896970112454, -1.084708748088091923, 0.8887398936019613727 ) ) ;
#4770=CARTESIAN_POINT ( 'NONE',  ( 0.1810483112700702890, -1.250999180832525148, 0.4405424963560370943 ) ) ;
#4771=CARTESIAN_POINT ( 'NONE',  ( 0.1316017208954911588, -1.248059642665102942, 0.5182417262812423209 ) ) ;
#4774=CARTESIAN_POINT ( 'NONE',  ( 0.5536319580448211264, -1.193555294463456873, 0.7337749688435845075 ) ) ;
#4784=EDGE_LOOP ( 'NONE', ( #32565, #38993, #28436, #17890, #26695, #27473 ) ) ;
#4785=CARTESIAN_POINT ( 'NONE',  ( 0.08016251834805442067, -1.309203902574839207, 0.5631135398343307674 ) ) ;
#4786=CARTESIAN_POINT ( 'NONE',  ( 0.1623264987558849792, -0.8004081683446899742, 0.5646416967012523047 ) ) ;
#4788=CARTESIAN_POINT ( 'NONE',  ( 0.2663090763754291657, -1.538339113173472716, 0.9867693543954003665 ) ) ;
#4790=CARTESIAN_POINT ( 'NONE',  ( 0.09796691250624214864, -0.5532864700090758259, 0.2008629083371975543 ) ) ;
#4791=CARTESIAN_POINT ( 'NONE',  ( 0.1133176935271576757, -0.6554924552526250059, -0.09368704978610124801 ) ) ;
#4793=CARTESIAN_POINT ( 'NONE',  ( 0.1596048412419493190, -1.234437691115734870, 0.6299358457907016096 ) ) ;
#4794=ORIENTED_EDGE ( 'NONE', *, *, #22222, .F. ) ;
#4797=CARTESIAN_POINT ( 'NONE',  ( 0.1541907618229372834, -0.5976806583976911336, 0.5269747745306871956 ) ) ;
#4798=CIRCLE ( 'NONE', #348, 0.03749999999977545601 ) ;
#4801=CARTESIAN_POINT ( 'NONE',  ( 0.07006815180907459417, -1.315301596572421294, 0.5080907171457548221 ) ) ;
#4804=CARTESIAN_POINT ( 'NONE',  ( 0.5675876754196318430, -1.214623637701154335, 0.7236292717493534310 ) ) ;
#4816=CARTESIAN_POINT ( 'NONE',  ( 0.5005350806643109607, -1.112410049453316008, 0.6916867713706035259 ) ) ;
#4817=CARTESIAN_POINT ( 'NONE',  ( 0.5106109609909708080, -1.176845144576392332, 0.4435443120481467050 ) ) ;
#4821=CARTESIAN_POINT ( 'NONE',  ( 0.04038401875063166863, -0.8587749605274695996, 0.3937922782597925164 ) ) ;
#4829=CARTESIAN_POINT ( 'NONE',  ( 0.4321750792481709458, -1.187405343333139296, 0.6822186175578013323 ) ) ;
#4831=CARTESIAN_POINT ( 'NONE',  ( 0.4964355788048083751, -1.123423484656395299, 0.5685061009866244630 ) ) ;
#4832=B_SPLINE_CURVE_WITH_KNOTS ( 'NONE', 3,
 ( #5714, #12858, #2031, #37951, #15172, #40266, #24061, #30815, #2636, #27731, #10785, #32172, #35877, #4191, #22531, #38342, #29088, #563 ),
 .UNSPECIFIED., .F., .F.,
 ( 4, 2, 2, 2, 2, 2, 2, 2, 4 ),
 ( 0.000000000000000000, 0.0007927102992442323307, 0.001585420598488464661, 0.002378130897732695908, 0.003170841196976927588, 0.003963551496221159702, 0.004756261795465391816, 0.005548972094709624797, 0.006341682393953856911 ),
 .UNSPECIFIED. ) ;
#4838=CARTESIAN_POINT ( 'NONE',  ( 0.07344452620781788399, -0.6304810646442478017, 0.4078118883576473674 ) ) ;
#4839=CARTESIAN_POINT ( 'NONE',  ( 0.08956013910934083888, -0.5501150684396665103, 0.1018409378312434832 ) ) ;
#4841=CARTESIAN_POINT ( 'NONE',  ( 0.2611244543265801576, -0.7808929225949666764, 0.1477649966949237115 ) ) ;
#4845=CARTESIAN_POINT ( 'NONE',  ( 0.3863603026027747078, -1.188791174525776650, 0.8283360454836284914 ) ) ;
#4846=ORIENTED_EDGE ( 'NONE', *, *, #10472, .T. ) ;
#4849=CIRCLE ( 'NONE', #29184, 0.08249999999977548903 ) ;
#4854=CARTESIAN_POINT ( 'NONE',  ( 0.1847208729320930221, -1.260429531918160206, 0.4290398900403852855 ) ) ;
#4858=CARTESIAN_POINT ( 'NONE',  ( 0.2506904587504640847, -0.6594178163634784040, 0.5852584525479398447 ) ) ;
#4859=EDGE_CURVE ( 'NONE', #32251, #39497, #10439, .T. ) ;
#4861=CARTESIAN_POINT ( 'NONE',  ( 0.07670268886588108015, -1.321079536449508485, 0.4808101794164899578 ) ) ;
#4867=CARTESIAN_POINT ( 'NONE',  ( 0.5832107232896035498, -1.609297431860164496, 0.5795114931753430065 ) ) ;
#4871=CARTESIAN_POINT ( 'NONE',  ( 0.02385183771220368218, -0.6100559285722760849, 0.5958381505304063408 ) ) ;
#4874=DIRECTION ( 'NONE',  ( 0.8660512985181135770, 0.4999551463232371762, 0.000000000000000000 ) ) ;
#4883=CARTESIAN_POINT ( 'NONE',  ( 0.05563540667800927902, -1.335270441939011121, 0.5197417262808780025 ) ) ;
#4889=CARTESIAN_POINT ( 'NONE',  ( 0.4377275372045464352, -1.201128267441582187, 0.7458237077910447876 ) ) ;
#4892=CARTESIAN_POINT ( 'NONE',  ( 0.1845475678902450123, -0.7902170579836453879, 0.1696330687313138408 ) ) ;
#4897=CARTESIAN_POINT ( 'NONE',  ( 0.02354069309169367838, -0.5479244848632992548, 0.2301531253923031484 ) ) ;
#4898=CARTESIAN_POINT ( 'NONE',  ( 0.6910729260980184030, -1.496094287350760332, 0.4693483012025433943 ) ) ;
#4899=CARTESIAN_POINT ( 'NONE',  ( 0.1877532238556526289, -0.5410535477826009521, 0.06280118956074845493 ) ) ;
#4900=CARTESIAN_POINT ( 'NONE',  ( 0.4094665197507286747, -1.132124008075320098, 0.5707417262808780478 ) ) ;
#4902=VERTEX_POINT ( 'NONE', #15700 ) ;
#4904=CARTESIAN_POINT ( 'NONE',  ( 0.1636912256974782376, -1.272012149535565850, 0.4251003766563813402 ) ) ;
#4906=CARTESIAN_POINT ( 'NONE',  ( 0.2747206457212271746, -1.194764396915172444, 0.7305384998433399613 ) ) ;
#4907=CARTESIAN_POINT ( 'NONE',  ( 0.1870397359536237203, -0.7179515242747687154, 0.07956602225022149644 ) ) ;
#4917=CARTESIAN_POINT ( 'NONE',  ( 0.3186320389496528627, -1.760431904683431359, 0.5682417262808792113 ) ) ;
#4921=CARTESIAN_POINT ( 'NONE',  ( 0.3880322814406260701, -1.147921704116221298, 0.4309387522554056216 ) ) ;
#4926=CARTESIAN_POINT ( 'NONE',  ( 0.01217710773476333823, -0.4281249367976072140, 0.1335689301494157322 ) ) ;
#4928=CARTESIAN_POINT ( 'NONE',  ( 0.2559395560537573444, -1.500125191510220279, 1.001930765150525593 ) ) ;
#4930=ORIENTED_EDGE ( 'NONE', *, *, #36054, .T. ) ;
#4932=EDGE_CURVE ( 'NONE', #4246, #18554, #24962, .T. ) ;
#4937=CARTESIAN_POINT ( 'NONE',  ( 0.4380679180091197611, -1.234484979903685664, 0.8225911399008282165 ) ) ;
#4939=CARTESIAN_POINT ( 'NONE',  ( 9.509834983668487914E-05, -0.6764735018835020819, -0.02209724360191241826 ) ) ;
#4940=VERTEX_POINT ( 'NONE', #28450 ) ;
#4943=CARTESIAN_POINT ( 'NONE',  ( 0.4411887824651631873, -1.114744685954409009, 0.8907908412112590657 ) ) ;
#4945=CARTESIAN_POINT ( 'NONE',  ( -0.01402042477169951340, -0.5319719165593393972, 0.1980928424870210536 ) ) ;
#4947=CARTESIAN_POINT ( 'NONE',  ( 0.2151567955658992837, -1.242576477413985137, 0.5631370738156890043 ) ) ;
#4953=ORIENTED_EDGE ( 'NONE', *, *, #201, .F. ) ;
#4954=CARTESIAN_POINT ( 'NONE',  ( 0.01135461203890102133, -0.9395716130340400207, 0.08695101789951617532 ) ) ;
#4956=CARTESIAN_POINT ( 'NONE',  ( 0.1008930477423943123, -1.308833506382407474, 0.7266393657083966007 ) ) ;
#4957=CARTESIAN_POINT ( 'NONE',  ( 0.1493143905638315838, -0.7774743300093324150, 0.6049429375722679136 ) ) ;
#4958=CARTESIAN_POINT ( 'NONE',  ( 0.1171945479475617752, -0.6032665890832976663, 0.3311638906348050582 ) ) ;
#4959=CARTESIAN_POINT ( 'NONE',  ( 0.1824040550974478092, -0.5173104186764061474, 0.2535968541610654214 ) ) ;
#4961=CARTESIAN_POINT ( 'NONE',  ( 0.06874771606299766302, -1.327481140994086317, 0.5533907816784044975 ) ) ;
#4963=CARTESIAN_POINT ( 'NONE',  ( 0.1876053338355621880, -0.6785855078148245179, 0.1477569985384105666 ) ) ;
#4967=CARTESIAN_POINT ( 'NONE',  ( 0.4599911587916594713, -1.116015572881478679, 0.5707053994389698071 ) ) ;
#4973=CARTESIAN_POINT ( 'NONE',  ( 0.1721302213443809126, -1.453494483496651890, 0.7931418093652549128 ) ) ;
#4974=CARTESIAN_POINT ( 'NONE',  ( 0.3877041582795131003, -1.010062466692070560, 0.6423187497268529889 ) ) ;
#4976=CARTESIAN_POINT ( 'NONE',  ( 0.7110566119663160878, -1.453354452021889731, 0.7718588955819412067 ) ) ;
#4983=CARTESIAN_POINT ( 'NONE',  ( 0.02977258242336560182, -0.7570884278691590863, 0.6213445499472508571 ) ) ;
#4984=ADVANCED_FACE ( 'NONE', ( #35026 ), #836, .T. ) ;
#4989=EDGE_CURVE ( 'NONE', #19731, #26082, #24708, .T. ) ;
#4991=CARTESIAN_POINT ( 'NONE',  ( 0.3319931610750171957, -0.8547376211461308326, 0.6892644829257473793 ) ) ;
#4992=ORIENTED_EDGE ( 'NONE', *, *, #35400, .F. ) ;
#4997=CARTESIAN_POINT ( 'NONE',  ( 0.4670213778778394831, -1.236191465557153757, 0.6057417262809817737 ) ) ;
#4999=DIRECTION ( 'NONE',  ( -0.4999551463232371762, 0.8660512985181134660, -0.000000000000000000 ) ) ;
#5003=CARTESIAN_POINT ( 'NONE',  ( 0.1740021755340503407, -0.8283876604043171055, 0.5873707361312400232 ) ) ;
#5004=CARTESIAN_POINT ( 'NONE',  ( 0.3018042201724753237, -1.665203873072418794, 0.9047098497351133695 ) ) ;
#5005=CARTESIAN_POINT ( 'NONE',  ( 0.1247534215796342189, -0.6769942796222839787, 0.4736701887020580704 ) ) ;
#5006=CARTESIAN_POINT ( 'NONE',  ( 0.1150778763548105377, -0.4543190241136206842, 0.08302619808872485629 ) ) ;
#5008=CARTESIAN_POINT ( 'NONE',  ( 0.09285408974215507427, -1.054165622298770089, 0.6121834013375294647 ) ) ;
#5009=CARTESIAN_POINT ( 'NONE',  ( 0.3313632526110646959, -1.291506781903942302, 0.5682210202584868641 ) ) ;
#5010=ORIENTED_EDGE ( 'NONE', *, *, #18967, .T. ) ;
#5013=CARTESIAN_POINT ( 'NONE',  ( 0.1913351458898694402, -0.4849373758447458882, 0.2686262507137537336 ) ) ;
#5020=CARTESIAN_POINT ( 'NONE',  ( 0.07776798027987287532, -1.310857805500537543, 0.4781333465564954754 ) ) ;
#5022=CARTESIAN_POINT ( 'NONE',  ( 0.1186006463096753172, -1.414144484500942989, 0.5682508211975187962 ) ) ;
#5023=CARTESIAN_POINT ( 'NONE',  ( 0.6169573538504090626, -1.299218888095586388, 0.5469722621913530869 ) ) ;
#5032=( BOUNDED_SURFACE ( )  B_SPLINE_SURFACE ( 3, 2, ( 
 ( #15340, #2792, #2398 ),
 ( #24998, #40218, #34460 ),
 ( #24818, #11838, #2587 ),
 ( #12053, #27896, #14936 ),
 ( #21327, #37149, #21716 ),
 ( #37530, #33864, #5667 ),
 ( #3193, #34249, #6274 ),
 ( #12261, #15733, #9354 ),
 ( #21534, #18222, #30769 ),
 ( #8961, #37340, #31389 ),
 ( #40434, #149, #5452 ),
 ( #12643, #15125, #34054 ),
 ( #9152, #6061, #18629 ),
 ( #31185, #28101, #3003 ) ),
 .UNSPECIFIED., .F., .F., .F. ) 
 B_SPLINE_SURFACE_WITH_KNOTS ( ( 4, 2, 2, 2, 2, 2, 4 ),
 ( 3, 3 ),
 ( 0.000000000000000000, 0.0009840465490818996620, 0.001476069823622849601, 0.001968093098163799324, 0.002460116372704749046, 0.002952139647245699203, 0.003936186196327598648 ),
 ( 0.000000000000000000, 1.000000000000000000 ),
 .UNSPECIFIED. ) 
 GEOMETRIC_REPRESENTATION_ITEM ( )  RATIONAL_B_SPLINE_SURFACE ( (
 ( 1.000000000000000000, 0.7087966873486530872, 1.000000000000000000),
 ( 1.000000000000000000, 0.7099442161580019617, 1.000000000000000000),
 ( 1.000000000000000000, 0.7112044574294733579, 1.000000000000000000),
 ( 1.000000000000000000, 0.7127234984257925232, 1.000000000000000000),
 ( 1.000000000000000000, 0.7131586427699522224, 1.000000000000000000),
 ( 1.000000000000000000, 0.7137747606611323237, 1.000000000000000000),
 ( 1.000000000000000000, 0.7139535051142154032, 1.000000000000000000),
 ( 1.000000000000000000, 0.7139024756042031683, 1.000000000000000000),
 ( 1.000000000000000000, 0.7136769813686398845, 1.000000000000000000),
 ( 1.000000000000000000, 0.7127126671718326811, 1.000000000000000000),
 ( 1.000000000000000000, 0.7119648005323482298, 1.000000000000000000),
 ( 1.000000000000000000, 0.7089786222043976682, 1.000000000000000000),
 ( 1.000000000000000000, 0.7059048385594330899, 1.000000000000000000),
 ( 1.000000000000000000, 0.7024277927095089469, 1.000000000000000000) ) ) 
 REPRESENTATION_ITEM ( '' )  SURFACE ( )  );
#5035=CARTESIAN_POINT ( 'NONE',  ( 0.2429745329104363027, -0.8738914638608461516, 0.4819356518895884789 ) ) ;
#5038=CARTESIAN_POINT ( 'NONE',  ( 0.1994650021643780136, -1.295469678022094229, 0.6991101051189098081 ) ) ;
#5044=CARTESIAN_POINT ( 'NONE',  ( 0.4675665044693247951, -1.237121799919192355, 0.6039218906317980196 ) ) ;
#5050=CARTESIAN_POINT ( 'NONE',  ( 0.4861228912811037528, -1.648612142294594074, 0.4182417262808776903 ) ) ;
#5053=CARTESIAN_POINT ( 'NONE',  ( 0.06047652861071878966, -0.5421273095757789262, 0.1825153154440289915 ) ) ;
#5054=CARTESIAN_POINT ( 'NONE',  ( 0.08859551772052549901, -0.5985747499489527668, 0.03208008976688550562 ) ) ;
#5055=CARTESIAN_POINT ( 'NONE',  ( 0.1983634613346075826, -0.7568214873327272496, 0.3192403157822673032 ) ) ;
#5056=CARTESIAN_POINT ( 'NONE',  ( 0.4062230848227149638, -1.145582794160931117, 0.4248905050063955802 ) ) ;
#5061=CARTESIAN_POINT ( 'NONE',  ( 0.1337051625169099478, -0.6233194395910383045, 0.3688355370247377585 ) ) ;
#5065=CARTESIAN_POINT ( 'NONE',  ( 0.6190054265851119286, -1.579626031360436222, 0.4182417262808776348 ) ) ;
#5066=CARTESIAN_POINT ( 'NONE',  ( 0.1228677259314389508, -1.296195397236784785, 0.4358613769847314301 ) ) ;
#5069=CARTESIAN_POINT ( 'NONE',  ( 0.4812359531826634340, -1.078470577594583979, 0.8616913018466071383 ) ) ;
#5072=B_SPLINE_CURVE_WITH_KNOTS ( 'NONE', 3,
 ( #24989, #8952, #31177, #37331, #21923, #8739, #36724, #30759, #2579, #21525, #1294, #16155, #38699, #19993, #10727, #15725 ),
 .UNSPECIFIED., .F., .F.,
 ( 4, 2, 2, 2, 2, 2, 2, 4 ),
 ( 0.002977954003792171109, 0.003350115585507550727, 0.003722277167222930346, 0.004094438748938309530, 0.004466600330653689582, 0.004838761912369069634, 0.005210923494084448819, 0.005955246657515208056 ),
 .UNSPECIFIED. ) ;
#5075=DIRECTION ( 'NONE',  ( 0.4999551463232372317, -0.8660512985181134660, 0.000000000000000000 ) ) ;
#5078=CARTESIAN_POINT ( 'NONE',  ( 0.008057578236607982475, -0.5544447393747381492, 0.4149153965127375110 ) ) ;
#5080=CARTESIAN_POINT ( 'NONE',  ( 0.1784822832398731962, -1.263697370786425411, 0.5370935804641795430 ) ) ;
#5081=CARTESIAN_POINT ( 'NONE',  ( 0.05582223227535057508, -1.291805717968274037, 0.5182417262812423209 ) ) ;
#5082=B_SPLINE_SURFACE_WITH_KNOTS ( 'NONE', 5, 5, ( 
 ( #550, #3579, #28877, #38127, #19628, #13047 ),
 ( #37730, #31968, #6854, #13454, #22930, #16338 ),
 ( #22130, #34646, #31549, #19018, #25187, #19822 ),
 ( #35044, #7059, #25599, #735, #7247, #15921 ),
 ( #9951, #13241, #12846, #342, #6646, #3366 ),
 ( #3972, #32163, #25407, #32355, #12623, #29075 ) ),
 .UNSPECIFIED., .F., .F., .F.,
 ( 6, 6 ),
 ( 6, 6 ),
 ( -6.477000000001651436, 6.477000000001639002 ),
 ( -2.080605796196421498, 4.396394203803585476 ),
 .UNSPECIFIED. ) ;
#5085=CARTESIAN_POINT ( 'NONE',  ( 0.4091335057472371695, -1.131547141905885789, 0.4177417262808780229 ) ) ;
#5088=CARTESIAN_POINT ( 'NONE',  ( 0.5224595318596155780, -1.331650646383924386, 0.6038439222826686992 ) ) ;
#5090=VERTEX_POINT ( 'NONE', #1127 ) ;
#5091=CARTESIAN_POINT ( 'NONE',  ( 0.4767475950167052168, -1.082687895696078595, 0.6905128956159171105 ) ) ;
#5094=ORIENTED_EDGE ( 'NONE', *, *, #28235, .T. ) ;
#5098=CARTESIAN_POINT ( 'NONE',  ( 0.3402366556150817622, -1.560274116414339884, 0.8083988018111346596 ) ) ;
#5099=CARTESIAN_POINT ( 'NONE',  ( 0.6706115226080072711, -1.534602134890148850, 0.4364891473496426699 ) ) ;
#5100=CARTESIAN_POINT ( 'NONE',  ( 0.1763856455429072267, -0.5524551084071943619, -0.04065491940077346072 ) ) ;
#5101=CARTESIAN_POINT ( 'NONE',  ( 0.4971920908461615607, -1.080069027881642052, 0.4687417262808780127 ) ) ;
#5102=EDGE_CURVE ( 'NONE', #33386, #35465, #39880, .T. ) ;
#5108=CARTESIAN_POINT ( 'NONE',  ( 0.1267896730660402760, -0.9030892566507676689, 0.5786158305868386309 ) ) ;
#5109=CARTESIAN_POINT ( 'NONE',  ( 0.3224764602545437953, -1.754077001593124185, 0.4780754602289729593 ) ) ;
#5110=DIRECTION ( 'NONE',  ( 0.2994471003784440755, -0.9541129042597328302, 0.000000000000000000 ) ) ;
#5112=CARTESIAN_POINT ( 'NONE',  ( 0.6596209037232241279, -1.565455939274822184, 0.3157417262808776548 ) ) ;
#5120=CARTESIAN_POINT ( 'NONE',  ( 0.4035007565703578325, -1.146148456392026116, 0.4243490465986823335 ) ) ;
#5121=CARTESIAN_POINT ( 'NONE',  ( 0.4474917948846165450, -1.247628998557391400, 0.6057417262809816627 ) ) ;
#5124=CARTESIAN_POINT ( 'NONE',  ( 1.372100516120995828E-05, -0.5265032726816540887, -0.06060675249349117139 ) ) ;
#5129=EDGE_LOOP ( 'NONE', ( #18820, #30719, #4794, #34099 ) ) ;
#5135=CARTESIAN_POINT ( 'NONE',  ( 0.0006976930216080560456, -0.6123561560918749924, -0.004704502767504344096 ) ) ;
#5137=ORIENTED_EDGE ( 'NONE', *, *, #28394, .T. ) ;
#5138=CARTESIAN_POINT ( 'NONE',  ( 0.3511079287476752686, -1.164805985122749687, 0.4335040596137051394 ) ) ;
#5140=( BOUNDED_SURFACE ( )  B_SPLINE_SURFACE ( 3, 2, ( 
 ( #36742, #27499, #33877 ),
 ( #11848, #34065, #39837 ),
 ( #15350, #18422, #5462 ),
 ( #12272, #27909, #24829 ) ),
 .UNSPECIFIED., .F., .F., .F. ) 
 B_SPLINE_SURFACE_WITH_KNOTS ( ( 4, 4 ),
 ( 3, 3 ),
 ( -2.744332538995308823E-15, 0.004359680035277800104 ),
 ( 0.000000000000000000, 1.000000000000000000 ),
 .UNSPECIFIED. ) 
 GEOMETRIC_REPRESENTATION_ITEM ( )  RATIONAL_B_SPLINE_SURFACE ( (
 ( 1.000000000000000000, 0.7004196158486113433, 1.000000000000000000),
 ( 1.000000000000000000, 0.7024542282359754752, 1.000000000000000000),
 ( 1.000000000000000000, 0.7046422212203753421, 1.000000000000000000),
 ( 1.000000000000000000, 0.7054447009685760328, 1.000000000000000000) ) ) 
 REPRESENTATION_ITEM ( '' )  SURFACE ( )  );
#5142=CARTESIAN_POINT ( 'NONE',  ( 0.2233061389546777964, -1.398491456369854280, 0.9267770701875633899 ) ) ;
#5144=CARTESIAN_POINT ( 'NONE',  ( 0.1399309073568716921, -1.253615150487832341, 0.6230334390714287185 ) ) ;
#5148=CARTESIAN_POINT ( 'NONE',  ( 0.7092779456818100181, -1.502766204822708174, 0.5668339295794848631 ) ) ;
#5151=B_SPLINE_CURVE_WITH_KNOTS ( 'NONE', 3,
 ( #5844, #37520, #33628, #6265, #5441, #27286 ),
 .UNSPECIFIED., .F., .F.,
 ( 4, 2, 4 ),
 ( 0.008641842504323983890, 0.009239025970640010743, 0.009836209436956035862 ),
 .UNSPECIFIED. ) ;
#5155=CARTESIAN_POINT ( 'NONE',  ( 0.1760646372844321683, -0.7862967544061189029, 0.6064719630404880046 ) ) ;
#5156=CARTESIAN_POINT ( 'NONE',  ( 0.1869504391848741121, -0.7244332150394979797, 0.03244844288826874423 ) ) ;
#5157=LINE ( 'NONE', #21018, #36933 ) ;
#5158=CARTESIAN_POINT ( 'NONE',  ( 0.6472156995107305466, -1.554538954898049052, 0.4226020063017070227 ) ) ;
#5159=CARTESIAN_POINT ( 'NONE',  ( 0.01220508677664999299, -0.4284039737085656996, 0.1457185332388702959 ) ) ;
#5160=DIRECTION ( 'NONE',  ( 0.01455087615875041117, 0.9998941303973198913, 0.000000000000000000 ) ) ;
#5161=CARTESIAN_POINT ( 'NONE',  ( 0.1927077495703349852, -0.8180328145591141409, 0.2791508387892263077 ) ) ;
#5166=CARTESIAN_POINT ( 'NONE',  ( 0.4377606765896609464, -1.229990982179016701, 0.5852478207895496221 ) ) ;
#5169=CARTESIAN_POINT ( 'NONE',  ( -8.537024980200822558E-17, -0.6872203660140394632, 0.1631394164078588394 ) ) ;
#5170=CARTESIAN_POINT ( 'NONE',  ( 0.4544126380536514520, -1.061573323663441704, 0.6302127423442334120 ) ) ;
#5171=CARTESIAN_POINT ( 'NONE',  ( 0.03176206407908215706, -0.9495151868022172481, 0.6313809608633471626 ) ) ;
#5173=CARTESIAN_POINT ( 'NONE',  ( 0.5012199843439465452, -1.111650260509063681, 0.8688705274730272876 ) ) ;
#5179=CARTESIAN_POINT ( 'NONE',  ( 0.04850978628623311278, -0.8094765694360999131, 0.6771444674279119003 ) ) ;
#5180=CARTESIAN_POINT ( 'NONE',  ( 0.5848005186207935191, -1.482150277494033608, 0.6650156861691463028 ) ) ;
#5181=CARTESIAN_POINT ( 'NONE',  ( 0.3003068002427916605, -1.655642049652715331, 0.4394976263036083353 ) ) ;
#5185=CARTESIAN_POINT ( 'NONE',  ( 0.6089993539687283963, -1.280207732015472333, 0.6563525730433853456 ) ) ;
#5187=ORIENTED_EDGE ( 'NONE', *, *, #36047, .F. ) ;
#5198=CARTESIAN_POINT ( 'NONE',  ( 0.1471926383934134275, -1.243287368939621773, 0.6046105284403431313 ) ) ;
#5200=CARTESIAN_POINT ( 'NONE',  ( 0.08692586860950439476, -0.7045980206078545915, 0.1457185332388693799 ) ) ;
#5201=CARTESIAN_POINT ( 'NONE',  ( 0.1371221799207314740, -1.062251636642305819, 0.9748385851047789430 ) ) ;
#5202=CARTESIAN_POINT ( 'NONE',  ( 0.1029772949285807093, -0.5926062987907158019, 0.3127404110831066841 ) ) ;
#5205=CARTESIAN_POINT ( 'NONE',  ( 0.000000000000000000, -0.9481888444201338473, 0.1457185332388702959 ) ) ;
#5207=ADVANCED_FACE ( 'NONE', ( #22649 ), #35548, .T. ) ;
#5208=EDGE_LOOP ( 'NONE', ( #756, #24455, #8581, #24753, #38506 ) ) ;
#5210=CARTESIAN_POINT ( 'NONE',  ( 0.3345257678029842086, -0.8717194449991449989, 0.6804045188348578632 ) ) ;
#5214=( NAMED_UNIT ( * ) PLANE_ANGLE_UNIT ( ) SI_UNIT ( $, .RADIAN. ) );
#5219=CARTESIAN_POINT ( 'NONE',  ( 0.3124895060288936377, -1.175537060766050246, 0.5079170196689681838 ) ) ;
#5220=CARTESIAN_POINT ( 'NONE',  ( 0.2766509774079478068, -0.8188515361471339071, 0.5743688119339978027 ) ) ;
#5226=CARTESIAN_POINT ( 'NONE',  ( 0.4567587145471871390, -1.219596911210154566, 0.5765795053216835608 ) ) ;
#5232=CARTESIAN_POINT ( 'NONE',  ( 0.06895221775114691865, -0.9317196315810322149, 0.6128942806377850605 ) ) ;
#5237=CARTESIAN_POINT ( 'NONE',  ( 0.4771042051721851029, -1.253291307408614053, 0.6140431522715210644 ) ) ;
#5244=EDGE_CURVE ( 'NONE', #15727, #1246, #31947, .T. ) ;
#5245=CARTESIAN_POINT ( 'NONE',  ( 0.4012118689501711910, -1.155916157891842211, 0.4182417262808778013 ) ) ;
#5246=ORIENTED_EDGE ( 'NONE', *, *, #33175, .F. ) ;
#5247=CARTESIAN_POINT ( 'NONE',  ( 0.1912830164987288084, -0.5477411782657776174, 0.1015045423513593059 ) ) ;
#5248=CARTESIAN_POINT ( 'NONE',  ( 0.4434119773370868711, -1.573474031461190581, 0.6057253118067152942 ) ) ;
#5249=CARTESIAN_POINT ( 'NONE',  ( 0.08770615875230125535, -0.6684773603782572238, 0.002659437449977570134 ) ) ;
#5251=CARTESIAN_POINT ( 'NONE',  ( 0.5884429758178558734, -1.489330091540539636, 0.4807459044743478405 ) ) ;
#5254=CARTESIAN_POINT ( 'NONE',  ( 0.4888238443203842265, -1.356165068348983205, 0.8108664833413182782 ) ) ;
#5255=CARTESIAN_POINT ( 'NONE',  ( 0.3301505661793556201, -1.753418133777565835, 0.5634441686133024874 ) ) ;
#5256=CARTESIAN_POINT ( 'NONE',  ( 0.6394864831434140529, -1.564145959968468169, 0.4219395085220526975 ) ) ;
#5257=CARTESIAN_POINT ( 'NONE',  ( 0.1472428470117045640, -1.270554630056540901, 0.4305824032786366162 ) ) ;
#5261=CARTESIAN_POINT ( 'NONE',  ( 0.3762811493344272451, -0.8989788859175238400, 0.7888608478858359918 ) ) ;
#5263=CARTESIAN_POINT ( 'NONE',  ( 0.07881452883472495063, -1.319805653379759525, 0.4755639510338647291 ) ) ;
#5270=CARTESIAN_POINT ( 'NONE',  ( -9.828236692375560680E-17, -0.4262518876079541830, 0.09312799375524088985 ) ) ;
#5273=FACE_OUTER_BOUND ( 'NONE', #32684, .T. ) ;
#5276=CARTESIAN_POINT ( 'NONE',  ( 0.3874633503144017110, -1.108325317417463873, 0.6051044758646879629 ) ) ;
#5278=CARTESIAN_POINT ( 'NONE',  ( 0.5328282478916582798, -1.349129593841621455, 0.6122296912113598388 ) ) ;
#5282=CARTESIAN_POINT ( 'NONE',  ( 0.4864609864856930255, -1.087049186798351608, 0.6366279691173203359 ) ) ;
#5284=DIRECTION ( 'NONE',  ( -1.000000000000000000, -0.000000000000000000, -0.000000000000000000 ) ) ;
#5288=CARTESIAN_POINT ( 'NONE',  ( 0.3554062530147323873, -1.622120902010288690, 0.5636526721968185827 ) ) ;
#5289=CARTESIAN_POINT ( 'NONE',  ( 0.7070466114709489380, -1.508851404092110826, 0.5588543131432650579 ) ) ;
#5297=CARTESIAN_POINT ( 'NONE',  ( 0.3319403630591542531, -1.291129383779237250, 0.5682417262808747704 ) ) ;
#5301=CARTESIAN_POINT ( 'NONE',  ( 0.07172816549509457296, -1.333591607576925187, 0.4986374818479088478 ) ) ;
#5302=CARTESIAN_POINT ( 'NONE',  ( 0.2625973931889362678, -0.6796768235205253861, 0.1477649966949237115 ) ) ;
#5304=CARTESIAN_POINT ( 'NONE',  ( 6.608588869366793274E-05, -0.9486129085773968850, 0.1942756810714297844 ) ) ;
#5307=CARTESIAN_POINT ( 'NONE',  ( 0.4285077932704187131, -1.141367488323234758, 0.4310073631607372335 ) ) ;
#5315=CARTESIAN_POINT ( 'NONE',  ( 0.01188081175741144760, -0.5563285785164118202, -0.07779187151457800375 ) ) ;
#5319=CARTESIAN_POINT ( 'NONE',  ( 0.5953303036072959964, -1.457508885835639978, 0.6057417262805095959 ) ) ;
#5320=EDGE_LOOP ( 'NONE', ( #36211, #16158, #9047, #14488 ) ) ;
#5326=CARTESIAN_POINT ( 'NONE',  ( -0.001385626645067268960, -0.8086677941022779592, 0.04152584225078851526 ) ) ;
#5330=DIRECTION ( 'NONE',  ( -0.4999551463232371762, 0.8660512985181134660, -0.000000000000000000 ) ) ;
#5333=CARTESIAN_POINT ( 'NONE',  ( 0.1004293403852877520, -0.9989955727027649557, 0.8255344432128082222 ) ) ;
#5339=CARTESIAN_POINT ( 'NONE',  ( 0.5382321766149029685, -1.161161941655082241, 0.5682417262808779901 ) ) ;
#5341=ORIENTED_EDGE ( 'NONE', *, *, #25341, .T. ) ;
#5344=CARTESIAN_POINT ( 'NONE',  ( 0.3709216698330897177, -1.101076713354972370, 0.7945692480043649031 ) ) ;
#5347=CARTESIAN_POINT ( 'NONE',  ( 0.1852718761952666104, -0.8389489029336036907, 0.1457185345930598341 ) ) ;
#5348=CARTESIAN_POINT ( 'NONE',  ( 0.2325938614944302874, -1.347997356825076487, 0.5182417262812506475 ) ) ;
#5351=CARTESIAN_POINT ( 'NONE',  ( 0.01220820732087773454, -0.4290243149126032329, 0.1652642515859651107 ) ) ;
#5352=CARTESIAN_POINT ( 'NONE',  ( 0.4165626002392254779, -1.713172581087865076, 0.4267767144038969729 ) ) ;
#5355=CARTESIAN_POINT ( 'NONE',  ( 0.3227706286670864455, -1.035098858529321930, 0.7546302758663894217 ) ) ;
#5356=ADVANCED_FACE ( 'NONE', ( #14171 ), #35965, .T. ) ;
#5361=CARTESIAN_POINT ( 'NONE',  ( 0.09104835764951833832, -0.9296025949902090302, 0.8700335549320106221 ) ) ;
#5362=CARTESIAN_POINT ( 'NONE',  ( 0.04079229832238050191, -0.9851896272356041040, 0.6760550084579007857 ) ) ;
#5365=CARTESIAN_POINT ( 'NONE',  ( 0.6791199086483500347, -1.400839286187941957, 0.8214794356666539343 ) ) ;
#5368=FACE_OUTER_BOUND ( 'NONE', #32642, .T. ) ;
#5378=CARTESIAN_POINT ( 'NONE',  ( 0.04104228371791049379, -0.8021798566012479093, 0.6857248727280681466 ) ) ;
#5380=CARTESIAN_POINT ( 'NONE',  ( 0.5632287970188207815, -1.453831970626443981, 0.7328793321959286011 ) ) ;
#5381=CARTESIAN_POINT ( 'NONE',  ( 0.2875448026290280401, -1.663016392949335565, 0.4537443422403701354 ) ) ;
#5384=CARTESIAN_POINT ( 'NONE',  ( 0.5231597928089396499, -1.148848539795074508, 0.7464108937515090414 ) ) ;
#5386=ORIENTED_EDGE ( 'NONE', *, *, #138, .F. ) ;
#5395=CARTESIAN_POINT ( 'NONE',  ( 0.2503298133092587974, -0.9500301554809115201, 0.6860627806878819568 ) ) ;
#5396=CARTESIAN_POINT ( 'NONE',  ( 0.2208413595467774437, -1.374101648533643250, 1.025128890476463051 ) ) ;
#5397=CARTESIAN_POINT ( 'NONE',  ( 0.4967266092558669799, -1.542263453013163588, 0.5610250318491952770 ) ) ;
#5398=CARTESIAN_POINT ( 'NONE',  ( 0.3235114482504872768, -1.763390692376212820, 0.5025175481131797239 ) ) ;
#5399=CARTESIAN_POINT ( 'NONE',  ( -0.002214229356001021481, -0.8555149127599896985, 0.1346324584729416685 ) ) ;
#5400=CARTESIAN_POINT ( 'NONE',  ( 0.005238257023236751568, -0.9818020271132209542, 0.4509873321765103249 ) ) ;
#5403=CARTESIAN_POINT ( 'NONE',  ( 0.3173336537065408192, -1.761100837031106536, 0.5505159244398599716 ) ) ;
#5404=CARTESIAN_POINT ( 'NONE',  ( 0.5377357579551512723, -1.280405483484106766, 0.8977613861871198697 ) ) ;
#5412=CARTESIAN_POINT ( 'NONE',  ( 0.3175115894100313252, -1.184234847365859933, 0.5079114793355775648 ) ) ;
#5413=CARTESIAN_POINT ( 'NONE',  ( 0.5556676709287090565, -1.190831894458023177, 0.5757950255497361614 ) ) ;
#5417=AXIS2_PLACEMENT_3D ( 'NONE', #4963, #33351, #5160 ) ;
#5423=ORIENTED_EDGE ( 'NONE', *, *, #9735, .F. ) ;
#5425=AXIS2_PLACEMENT_3D ( 'NONE', #24881, #222, #21397 ) ;
#5428=CARTESIAN_POINT ( 'NONE',  ( 0.01030066036532899590, -0.8502541615097699568, 0.2885088771235587712 ) ) ;
#5438=AXIS2_PLACEMENT_3D ( 'NONE', #26834, #8493, #32776 ) ;
#5439=CARTESIAN_POINT ( 'NONE',  ( 0.3842197382819592666, -1.129692149189392314, 0.6942442540008864071 ) ) ;
#5441=CARTESIAN_POINT ( 'NONE',  ( 0.4782148911042844452, -1.678884647045308265, 0.5560315867989329419 ) ) ;
#5445=CARTESIAN_POINT ( 'NONE',  ( 0.2137558955837162433, -0.8305973034474390948, 0.6882441447716853844 ) ) ;
#5447=VECTOR ( 'NONE', #9079, 39.37007874015748143 ) ;
#5449=ADVANCED_FACE ( 'NONE', ( #36775 ), #8394, .F. ) ;
#5450=CARTESIAN_POINT ( 'NONE',  ( 0.4430914525986213715, -1.573752655959022695, 0.5975272644295865909 ) ) ;
#5452=CARTESIAN_POINT ( 'NONE',  ( 0.5670143714999978934, -1.627296631171844643, 0.5238801071547340982 ) ) ;
#5454=ORIENTED_EDGE ( 'NONE', *, *, #7418, .T. ) ;
#5458=CARTESIAN_POINT ( 'NONE',  ( 0.3295425949762220696, -1.070172357806076890, 0.7949539627233549455 ) ) ;
#5459=CARTESIAN_POINT ( 'NONE',  ( 0.4805909393811602093, -1.666072907763637145, 0.5622759738902064486 ) ) ;
#5462=CARTESIAN_POINT ( 'NONE',  ( 0.5409306160700753097, -1.629405757603852756, 0.4283118798799024907 ) ) ;
#5466=CARTESIAN_POINT ( 'NONE',  ( 0.3337757566908341467, -0.8338946305499669309, 0.7209303476996544724 ) ) ;
#5468=AXIS2_PLACEMENT_3D ( 'NONE', #22627, #34333, #28583 ) ;
#5469=CARTESIAN_POINT ( 'NONE',  ( 0.07954607876224152607, -1.328936092439369832, 0.4736269073421923714 ) ) ;
#5474=CARTESIAN_POINT ( 'NONE',  ( 0.6699292074404746833, -1.569526485364061807, 0.6071573546319920522 ) ) ;
#5476=DIRECTION ( 'NONE',  ( 0.000000000000000000, 1.000000000000000000, 1.566396143878659165E-12 ) ) ;
#5481=CARTESIAN_POINT ( 'NONE',  ( 0.07120675875603865723, -0.8149881486554784171, 0.8228864848196146831 ) ) ;
#5488=CARTESIAN_POINT ( 'NONE',  ( 0.3540817610093318635, -1.633452470505663667, 0.5182417262812423209 ) ) ;
#5492=CARTESIAN_POINT ( 'NONE',  ( 0.4465842785464451681, -1.213871555848032191, 0.7431748963014650489 ) ) ;
#5496=CARTESIAN_POINT ( 'NONE',  ( 0.4679067357895266843, -1.070896998011005019, 0.6479521087143890190 ) ) ;
#5498=ADVANCED_FACE ( 'NONE', ( #15392 ), #40487, .F. ) ;
#5504=CARTESIAN_POINT ( 'NONE',  ( 0.3557947951631240113, -1.622273835114473872, 0.5692848210717039725 ) ) ;
#5505=CARTESIAN_POINT ( 'NONE',  ( 0.06671723372763513349, -0.6968592392116272904, -0.001943235594188709708 ) ) ;
#5506=CARTESIAN_POINT ( 'NONE',  ( 0.1763220507667064563, -0.5650253974486517672, -0.04914117235521991284 ) ) ;
#5509=EDGE_LOOP ( 'NONE', ( #15231, #30470, #20552, #39415, #3368 ) ) ;
#5510=CARTESIAN_POINT ( 'NONE',  ( 0.5218509088173163279, -1.137553602289696819, 0.6585442127631569997 ) ) ;
#5511=B_SPLINE_CURVE_WITH_KNOTS ( 'NONE', 3,
 ( #38263, #677, #32702, #26155, #29223, #3725 ),
 .UNSPECIFIED., .F., .F.,
 ( 4, 2, 4 ),
 ( 3.469446951953614189E-18, 0.0006014525054105407170, 0.001202905010821077965 ),
 .UNSPECIFIED. ) ;
#5517=CARTESIAN_POINT ( 'NONE',  ( 0.3843371407211308433, -1.261522862150258995, 0.5783999743260659354 ) ) ;
#5519=B_SPLINE_CURVE_WITH_KNOTS ( 'NONE', 3,
 ( #6705, #31819, #15586, #38181, #10007, #22579, #6910, #32016, #16381, #28921, #786, #13296 ),
 .UNSPECIFIED., .F., .F.,
 ( 4, 2, 2, 2, 2, 4 ),
 ( 0.001537871260908298121, 0.002663464713205636845, 0.003789058165502975570, 0.004351854891651643631, 0.004914651617800311692, 0.006040245070097646947 ),
 .UNSPECIFIED. ) ;
#5522=CARTESIAN_POINT ( 'NONE',  ( 0.4136294883733862005, -1.694877849074643672, 0.4182417262808776903 ) ) ;
#5524=CARTESIAN_POINT ( 'NONE',  ( 0.3924513946351673721, -1.141110873382124913, 0.4807468720547258823 ) ) ;
#5525=CARTESIAN_POINT ( 'NONE',  ( 0.05447883519600660307, -1.297772118441766542, 0.6273051521731305424 ) ) ;
#5530=CARTESIAN_POINT ( 'NONE',  ( 0.4668492548151236265, -1.130293246669365370, 0.4644915327382355685 ) ) ;
#5531=CARTESIAN_POINT ( 'NONE',  ( 0.5623916231413996769, -1.181299486036711199, 0.6057417262809813296 ) ) ;
#5536=CARTESIAN_POINT ( 'NONE',  ( 0.0001449614208580852083, -0.5613537431353852192, -0.06918609228517788590 ) ) ;
#5537=CARTESIAN_POINT ( 'NONE',  ( 0.3247324306352935563, -1.759421949583405365, 0.4854534786567430427 ) ) ;
#5538=CARTESIAN_POINT ( 'NONE',  ( 0.0006674789801655854095, -0.4508007590529634068, 0.2320570027856783679 ) ) ;
#5540=CIRCLE ( 'NONE', #18032, 0.01000000000000009388 ) ;
#5547=CARTESIAN_POINT ( 'NONE',  ( 0.5985082606850495868, -1.473464502187743941, 0.6023744451300401259 ) ) ;
#5552=CARTESIAN_POINT ( 'NONE',  ( -0.001590528238760143074, -0.5283317060040648716, 0.1648872331919332412 ) ) ;
#5554=CARTESIAN_POINT ( 'NONE',  ( 0.1199895787080857840, -1.258723611029123557, 0.6044653572558237320 ) ) ;
#5559=VERTEX_POINT ( 'NONE', #31241 ) ;
#5562=CARTESIAN_POINT ( 'NONE',  ( 0.3612865554702208715, -1.133767101051816883, 0.6202026458649380070 ) ) ;
#5566=CARTESIAN_POINT ( 'NONE',  ( 0.4538561152830952738, -1.255326032114347568, 0.8184392061610863411 ) ) ;
#5568=CARTESIAN_POINT ( 'NONE',  ( 0.1865116958955829740, -0.7545155313687175180, 0.04158996775387410749 ) ) ;
#5571=CARTESIAN_POINT ( 'NONE',  ( 0.6011193747858227798, -1.595581932925101976, 0.4276689662439276396 ) ) ;
#5573=CARTESIAN_POINT ( 'NONE',  ( 0.3860498842613241943, -1.725354837844226052, 0.4274986991496981803 ) ) ;
#5578=CARTESIAN_POINT ( 'NONE',  ( 0.4085116948120698366, -1.104829239061055013, 0.5999620787602801819 ) ) ;
#5582=CARTESIAN_POINT ( 'NONE',  ( 0.008057578236607982475, -0.5544447393747381492, 0.4149153965127375110 ) ) ;
#5583=CARTESIAN_POINT ( 'NONE',  ( 0.07862385513909125878, -1.240140462211094530, 0.7484620922004757704 ) ) ;
#5585=CARTESIAN_POINT ( 'NONE',  ( 0.5753152089321617035, -1.233008725051026655, 0.8518361925389578149 ) ) ;
#5594=CARTESIAN_POINT ( 'NONE',  ( 0.03184741477609578930, -0.7213761098217522649, 0.5732232197377126193 ) ) ;
#5595=CARTESIAN_POINT ( 'NONE',  ( 0.5878605360589412854, -1.491219481631713029, 0.5721084594529655121 ) ) ;
#5596=CARTESIAN_POINT ( 'NONE',  ( 0.3476685035120829492, -1.750311407975150280, 0.4514359344836209043 ) ) ;
#5599=CARTESIAN_POINT ( 'NONE',  ( 0.6136594321969363053, -1.288375518029639233, 0.6368171400845314967 ) ) ;
#5602=CARTESIAN_POINT ( 'NONE',  ( 0.6687172182925377184, -1.381928324059317426, 0.7472473190455153347 ) ) ;
#5604=CARTESIAN_POINT ( 'NONE',  ( 0.4380553862277722921, -1.229819722584721164, 0.5856983068965045947 ) ) ;
#5605=B_SPLINE_CURVE_WITH_KNOTS ( 'NONE', 3,
 ( #13495, #10816, #38580, #19864, #32399, #16790 ),
 .UNSPECIFIED., .F., .F.,
 ( 4, 2, 4 ),
 ( 0.001086186341203851033, 0.004311068202048287321, 0.007535950062892723608 ),
 .UNSPECIFIED. ) ;
#5606=CARTESIAN_POINT ( 'NONE',  ( 0.1890965627226634804, -1.347655541994686068, 0.5182417262812423209 ) ) ;
#5609=CARTESIAN_POINT ( 'NONE',  ( 0.1020195082480463700, -0.7293290528718650023, 0.3482666274738245304 ) ) ;
#5611=CARTESIAN_POINT ( 'NONE',  ( 0.3059622673449214902, -1.701610228655562773, 0.8344189609799835816 ) ) ;
#5612=CARTESIAN_POINT ( 'NONE',  ( 0.3795518307925651036, -1.261362786936248037, 0.8506242053835164629 ) ) ;
#5614=CARTESIAN_POINT ( 'NONE',  ( 0.06954796871655651025, -1.315582234632707515, 0.5182417262812430980 ) ) ;
#5615=CARTESIAN_POINT ( 'NONE',  ( 0.01675195241592676923, -1.055683844097430324, 0.6015879664242336222 ) ) ;
#5620=CARTESIAN_POINT ( 'NONE',  ( 0.2919827015984412522, -0.8702395470303202485, 0.7938945491903462992 ) ) ;
#5625=PRODUCT_DEFINITION_FORMATION_WITH_SPECIFIED_SOURCE ( 'ANY', '', #39358, .NOT_KNOWN. ) ;
#5627=DIRECTION ( 'NONE',  ( 0.8660512985181132439, 0.4999551463232376758, 0.000000000000000000 ) ) ;
#5631=CARTESIAN_POINT ( 'NONE',  ( 0.2618294899476097393, -0.7990503781373888836, 0.5447687035333291794 ) ) ;
#5634=CARTESIAN_POINT ( 'NONE',  ( 0.5772157698596116493, -1.612763119636421383, 0.5867784257054611263 ) ) ;
#5635=EDGE_CURVE ( 'NONE', #6325, #13571, #40299, .T. ) ;
#5643=CARTESIAN_POINT ( 'NONE',  ( 0.2698036132048247104, -0.9625005881386677897, 0.7146062034794288254 ) ) ;
#5644=EDGE_LOOP ( 'NONE', ( #11088, #31673, #20106, #7309, #24098 ) ) ;
#5647=CARTESIAN_POINT ( 'NONE',  ( 0.09909909854404998220, -1.020393566678226005, 0.7132605819709517680 ) ) ;
#5648=ORIENTED_EDGE ( 'NONE', *, *, #23113, .F. ) ;
#5653=CARTESIAN_POINT ( 'NONE',  ( 0.7426951793279046310, -1.510662807742832348, 0.6358527240479500131 ) ) ;
#5655=CARTESIAN_POINT ( 'NONE',  ( 0.4691437399998080737, -1.240809866259031002, 0.5800955640248587342 ) ) ;
#5657=CARTESIAN_POINT ( 'NONE',  ( 0.008480392309630364542, -0.9466935224705154139, 0.1457226493340757767 ) ) ;
#5659=ORIENTED_EDGE ( 'NONE', *, *, #35292, .F. ) ;
#5662=ORIENTED_EDGE ( 'NONE', *, *, #18862, .F. ) ;
#5664=CARTESIAN_POINT ( 'NONE',  ( 0.6728294579378611973, -1.556433697830899687, 0.6139941624117232211 ) ) ;
#5665=CARTESIAN_POINT ( 'NONE',  ( 0.4436065027728119947, -1.573014041395296436, 0.6136667051735021916 ) ) ;
#5667=CARTESIAN_POINT ( 'NONE',  ( 0.5722925517058021772, -1.623342969514509182, 0.4835929536261462380 ) ) ;
#5668=CARTESIAN_POINT ( 'NONE',  ( 0.4870042317405073873, -1.170188898918880893, 0.4224809036138285623 ) ) ;
#5670=EDGE_LOOP ( 'NONE', ( #19353, #30949, #10333, #30249 ) ) ;
#5675=CARTESIAN_POINT ( 'NONE',  ( 0.5488630487633856525, -1.446887613430648090, 0.7481907029641444717 ) ) ;
#5676=CARTESIAN_POINT ( 'NONE',  ( 0.4590038926919776108, -1.675844875513867294, 0.4569803339803656939 ) ) ;
#5684=CARTESIAN_POINT ( 'NONE',  ( 0.3679852976493193095, -0.8933044249262621639, 0.7616870389678419562 ) ) ;
#5686=ADVANCED_FACE ( 'NONE', ( #2012 ), #28461, .F. ) ;
#5687=CARTESIAN_POINT ( 'NONE',  ( 0.009064896295912058116, -1.006671522247063022, 0.5204707375227085597 ) ) ;
#5691=CARTESIAN_POINT ( 'NONE',  ( -2.070903537920736781, -2.678131749591557309, 0.6057417262810178560 ) ) ;
#5698=DIRECTION ( 'NONE',  ( 0.8660512985181132439, 0.4999551463232376758, 0.000000000000000000 ) ) ;
#5701=ORIENTED_EDGE ( 'NONE', *, *, #26598, .T. ) ;
#5702=CARTESIAN_POINT ( 'NONE',  ( 0.3709243015156632461, -1.147037477812652195, 0.6031947222724455271 ) ) ;
#5705=CARTESIAN_POINT ( 'NONE',  ( 0.4551546549851303580, -1.225298050788209414, 0.7259450990592548614 ) ) ;
#5708=CARTESIAN_POINT ( 'NONE',  ( 0.3711835952353229051, -0.9982156264046870842, 0.6339317236198600547 ) ) ;
#5714=CARTESIAN_POINT ( 'NONE',  ( 0.01054817777343857940, -0.5296544771352952319, 0.1457185332388703236 ) ) ;
#5717=CARTESIAN_POINT ( 'NONE',  ( 0.03638364785045244965, -0.5559812057408780595, 0.2471708904571671417 ) ) ;
#5718=CARTESIAN_POINT ( 'NONE',  ( 0.06682908180107070828, -0.6872203660146791737, -0.001923513761143209400 ) ) ;
#5719=CARTESIAN_POINT ( 'NONE',  ( 0.1863655194128141790, -0.6771278842445480617, -0.02150419001686059914 ) ) ;
#5723=ORIENTED_EDGE ( 'NONE', *, *, #19465, .T. ) ;
#5725=CARTESIAN_POINT ( 'NONE',  ( 0.3308510979688408238, -0.9309371998241751101, 0.6266194620381673186 ) ) ;
#5726=CARTESIAN_POINT ( 'NONE',  ( 0.5536301873218408831, -1.511148576249882192, 0.5861183057439698363 ) ) ;
#5731=EDGE_CURVE ( 'NONE', #36006, #19301, #33266, .T. ) ;
#5735=CARTESIAN_POINT ( 'NONE',  ( 0.1089214313634646741, -1.279151142302971778, 0.6159407968199497319 ) ) ;
#5737=CARTESIAN_POINT ( 'NONE',  ( 1.365923996832131609E-16, -0.9481888444201336252, 0.1622877746734860682 ) ) ;
#5741=CARTESIAN_POINT ( 'NONE',  ( 0.4727378706625928184, -1.129322216815012325, 0.4725836227227263597 ) ) ;
#5742=CARTESIAN_POINT ( 'NONE',  ( 0.4580986008033318679, -1.241505888743733577, 0.6057417262809813296 ) ) ;
#5744=CARTESIAN_POINT ( 'NONE',  ( 0.1873045545006853108, -1.548079183614573306, 0.6123590530682133659 ) ) ;
#5745=CARTESIAN_POINT ( 'NONE',  ( 0.2615957342988080581, -1.678037082261113921, 0.5379576451024024042 ) ) ;
#5749=VERTEX_POINT ( 'NONE', #24424 ) ;
#5752=ORIENTED_EDGE ( 'NONE', *, *, #24141, .F. ) ;
#5754=CARTESIAN_POINT ( 'NONE',  ( 0.6252338399778394340, -1.468100857423625838, 0.5182417262812428760 ) ) ;
#5755=CARTESIAN_POINT ( 'NONE',  ( 0.001385844221826001152, -0.5662722994882537497, 0.04168102574831390045 ) ) ;
#5759=ORIENTED_EDGE ( 'NONE', *, *, #12225, .T. ) ;
#5760=CARTESIAN_POINT ( 'NONE',  ( 0.2691513416950872539, -1.675382000085723133, 0.6134701876119651454 ) ) ;
#5761=CARTESIAN_POINT ( 'NONE',  ( 0.4341051395151963033, -1.228754679272166861, 0.6047424332237795186 ) ) ;
#5762=CARTESIAN_POINT ( 'NONE',  ( 0.1025666744235219086, -1.287399128809481930, 0.6111874459470316712 ) ) ;
#5770=CARTESIAN_POINT ( 'NONE',  ( 0.01161528454259690320, -0.8017023655927671966, -0.08667232896669077591 ) ) ;
#5774=CARTESIAN_POINT ( 'NONE',  ( 0.2397879752593336244, -0.9193312231006620650, 0.6873777895663281123 ) ) ;
#5776=CARTESIAN_POINT ( 'NONE',  ( 0.2563022272722030315, -1.568531830826473961, 0.8673523457354177513 ) ) ;
#5777=CARTESIAN_POINT ( 'NONE',  ( 0.03505638526559837903, -0.6086893780663767961, 0.5882652742279115277 ) ) ;
#5779=CARTESIAN_POINT ( 'NONE',  ( 0.4103533436992015671, -1.245885857446504374, 0.5182417262812503145 ) ) ;
#5781=CARTESIAN_POINT ( 'NONE',  ( -0.0004160691872336406234, -0.9369703133356521718, 0.1337599650683027885 ) ) ;
#5782=CARTESIAN_POINT ( 'NONE',  ( 0.2215734864168983353, -1.328907224007676913, 0.5182417262812423209 ) ) ;
#5785=CARTESIAN_POINT ( 'NONE',  ( 0.2721752123224986386, -1.596339224327277595, 0.9197038883954219424 ) ) ;
#5786=CARTESIAN_POINT ( 'NONE',  ( 0.06169161831772442678, -1.079659987968021762, 0.7429596578979000832 ) ) ;
#5788=CARTESIAN_POINT ( 'NONE',  ( 0.5517781715537678489, -1.195290833855036983, 0.8540039827052086086 ) ) ;
#5794=CARTESIAN_POINT ( 'NONE',  ( 0.2073178280655720573, -1.399379311278335480, 0.9347264154772038092 ) ) ;
#5795=CARTESIAN_POINT ( 'NONE',  ( 0.5807400140824149348, -1.476489732972543489, 0.6842656776274327335 ) ) ;
#5798=CARTESIAN_POINT ( 'NONE',  ( 0.1896483993057378192, -0.6911749089203499397, 0.2228938739458891649 ) ) ;
#5801=CARTESIAN_POINT ( 'NONE',  ( 0.5439789624071748042, -1.183015531583673674, 0.8191768695127470412 ) ) ;
#5807=CARTESIAN_POINT ( 'NONE',  ( 0.08692586860950433925, -0.7045980206078551467, 0.1576013572116870820 ) ) ;
#5809=CARTESIAN_POINT ( 'NONE',  ( 0.5252982915109456474, -1.526881808260259987, 0.5746848141541492927 ) ) ;
#5810=CARTESIAN_POINT ( 'NONE',  ( 0.3252627854908551330, -1.766295133273483309, 0.5020845719335209623 ) ) ;
#5811=CARTESIAN_POINT ( 'NONE',  ( 9.210829332990911559E-05, -0.6768113429346261922, -0.02211036473533352364 ) ) ;
#5815=CARTESIAN_POINT ( 'NONE',  ( 0.5472056306734645048, -1.297393719792277134, 0.8953388641935672299 ) ) ;
#5818=CARTESIAN_POINT ( 'NONE',  ( 0.3704697912810961946, -1.166474544107111599, 0.4182417262808778013 ) ) ;
#5821=CARTESIAN_POINT ( 'NONE',  ( 0.2322244407957205770, -0.7584751632699872070, 0.4677412183550399005 ) ) ;
#5825=FACE_OUTER_BOUND ( 'NONE', #39488, .T. ) ;
#5829=DIRECTION ( 'NONE',  ( 0.8660512985181132439, 0.4999551463232376758, 0.000000000000000000 ) ) ;
#5831=ORIENTED_EDGE ( 'NONE', *, *, #23024, .T. ) ;
#5834=CARTESIAN_POINT ( 'NONE',  ( 0.09299045696175671505, -1.001796792555563087, 0.6985355088916623822 ) ) ;
#5844=CARTESIAN_POINT ( 'NONE',  ( 0.4841487358689927634, -1.673745430023940717, 0.5182417262823179049 ) ) ;
#5847=CARTESIAN_POINT ( 'NONE',  ( 0.2581756672896094451, -0.9092364711756537599, 0.7438128635199100502 ) ) ;
#5850=CARTESIAN_POINT ( 'NONE',  ( 0.4229029504711039888, -1.459654819224503353, 0.8188420036968601101 ) ) ;
#5854=CARTESIAN_POINT ( 'NONE',  ( 0.5611303468409032380, -1.505106176321531875, 0.5084158906598846839 ) ) ;
#5860=CARTESIAN_POINT ( 'NONE',  ( 0.1504400051554825868, -0.6766857922489548649, 0.4634885189021805685 ) ) ;
#5861=CARTESIAN_POINT ( 'NONE',  ( 0.4400739460935926273, -1.687131003255787354, 0.4386290681939620240 ) ) ;
#5863=( BOUNDED_SURFACE ( )  B_SPLINE_SURFACE ( 3, 2, ( 
 ( #19500, #28748, #6718 ),
 ( #10022, #7116, #29145 ),
 ( #13523, #25469, #10235 ),
 ( #25881, #12914, #32029 ),
 ( #801, #3836, #9812 ),
 ( #26085, #38604, #4248 ),
 ( #34910, #25663, #25259 ),
 ( #19292, #16816, #29360 ),
 ( #37801, #10424, #28934 ),
 ( #3652, #13103, #9620 ),
 ( #22985, #16213, #22194 ),
 ( #38399, #15998, #31625 ),
 ( #22804, #28546, #420 ),
 ( #7312, #610, #38197 ),
 ( #35123, #35327, #19682 ),
 ( #32217, #4035, #13705 ),
 ( #17411, #39007, #8140 ),
 ( #32639, #20304, #23802 ),
 ( #4444, #5249, #17802 ),
 ( #30365, #20108, #1593 ),
 ( #8351, #36539, #39412 ),
 ( #26692, #26273, #38789 ),
 ( #7533, #11045, #17006 ),
 ( #10621, #5054, #23197 ),
 ( #29549, #1388, #29751 ),
 ( #20921, #35720, #13899 ),
 ( #11230, #39225, #7926 ),
 ( #33441, #26880, #26472 ),
 ( #23605, #17615, #36119 ),
 ( #10843, #4839, #33037 ),
 ( #23418, #29971, #35932 ),
 ( #7740, #32824, #4630 ),
 ( #17206, #14120, #1805 ),
 ( #20503, #14321, #36321 ) ),
 .UNSPECIFIED., .F., .F., .T. ) 
 B_SPLINE_SURFACE_WITH_KNOTS ( ( 4, 2, 2, 2, 2, 2, 2, 2, 2, 2, 2, 2, 2, 2, 2, 2, 4 ),
 ( 3, 3 ),
 ( 0.001710004797882772650, 0.002329098799114573057, 0.002948192800346373897, 0.003567286801578174304, 0.004186380802809974710, 0.004805474804041774683, 0.005424568805273575524, 0.006043662806505376364, 0.006662756807737176337, 0.007281850808968977178, 0.007900944810200778018, 0.008520038811432577991, 0.009139132812664377964, 0.009758226813896177937, 0.01037732081512797791, 0.01099641481635977788, 0.01161550881759157959 ),
 ( 0.000000000000000000, 1.000000000000000000 ),
 .UNSPECIFIED. ) 
 GEOMETRIC_REPRESENTATION_ITEM ( )  RATIONAL_B_SPLINE_SURFACE ( (
 ( 1.000000000000000000, 0.7661775686432606980, 1.000000000000000000),
 ( 1.000000000000000000, 0.7660633144985160570, 1.000000000000000000),
 ( 1.000000000000000000, 0.7659625556653616441, 1.000000000000000000),
 ( 1.000000000000000000, 0.7657843064335759786, 1.000000000000000000),
 ( 1.000000000000000000, 0.7657059323776339577, 1.000000000000000000),
 ( 1.000000000000000000, 0.7655651667306325736, 1.000000000000000000),
 ( 1.000000000000000000, 0.7655031821185447338, 1.000000000000000000),
 ( 1.000000000000000000, 0.7654067721134163449, 1.000000000000000000),
 ( 1.000000000000000000, 0.7653717631867683613, 1.000000000000000000),
 ( 1.000000000000000000, 0.7653379689688158960, 1.000000000000000000),
 ( 1.000000000000000000, 0.7653399838946506328, 1.000000000000000000),
 ( 1.000000000000000000, 0.7653826612811753805, 1.000000000000000000),
 ( 1.000000000000000000, 0.7654239822339510280, 1.000000000000000000),
 ( 1.000000000000000000, 0.7655382443605589504, 1.000000000000000000),
 ( 1.000000000000000000, 0.7656103788928951825, 1.000000000000000000),
 ( 1.000000000000000000, 0.7657736866170623546, 1.000000000000000000),
 ( 1.000000000000000000, 0.7658654630984720324, 1.000000000000000000),
 ( 1.000000000000000000, 0.7660476170358867520, 1.000000000000000000),
 ( 1.000000000000000000, 0.7661388857263637941, 1.000000000000000000),
 ( 1.000000000000000000, 0.7663086609638074531, 1.000000000000000000),
 ( 1.000000000000000000, 0.7663852831037184510, 1.000000000000000000),
 ( 1.000000000000000000, 0.7665082163394573156, 1.000000000000000000),
 ( 1.000000000000000000, 0.7665553051685600749, 1.000000000000000000),
 ( 1.000000000000000000, 0.7666099424742220947, 1.000000000000000000),
 ( 1.000000000000000000, 0.7666174550739168758, 1.000000000000000000),
 ( 1.000000000000000000, 0.7665941758084844349, 1.000000000000000000),
 ( 1.000000000000000000, 0.7665628199831622247, 1.000000000000000000),
 ( 1.000000000000000000, 0.7664711555354097872, 1.000000000000000000),
 ( 1.000000000000000000, 0.7664113945286483709, 1.000000000000000000),
 ( 1.000000000000000000, 0.7662685914096645234, 1.000000000000000000),
 ( 1.000000000000000000, 0.7661862752594525983, 1.000000000000000000),
 ( 1.000000000000000000, 0.7659979125830966851, 1.000000000000000000),
 ( 1.000000000000000000, 0.7658906909088671888, 1.000000000000000000),
 ( 1.000000000000000000, 0.7657622705003380714, 1.000000000000000000) ) ) 
 REPRESENTATION_ITEM ( '' )  SURFACE ( )  );
#5867=CARTESIAN_POINT ( 'NONE',  ( 0.2334441654029815461, -1.232220874905952002, 0.5357669168543389704 ) ) ;
#5868=CARTESIAN_POINT ( 'NONE',  ( 0.3136609249452982917, -0.7980415872784507592, 0.6920156437578004471 ) ) ;
#5871=CARTESIAN_POINT ( 'NONE',  ( 0.0007958614940114835511, -0.9534529561155069555, 0.2845628645576042670 ) ) ;
#5875=CARTESIAN_POINT ( 'NONE',  ( 0.08509462337972420465, -0.8106601073620037790, 0.1457185332388698795 ) ) ;
#5876=CARTESIAN_POINT ( 'NONE',  ( 0.06954796871655651025, -1.315582234632707515, 0.5182417262812430980 ) ) ;
#5877=CARTESIAN_POINT ( 'NONE',  ( 0.5972649584706940518, -1.597985788488442527, 0.4298582196018018720 ) ) ;
#5878=ADVANCED_FACE ( 'NONE', ( #3210 ), #22725, .F. ) ;
#5883=CARTESIAN_POINT ( 'NONE',  ( 0.6636547731126125615, -1.509847865698558556, 0.4182417262808776903 ) ) ;
#5890=CARTESIAN_POINT ( 'NONE',  ( 0.3332069212083951792, -1.175771073360517116, 0.5719569841860573378 ) ) ;
#5893=CARTESIAN_POINT ( 'NONE',  ( 0.4874005273354089507, -1.272337409915087258, 0.6815837265936333100 ) ) ;
#5896=CARTESIAN_POINT ( 'NONE',  ( 0.5133443775832216005, -1.117606250044787863, 0.5819851345710455037 ) ) ;
#5902=CARTESIAN_POINT ( 'NONE',  ( 0.2499116230160881025, -1.320538391621939533, 0.9121915517445829957 ) ) ;
#5905=CARTESIAN_POINT ( 'NONE',  ( 0.1138168093370103690, -0.5794347803528829832, -0.06987067695535194300 ) ) ;
#5911=CARTESIAN_POINT ( 'NONE',  ( 0.3349705278058782709, -1.064816160538507139, 0.6377121673170756955 ) ) ;
#5912=CARTESIAN_POINT ( 'NONE',  ( 0.4769129862565332223, -1.388126235601429892, 0.8131988394239295648 ) ) ;
#5915=DIRECTION ( 'NONE',  ( 0.8660512985181132439, 0.4999551463232376758, 0.000000000000000000 ) ) ;
#5919=CARTESIAN_POINT ( 'NONE',  ( 0.3740960844805631957, -1.108072201694596526, 0.5182417262812423209 ) ) ;
#5920=CARTESIAN_POINT ( 'NONE',  ( 0.3056347003372518745, -1.768333716703696323, 0.5707417262808793801 ) ) ;
#5921=CARTESIAN_POINT ( 'NONE',  ( 0.09106859344845208426, -1.304999351207305480, 0.5974602131358454082 ) ) ;
#5923=CARTESIAN_POINT ( 'NONE',  ( 0.08042334443895514384, -1.362032735465325661, 0.6028738014108521170 ) ) ;
#5925=CARTESIAN_POINT ( 'NONE',  ( 0.3459602365858145401, -1.002069219538038736, 0.6041729112776661470 ) ) ;
#5926=CARTESIAN_POINT ( 'NONE',  ( 0.4826234098002670780, -1.120895762997321077, 0.5150456658529999343 ) ) ;
#5927=CARTESIAN_POINT ( 'NONE',  ( 0.4568206499005321164, -1.218986888361895282, 0.5856983068965044836 ) ) ;
#5930=CARTESIAN_POINT ( 'NONE',  ( 0.1172025164431036715, -1.392648223243311723, 0.6963985612953286219 ) ) ;
#5935=CARTESIAN_POINT ( 'NONE',  ( 0.3177856290042974652, -1.645584934368151009, 0.5182417262812344383 ) ) ;
#5942=EDGE_CURVE ( 'NONE', #38229, #15275, #22809, .T. ) ;
#5945=AXIS2_PLACEMENT_3D ( 'NONE', #12052, #3002, #40014 ) ;
#5954=CARTESIAN_POINT ( 'NONE',  ( -0.001446413187643280814, -0.5403182641434959299, 0.2206895948476451930 ) ) ;
#5955=CARTESIAN_POINT ( 'NONE',  ( 0.4190035292061285999, -1.208494183746581463, 0.6641413202029121665 ) ) ;
#5961=ORIENTED_EDGE ( 'NONE', *, *, #514, .F. ) ;
#5966=CARTESIAN_POINT ( 'NONE',  ( 0.5132325995285942355, -1.352621407328026493, 0.8007139552203286215 ) ) ;
#5967=CARTESIAN_POINT ( 'NONE',  ( 0.2230041220662333790, -0.9268358352298275982, 0.6424936301217993861 ) ) ;
#5970=CARTESIAN_POINT ( 'NONE',  ( 0.3192871411569696005, -1.699607763058582632, 0.8452318849098621190 ) ) ;
#5971=B_SPLINE_CURVE_WITH_KNOTS ( 'NONE', 3,
 ( #14695, #7495, #20075, #31359 ),
 .UNSPECIFIED., .F., .F.,
 ( 4, 4 ),
 ( 0.000000000000000000, 0.004353774562966205262 ),
 .UNSPECIFIED. ) ;
#5973=CARTESIAN_POINT ( 'NONE',  ( 0.5708401535611469235, -1.615683077095924736, 0.5197417262808792238 ) ) ;
#5978=CARTESIAN_POINT ( 'NONE',  ( -6.552157794917040043E-17, -0.4262518876079541830, 0.1106581735831166785 ) ) ;
#5979=CARTESIAN_POINT ( 'NONE',  ( 0.09137806685966429199, -1.251329420820371352, 0.7514797811827245155 ) ) ;
#5981=CARTESIAN_POINT ( 'NONE',  ( 0.6116693357450743163, -1.291191393066782211, 0.8405059385265429839 ) ) ;
#5991=CARTESIAN_POINT ( 'NONE',  ( 0.2706767884852234185, -1.629893486181000384, 0.7916626055961630826 ) ) ;
#5993=CARTESIAN_POINT ( 'NONE',  ( 0.1286531880915039450, -0.5504795770112219655, 0.1457185332388692689 ) ) ;
#5997=CARTESIAN_POINT ( 'NONE',  ( 0.3677026761718887315, -0.9383931188863808837, 0.6934371584156296953 ) ) ;
#5999=ORIENTED_EDGE ( 'NONE', *, *, #39380, .F. ) ;
#6000=CARTESIAN_POINT ( 'NONE',  ( 0.2186022828414512231, -0.6499659907669792513, 0.4387193036502484711 ) ) ;
#6007=ADVANCED_FACE ( 'NONE', ( #31360 ), #20537, .T. ) ;
#6008=CARTESIAN_POINT ( 'NONE',  ( 0.09634828771505739298, -0.7600076796586502370, 0.3121834059226053504 ) ) ;
#6010=CARTESIAN_POINT ( 'NONE',  ( 0.5252677807972566670, -1.526876841991572142, 0.5741887749453796763 ) ) ;
#6011=CARTESIAN_POINT ( 'NONE',  ( 0.3499317094845418308, -1.754137739073130753, 0.4513909310129528007 ) ) ;
#6012=CARTESIAN_POINT ( 'NONE',  ( 0.0001905119757726109924, -0.6656977259803509295, -0.02102838956235005691 ) ) ;
#6014=ORIENTED_EDGE ( 'NONE', *, *, #4618, .F. ) ;
#6015=CARTESIAN_POINT ( 'NONE',  ( 0.4327791790642120384, -1.706049035981101358, 0.6054719847766963925 ) ) ;
#6016=B_SPLINE_CURVE_WITH_KNOTS ( 'NONE', 3,
 ( #39087, #7604, #29619, #13976 ),
 .UNSPECIFIED., .F., .F.,
 ( 4, 4 ),
 ( 8.673617379884035472E-19, 0.0008438904120417860255 ),
 .UNSPECIFIED. ) ;
#6017=CARTESIAN_POINT ( 'NONE',  ( 0.2866465215685243817, -0.7220565828703142675, 0.6519108322339883799 ) ) ;
#6019=CARTESIAN_POINT ( 'NONE',  ( 0.006030796843114796454, -0.8457574864219309374, 0.1381917444211341606 ) ) ;
#6024=CARTESIAN_POINT ( 'NONE',  ( 0.1614670899430008522, -0.7569536277469717245, 0.1022936816274460647 ) ) ;
#6025=CARTESIAN_POINT ( 'NONE',  ( 0.5342447626335863342, -1.156090923338821463, 0.6541422520001994867 ) ) ;
#6029=CARTESIAN_POINT ( 'NONE',  ( 0.6477906992409429021, -1.570672284941449615, 0.6203763125787145061 ) ) ;
#6031=B_SPLINE_CURVE_WITH_KNOTS ( 'NONE', 3,
 ( #36355, #7769, #32857, #20534, #29786, #23834, #32668, #11477, #26301, #8377 ),
 .UNSPECIFIED., .F., .F.,
 ( 4, 3, 3, 4 ),
 ( -6.000000000173966796E-08, 0.000000000000000000, 1.599765854542544604E-05, 3.053234943348237166E-05 ),
 .UNSPECIFIED. ) ;
#6033=CARTESIAN_POINT ( 'NONE',  ( 0.3986508974220148160, -1.711168768618083869, 0.4182305167228609899 ) ) ;
#6036=CARTESIAN_POINT ( 'NONE',  ( 0.4730613458671842353, -1.134798785001164712, 0.4646432420420624210 ) ) ;
#6041=CARTESIAN_POINT ( 'NONE',  ( 0.07383395682904796142, -1.276537601224291274, 0.7475687110354797271 ) ) ;
#6051=LINE ( 'NONE', #28093, #12213 ) ;
#6054=CARTESIAN_POINT ( 'NONE',  ( 0.07795955261373284373, -1.322072399571159407, 0.5462526511609022695 ) ) ;
#6055=ORIENTED_EDGE ( 'NONE', *, *, #28191, .F. ) ;
#6059=CARTESIAN_POINT ( 'NONE',  ( 0.4708967593789014638, -1.552455728631323417, 0.6553166368004886833 ) ) ;
#6061=CARTESIAN_POINT ( 'NONE',  ( 0.5678328055818865350, -1.616694484607086313, 0.5530647866453864969 ) ) ;
#6068=CARTESIAN_POINT ( 'NONE',  ( 0.5817289510859825485, -1.495063960572125872, 0.5924595019112512961 ) ) ;
#6069=CARTESIAN_POINT ( 'NONE',  ( 0.4792821459481910740, -1.664810697191674960, 0.5161465343054540966 ) ) ;
#6070=CYLINDRICAL_SURFACE ( 'NONE', #8175, 0.2500000000000000000 ) ;
#6071=CARTESIAN_POINT ( 'NONE',  ( 0.2183697179345998052, -1.229346570154329799, 0.5436728950768712210 ) ) ;
#6072=CARTESIAN_POINT ( 'NONE',  ( 0.2225889308918536924, -1.238345268919997855, 0.5682417262808776570 ) ) ;
#6073=CARTESIAN_POINT ( 'NONE',  ( 0.3585389588907697545, -1.160913934521024649, 0.4273619767025411131 ) ) ;
#6074=CARTESIAN_POINT ( 'NONE',  ( 0.2232487200984690223, -0.6189500806901601093, 0.4773341886849224447 ) ) ;
#6076=CARTESIAN_POINT ( 'NONE',  ( 0.06844863008403212490, -1.325512397932680608, 0.5829276846574326099 ) ) ;
#6080=CARTESIAN_POINT ( 'NONE',  ( 0.1070150395144117139, -0.8615151753913300459, 0.4568215877972369166 ) ) ;
#6088=CARTESIAN_POINT ( 'NONE',  ( 0.6499217190830813839, -1.534003153280716569, 0.4182417262808776903 ) ) ;
#6090=DIRECTION ( 'NONE',  ( -0.4999551463232372317, 0.8660512985181135770, -0.000000000000000000 ) ) ;
#6093=CIRCLE ( 'NONE', #15307, 0.01000000000000001582 ) ;
#6094=CARTESIAN_POINT ( 'NONE',  ( 0.3528210451890865795, -1.143700418102651994, 0.6155400910483455057 ) ) ;
#6095=CARTESIAN_POINT ( 'NONE',  ( 0.3499317094845083576, -1.754137739073151847, 0.4513909310129906038 ) ) ;
#6097=CARTESIAN_POINT ( 'NONE',  ( 0.4076508935747791273, -1.158461938185323392, 0.7296380582302550710 ) ) ;
#6100=CARTESIAN_POINT ( 'NONE',  ( 0.5003933895997771941, -1.101010879683239629, 0.6202731239902519178 ) ) ;
#6101=EDGE_LOOP ( 'NONE', ( #11862, #7628, #29405, #36324 ) ) ;
#6105=ORIENTED_EDGE ( 'NONE', *, *, #11565, .T. ) ;
#6108=CARTESIAN_POINT ( 'NONE',  ( 0.2483516944684627248, -1.248337998612542687, 0.8972023426632544929 ) ) ;
#6110=CARTESIAN_POINT ( 'NONE',  ( 0.1856984011870668194, -0.7578896140594062469, -0.005504663353492499946 ) ) ;
#6116=CARTESIAN_POINT ( 'NONE',  ( 0.4047361405965239078, -1.117070546656567132, 0.6130903832934563313 ) ) ;
#6118=CARTESIAN_POINT ( 'NONE',  ( 0.4651104592015646855, -1.341950376707688797, 0.8227063177025514262 ) ) ;
#6128=ADVANCED_FACE ( 'NONE', ( #5825 ), #29791, .T. ) ;
#6135=CARTESIAN_POINT ( 'NONE',  ( 0.05651694441833610832, -1.310850388052192894, 0.6148622741790434887 ) ) ;
#6137=CARTESIAN_POINT ( 'NONE',  ( 0.1875000000000000833, -0.9151275355372969766, 0.1556228124470683261 ) ) ;
#6139=CARTESIAN_POINT ( 'NONE',  ( 0.4800703505524585579, -1.119839909059815897, 0.5356543536187720056 ) ) ;
#6140=CARTESIAN_POINT ( 'NONE',  ( 0.4444713835028593629, -1.226065644031627766, 0.6057417262810037561 ) ) ;
#6144=CARTESIAN_POINT ( 'NONE',  ( -0.003124719664520032511, -0.8057675726412022454, 0.1130684494947832019 ) ) ;
#6157=CARTESIAN_POINT ( 'NONE',  ( 0.4850466889450024688, -1.276291303272052646, 0.8070895406851786857 ) ) ;
#6158=CARTESIAN_POINT ( 'NONE',  ( 0.009593988611378652040, -0.5674229550368337094, 0.04256757953983118098 ) ) ;
#6165=CARTESIAN_POINT ( 'NONE',  ( 0.01081953179195768375, -0.5297023241700837826, 0.1548607054831544205 ) ) ;
#6166=CARTESIAN_POINT ( 'NONE',  ( 0.4349570274192550712, -1.230519544206422733, 0.5941052033352403061 ) ) ;
#6167=CARTESIAN_POINT ( 'NONE',  ( 0.08350584784635078917, -1.306523181150644364, 0.5696879678309485495 ) ) ;
#6170=ORIENTED_EDGE ( 'NONE', *, *, #510, .F. ) ;
#6171=VERTEX_POINT ( 'NONE', #9939 ) ;
#6175=EDGE_CURVE ( 'NONE', #15591, #3151, #7434, .T. ) ;
#6176=CARTESIAN_POINT ( 'NONE',  ( 0.5399288831475632655, -1.362507449995920217, 0.7674847699393548828 ) ) ;
#6177=CARTESIAN_POINT ( 'NONE',  ( 0.6984993753693692353, -1.438786077763939852, 0.5682417262808782121 ) ) ;
#6181=CARTESIAN_POINT ( 'NONE',  ( 0.3195334067233912001, -1.760651528094834939, 0.5793234143701277983 ) ) ;
#6184=CARTESIAN_POINT ( 'NONE',  ( 0.07592650758779409537, -1.323220219138284026, 0.5682417262808779901 ) ) ;
#6185=CARTESIAN_POINT ( 'NONE',  ( 0.2698036132048247104, -0.9625005881386677897, 0.7146062034794288254 ) ) ;
#6187=CARTESIAN_POINT ( 'NONE',  ( 0.3830853140175753957, -1.124506747416974761, 0.7559036875749386430 ) ) ;
#6194=CARTESIAN_POINT ( 'NONE',  ( 0.03991172363000938111, -1.025282391162960938, 0.7023476162170446679 ) ) ;
#6196=CARTESIAN_POINT ( 'NONE',  ( 0.2870953417136587471, -0.7492508933039718766, 0.6466144559156578042 ) ) ;
#6199=FACE_OUTER_BOUND ( 'NONE', #29864, .T. ) ;
#6204=CARTESIAN_POINT ( 'NONE',  ( 0.2532909672037780280, -1.579627038668091732, 0.8749452808108927337 ) ) ;
#6206=CARTESIAN_POINT ( 'NONE',  ( 0.4608701369652646318, -1.284683416556681390, 0.8202635153794951561 ) ) ;
#6210=B_SPLINE_CURVE_WITH_KNOTS ( 'NONE', 3,
 ( #25430, #9770, #12644, #571, #38150, #9973, #22543, #7646, #29655, #22752, #8252, #20824, #36224, #23513, #14014, #26586, #35833, #8447, #26974, #8038, #39127, #38348, #10951, #23697, #36028, #14842, #11138, #23909, #32735, #4956, #10183, #39508, #20210, #20614, #29867, #17906, #30070, #33148, #17520, #11558, #7832, #20403, #17107, #11339, #32935, #1899 ),
 .UNSPECIFIED., .F., .F.,
 ( 4, 2, 2, 2, 2, 2, 2, 2, 2, 2, 2, 2, 2, 2, 2, 2, 2, 2, 2, 2, 2, 2, 4 ),
 ( -6.000000007858409836E-08, 0.003552629519589487611, 0.007105319039179053796, 0.008881663798973832985, 0.01065800855876861478, 0.01154618093866600914, 0.01243435331856340177, 0.01421069807835819744, 0.01509887045825559528, 0.01598704283815299138, 0.01776338759794778357, 0.01865155997784517794, 0.01953973235774257231, 0.02131607711753736104, 0.02309242187733215323, 0.02398059425722953719, 0.02486876663712692115, 0.02575693901702430857, 0.02664511139692169253, 0.02753328377681907649, 0.02797736996676776153, 0.02819941306174210405, 0.02842145615671644310 ),
 .UNSPECIFIED. ) ;
#6211=CARTESIAN_POINT ( 'NONE',  ( 0.2003179398552689949, -0.7109237300142917659, 0.3290305662194804026 ) ) ;
#6212=VERTEX_POINT ( 'NONE', #4377 ) ;
#6214=CARTESIAN_POINT ( 'NONE',  ( 0.5289566482161313088, -1.159595167906385393, 0.8177397053652041281 ) ) ;
#6219=DIRECTION ( 'NONE',  ( -0.4999551463232372317, 0.8660512985181135770, -0.000000000000000000 ) ) ;
#6221=CARTESIAN_POINT ( 'NONE',  ( 0.3047812724409711960, -1.756857659564785568, 0.5654036402351543256 ) ) ;
#6223=CARTESIAN_POINT ( 'NONE',  ( 0.09832617150614605950, -0.7626014107058197711, 0.3272609970532458501 ) ) ;
#6225=CARTESIAN_POINT ( 'NONE',  ( 0.3254386620852590672, -1.747205596724848986, 0.7223889833057646204 ) ) ;
#6226=CARTESIAN_POINT ( 'NONE',  ( 0.5259394649249050646, -1.526850962987742255, 0.5868731501866165656 ) ) ;
#6229=ORIENTED_EDGE ( 'NONE', *, *, #26883, .F. ) ;
#6231=DIRECTION ( 'NONE',  ( -0.9848077530122080203, 0.000000000000000000, -0.1736481776669303589 ) ) ;
#6232=CARTESIAN_POINT ( 'NONE',  ( 0.6631499315851888676, -1.372742098333818772, 0.7573330281475406656 ) ) ;
#6233=B_SPLINE_CURVE_WITH_KNOTS ( 'NONE', 3,
 ( #26073, #25244, #35106, #28318 ),
 .UNSPECIFIED., .F., .F.,
 ( 4, 4 ),
 ( 2.914079691781330694E-05, 0.001162144789400721811 ),
 .UNSPECIFIED. ) ;
#6234=CARTESIAN_POINT ( 'NONE',  ( 0.1061812928925085775, -1.412809043690689492, 0.5685481090398675219 ) ) ;
#6235=CARTESIAN_POINT ( 'NONE',  ( 0.1914385470493136510, -0.8272674967231937737, 0.2680172446836712741 ) ) ;
#6237=CARTESIAN_POINT ( 'NONE',  ( 0.3210085668004670767, -1.182910313946810010, 0.5197417262808780025 ) ) ;
#6240=CARTESIAN_POINT ( 'NONE',  ( 1.365923996832131609E-16, -0.9481888444201336252, 0.1622877746734860682 ) ) ;
#6241=CARTESIAN_POINT ( 'NONE',  ( 0.1876168051218740918, -0.6873969840233377093, 0.1659352930446481023 ) ) ;
#6244=CARTESIAN_POINT ( 'NONE',  ( 0.1905436384893574864, -0.5945559727383912252, 0.3046096357648204189 ) ) ;
#6248=CARTESIAN_POINT ( 'NONE',  ( 0.4899975086607765151, -1.544818463987469803, 0.5363230707130959285 ) ) ;
#6252=CARTESIAN_POINT ( 'NONE',  ( 0.4776788183558685064, -1.117332377667354049, 0.5554309925805337445 ) ) ;
#6254=CARTESIAN_POINT ( 'NONE',  ( 0.1854355241872554794, -0.8269808566380300041, 0.2443189868772147610 ) ) ;
#6255=ORIENTED_EDGE ( 'NONE', *, *, #37358, .T. ) ;
#6257=CARTESIAN_POINT ( 'NONE',  ( -0.01106515159914605619, -0.8690226371807162620, 0.4019604355119212324 ) ) ;
#6259=ORIENTED_EDGE ( 'NONE', *, *, #35088, .T. ) ;
#6265=CARTESIAN_POINT ( 'NONE',  ( 0.4805029911762458417, -1.677157326917623648, 0.5488390883013556376 ) ) ;
#6268=CARTESIAN_POINT ( 'NONE',  ( 0.2063381384019259968, -0.8323430845776256248, 0.6661612056125681969 ) ) ;
#6272=CARTESIAN_POINT ( 'NONE',  ( 0.07288528088268256266, -0.5428011791350080273, 0.1723887882660675164 ) ) ;
#6274=CARTESIAN_POINT ( 'NONE',  ( 0.5705380599090917881, -1.624401057953443361, 0.4891858033826676500 ) ) ;
#6276=CARTESIAN_POINT ( 'NONE',  ( 0.2865981181406410117, -0.9694992659984323913, 0.5430900387768758941 ) ) ;
#6280=CARTESIAN_POINT ( 'NONE',  ( 0.1180522936230993386, -1.414511114437261297, 0.5471422669605355837 ) ) ;
#6282=CARTESIAN_POINT ( 'NONE',  ( 0.5806409787221022967, -1.495190593209716701, 0.5680879804946280531 ) ) ;
#6289=CARTESIAN_POINT ( 'NONE',  ( 0.2173028089842584942, -0.6047810126270140030, 0.4525757583899530645 ) ) ;
#6291=CARTESIAN_POINT ( 'NONE',  ( 0.04296213034915628143, -1.142534290635602856, 0.6595617262123023572 ) ) ;
#6303=CARTESIAN_POINT ( 'NONE',  ( 0.6581239352572101353, -1.508981307375261371, 0.4182417262808776903 ) ) ;
#6312=CARTESIAN_POINT ( 'NONE',  ( 0.4916533138082907484, -1.278983340569261884, 0.6751784830682899807 ) ) ;
#6315=CARTESIAN_POINT ( 'NONE',  ( 0.1854168535569865883, -0.8697360073808750869, 0.1550939566555308846 ) ) ;
#6318=CARTESIAN_POINT ( 'NONE',  ( 0.03830788332888396264, -1.018305589505236863, 0.6966598605597207339 ) ) ;
#6320=CARTESIAN_POINT ( 'NONE',  ( 0.3853907798681502350, -1.605660261670780020, 0.5762609820462575305 ) ) ;
#6322=CARTESIAN_POINT ( 'NONE',  ( 0.1124781747783372837, -0.7882225145822692181, -0.07339066647304182123 ) ) ;
#6324=ORIENTED_EDGE ( 'NONE', *, *, #13749, .T. ) ;
#6325=VERTEX_POINT ( 'NONE', #934 ) ;
#6326=ORIENTED_EDGE ( 'NONE', *, *, #32447, .F. ) ;
#6327=CARTESIAN_POINT ( 'NONE',  ( 0.4351293263873937667, -1.231514889939106849, 0.5832342842089121016 ) ) ;
#6328=CARTESIAN_POINT ( 'NONE',  ( 0.1365985329653890135, -0.6540515576326647595, 0.4294670187197495714 ) ) ;
#6330=CARTESIAN_POINT ( 'NONE',  ( 0.1860814369969508164, -0.7839612642874815851, 0.05803861901368200654 ) ) ;
#6345=CARTESIAN_POINT ( 'NONE',  ( 0.4383612739836618144, -1.052766492039166391, 0.6342478131430038246 ) ) ;
#6347=CARTESIAN_POINT ( 'NONE',  ( 0.5494029794155456115, -1.165490604795236029, 0.6057417262810063097 ) ) ;
#6349=CARTESIAN_POINT ( 'NONE',  ( 0.1512804210101734992, -1.367800832853933501, 0.8372142429942934783 ) ) ;
#6353=CARTESIAN_POINT ( 'NONE',  ( 0.3218706003014081274, -1.643225927452630852, 0.4993898684233093466 ) ) ;
#6355=ADVANCED_FACE ( 'NONE', ( #1135 ), #13635, .T. ) ;
#6356=ORIENTED_EDGE ( 'NONE', *, *, #7687, .T. ) ;
#6364=CARTESIAN_POINT ( 'NONE',  ( 0.4600226136112777198, -1.237287929595064062, 0.8135617580924977554 ) ) ;
#6365=CARTESIAN_POINT ( 'NONE',  ( 0.001804213231561386209, -0.5433067823503371363, 0.07704719339775437104 ) ) ;
#6367=ADVANCED_FACE ( 'NONE', ( #5368 ), #21478, .T. ) ;
#6369=CARTESIAN_POINT ( 'NONE',  ( 0.5737921459139804226, -1.611029524247286293, 0.4522236539011413869 ) ) ;
#6370=EDGE_LOOP ( 'NONE', ( #25420, #4478, #33032 ) ) ;
#6371=CARTESIAN_POINT ( 'NONE',  ( 0.1840027845416183361, -1.200052452841920303, 0.9022922089355089881 ) ) ;
#6372=CARTESIAN_POINT ( 'NONE',  ( 0.2800658575624323521, -1.022046468236217143, 0.7264731327323665777 ) ) ;
#6384=CARTESIAN_POINT ( 'NONE',  ( 0.1592870015680986351, -0.8540808306954126294, 0.4623900724923409311 ) ) ;
#6387=CARTESIAN_POINT ( 'NONE',  ( 0.1938292101578000248, -1.228094556586287300, 1.021854484236047522 ) ) ;
#6389=CARTESIAN_POINT ( 'NONE',  ( 0.07556315841227354002, -1.331191507351498160, 0.4849083929475443422 ) ) ;
#6390=CARTESIAN_POINT ( 'NONE',  ( 0.3704697912810950289, -1.166474544107111599, 0.4282417262808793090 ) ) ;
#6394=CARTESIAN_POINT ( 'NONE',  ( 0.3098984767712536503, -1.765718780359063267, 0.5682417262808785452 ) ) ;
#6395=CARTESIAN_POINT ( 'NONE',  ( 0.05438524155173456165, -1.080864667231560716, 0.7434867514774906594 ) ) ;
#6398=CARTESIAN_POINT ( 'NONE',  ( 0.7030074634613492357, -1.521190031500555317, 0.5774844009317151583 ) ) ;
#6403=CARTESIAN_POINT ( 'NONE',  ( 0.2664482867961980306, -1.636644802795437892, 0.8064424891061348077 ) ) ;
#6405=CARTESIAN_POINT ( 'NONE',  ( 0.2204199330889215214, -0.8297487780498332688, 0.6443566085987398884 ) ) ;
#6406=CARTESIAN_POINT ( 'NONE',  ( 0.5433647090050529593, -1.169020713861581129, 0.5880578810646379662 ) ) ;
#6409=ORIENTED_EDGE ( 'NONE', *, *, #13256, .T. ) ;
#6411=CARTESIAN_POINT ( 'NONE',  ( 0.4391485520781965302, -1.022841741781851388, 0.7808255053512450639 ) ) ;
#6415=CARTESIAN_POINT ( 'NONE',  ( 0.3186747540252977684, -1.760357293763689546, 0.5625916045222835171 ) ) ;
#6417=CARTESIAN_POINT ( 'NONE',  ( 0.1078177687349250041, -0.7744679009142783066, 0.3837020403678208513 ) ) ;
#6419=CARTESIAN_POINT ( 'NONE',  ( 0.5252367033251564843, -1.526871148930892153, 0.5736917532057838054 ) ) ;
#6424=CARTESIAN_POINT ( 'NONE',  ( 0.4140281424214005135, -1.705551847233233831, 0.6094650255398795791 ) ) ;
#6425=CARTESIAN_POINT ( 'NONE',  ( 0.6658116889046563625, -1.561543021530046094, 0.5673474868851250408 ) ) ;
#6426=CARTESIAN_POINT ( 'NONE',  ( 0.2101951102887192890, -1.233953443661628846, 0.5631135429232324574 ) ) ;
#6427=CARTESIAN_POINT ( 'NONE',  ( 0.6053889014930310397, -1.470157484751941634, 0.6617915113480205003 ) ) ;
#6431=CARTESIAN_POINT ( 'NONE',  ( 0.2642159376432997031, -1.676617828451314907, 0.5053660846951645302 ) ) ;
#6432=CARTESIAN_POINT ( 'NONE',  ( 0.07801557919154505916, -1.344960384177054546, 0.6336995499099050688 ) ) ;
#6433=CARTESIAN_POINT ( 'NONE',  ( 0.2316395767834320274, -0.8375294501127626967, 0.4569101180231894821 ) ) ;
#6436=CARTESIAN_POINT ( 'NONE',  ( 0.5374399095249312586, -1.518357447092129497, 0.5359417805910808852 ) ) ;
#6443=ADVANCED_FACE ( 'NONE', ( #8473 ), #34616, .T. ) ;
#6444=CARTESIAN_POINT ( 'NONE',  ( 0.1920071873703446952, -0.8110264159798785677, 0.2735051980380693304 ) ) ;
#6445=ORIENTED_EDGE ( 'NONE', *, *, #33421, .F. ) ;
#6446=CARTESIAN_POINT ( 'NONE',  ( 0.000000000000000000, -0.6872203660140440151, 0.1457185332388702681 ) ) ;
#6447=EDGE_CURVE ( 'NONE', #35222, #10169, #10313, .T. ) ;
#6448=CARTESIAN_POINT ( 'NONE',  ( 0.1442265625138574037, -1.313102518721056100, 0.7083091578507269004 ) ) ;
#6453=CARTESIAN_POINT ( 'NONE',  ( 0.09972103128818979312, -1.308064159787032832, 0.4441314049251992024 ) ) ;
#6463=CARTESIAN_POINT ( 'NONE',  ( 0.1370807591037170314, -0.7115665574697015439, 0.5098665575104406322 ) ) ;
#6467=CARTESIAN_POINT ( 'NONE',  ( 0.08383286731608259601, -0.6201591115495469486, 0.3831915389127222848 ) ) ;
#6469=CARTESIAN_POINT ( 'NONE',  ( 0.002464792031906918451, -0.5324439718320103099, 0.2218667994837078550 ) ) ;
#6472=CARTESIAN_POINT ( 'NONE',  ( 0.3880537965025097624, -1.025164508700765031, 0.6277837196461664160 ) ) ;
#6477=CARTESIAN_POINT ( 'NONE',  ( 0.1262144102814217184, -0.5727411025276200052, 0.2466681503346596915 ) ) ;
#6481=CARTESIAN_POINT ( 'NONE',  ( 0.07565767122873574835, -0.5864987862812711672, 0.3100368675900313509 ) ) ;
#6483=CARTESIAN_POINT ( 'NONE',  ( 0.2790103250938448243, -0.7681568326658522183, 0.6036499921438334137 ) ) ;
#6484=CARTESIAN_POINT ( 'NONE',  ( 0.4738611546896250859, -1.197946575156342286, 0.3905537834340729320 ) ) ;
#6485=CARTESIAN_POINT ( 'NONE',  ( 0.02686770367197182513, -1.121034573699498216, 0.6519664731740556496 ) ) ;
#6488=CARTESIAN_POINT ( 'NONE',  ( 0.1407851177556478373, -0.8464084508146803021, 0.4976936549835760948 ) ) ;
#6493=CARTESIAN_POINT ( 'NONE',  ( 0.3606017550323884491, -1.088889236884987843, 0.7735338957822750494 ) ) ;
#6501=DIRECTION ( 'NONE',  ( 0.4999551463232372317, -0.8660512985181135770, 0.000000000000000000 ) ) ;
#6504=CARTESIAN_POINT ( 'NONE',  ( 0.3632630838000410756, -1.100250190083209789, 0.7354547643755756647 ) ) ;
#6506=CARTESIAN_POINT ( 'NONE',  ( 0.3959972151391356610, -1.707195898057176642, 0.4182417262808776903 ) ) ;
#6507=CARTESIAN_POINT ( 'NONE',  ( 0.4929465528686912679, -1.082715557938388029, 0.5639242819095140469 ) ) ;
#6510=CARTESIAN_POINT ( 'NONE',  ( 0.6498387395261642219, -1.464631408770378451, 0.4282417262808778102 ) ) ;
#6511=EDGE_LOOP ( 'NONE', ( #11984, #18840, #1998, #25969 ) ) ;
#6513=CARTESIAN_POINT ( 'NONE',  ( 0.3875464983679292041, -1.604953645996557432, 0.6166661730678868469 ) ) ;
#6515=CARTESIAN_POINT ( 'NONE',  ( 0.1129260651966456502, -0.7196690655787660873, -0.09367555582725564656 ) ) ;
#6521=CARTESIAN_POINT ( 'NONE',  ( 0.5435177775687849433, -1.464638892555605754, 0.7383152199638944868 ) ) ;
#6523=CARTESIAN_POINT ( 'NONE',  ( 0.1873417209643421233, -0.6975452635715222449, 0.03245562858311761001 ) ) ;
#6528=DIRECTION ( 'NONE',  ( 1.060606950627616897E-16, 6.122684696619992497E-17, 1.000000000000000000 ) ) ;
#6529=CARTESIAN_POINT ( 'NONE',  ( 0.4527140395159202080, -1.709300500385005250, 0.5182417262812423209 ) ) ;
#6537=CARTESIAN_POINT ( 'NONE',  ( 0.4471380481896147785, -1.057582006303192657, 0.6325253032963528144 ) ) ;
#6539=CARTESIAN_POINT ( 'NONE',  ( 0.5145696469471491286, -1.185649477150961806, 0.5856983068964181083 ) ) ;
#6540=CARTESIAN_POINT ( 'NONE',  ( 0.2623806002910373247, -1.682816372174909203, 0.5558257937731609921 ) ) ;
#6541=CARTESIAN_POINT ( 'NONE',  ( -0.002083146443013344888, -0.8967360763018595859, 0.09758087637170891060 ) ) ;
#6542=CARTESIAN_POINT ( 'NONE',  ( -0.0002645986387457673820, -0.8856723859976365354, -0.006055055896265703307 ) ) ;
#6545=CARTESIAN_POINT ( 'NONE',  ( 0.2320387611536686712, -1.233193230799448203, 0.4282290774773019337 ) ) ;
#6552=DIRECTION ( 'NONE',  ( -0.4999551463232372317, 0.8660512985181134660, 0.000000000000000000 ) ) ;
#6557=CARTESIAN_POINT ( 'NONE',  ( 0.1995338205807487553, -0.7602668576148212676, 0.3267161968192467403 ) ) ;
#6559=CIRCLE ( 'NONE', #20384, 0.009999999999999993269 ) ;
#6560=CARTESIAN_POINT ( 'NONE',  ( 0.2985895772694463490, -1.656929904383750873, 0.5927621635699326097 ) ) ;
#6561=CARTESIAN_POINT ( 'NONE',  ( 0.2085664583100847180, -0.9408741989701879804, 0.6570105467478477568 ) ) ;
#6569=CARTESIAN_POINT ( 'NONE',  ( 0.1862143093560919282, -0.9153542374866575626, 0.1443021394692982906 ) ) ;
#6570=CARTESIAN_POINT ( 'NONE',  ( 0.3558114376875948781, -1.251414176327350525, 0.5182417262812423209 ) ) ;
#6571=CARTESIAN_POINT ( 'NONE',  ( 0.5698248817562774349, -1.454081016919124281, 0.7261892429133063320 ) ) ;
#6572=CARTESIAN_POINT ( 'NONE',  ( 0.1882935783789653206, -0.8844134358759655479, 0.5622750411365140533 ) ) ;
#6573=CARTESIAN_POINT ( 'NONE',  ( 0.2339608829160596815, -1.489014943295124294, 0.9134659781549987478 ) ) ;
#6574=CARTESIAN_POINT ( 'NONE',  ( 0.1275022910136354160, -0.9890455054698116255, 0.9358088192774665082 ) ) ;
#6575=CARTESIAN_POINT ( 'NONE',  ( 0.4042633028796379646, -1.711240744074478570, 0.4220515681607872605 ) ) ;
#6581=CARTESIAN_POINT ( 'NONE',  ( 0.1587139193017044758, -1.140357826010188314, 1.006504499293092714 ) ) ;
#6582=CARTESIAN_POINT ( 'NONE',  ( 0.09896627915743715087, -1.366272486005550180, 0.6737215609984372744 ) ) ;
#6585=CARTESIAN_POINT ( 'NONE',  ( 0.7004187681061331272, -1.489996274278563071, 0.4963418890236395709 ) ) ;
#6588=CARTESIAN_POINT ( 'NONE',  ( 0.1895845073671591496, -0.5861495762347013194, 0.2988846075130171531 ) ) ;
#6592=CARTESIAN_POINT ( 'NONE',  ( 0.2367319421433582705, -1.498621928344235910, 0.9091324809083795033 ) ) ;
#6593=CARTESIAN_POINT ( 'NONE',  ( 0.5007062318473965989, -1.350239968012811209, 0.8060270520129010352 ) ) ;
#6604=CARTESIAN_POINT ( 'NONE',  ( 0.6129335297421601991, -1.616808798314981921, 0.5182417262812423209 ) ) ;
#6606=CARTESIAN_POINT ( 'NONE',  ( 0.1266283464120225577, -0.7967538953625531439, 0.4596558820756620478 ) ) ;
#6607=CARTESIAN_POINT ( 'NONE',  ( 0.08990536851188075940, -0.5646295468556798980, 0.1370866209488758869 ) ) ;
#6609=CARTESIAN_POINT ( 'NONE',  ( 0.1056960294869904032, -0.5719007525085089139, 0.2557726251434392362 ) ) ;
#6615=CARTESIAN_POINT ( 'NONE',  ( 0.4032474725367772295, -1.711818401373710108, 0.6107726817123948493 ) ) ;
#6616=CARTESIAN_POINT ( 'NONE',  ( 0.6494194904526725542, -1.505054641034485163, 0.7731478513741499858 ) ) ;
#6619=ADVANCED_FACE ( 'NONE', ( #6199 ), #4543, .F. ) ;
#6620=CARTESIAN_POINT ( 'NONE',  ( 0.6085670229761270811, -1.478915227102408414, 0.5633428062726970609 ) ) ;
#6628=CARTESIAN_POINT ( 'NONE',  ( 0.08075236803977006717, -1.368778601871594836, 0.5682417262808778791 ) ) ;
#6630=CARTESIAN_POINT ( 'NONE',  ( 0.5117280326951013647, -1.115088012504228621, 0.5923667439031021775 ) ) ;
#6634=CARTESIAN_POINT ( 'NONE',  ( 0.4660507111952964521, -1.558206335128884845, 0.5363334130509328501 ) ) ;
#6640=CARTESIAN_POINT ( 'NONE',  ( 0.4475777147736147987, -1.570831683793988187, 0.5814946475837428075 ) ) ;
#6644=CARTESIAN_POINT ( 'NONE',  ( 0.08839720336850717675, -0.6253492388939145830, 0.03921914501878817627 ) ) ;
#6645=ORIENTED_EDGE ( 'NONE', *, *, #24745, .F. ) ;
#6646=CARTESIAN_POINT ( 'NONE',  ( 0.4090604450045443596, -1.131420581850358653, 0.3667417262808778666 ) ) ;
#6647=CARTESIAN_POINT ( 'NONE',  ( 0.04292188072724165138, -1.133578733677452099, 0.7617704846099633276 ) ) ;
#6651=CARTESIAN_POINT ( 'NONE',  ( 0.1536596445529307131, -1.277574755431481579, 0.4245438548657216038 ) ) ;
#6661=CARTESIAN_POINT ( 'NONE',  ( 0.1537277655112500585, -0.7413063141131301936, 0.5573565750015010423 ) ) ;
#6666=CARTESIAN_POINT ( 'NONE',  ( 0.07297943341930077099, -0.5464194006479311527, 0.1919652695815136645 ) ) ;
#6670=CARTESIAN_POINT ( 'NONE',  ( 0.2020865016433360528, -0.9231306475095830688, 0.3258051546269021825 ) ) ;
#6672=CARTESIAN_POINT ( 'NONE',  ( 0.1897112079047655053, -0.5340520988484990239, 0.1385946963835808510 ) ) ;
#6673=CARTESIAN_POINT ( 'NONE',  ( 0.2166550137285412070, -0.8304811269046187272, 0.6463872802090209202 ) ) ;
#6681=CARTESIAN_POINT ( 'NONE',  ( 0.08296493955445416457, -0.6173275490175130775, 0.3808511444712925353 ) ) ;
#6684=CARTESIAN_POINT ( 'NONE',  ( 0.4605766076693431632, -1.054687064863744750, 0.7953974510635947182 ) ) ;
#6686=CARTESIAN_POINT ( 'NONE',  ( 0.05596281731547365912, -1.307106975853646658, 0.6186298968216493721 ) ) ;
#6689=CARTESIAN_POINT ( 'NONE',  ( 0.1914801911188975247, -0.6027644909819236396, 0.3101999008291455029 ) ) ;
#6690=CARTESIAN_POINT ( 'NONE',  ( 0.1007139418999222075, -0.8573875874287576471, 0.4354917424624366040 ) ) ;
#6692=CARTESIAN_POINT ( 'NONE',  ( 0.6627797186572951249, -1.546517967009319205, 0.4296449949859427742 ) ) ;
#6694=ORIENTED_EDGE ( 'NONE', *, *, #14506, .F. ) ;
#6695=DIRECTION ( 'NONE',  ( 0.4999551463232372317, -0.8660512985181135770, 0.000000000000000000 ) ) ;
#6696=CARTESIAN_POINT ( 'NONE',  ( 0.1454652487279074757, -0.7477097220224196983, 0.5302102881989955163 ) ) ;
#6698=CARTESIAN_POINT ( 'NONE',  ( 0.1016010970546381426, -1.316932408029475532, 0.4414108731151945575 ) ) ;
#6705=CARTESIAN_POINT ( 'NONE',  ( 0.1802350563441833808, -0.5022327775090948965, 0.1477559389858786043 ) ) ;
#6706=CARTESIAN_POINT ( 'NONE',  ( 0.4516520847856119181, -1.680408577508558210, 0.4354989228371364818 ) ) ;
#6708=CARTESIAN_POINT ( 'NONE',  ( 0.4751785028721121629, -1.252254961389827503, 0.6770357329939598046 ) ) ;
#6710=CARTESIAN_POINT ( 'NONE',  ( 0.3197311927886214988, -1.759354868725874432, 0.4922608866671225880 ) ) ;
#6711=CARTESIAN_POINT ( 'NONE',  ( 0.3924682913416943086, -1.027586590250060272, 0.6289202682814357681 ) ) ;
#6712=ORIENTED_EDGE ( 'NONE', *, *, #37142, .T. ) ;
#6714=CARTESIAN_POINT ( 'NONE',  ( 0.08560287521161533131, -1.284824326520781490, 0.7328930470927262908 ) ) ;
#6717=CARTESIAN_POINT ( 'NONE',  ( 0.3854321820439991497, -1.605669856351402691, 0.5768392551633937382 ) ) ;
#6718=CARTESIAN_POINT ( 'NONE',  ( 0.08509577109033511499, -0.8106501036565759710, 0.1481698590609797916 ) ) ;
#6720=CARTESIAN_POINT ( 'NONE',  ( 0.06739064528196411774, -0.6397219464422030377, 0.005700442802499041187 ) ) ;
#6723=EDGE_LOOP ( 'NONE', ( #35718, #29968, #27829, #22475, #6326, #16896, #12801 ) ) ;
#6724=CARTESIAN_POINT ( 'NONE',  ( 0.3245308759113119113, -1.295391163961464365, 0.5682442948123348492 ) ) ;
#6725=CARTESIAN_POINT ( 'NONE',  ( 0.5669662277262230710, -1.503240378328975613, 0.5737068391451652927 ) ) ;
#6728=CARTESIAN_POINT ( 'NONE',  ( 0.4974456442574050619, -1.184401136727558868, 0.4224083929475309640 ) ) ;
#6731=CARTESIAN_POINT ( 'NONE',  ( 0.1840771369943047242, -0.8547796389794056759, 0.1590146724173516768 ) ) ;
#6736=CARTESIAN_POINT ( 'NONE',  ( 0.6551261771431925451, -1.361944467462807395, 0.8444247977208539924 ) ) ;
#6739=CARTESIAN_POINT ( 'NONE',  ( 0.4138729472876766513, -1.128955312352843965, 0.5470489658417444501 ) ) ;
#6743=LINE ( 'NONE', #35149, #3485 ) ;
#6745=CARTESIAN_POINT ( 'NONE',  ( 0.4580278197616229896, -1.241383277718457911, 0.6057417262809816627 ) ) ;
#6747=CARTESIAN_POINT ( 'NONE',  ( 0.01179864804857342665, -0.6562760587974182380, 0.4561945812754703011 ) ) ;
#6748=CARTESIAN_POINT ( 'NONE',  ( 0.0004433609336470854898, -0.4385931729850870431, 0.1292661587538940227 ) ) ;
#6749=EDGE_CURVE ( 'NONE', #3992, #20653, #6559, .T. ) ;
#6752=EDGE_CURVE ( 'NONE', #9135, #30000, #11352, .T. ) ;
#6753=ORIENTED_EDGE ( 'NONE', *, *, #14535, .F. ) ;
#6757=CARTESIAN_POINT ( 'NONE',  ( 0.3606884409928574620, -1.747583433209421333, 0.4408685289531725227 ) ) ;
#6758=CYLINDRICAL_SURFACE ( 'NONE', #36400, 0.01000000000000005398 ) ;
#6760=CARTESIAN_POINT ( 'NONE',  ( 0.06682908180107070828, -0.6872203660146791737, -0.001923513761143209400 ) ) ;
#6763=VERTEX_POINT ( 'NONE', #28633 ) ;
#6768=CARTESIAN_POINT ( 'NONE',  ( 0.2970029333241409608, -1.656601473353111365, 0.5710316030164380718 ) ) ;
#6769=CARTESIAN_POINT ( 'NONE',  ( 0.6035974019387861933, -1.594473330473194839, 0.4258042085085226858 ) ) ;
#6771=CARTESIAN_POINT ( 'NONE',  ( 0.3099480278792562382, -1.763253171224924420, 0.5409204437200131332 ) ) ;
#6772=CARTESIAN_POINT ( 'NONE',  ( 0.01176869885886682073, -0.6532089530866552751, -0.1114877525985862178 ) ) ;
#6777=CARTESIAN_POINT ( 'NONE',  ( 0.1109210135120192453, -0.9286415089466554251, 0.1524864793821099351 ) ) ;
#6785=CARTESIAN_POINT ( 'NONE',  ( 0.1291001614701467459, -0.9254250030040105379, 0.1457122326985881844 ) ) ;
#6791=CARTESIAN_POINT ( 'NONE',  ( -0.0003003500745766487395, -0.9376955769830692677, 0.2168050107958245654 ) ) ;
#6792=CARTESIAN_POINT ( 'NONE',  ( 0.2750825180155820338, -1.558163865710181728, 0.9909808761736236260 ) ) ;
#6798=CARTESIAN_POINT ( 'NONE',  ( 0.3269961855704987541, -1.756646017944762939, 0.5657241070551874973 ) ) ;
#6803=CARTESIAN_POINT ( 'NONE',  ( 0.1844620385557431963, -0.5656468219106428608, 0.2771782185203255922 ) ) ;
#6806=CARTESIAN_POINT ( 'NONE',  ( 0.2572930768252133515, -1.677938012603978013, 0.5362869298745072122 ) ) ;
#6807=CARTESIAN_POINT ( 'NONE',  ( 0.2478791248605221043, -0.8877234785324099597, 0.6911795992708721359 ) ) ;
#6820=DIRECTION ( 'NONE',  ( 0.8660512985181125778, 0.4999551463232387860, 0.000000000000000000 ) ) ;
#6821=ORIENTED_EDGE ( 'NONE', *, *, #5942, .T. ) ;
#6822=CARTESIAN_POINT ( 'NONE',  ( 0.08658218366773377805, -0.7469030435693181369, 0.1915370112333746877 ) ) ;
#6823=CARTESIAN_POINT ( 'NONE',  ( 0.08990617429856566367, -0.5646418133096463565, 0.1474873524130712044 ) ) ;
#6825=CARTESIAN_POINT ( 'NONE',  ( 0.4848907914328412505, -1.427831231083330765, 0.7974248085317546808 ) ) ;
#6828=CARTESIAN_POINT ( 'NONE',  ( 0.6537467011358751856, -1.544991604632938609, 0.4236745214088577516 ) ) ;
#6830=CARTESIAN_POINT ( 'NONE',  ( 0.6994016379560119567, -1.437929643118011969, 0.6007912156904529066 ) ) ;
#6833=CARTESIAN_POINT ( 'NONE',  ( 0.1412211329182320174, -0.6053832490378043829, 0.3245192810377299231 ) ) ;
#6835=CARTESIAN_POINT ( 'NONE',  ( -0.002294379339023699775, -0.8554970241181312218, 0.1489098701495673027 ) ) ;
#6839=CARTESIAN_POINT ( 'NONE',  ( 0.3465599992496842807, -0.9476710551646405634, 0.6409924101657002993 ) ) ;
#6841=DIRECTION ( 'NONE',  ( 0.007367783058131798131, 0.4999457213560383195, -0.8660253988599866393 ) ) ;
#6842=CIRCLE ( 'NONE', #22660, 0.01000000000000002970 ) ;
#6844=CARTESIAN_POINT ( 'NONE',  ( 0.3793181961223202059, -1.724015678557583309, 0.4221277619539304804 ) ) ;
#6851=CARTESIAN_POINT ( 'NONE',  ( 0.002367394983758686153, -0.5282119844061595737, 0.1431176680404078472 ) ) ;
#6852=CARTESIAN_POINT ( 'NONE',  ( 0.08625494239356501502, -0.7682695115869180302, 0.05259860062006292691 ) ) ;
#6853=ORIENTED_EDGE ( 'NONE', *, *, #14451, .F. ) ;
#6854=CARTESIAN_POINT ( 'NONE',  ( 0.1436225252650951412, -1.283668529478381393, 0.4687417262808780127 ) ) ;
#6856=VECTOR ( 'NONE', #29265, 39.37007874015748143 ) ;
#6857=CARTESIAN_POINT ( 'NONE',  ( 0.1560064421674209612, -1.343171649511100796, 0.6771907574492684878 ) ) ;
#6859=VERTEX_POINT ( 'NONE', #5319 ) ;
#6865=CARTESIAN_POINT ( 'NONE',  ( 0.5986388623866938374, -1.596970510946166266, 0.4258794442771735023 ) ) ;
#6866=CARTESIAN_POINT ( 'NONE',  ( 0.2626070881998294193, -0.6796769646063650638, 0.05684369497733833543 ) ) ;
#6868=CARTESIAN_POINT ( 'NONE',  ( 0.09375000000000006939, -0.4427825420493723962, 0.1899451958498858395 ) ) ;
#6870=CARTESIAN_POINT ( 'NONE',  ( 0.1579683488041129513, -0.7702448364953791149, 0.5611987017360021701 ) ) ;
#6872=CARTESIAN_POINT ( 'NONE',  ( 0.05196282386221179328, -0.7503617116158776135, 0.7499995989107329786 ) ) ;
#6873=CARTESIAN_POINT ( 'NONE',  ( 0.4704130467040563701, -1.558075432898772261, 0.5842460006296394948 ) ) ;
#6876=CARTESIAN_POINT ( 'NONE',  ( 0.6252332368506442473, -1.468099812651720182, 0.5083331137473884320 ) ) ;
#6880=CARTESIAN_POINT ( 'NONE',  ( 0.1153471661800046788, -0.4465907051537519323, 0.1458683203705896103 ) ) ;
#6891=CARTESIAN_POINT ( 'NONE',  ( 0.1927699586607699855, -0.5931527414817471255, 0.2350819919684725701 ) ) ;
#6893=CARTESIAN_POINT ( 'NONE',  ( 0.06748114818349953969, -1.314123476931967405, 0.6039052066682303321 ) ) ;
#6894=B_SPLINE_CURVE_WITH_KNOTS ( 'NONE', 3,
 ( #30877, #15652, #12769, #28201, #2694, #21839, #65, #12557, #25117, #15241, #2503, #31488, #3295, #9687, #37044, #21445, #5776, #37255, #40120, #6573, #21635, #273, #25332, #34157, #31084, #37871, #30686, #1076, #19151, #13373, #31901, #7177, #10485, #25947, #6995, #7378, #19745, #3719, #32281, #23050, #13767, #9873, #28616, #35387, #34976, #25532, #23261, #19954, #35195, #10688, #3512, #22870, #866, #13585, #13160, #19565 ),
 .UNSPECIFIED., .F., .F.,
 ( 4, 2, 2, 2, 2, 2, 2, 2, 2, 2, 2, 2, 2, 2, 2, 2, 2, 2, 2, 2, 2, 2, 2, 2, 2, 2, 2, 4 ),
 ( 0.000000000000000000, 0.001448614964254715766, 0.002897229928509431531, 0.004345844892764147947, 0.005070152374891505505, 0.005794459857018863062, 0.006518767339146220620, 0.007243074821273579045, 0.008691689785528287221, 0.01014030474978299540, 0.01158891971403770357, 0.01303753467829241175, 0.01448614964254711819, 0.01738337957105653281, 0.02028060949956596304, 0.02172922446382067468, 0.02317783942807537939, 0.02462645439233009104, 0.02607506935658480268, 0.02897229928509421557, 0.03186952921360363539, 0.03476675914211305174, 0.04056121899913189138, 0.04345844892764130774, 0.04490706389189601244, 0.04563137137402337173, 0.04599352511508705138, 0.04635567885615073103 ),
 .UNSPECIFIED. ) ;
#6897=CARTESIAN_POINT ( 'NONE',  ( 0.2755167558405882677, -0.9831624882773356555, 0.7046348054233062541 ) ) ;
#6905=CARTESIAN_POINT ( 'NONE',  ( 0.1282169094755595540, -1.302307706640518203, 0.4238844375282422861 ) ) ;
#6910=CARTESIAN_POINT ( 'NONE',  ( 0.1842405141775073085, -0.5317127165793841259, 0.2455185872253249635 ) ) ;
#6915=CARTESIAN_POINT ( 'NONE',  ( 0.4523950064470654286, -1.218585674146387410, 0.6985505283395704312 ) ) ;
#6918=CARTESIAN_POINT ( 'NONE',  ( 0.3689192748036780878, -1.014666054483551294, 0.6186952232919745720 ) ) ;
#6919=ORIENTED_EDGE ( 'NONE', *, *, #18967, .F. ) ;
#6926=CARTESIAN_POINT ( 'NONE',  ( 0.04803225083625260738, -0.5400094135379269744, 0.1831641058994340765 ) ) ;
#6927=FACE_OUTER_BOUND ( 'NONE', #8095, .T. ) ;
#6928=CARTESIAN_POINT ( 'NONE',  ( 0.2028802569692557956, -0.6553668614656892322, 0.3449618718442576393 ) ) ;
#6929=CARTESIAN_POINT ( 'NONE',  ( 0.06889123515197598246, -0.5474947681545639933, 0.09816793099005483025 ) ) ;
#6933=CARTESIAN_POINT ( 'NONE',  ( 0.5667293957721729614, -1.503181826980968472, 0.5693608068383182452 ) ) ;
#6944=AXIS2_PLACEMENT_3D ( 'NONE', #19801, #4370, #7661 ) ;
#6945=LINE ( 'NONE', #28564, #15964 ) ;
#6952=CARTESIAN_POINT ( 'NONE',  ( 0.1676768030379193752, -1.385557720720546060, 0.5132863183250160333 ) ) ;
#6958=CARTESIAN_POINT ( 'NONE',  ( 0.004299088327612451445, -0.5973376383060815531, 0.3026940496400818970 ) ) ;
#6959=CARTESIAN_POINT ( 'NONE',  ( -0.0003770264812326959230, -0.9303068966317035171, 0.08922538226795197203 ) ) ;
#6961=FACE_OUTER_BOUND ( 'NONE', #25555, .T. ) ;
#6971=CARTESIAN_POINT ( 'NONE',  ( 0.5725852423738272412, -1.416104505180847850, 0.6504252674398794953 ) ) ;
#6973=ORIENTED_EDGE ( 'NONE', *, *, #37835, .T. ) ;
#6974=CARTESIAN_POINT ( 'NONE',  ( 0.4220340746365390805, -1.009949560908969035, 0.7308913177996746446 ) ) ;
#6979=CARTESIAN_POINT ( 'NONE',  ( 0.2997790868238941475, -1.656668618253792857, 0.6120939283712725221 ) ) ;
#6984=CARTESIAN_POINT ( 'NONE',  ( 0.1834116704161121436, -0.8266995537623093027, 0.1479976049341028554 ) ) ;
#6990=CARTESIAN_POINT ( 'NONE',  ( 0.1852697703518005334, -0.8388889655799377509, 0.1443021394693011494 ) ) ;
#6993=EDGE_CURVE ( 'NONE', #10719, #6859, #37886, .T. ) ;
#6994=CARTESIAN_POINT ( 'NONE',  ( 0.1033812429324503235, -0.8292951995117538999, 0.2127542378592026939 ) ) ;
#6995=CARTESIAN_POINT ( 'NONE',  ( 0.09312660137187182829, -1.001924882690514051, 0.8305037475052123863 ) ) ;
#6998=EDGE_CURVE ( 'NONE', #24800, #38179, #12376, .T. ) ;
#7014=FACE_OUTER_BOUND ( 'NONE', #15885, .T. ) ;
#7017=CARTESIAN_POINT ( 'NONE',  ( 0.2640642850859278856, -1.687144750073774624, 0.5604289873973611336 ) ) ;
#7019=CARTESIAN_POINT ( 'NONE',  ( 0.5948731947484026117, -1.487188044069185144, 0.5720353766658540229 ) ) ;
#7023=VERTEX_POINT ( 'NONE', #21188 ) ;
#7024=VERTEX_POINT ( 'NONE', #27566 ) ;
#7025=CARTESIAN_POINT ( 'NONE',  ( 0.6457951246584852090, -1.496021715571339339, 0.7857184687380228683 ) ) ;
#7027=CARTESIAN_POINT ( 'NONE',  ( 0.3663209872086246599, -1.109675523170870148, 0.7013152411065209924 ) ) ;
#7028=CARTESIAN_POINT ( 'NONE',  ( 0.4042633028796379646, -1.711240744074478570, 0.4220515681607872605 ) ) ;
#7030=CARTESIAN_POINT ( 'NONE',  ( -0.004127514673257773846, -0.8469330747986104635, 0.1483282180229327507 ) ) ;
#7031=ORIENTED_EDGE ( 'NONE', *, *, #1924, .F. ) ;
#7033=CARTESIAN_POINT ( 'NONE',  ( 0.08599367632086754587, -0.8130461822548644690, 0.1957551766224920053 ) ) ;
#7034=CARTESIAN_POINT ( 'NONE',  ( 0.08991114079686372829, -0.5436709457187953731, 0.1483399283896538745 ) ) ;
#7035=CARTESIAN_POINT ( 'NONE',  ( 0.5397793955047566206, -1.519018766216045702, 0.5864989580874288011 ) ) ;
#7043=CARTESIAN_POINT ( 'NONE',  ( 0.1634626058761369516, -0.6765147025655514623, 0.4580962369789614019 ) ) ;
#7044=CARTESIAN_POINT ( 'NONE',  ( -0.0001224597784096040007, -0.7987101862150752796, -0.07726980077153194904 ) ) ;
#7045=CARTESIAN_POINT ( 'NONE',  ( 0.2316917763911649497, -1.232208891764917880, 0.5707417262808780478 ) ) ;
#7047=CARTESIAN_POINT ( 'NONE',  ( 0.01226155556033644428, -1.026869578359442370, 0.5617476425356938696 ) ) ;
#7049=CARTESIAN_POINT ( 'NONE',  ( 0.3816662009041032477, -0.9823246188028521564, 0.6672886469660396225 ) ) ;
#7056=CARTESIAN_POINT ( 'NONE',  ( 0.01055999354155195448, -0.5296565605740115590, 0.1369805761320318227 ) ) ;
#7058=EDGE_LOOP ( 'NONE', ( #14508, #31437, #13961 ) ) ;
#7059=CARTESIAN_POINT ( 'NONE',  ( 0.3210085668004670767, -1.182910313946810010, 0.5197417262808780025 ) ) ;
#7061=CARTESIAN_POINT ( 'NONE',  ( 0.5586414499496984432, -1.205790344466990627, 0.8068181458027993136 ) ) ;
#7063=ORIENTED_EDGE ( 'NONE', *, *, #19478, .T. ) ;
#7066=DIRECTION ( 'NONE',  ( -0.8660512985181134660, -0.4999551463232372317, 0.000000000000000000 ) ) ;
#7068=CARTESIAN_POINT ( 'NONE',  ( 0.1891522879705697380, -0.6779850459293743636, 0.7094297601507593143 ) ) ;
#7069=CARTESIAN_POINT ( 'NONE',  ( 0.08990515874724788747, -0.5631160408504085613, 0.1457185332388709342 ) ) ;
#7070=CARTESIAN_POINT ( 'NONE',  ( 0.001612557744564022772, -0.4658981512586417018, 0.3165272632837566325 ) ) ;
#7071=CARTESIAN_POINT ( 'NONE',  ( 0.1678425801914835702, -0.8396823097241469247, 0.6722826835357673669 ) ) ;
#7074=CARTESIAN_POINT ( 'NONE',  ( 0.4296888835344449542, -1.088254846990821090, 0.6262898891649716360 ) ) ;
#7077=CARTESIAN_POINT ( 'NONE',  ( 0.3786378199821132107, -1.610465949109882722, 0.5371432465038092907 ) ) ;
#7079=CARTESIAN_POINT ( 'NONE',  ( 0.1897120355916300793, -0.5340628431043178415, 0.1475512043905171100 ) ) ;
#7082=CARTESIAN_POINT ( 'NONE',  ( 0.4165761542997364897, -1.741708882820427906, 0.5182417262812423209 ) ) ;
#7084=CARTESIAN_POINT ( 'NONE',  ( 0.5289273032196292190, -1.159758851219879094, 0.8099624798310959273 ) ) ;
#7086=CARTESIAN_POINT ( 'NONE',  ( -0.002288348195439183011, -0.8555288687844084805, 0.1911206019478631501 ) ) ;
#7090=CARTESIAN_POINT ( 'NONE',  ( 0.2388518348206360165, -0.9447629884332594541, 0.6674861025992597785 ) ) ;
#7097=CARTESIAN_POINT ( 'NONE',  ( 0.1209954157056817858, -1.306288454297929169, 0.4272974746133751944 ) ) ;
#7098=CARTESIAN_POINT ( 'NONE',  ( 0.2750207689086996421, -1.313593350392348036, 0.6206863215409638146 ) ) ;
#7101=ADVANCED_FACE ( 'NONE', ( #31268 ), #24278, .T. ) ;
#7103=CARTESIAN_POINT ( 'NONE',  ( 0.4805026040976208002, -1.666128583310215294, 0.5622881460297129985 ) ) ;
#7105=CARTESIAN_POINT ( 'NONE',  ( 0.1858317078876725870, -0.7573081918228976583, 0.1167702249826223643 ) ) ;
#7106=CARTESIAN_POINT ( 'NONE',  ( 0.4598716470225525654, -1.229368431601224110, 0.6930793938347281635 ) ) ;
#7109=CARTESIAN_POINT ( 'NONE',  ( 0.4916028908188559421, -1.081978336766327820, 0.5838299722441698814 ) ) ;
#7110=ORIENTED_EDGE ( 'NONE', *, *, #37358, .F. ) ;
#7112=CARTESIAN_POINT ( 'NONE',  ( 0.07011823623339116796, -1.185871634737858171, 0.7567465950153516863 ) ) ;
#7115=CARTESIAN_POINT ( 'NONE',  ( 0.08620743421842372300, -0.7306438661145220337, 0.5678638921208791768 ) ) ;
#7116=CARTESIAN_POINT ( 'NONE',  ( 0.08513901846483432068, -0.8317911747034616443, 0.1390917317614507875 ) ) ;
#7117=CARTESIAN_POINT ( 'NONE',  ( 0.1842589411986597370, -0.8539449830211861547, 0.1384146430135328731 ) ) ;
#7118=CARTESIAN_POINT ( 'NONE',  ( 0.06806991437983572757, -0.5898870860155140949, 0.03457737503348648489 ) ) ;
#7121=CARTESIAN_POINT ( 'NONE',  ( 0.5350245160856361704, -1.154637332899181246, 0.6150156329573506220 ) ) ;
#7122=CARTESIAN_POINT ( 'NONE',  ( 0.2091282673351387011, -0.8319368543454188636, 0.6504350734237481779 ) ) ;
#7124=CARTESIAN_POINT ( 'NONE',  ( 0.1874519294469400021, -0.6898179517609425160, 0.05346267245209616881 ) ) ;
#7130=CARTESIAN_POINT ( 'NONE',  ( 0.08807197818943472700, -0.6448060706081871762, 0.02183434420668394632 ) ) ;
#7132=CARTESIAN_POINT ( 'NONE',  ( 0.7433653656267760201, -1.515745490836327924, 0.5775132586956883696 ) ) ;
#7141=CARTESIAN_POINT ( 'NONE',  ( 0.1841294022395738306, -0.8546492471812711100, 0.1354054936157914613 ) ) ;
#7143=CARTESIAN_POINT ( 'NONE',  ( 0.4229018694943574297, -1.238637407943166791, 0.4882188691235973543 ) ) ;
#7145=CARTESIAN_POINT ( 'NONE',  ( 0.006982617232424345385, -0.7536834681452820872, 0.4384055362127323718 ) ) ;
#7146=CARTESIAN_POINT ( 'NONE',  ( 0.0001836465996860709934, -0.5357902603937784169, -0.05245457546160120499 ) ) ;
#7150=ORIENTED_EDGE ( 'NONE', *, *, #10546, .T. ) ;
#7153=CARTESIAN_POINT ( 'NONE',  ( 0.1614670899430008522, -0.7569536277469717245, 0.1022936816274460647 ) ) ;
#7157=CARTESIAN_POINT ( 'NONE',  ( 0.3983136147636711644, -1.144903201110497593, 0.7729865516086456001 ) ) ;
#7160=CARTESIAN_POINT ( 'NONE',  ( 0.1937691639527174270, -0.6993326081247003279, 0.2764035553309984738 ) ) ;
#7162=ORIENTED_EDGE ( 'NONE', *, *, #17922, .T. ) ;
#7163=CARTESIAN_POINT ( 'NONE',  ( 0.5534916983399480461, -1.623563701787261948, 0.5248117263889745532 ) ) ;
#7165=CARTESIAN_POINT ( 'NONE',  ( 0.3024541409145408144, -1.545329219595432013, 0.8499871361866473407 ) ) ;
#7166=DIRECTION ( 'NONE',  ( 0.01455087615875040596, 0.9998941303973200023, 0.000000000000000000 ) ) ;
#7167=CARTESIAN_POINT ( 'NONE',  ( 0.1127355578498012850, -0.7499205974406458752, -0.08760834960717918396 ) ) ;
#7169=B_SPLINE_CURVE_WITH_KNOTS ( 'NONE', 3,
 ( #18569, #40158, #18785, #27440 ),
 .UNSPECIFIED., .F., .F.,
 ( 4, 4 ),
 ( 0.000000000000000000, 0.0002162507978265289883 ),
 .UNSPECIFIED. ) ;
#7173=CARTESIAN_POINT ( 'NONE',  ( 0.1868897438152673229, -0.9157227589292166181, 0.1874177539017474192 ) ) ;
#7176=CARTESIAN_POINT ( 'NONE',  ( 0.3865734956547689505, -1.160490560906283219, 0.7180718003458185228 ) ) ;
#7177=CARTESIAN_POINT ( 'NONE',  ( 0.1102377350431349573, -1.066750407935357359, 0.8659539359857927332 ) ) ;
#7178=CARTESIAN_POINT ( 'NONE',  ( 0.4395900988209245353, -1.153183135083376998, 0.4182417262808778013 ) ) ;
#7179=CARTESIAN_POINT ( 'NONE',  ( 0.4753068003148404608, -1.208388544553129496, 0.5281503392817822329 ) ) ;
#7180=EDGE_CURVE ( 'NONE', #3992, #15271, #13318, .T. ) ;
#7181=( BOUNDED_SURFACE ( )  B_SPLINE_SURFACE ( 3, 2, ( 
 ( #30373, #15347, #34255 ),
 ( #5459, #18230, #40445 ),
 ( #33649, #31193, #40635 ),
 ( #18020, #2799, #11845 ),
 ( #21941, #3012, #27693 ),
 ( #14944, #6069, #12268 ),
 ( #37348, #30583, #9158 ),
 ( #27496, #24623, #34468 ),
 ( #12061, #2405, #37158 ),
 ( #27904, #40022, #18636 ),
 ( #33871, #24410, #36944 ),
 ( #12454, #5676, #2594 ),
 ( #15559, #8968, #34061 ),
 ( #28107, #8758, #21543 ),
 ( #24824, #5861, #25005 ),
 ( #40226, #18418, #21723 ),
 ( #37538, #21335, #9361 ),
 ( #21120, #30973, #30777 ) ),
 .UNSPECIFIED., .F., .F., .F. ) 
 B_SPLINE_SURFACE_WITH_KNOTS ( ( 4, 2, 2, 2, 2, 2, 2, 2, 4 ),
 ( 3, 3 ),
 ( 0.008382955743108795946, 0.008983498031186799154, 0.009584040319264800628, 0.01018458260734280384, 0.01078512489542080705, 0.01138566718349881025, 0.01198620947157681346, 0.01258675175965481494, 0.01318729404773281814 ),
 ( 0.000000000000000000, 1.000000000000000000 ),
 .UNSPECIFIED. ) 
 GEOMETRIC_REPRESENTATION_ITEM ( )  RATIONAL_B_SPLINE_SURFACE ( (
 ( 1.000000000000000000, 0.6939742941274812393, 1.000000000000000000),
 ( 1.000000000000000000, 0.6959340198092514029, 1.000000000000000000),
 ( 1.000000000000000000, 0.6976516493059798929, 1.000000000000000000),
 ( 1.000000000000000000, 0.7006068099166593566, 1.000000000000000000),
 ( 1.000000000000000000, 0.7018521079552784148, 1.000000000000000000),
 ( 1.000000000000000000, 0.7037991596780079906, 1.000000000000000000),
 ( 1.000000000000000000, 0.7045225278982292227, 1.000000000000000000),
 ( 1.000000000000000000, 0.7055270582749912922, 1.000000000000000000),
 ( 1.000000000000000000, 0.7057932885961764047, 1.000000000000000000),
 ( 1.000000000000000000, 0.7059503901902282053, 1.000000000000000000),
 ( 1.000000000000000000, 0.7058345562627796888, 1.000000000000000000),
 ( 1.000000000000000000, 0.7053003576585554768, 1.000000000000000000),
 ( 1.000000000000000000, 0.7048799844294983963, 1.000000000000000000),
 ( 1.000000000000000000, 0.7038033628364895877, 1.000000000000000000),
 ( 1.000000000000000000, 0.7031605846919154468, 1.000000000000000000),
 ( 1.000000000000000000, 0.7017073847940890063, 1.000000000000000000),
 ( 1.000000000000000000, 0.7008898196324485630, 1.000000000000000000),
 ( 1.000000000000000000, 0.7000494314910841176, 1.000000000000000000) ) ) 
 REPRESENTATION_ITEM ( '' )  SURFACE ( )  );
#7182=CARTESIAN_POINT ( 'NONE',  ( 0.6404849880159927400, -1.549707582517539484, 0.4182417262808776348 ) ) ;
#7195=CARTESIAN_POINT ( 'NONE',  ( 0.6848280183511104013, -1.503484069889266861, 0.4560562289926599622 ) ) ;
#7198=CARTESIAN_POINT ( 'NONE',  ( 0.4314124229533453647, -1.133331723961105819, 0.4386204930848898176 ) ) ;
#7202=CARTESIAN_POINT ( 'NONE',  ( 0.1428682958407643810, -0.6238724032974017897, 0.3658253297163516771 ) ) ;
#7214=CARTESIAN_POINT ( 'NONE',  ( -0.0006246251967113254687, -0.4210325180397648248, 0.04185307883324617534 ) ) ;
#7215=VERTEX_POINT ( 'NONE', #32246 ) ;
#7216=CARTESIAN_POINT ( 'NONE',  ( 0.1776584764503561786, -0.8975873772128478700, 0.5749469949248323664 ) ) ;
#7218=CARTESIAN_POINT ( 'NONE',  ( 0.3610670237709067143, -1.199828779861834338, 0.8410762739891641804 ) ) ;
#7222=CARTESIAN_POINT ( 'NONE',  ( 0.6724801181750063028, -1.503114220331229323, 0.4114077743496406536 ) ) ;
#7223=CIRCLE ( 'NONE', #30225, 0.09249999999977555343 ) ;
#7224=CARTESIAN_POINT ( 'NONE',  ( 0.3974630593302357906, -1.726538153429652889, 0.6106779617088041734 ) ) ;
#7225=CARTESIAN_POINT ( 'NONE',  ( 0.6893317334094206661, -1.420342506522920489, 0.6035468486318071868 ) ) ;
#7229=CARTESIAN_POINT ( 'NONE',  ( 0.6092734426852441931, -1.479046879995318031, 0.5776141568224868461 ) ) ;
#7230=CARTESIAN_POINT ( 'NONE',  ( -1.913577643379703278E-05, -0.8855436973319782412, -0.02478299547526676208 ) ) ;
#7231=EDGE_CURVE ( 'NONE', #14919, #33383, #4070, .T. ) ;
#7232=CARTESIAN_POINT ( 'NONE',  ( 0.008263909818985001182, -0.6872203660130532521, -0.01225013371141639093 ) ) ;
#7235=CARTESIAN_POINT ( 'NONE',  ( 0.08897272204609851798, -1.263855944153051469, 0.7613784839713820807 ) ) ;
#7236=CARTESIAN_POINT ( 'NONE',  ( 0.2389902554220701691, -0.8445547280628969977, 0.4765619450694277281 ) ) ;
#7242=CARTESIAN_POINT ( 'NONE',  ( 0.002367446934001495983, -0.5282228851542395409, 0.1479114972776863768 ) ) ;
#7247=CARTESIAN_POINT ( 'NONE',  ( 0.3207148961678939481, -1.182401600646133089, 0.3667417262808778111 ) ) ;
#7248=CARTESIAN_POINT ( 'NONE',  ( 0.6714320665202346827, -1.386459733509071368, 0.6790741990638067271 ) ) ;
#7249=VERTEX_POINT ( 'NONE', #30942 ) ;
#7258=ORIENTED_EDGE ( 'NONE', *, *, #17720, .T. ) ;
#7259=CARTESIAN_POINT ( 'NONE',  ( 0.1406250000000003331, -0.4510478692700826131, 0.1883489205008177791 ) ) ;
#7260=CARTESIAN_POINT ( 'NONE',  ( 0.08922154937966106369, -0.6455529212171776665, 0.1844887113699342218 ) ) ;
#7261=CARTESIAN_POINT ( 'NONE',  ( 0.07788054139780381524, -0.8406284514424815502, 0.8421199864423437598 ) ) ;
#7262=CARTESIAN_POINT ( 'NONE',  ( 0.08912494520596493663, -0.5821696580930801890, 0.2929835240246161376 ) ) ;
#7265=CARTESIAN_POINT ( 'NONE',  ( 0.1334932820914363771, -0.9851919633086514416, 0.5193490242086087338 ) ) ;
#7269=CARTESIAN_POINT ( 'NONE',  ( 0.1153666297353847375, -0.4471033958673064079, 0.1626010152724407243 ) ) ;
#7277=CARTESIAN_POINT ( 'NONE',  ( 0.4241633753480167357, -0.9987333192354345135, 0.7764642562231158784 ) ) ;
#7285=CARTESIAN_POINT ( 'NONE',  ( 0.2826350996111168246, -0.9783784622179060309, 0.7275809683755095625 ) ) ;
#7292=CARTESIAN_POINT ( 'NONE',  ( 0.3713045181390347560, -1.116680715442327942, 0.6055992876344371556 ) ) ;
#7295=CARTESIAN_POINT ( 'NONE',  ( 0.2445499268847527441, -1.256775376714664549, 0.7081412490047852559 ) ) ;
#7299=CARTESIAN_POINT ( 'NONE',  ( 0.4826365958783261356, -1.664573153218981361, 0.5561147440369655914 ) ) ;
#7301=CARTESIAN_POINT ( 'NONE',  ( 0.3776575240040908610, -1.119978095218312708, 0.7246888332089733709 ) ) ;
#7303=CARTESIAN_POINT ( 'NONE',  ( 0.2615233978049238406, -1.678084768816710648, 0.5373352594323992371 ) ) ;
#7304=B_SPLINE_CURVE_WITH_KNOTS ( 'NONE', 3,
 ( #3887, #3490, #28596, #29199, #6369, #653, #468, #12965, #38045, #22430, #38454, #25097, #7163, #38239, #35174, #10289 ),
 .UNSPECIFIED., .F., .F.,
 ( 4, 2, 2, 2, 2, 2, 2, 4 ),
 ( 0.000000000000000000, 0.0004934348547721647844, 0.0009868697095443295687, 0.001480304564316494570, 0.001973739419088659137, 0.002467174273860823705, 0.002960609128632989140, 0.003947478838177317408 ),
 .UNSPECIFIED. ) ;
#7309=ORIENTED_EDGE ( 'NONE', *, *, #24826, .F. ) ;
#7311=CARTESIAN_POINT ( 'NONE',  ( 0.4136164036920929599, -1.589545870387133908, 0.5737237853280422462 ) ) ;
#7312=CARTESIAN_POINT ( 'NONE',  ( 0.06625991551443329020, -0.7353711572464834978, 0.005698596487343925848 ) ) ;
#7313=CARTESIAN_POINT ( 'NONE',  ( 0.2017021523379468051, -0.6567308881480256044, 0.3367814055878157187 ) ) ;
#7316=ORIENTED_EDGE ( 'NONE', *, *, #37029, .F. ) ;
#7318=CARTESIAN_POINT ( 'NONE',  ( 0.5711473416986291296, -1.490055735821753435, 0.6671231403163234708 ) ) ;
#7320=CARTESIAN_POINT ( 'NONE',  ( 0.07344419321621749319, -1.332345885986941036, 0.4917313231282066655 ) ) ;
#7325=DIRECTION ( 'NONE',  ( 0.000000000000000000, 0.000000000000000000, -1.000000000000000000 ) ) ;
#7327=CARTESIAN_POINT ( 'NONE',  ( 0.7437969124434082868, -1.515212563166708604, 0.5942788597236812187 ) ) ;
#7329=CARTESIAN_POINT ( 'NONE',  ( 0.06805471781164178224, -1.337523778089659610, 0.5185330071074899516 ) ) ;
#7335=CARTESIAN_POINT ( 'NONE',  ( 0.1843448470596803501, -0.5982784986119861204, -0.009472559150814239756 ) ) ;
#7337=CARTESIAN_POINT ( 'NONE',  ( 0.1394132134375135335, -1.285647836448881698, 0.4252245862416944577 ) ) ;
#7341=CARTESIAN_POINT ( 'NONE',  ( 0.2922741047311901985, -1.688215408676643658, 0.8015225518757634893 ) ) ;
#7349=CARTESIAN_POINT ( 'NONE',  ( 0.05567535398968421340, -1.335339640988971288, 0.4687417262808780127 ) ) ;
#7351=CARTESIAN_POINT ( 'NONE',  ( 0.3862110256088818194, -1.731934476144515900, 0.4282538419479027247 ) ) ;
#7353=CARTESIAN_POINT ( 'NONE',  ( 0.3894655533085423782, -1.132081281638208647, 0.7727388183733103766 ) ) ;
#7356=CARTESIAN_POINT ( 'NONE',  ( 0.3725907112986628911, -0.9732892004818366471, 0.6614114956809742374 ) ) ;
#7363=CARTESIAN_POINT ( 'NONE',  ( 0.3264869902747437047, -1.638973361554033170, 0.5665452580153856887 ) ) ;
#7364=CARTESIAN_POINT ( 'NONE',  ( 0.6355551670791450558, -1.580035597652303281, 0.4260930208334881564 ) ) ;
#7365=CARTESIAN_POINT ( 'NONE',  ( 0.1129301055607959681, -0.7190106171137882196, -0.09375086704596295728 ) ) ;
#7373=CARTESIAN_POINT ( 'NONE',  ( 0.1113455598878015373, -0.9288604395749201492, 0.1798995508551040623 ) ) ;
#7377=CARTESIAN_POINT ( 'NONE',  ( 0.3287827152071736703, -1.178255865141498271, 0.7250580491420484108 ) ) ;
#7378=CARTESIAN_POINT ( 'NONE',  ( 0.08525625553564522563, -0.9707879525957265887, 0.8108029995381474953 ) ) ;
#7380=CARTESIAN_POINT ( 'NONE',  ( 0.4656188692126475015, -1.154221074868963415, 0.4228768485321867665 ) ) ;
#7390=FACE_OUTER_BOUND ( 'NONE', #40150, .T. ) ;
#7403=CARTESIAN_POINT ( 'NONE',  ( 0.2687115422113643959, -1.674045828432256355, 0.5754129880667321340 ) ) ;
#7405=CARTESIAN_POINT ( 'NONE',  ( 0.6020297351734736901, -1.483137940370031327, 0.5741727644973939615 ) ) ;
#7411=CARTESIAN_POINT ( 'NONE',  ( 0.2010011132812319357, -0.7031246823302816917, 0.6588550337264904577 ) ) ;
#7414=CARTESIAN_POINT ( 'NONE',  ( -0.01277482466110092980, -0.5582999514612219105, 0.2804546619028133181 ) ) ;
#7418=EDGE_CURVE ( 'NONE', #34759, #27340, #11185, .T. ) ;
#7419=CARTESIAN_POINT ( 'NONE',  ( -0.004891214258241028887, -0.7404579356088991648, 0.1483282180229323066 ) ) ;
#7422=EDGE_CURVE ( 'NONE', #23907, #3591, #28260, .T. ) ;
#7423=CARTESIAN_POINT ( 'NONE',  ( 0.2109547519922409242, -0.9305643203978569700, 0.6267875559574144217 ) ) ;
#7424=APPLICATION_CONTEXT ( 'configuration controlled 3d designs of mechanical parts and assemblies' ) ;
#7425=B_SPLINE_CURVE_WITH_KNOTS ( 'NONE', 3,
 ( #39617, #17212, #14126, #30168, #32645, #20721 ),
 .UNSPECIFIED., .F., .F.,
 ( 4, 2, 4 ),
 ( 0.002514931666163710763, 0.002746441579761122430, 0.002977951493358533663 ),
 .UNSPECIFIED. ) ;
#7427=( BOUNDED_SURFACE ( )  B_SPLINE_SURFACE ( 3, 2, ( 
 ( #8511, #27260, #36899 ),
 ( #39789, #8709, #17769 ),
 ( #11406, #34212, #24575 ),
 ( #37304, #30537, #20888 ),
 ( #31149, #11804, #15516 ),
 ( #2156, #17978, #21285 ),
 ( #2557, #30735, #2362 ),
 ( #40397, #5412, #5219 ),
 ( #14692, #30322, #8318 ),
 ( #11620, #18185, #34018 ),
 ( #24178, #33827, #36703 ),
 ( #23974, #15092, #14900 ),
 ( #27459, #15303, #39982 ),
 ( #30928, #40179, #18594 ),
 ( #12016, #28067, #37108 ),
 ( #8926, #21500, #36507 ) ),
 .UNSPECIFIED., .F., .F., .T. ) 
 B_SPLINE_SURFACE_WITH_KNOTS ( ( 4, 2, 2, 2, 2, 2, 2, 4 ),
 ( 3, 3 ),
 ( -2.352153712789272500E-05, 0.0004694506785108612111, 0.0009624228941496151303, 0.001455395109788369104, 0.001948367325427123077, 0.002441339541065876834, 0.002934311756704631024, 0.003920256187982138971 ),
 ( 0.000000000000000000, 1.000000000000000000 ),
 .UNSPECIFIED. ) 
 GEOMETRIC_REPRESENTATION_ITEM ( )  RATIONAL_B_SPLINE_SURFACE ( (
 ( 1.000000000000000000, 0.7057019905713519670, 1.000000000000000000),
 ( 1.000000000000000000, 0.7055894858937867831, 1.000000000000000000),
 ( 1.000000000000000000, 0.7055144135113683435, 1.000000000000000000),
 ( 1.000000000000000000, 0.7054271390702308020, 1.000000000000000000),
 ( 1.000000000000000000, 0.7054151093076957979, 1.000000000000000000),
 ( 1.000000000000000000, 0.7054386977650431989, 1.000000000000000000),
 ( 1.000000000000000000, 0.7054733622895101863, 1.000000000000000000),
 ( 1.000000000000000000, 0.7055688516086890960, 1.000000000000000000),
 ( 1.000000000000000000, 0.7056302112408742166, 1.000000000000000000),
 ( 1.000000000000000000, 0.7057581921034653538, 1.000000000000000000),
 ( 1.000000000000000000, 0.7058253497257075404, 1.000000000000000000),
 ( 1.000000000000000000, 0.7059550172059571027, 1.000000000000000000),
 ( 1.000000000000000000, 0.7060161488338141389, 1.000000000000000000),
 ( 1.000000000000000000, 0.7061761676825132339, 1.000000000000000000),
 ( 1.000000000000000000, 0.7062536236208033502, 1.000000000000000000),
 ( 1.000000000000000000, 0.7062849495007524903, 1.000000000000000000) ) ) 
 REPRESENTATION_ITEM ( '' )  SURFACE ( )  );
#7428=CARTESIAN_POINT ( 'NONE',  ( 0.1104829199723380839, -0.5612026451200987642, 0.2208380843409518401 ) ) ;
#7431=CARTESIAN_POINT ( 'NONE',  ( 0.2038749045098602886, -1.364881829950852721, 0.4182417262808790226 ) ) ;
#7434=B_SPLINE_CURVE_WITH_KNOTS ( 'NONE', 3,
 ( #23122, #13040, #26400, #19621 ),
 .UNSPECIFIED., .F., .F.,
 ( 4, 4 ),
 ( 0.001505104451090290719, 0.001946516628694922859 ),
 .UNSPECIFIED. ) ;
#7435=CARTESIAN_POINT ( 'NONE',  ( 0.3473585933147235738, -1.744357246013940044, 0.5876618537173693424 ) ) ;
#7436=CARTESIAN_POINT ( 'NONE',  ( 0.6928118984338402786, -1.426853195981605316, 0.5961107746216205427 ) ) ;
#7439=DIRECTION ( 'NONE',  ( 0.9549552564275718414, 0.000000000000000000, 0.2967498242987692270 ) ) ;
#7442=CARTESIAN_POINT ( 'NONE',  ( -0.0002026554222459760483, -0.8535802774609255739, -0.04061330533372662505 ) ) ;
#7447=CARTESIAN_POINT ( 'NONE',  ( -0.002083146443013344888, -0.8967360763018595859, 0.09758087637170891060 ) ) ;
#7449=CARTESIAN_POINT ( 'NONE',  ( 0.3960970180006803121, -1.016137033769514808, 0.6457357589753065508 ) ) ;
#7456=CARTESIAN_POINT ( 'NONE',  ( 0.002465946970083897002, -0.5375442681548233681, 0.2095628591970551957 ) ) ;
#7457=AXIS2_PLACEMENT_3D ( 'NONE', #648, #29399, #10281 ) ;
#7458=CARTESIAN_POINT ( 'NONE',  ( 0.3790996791422692747, -1.751796687822255949, 0.5182417262812423209 ) ) ;
#7461=CARTESIAN_POINT ( 'NONE',  ( 0.6326847266287998206, -1.322366380368365180, 0.7606069447649664861 ) ) ;
#7465=EDGE_CURVE ( 'NONE', #15823, #26063, #19160, .T. ) ;
#7468=CARTESIAN_POINT ( 'NONE',  ( 0.4496398668279690813, -1.226616743782979135, 0.5966018278806392017 ) ) ;
#7472=CARTESIAN_POINT ( 'NONE',  ( 0.4582297113153581125, -1.232395013690232632, 1.043719859503123404 ) ) ;
#7473=CARTESIAN_POINT ( 'NONE',  ( 0.1819313570110824285, -0.8286255242310253122, 0.6065153366566046200 ) ) ;
#7475=CARTESIAN_POINT ( 'NONE',  ( 0.09745522806139698957, -0.8755261795257442969, 0.8646684577488064072 ) ) ;
#7476=CARTESIAN_POINT ( 'NONE',  ( 0.4073001593474919746, -1.370116077848211766, 0.8465991415876540360 ) ) ;
#7478=CARTESIAN_POINT ( 'NONE',  ( 0.1061776879072938579, -1.071297230844371340, 0.8824484360082986978 ) ) ;
#7479=DIRECTION ( 'NONE',  ( 0.8660512985181133550, 0.4999551463232370652, 0.000000000000000000 ) ) ;
#7480=CARTESIAN_POINT ( 'NONE',  ( 0.3452606047117887655, -1.113321646336553394, 0.6365754745706553308 ) ) ;
#7483=CARTESIAN_POINT ( 'NONE',  ( 0.3339310430327372403, -1.636299247267255286, 0.5510156998079677182 ) ) ;
#7484=CARTESIAN_POINT ( 'NONE',  ( 0.1173700203642584067, -0.4709408336746424562, 0.2678698260706097178 ) ) ;
#7491=CARTESIAN_POINT ( 'NONE',  ( 0.08989780363036058153, -0.5646359461869331353, 0.1460065308160271857 ) ) ;
#7492=CARTESIAN_POINT ( 'NONE',  ( 0.5890075386511577360, -1.247786712317649815, 0.6995832148063678702 ) ) ;
#7495=CARTESIAN_POINT ( 'NONE',  ( 0.4911277369064176446, -1.657269195667506967, 0.4283731361201775223 ) ) ;
#7501=CARTESIAN_POINT ( 'NONE',  ( 0.3511827046531754148, -1.077246269942499612, 0.7624202803643029824 ) ) ;
#7511=B_SPLINE_CURVE_WITH_KNOTS ( 'NONE', 3,
 ( #39980, #21283, #18378, #21680, #27457, #30534 ),
 .UNSPECIFIED., .F., .F.,
 ( 4, 2, 4 ),
 ( 0.001203677602004720381, 0.004507238951556864770, 0.007810800301109012411 ),
 .UNSPECIFIED. ) ;
#7512=CARTESIAN_POINT ( 'NONE',  ( 0.4026621603086822931, -1.135280432806801132, 0.5010831896812795172 ) ) ;
#7513=CARTESIAN_POINT ( 'NONE',  ( 0.07424435375522935032, -0.8686257631445842842, 0.4612673976281420618 ) ) ;
#7520=CARTESIAN_POINT ( 'NONE',  ( 0.3640235822487147832, -1.104155517840267775, 0.7181720340464149421 ) ) ;
#7523=CARTESIAN_POINT ( 'NONE',  ( 0.2648760513428040086, -1.303909466691514973, 0.5182417262812423209 ) ) ;
#7526=CIRCLE ( 'NONE', #12800, 0.07749999999977547072 ) ;
#7532=CARTESIAN_POINT ( 'NONE',  ( 0.4151474250827118517, -1.589570192129442727, 0.5985126306996821910 ) ) ;
#7533=CARTESIAN_POINT ( 'NONE',  ( 0.06774469294687966714, -0.6123281028958347250, 0.01828842993687508287 ) ) ;
#7534=CARTESIAN_POINT ( 'NONE',  ( 0.1947297287360276741, -0.6386476969732345355, 0.3263804930690787365 ) ) ;
#7535=CARTESIAN_POINT ( 'NONE',  ( 0.1543908734882358524, -1.277778445049856826, 0.4807399974149955679 ) ) ;
#7540=CARTESIAN_POINT ( 'NONE',  ( 0.1337456116390407512, -0.6334664691652446278, 0.3892934226950710563 ) ) ;
#7543=CARTESIAN_POINT ( 'NONE',  ( 0.1874400581894105633, -0.6906950488587336734, 0.04510364496225629377 ) ) ;
#7545=CARTESIAN_POINT ( 'NONE',  ( 0.6544078563150326211, -1.544269123161558177, 0.4241055859090113733 ) ) ;
#7546=CARTESIAN_POINT ( 'NONE',  ( 0.1668829993946232826, -1.259189101050422366, 0.4341909677000992951 ) ) ;
#7549=CARTESIAN_POINT ( 'NONE',  ( 0.5453389350593388363, -1.184144166247469876, 0.8773366473911075047 ) ) ;
#7559=CARTESIAN_POINT ( 'NONE',  ( 0.1844024556850973051, -0.8470684581476211061, 0.09518424029853758683 ) ) ;
#7560=CARTESIAN_POINT ( 'NONE',  ( 0.4111945703227398163, -1.245400387139686815, 0.5084384360591323038 ) ) ;
#7561=B_SPLINE_CURVE_WITH_KNOTS ( 'NONE', 3,
 ( #5159, #33541, #24127, #36649, #5351, #17913, #12365, #24921, #21446, #2906, #37448, #22057, #25120, #33973, #18953, #3296, #9262, #15852, #5777, #9073, #19153, #18749, #21841, #37046, #34581, #28009, #31302, #6574, #21636, #25333, #28406, #6387, #18333, #37658, #15459, #31489, #34159, #40123, #276, #31694, #3513, #12771, #22256, #27594, #37873, #11953, #37256, #31087, #5970, #28202, #34366, #9474, #9688, #3110, #34767, #27800, #12558, #24517, #67, #2696, #6181, #8868, #30879 ),
 .UNSPECIFIED., .F., .F.,
 ( 4, 2, 1, 2, 2, 2, 2, 2, 2, 2, 2, 2, 2, 2, 2, 2, 2, 2, 2, 2, 2, 2, 2, 2, 2, 2, 2, 2, 2, 2, 2, 4 ),
 ( -5.999999999593325711E-08, 0.0002089317286102376910, 0.0004179234572204712853, 0.0008359069144409385279, 0.001671873828881873013, 0.003343807657763743068, 0.005015741486645609870, 0.006687675315527477106, 0.01003154297329121244, 0.01170347680217307881, 0.01337541063105494692, 0.02006314594658243147, 0.02173507977546430131, 0.02340701360434616768, 0.02675088126210990735, 0.03009474891987364703, 0.03343861657763738671, 0.03511055040651924614, 0.03678248423540111250, 0.03845441806428297887, 0.04012635189316483830, 0.04179828572204669773, 0.04347021955092856410, 0.04514215337981042353, 0.04597812029425134978, 0.04681408720869228296, 0.04848602103757415627, 0.05015795486645601570, 0.05182988869533788207, 0.05266585560977881525, 0.05308383906699928184, 0.05350182252421974149 ),
 .UNSPECIFIED. ) ;
#7562=CARTESIAN_POINT ( 'NONE',  ( 0.1049860589904711705, -1.308425076921832408, 0.4359114761720587206 ) ) ;
#7564=CARTESIAN_POINT ( 'NONE',  ( 0.1835387414513457993, -1.269102812158692473, 1.002600033288329140 ) ) ;
#7572=CARTESIAN_POINT ( 'NONE',  ( 0.1438681892407857876, -1.284094082863941111, 0.3157417262808777658 ) ) ;
#7574=CARTESIAN_POINT ( 'NONE',  ( 0.6011193747858227798, -1.595581932925101976, 0.4276689662439276396 ) ) ;
#7576=CARTESIAN_POINT ( 'NONE',  ( 0.5324855789941030926, -1.347847315281903491, 0.7002209793041090924 ) ) ;
#7578=ORIENTED_EDGE ( 'NONE', *, *, #39452, .F. ) ;
#7579=CARTESIAN_POINT ( 'NONE',  ( 0.4100600194349330319, -1.011029760475403494, 0.6817144834752139060 ) ) ;
#7582=CARTESIAN_POINT ( 'NONE',  ( 0.3247353678145296074, -1.174695915522060652, 0.5636564603779772309 ) ) ;
#7584=CARTESIAN_POINT ( 'NONE',  ( 0.02592883741220372920, -0.5747094013104246946, 0.3049468829503017564 ) ) ;
#7585=CARTESIAN_POINT ( 'NONE',  ( 0.6950632297095953316, -1.495237220361341102, 0.4800255380849818287 ) ) ;
#7586=CARTESIAN_POINT ( 'NONE',  ( 0.5826217342940260835, -1.634307228436295167, 0.5182417262812423209 ) ) ;
#7587=CARTESIAN_POINT ( 'NONE',  ( 0.05560027925352286488, -1.335209592177159843, 0.5707417262808780478 ) ) ;
#7590=AXIS2_PLACEMENT_3D ( 'NONE', #23790, #29540, #8342 ) ;
#7595=CARTESIAN_POINT ( 'NONE',  ( 0.4335229873338388717, -1.223245311458436069, 0.6222225527454730010 ) ) ;
#7597=CARTESIAN_POINT ( 'NONE',  ( 0.3253942546199506958, -1.752804466647932546, 0.4715143355759890409 ) ) ;
#7598=CARTESIAN_POINT ( 'NONE',  ( 0.4618534464035452536, -1.161788201396328546, 0.4182417262808778013 ) ) ;
#7604=CARTESIAN_POINT ( 'NONE',  ( 0.1678534701465425882, -1.280328660040236377, 0.4182417262808778013 ) ) ;
#7606=CARTESIAN_POINT ( 'NONE',  ( 0.006374870886235760488, -0.9785717880618779452, 0.4789926383131983822 ) ) ;
#7607=ADVANCED_FACE ( 'NONE', ( #19625 ), #27159, .T. ) ;
#7611=CARTESIAN_POINT ( 'NONE',  ( 0.7066109249242027435, -1.499057094600571238, 0.5182417262806440217 ) ) ;
#7615=CARTESIAN_POINT ( 'NONE',  ( 0.2716900230296190322, -1.558453453380033604, 0.9768685533762022644 ) ) ;
#7616=CLOSED_SHELL ( 'NONE', ( #13068, #16811, #12641, #39164, #3669, #8238, #13744, #17739, #1369, #19577, #31586, #3472, #32506, #30124, #31794, #16296, #36779, #11253, #4457, #25487, #36815, #26813, #34337, #32524, #28527, #31102, #3631, #24043, #15759, #5498, #28349, #39333, #18031, #23008, #8933, #39435, #972, #39856, #12790, #18428, #38669, #21490, #29047, #33008, #33646, #6007, #24432, #23757, #33558, #18055, #13921, #2943, #30383, #30324, #32562, #32779, #10684, #26034, #5449, #17864, #24310, #10178, #17581, #6355, #9677, #33401, #29025, #16804, #28895, #3945, #34182, #20324, #14214, #30104, #13071, #5356, #8997, #27522, #9263, #4984, #10423, #24986, #8469, #10408, #15753, #18448, #26299, #18491, #12047, #18695, #2601, #30798, #23013, #22342, #40074, #22815, #22842, #36391, #5686, #1208, #6619, #21751, #4674, #25876, #40249, #744, #17988, #34269, #24313, #17229, #13915, #37437, #15272, #3688, #6367, #22871, #11004, #6443, #18551, #24775, #29532, #36627, #4724, #7101, #30330, #2458, #11761, #38541, #22574, #3686, #26373, #11009, #17186, #31532, #12515, #9445, #5207, #133, #29076, #39357, #6128, #9891, #28360, #40331, #12728, #27148, #19984, #11297, #20272, #11070, #17834, #7607, #39947, #8455, #1426, #17679, #13431, #1003, #23904, #31692, #22002, #5878 ) ) ;
#7622=CARTESIAN_POINT ( 'NONE',  ( 0.1877434453300698414, -0.5089539054925988903, 0.1080467165728084405 ) ) ;
#7623=EDGE_LOOP ( 'NONE', ( #23172, #38094, #24705, #5723, #22197 ) ) ;
#7625=CARTESIAN_POINT ( 'NONE',  ( 0.2603803840244302559, -1.679120311287623624, 0.5759385929908824586 ) ) ;
#7626=CARTESIAN_POINT ( 'NONE',  ( 0.5066971731404251722, -1.347239037406359197, 0.8035729607927099005 ) ) ;
#7627=CARTESIAN_POINT ( 'NONE',  ( -0.001991110985728673961, -0.8396244724827389705, 0.09658552693076032092 ) ) ;
#7628=ORIENTED_EDGE ( 'NONE', *, *, #25563, .F. ) ;
#7635=CARTESIAN_POINT ( 'NONE',  ( 0.1820039756314770496, -1.353402374702050048, 0.9460902548477880813 ) ) ;
#7644=CARTESIAN_POINT ( 'NONE',  ( 0.1297863134137367813, -0.8346111980775223760, 0.4665308214793116304 ) ) ;
#7645=B_SPLINE_CURVE_WITH_KNOTS ( 'NONE', 3,
 ( #5537, #2664, #8834, #40296, #37010, #12527 ),
 .UNSPECIFIED., .F., .F.,
 ( 4, 2, 4 ),
 ( 0.000000000000000000, 0.0005427992237399233491, 0.001085598447479846698 ),
 .UNSPECIFIED. ) ;
#7646=CARTESIAN_POINT ( 'NONE',  ( 0.01703266676564623230, -0.8936126741228921366, 0.5128946615551410737 ) ) ;
#7647=CARTESIAN_POINT ( 'NONE',  ( 0.09106748660175942311, -0.5564522452151119403, 0.2171823283136207761 ) ) ;
#7648=CARTESIAN_POINT ( 'NONE',  ( 0.5372047856502307761, -1.509560927297886934, 0.6722531729593694827 ) ) ;
#7649=CARTESIAN_POINT ( 'NONE',  ( 0.1978587402095111636, -0.5849795632145003976, 0.3178455878192510409 ) ) ;
#7650=DIRECTION ( 'NONE',  ( 0.9998941247116546194, -0.01455087607601020239, 0.0001066420868422379362 ) ) ;
#7651=CARTESIAN_POINT ( 'NONE',  ( 0.6586055134406099132, -1.459595632619679950, 0.4243909478079631037 ) ) ;
#7652=CARTESIAN_POINT ( 'NONE',  ( 0.3701867111158838042, -1.742907794848391978, 0.6016813899000484911 ) ) ;
#7654=CARTESIAN_POINT ( 'NONE',  ( 0.4136294883733862005, -1.694877849074643672, 0.4182417262808776903 ) ) ;
#7657=CARTESIAN_POINT ( 'NONE',  ( -6.702082025768050936E-05, -0.7526509584479209591, -0.09479413075768641783 ) ) ;
#7658=CARTESIAN_POINT ( 'NONE',  ( 0.5817652315481057768, -1.478716734979794944, 0.6771717844549590692 ) ) ;
#7661=DIRECTION ( 'NONE',  ( 0.5196341416262992841, -0.8543888803444829039, 0.000000000000000000 ) ) ;
#7664=CARTESIAN_POINT ( 'NONE',  ( 0.1235390412447300995, -1.439500955437662766, 0.5982358349985300583 ) ) ;
#7665=CARTESIAN_POINT ( 'NONE',  ( 0.4916028908188559421, -1.081978336766327820, 0.5838299722441698814 ) ) ;
#7668=CARTESIAN_POINT ( 'NONE',  ( 0.5827378505010344378, -1.244973309454295629, 0.8759922176168969399 ) ) ;
#7671=DIRECTION ( 'NONE',  ( 0.8660512985181135770, 0.4999551463232372317, 0.000000000000000000 ) ) ;
#7673=CARTESIAN_POINT ( 'NONE',  ( 0.3136699570144902971, -1.762202131979911712, 0.5691132299474264133 ) ) ;
#7676=CARTESIAN_POINT ( 'NONE',  ( 0.002369698199515762795, -0.5286367086536888360, 0.1583934855509527007 ) ) ;
#7681=CARTESIAN_POINT ( 'NONE',  ( 0.4763737863547038431, -1.078928959615589100, 0.8012595312036666639 ) ) ;
#7685=( BOUNDED_SURFACE ( )  B_SPLINE_SURFACE ( 3, 2, ( 
 ( #9822, #428, #22601 ),
 ( #35336, #22813, #28943 ),
 ( #32225, #25477, #7320 ),
 ( #16607, #34921, #38012 ) ),
 .UNSPECIFIED., .F., .F., .T. ) 
 B_SPLINE_SURFACE_WITH_KNOTS ( ( 4, 4 ),
 ( 3, 3 ),
 ( -1.198043400596482400E-17, 0.0005284928876949268779 ),
 ( 0.000000000000000000, 1.000000000000000000 ),
 .UNSPECIFIED. ) 
 GEOMETRIC_REPRESENTATION_ITEM ( )  RATIONAL_B_SPLINE_SURFACE ( (
 ( 1.000000000000000000, 0.8671479162384729822, 1.000000000000000000),
 ( 1.000000000000000000, 0.8820622678756920854, 1.000000000000000000),
 ( 1.000000000000000000, 0.8880894362480542537, 1.000000000000000000),
 ( 1.000000000000000000, 0.8864945003981776761, 1.000000000000000000) ) ) 
 REPRESENTATION_ITEM ( '' )  SURFACE ( )  );
#7687=EDGE_CURVE ( 'NONE', #18202, #4342, #10929, .T. ) ;
#7688=CARTESIAN_POINT ( 'NONE',  ( 0.2898911397524138733, -1.200022992789476328, 0.4282476769854300369 ) ) ;
#7691=CARTESIAN_POINT ( 'NONE',  ( 0.1406250000000001388, -0.4888214998617192442, 0.3238651926494596767 ) ) ;
#7692=CARTESIAN_POINT ( 'NONE',  ( 0.2560554501240281389, -0.9391908526076655495, 0.7069755978740671631 ) ) ;
#7693=CARTESIAN_POINT ( 'NONE',  ( 0.1969934931346632723, -1.289641399371132424, 1.023064179873733659 ) ) ;
#7694=CARTESIAN_POINT ( 'NONE',  ( 0.1117195309642857459, -0.6771241826238267869, 0.4786975410683091958 ) ) ;
#7695=CARTESIAN_POINT ( 'NONE',  ( 0.2713523440619998173, -1.672253707410367829, 0.7222851353733067414 ) ) ;
#7697=CARTESIAN_POINT ( 'NONE',  ( 0.1521791078991787949, -1.215866141468441963, 0.6421765199397219126 ) ) ;
#7700=CARTESIAN_POINT ( 'NONE',  ( 0.1317003362355874119, -0.5351829081616051864, 0.4217891011909937760 ) ) ;
#7701=DIRECTION ( 'NONE',  ( -0.4999551463232372317, 0.8660512985181135770, -0.000000000000000000 ) ) ;
#7703=CARTESIAN_POINT ( 'NONE',  ( 0.002290818369124609372, -0.5198888459286679087, 0.1457185332388686583 ) ) ;
#7705=CARTESIAN_POINT ( 'NONE',  ( 0.6150013826522254812, -1.299199899150926374, 0.5044333340123036136 ) ) ;
#7711=VERTEX_POINT ( 'NONE', #26568 ) ;
#7712=CARTESIAN_POINT ( 'NONE',  ( 0.4411652911884185180, -1.201865629404675229, 0.6973157100092504113 ) ) ;
#7721=CARTESIAN_POINT ( 'NONE',  ( 0.4321640349418070515, -1.121330984503925876, 0.5310794168832609907 ) ) ;
#7722=CARTESIAN_POINT ( 'NONE',  ( 0.03247176862405053849, -0.8418478330200259707, 0.2157142965010831193 ) ) ;
#7723=ORIENTED_EDGE ( 'NONE', *, *, #4859, .F. ) ;
#7727=CARTESIAN_POINT ( 'NONE',  ( 0.1817793365275204021, -1.377674457685613696, 0.4214207381694095589 ) ) ;
#7729=CARTESIAN_POINT ( 'NONE',  ( 0.6544078563150221850, -1.544269123161552626, 0.4241055859090109292 ) ) ;
#7730=CARTESIAN_POINT ( 'NONE',  ( 0.4795933240383793428, -1.258180956532618744, 0.5929850450974815113 ) ) ;
#7732=CARTESIAN_POINT ( 'NONE',  ( 0.4688079631758284016, -1.116561345930851656, 0.5688791344137259509 ) ) ;
#7738=CARTESIAN_POINT ( 'NONE',  ( 0.1825071904178995619, -0.7337134285967986669, 0.1479976049341028554 ) ) ;
#7739=CARTESIAN_POINT ( 'NONE',  ( 0.05587308000523566465, -0.6076548949599507310, 0.3685913880743675319 ) ) ;
#7740=CARTESIAN_POINT ( 'NONE',  ( 0.06914125879787166862, -0.5405346344223664889, 0.1297049665551865405 ) ) ;
#7742=CARTESIAN_POINT ( 'NONE',  ( 0.1665044839944595234, -1.270767161555115932, 0.4854677671074156264 ) ) ;
#7746=CARTESIAN_POINT ( 'NONE',  ( 0.1193013743603501958, -0.5494898923379011313, 0.1617980040493336713 ) ) ;
#7752=CARTESIAN_POINT ( 'NONE',  ( 0.1571803435121711390, -1.276327713282634058, 0.4309217000577236223 ) ) ;
#7754=CARTESIAN_POINT ( 'NONE',  ( 0.08989082913961529697, -0.5631763781711711658, 0.1462941165619876527 ) ) ;
#7755=CARTESIAN_POINT ( 'NONE',  ( 0.1875000000000000833, -0.4595382586000822389, 0.1581505021253525878 ) ) ;
#7760=CARTESIAN_POINT ( 'NONE',  ( 0.2165002020277727868, -1.357372643808337775, 0.4854677670904418152 ) ) ;
#7761=CARTESIAN_POINT ( 'NONE',  ( 0.1841981897273382851, -0.8536146481143929154, 0.1250772005134268283 ) ) ;
#7763=CYLINDRICAL_SURFACE ( 'NONE', #15943, 0.1000000000000000194 ) ;
#7766=DIRECTION ( 'NONE',  ( 0.2841200139107300515, 0.1745296787418094686, -0.9427699660753134925 ) ) ;
#7769=CARTESIAN_POINT ( 'NONE',  ( 0.3047917018647445242, -1.756872442562883219, 0.5682425124847924058 ) ) ;
#7773=CARTESIAN_POINT ( 'NONE',  ( 0.1050286246271734808, -1.410831341392925209, 0.5682417262808875380 ) ) ;
#7774=CARTESIAN_POINT ( 'NONE',  ( 0.2319960710055803677, -1.232736008543062090, 0.4687417262808780127 ) ) ;
#7778=CARTESIAN_POINT ( 'NONE',  ( 0.5509096165736990791, -1.379093160209163615, 0.7167504442928195330 ) ) ;
#7780=ORIENTED_EDGE ( 'NONE', *, *, #16199, .F. ) ;
#7781=CARTESIAN_POINT ( 'NONE',  ( 0.2467813525974754951, -0.8519813862200177335, 0.4954293255957377684 ) ) ;
#7783=ORIENTED_EDGE ( 'NONE', *, *, #8505, .T. ) ;
#7785=CARTESIAN_POINT ( 'NONE',  ( 0.04494180016761560592, -0.6777367256777560023, 0.5045707990937741139 ) ) ;
#7786=CARTESIAN_POINT ( 'NONE',  ( 0.7013323771326090972, -1.495406364347797279, 0.4952476761773726421 ) ) ;
#7787=CARTESIAN_POINT ( 'NONE',  ( 0.1150990105419666260, -0.4532349895251732708, 0.08714482709981570541 ) ) ;
#7790=ORIENTED_EDGE ( 'NONE', *, *, #4859, .T. ) ;
#7792=CARTESIAN_POINT ( 'NONE',  ( 0.1781669208264307913, -1.264215222379440506, 0.4272368710745190201 ) ) ;
#7795=CARTESIAN_POINT ( 'NONE',  ( 0.2044132264669150933, -0.9676013961680371978, 0.6836346618487517679 ) ) ;
#7798=CARTESIAN_POINT ( 'NONE',  ( 0.1118742967071392064, -0.9291314186530351682, 0.2025174426234049585 ) ) ;
#7801=CARTESIAN_POINT ( 'NONE',  ( 0.4265404446467185307, -1.123912635142109817, 0.5182417262812248904 ) ) ;
#7804=CARTESIAN_POINT ( 'NONE',  ( 0.3698622724915323068, -1.154283567815744149, 0.4343510435345701026 ) ) ;
#7805=CARTESIAN_POINT ( 'NONE',  ( 0.1792004983600124779, -0.4937710491622425146, 0.1299056045165895845 ) ) ;
#7809=CARTESIAN_POINT ( 'NONE',  ( 0.5971614065082352374, -1.461417804984935342, 0.6057417262805111502 ) ) ;
#7810=CARTESIAN_POINT ( 'NONE',  ( 0.1683513884741227873, -1.188089823937052758, 1.006248355024246477 ) ) ;
#7814=CARTESIAN_POINT ( 'NONE',  ( 0.1871607900928699830, -0.5063091123542899918, 0.1282519021220327460 ) ) ;
#7817=CARTESIAN_POINT ( 'NONE',  ( 0.6014930981134155585, -1.483010901933850434, 0.5633614063092290403 ) ) ;
#7818=CARTESIAN_POINT ( 'NONE',  ( 0.008162182821621307913, -0.6980416593638927303, -0.01224155801182983359 ) ) ;
#7821=CARTESIAN_POINT ( 'NONE',  ( 0.1183139781708525268, -0.4784996548529213967, 0.2899008765515939667 ) ) ;
#7823=CARTESIAN_POINT ( 'NONE',  ( -0.01357511779432049766, -0.5467070939194554891, 0.2476534432211799919 ) ) ;
#7828=CARTESIAN_POINT ( 'NONE',  ( -0.0002183011148504172990, -0.4210325180397647693, 0.09509064842808868934 ) ) ;
#7831=CARTESIAN_POINT ( 'NONE',  ( 0.09767084295088891699, -0.8240199256239116865, 0.3227011382480390878 ) ) ;
#7832=CARTESIAN_POINT ( 'NONE',  ( 0.1188152677000469254, -1.411957481029216588, 0.5917154036330487532 ) ) ;
#7833=CARTESIAN_POINT ( 'NONE',  ( 0.1031995293798165930, -0.6385813952848361508, 0.3661202089783873181 ) ) ;
#7834=CARTESIAN_POINT ( 'NONE',  ( 0.5069166605951295201, -1.436909806687399316, 0.7822455750953455356 ) ) ;
#7835=CARTESIAN_POINT ( 'NONE',  ( 0.02776779319759564019, -1.047279001274500798, 0.5925557623338770785 ) ) ;
#7837=CARTESIAN_POINT ( 'NONE',  ( 0.5446855849587005638, -1.168303032256096108, 0.4182417297899396202 ) ) ;
#7838=DIRECTION ( 'NONE',  ( 0.8660512985181134660, 0.4999551463232372317, 0.000000000000000000 ) ) ;
#7839=CARTESIAN_POINT ( 'NONE',  ( 0.6935470237484337996, -1.428868995382490237, 0.5856070495622788252 ) ) ;
#7840=DIRECTION ( 'NONE',  ( 0.8660512985181134660, 0.4999551463232371762, 0.000000000000000000 ) ) ;
#7843=CARTESIAN_POINT ( 'NONE',  ( -2.485268943553615236E-05, -0.9232881051602984668, 0.03311238697358490773 ) ) ;
#7844=CARTESIAN_POINT ( 'NONE',  ( 0.07442653783876213014, -0.5806215649999981743, 0.2956838457824742528 ) ) ;
#7847=CARTESIAN_POINT ( 'NONE',  ( -0.003124719664520024271, -0.8057675726412024675, 0.09674340762273991867 ) ) ;
#7848=CARTESIAN_POINT ( 'NONE',  ( 0.4929286275565831765, -1.082705722935900727, 0.5701913825460898089 ) ) ;
#7850=CARTESIAN_POINT ( 'NONE',  ( 0.3632211645871377126, -0.8757803013682723403, 0.7750855204132592879 ) ) ;
#7857=CARTESIAN_POINT ( 'NONE',  ( 0.09587822187434574817, -1.032686032632677886, 0.8621212271250301429 ) ) ;
#7858=CARTESIAN_POINT ( 'NONE',  ( 0.08510660916195567083, -1.306596824278190905, 0.4649156698885984484 ) ) ;
#7861=CARTESIAN_POINT ( 'NONE',  ( 0.3240364041276366236, -1.756843918532213333, 0.4781731194503076043 ) ) ;
#7862=CARTESIAN_POINT ( 'NONE',  ( 0.1914513227106267590, -0.5214848928147161056, 0.2513073325497693911 ) ) ;
#7868=CARTESIAN_POINT ( 'NONE',  ( 0.5686879079206863530, -1.501072830572683925, 0.5436612324038465616 ) ) ;
#7872=CARTESIAN_POINT ( 'NONE',  ( 0.2101951102887192890, -1.233953443661628846, 0.5631135429232324574 ) ) ;
#7873=CARTESIAN_POINT ( 'NONE',  ( 0.09953826690698990010, -0.7070161591386062705, 0.3305937928836391593 ) ) ;
#7875=CARTESIAN_POINT ( 'NONE',  ( 0.1159210378633096922, -0.9846889132052908389, 0.9373222049632897734 ) ) ;
#7877=CARTESIAN_POINT ( 'NONE',  ( 0.09775142746979462172, -0.5484789642255779585, 0.1807369083563863665 ) ) ;
#7878=CARTESIAN_POINT ( 'NONE',  ( 0.1842706337052801013, -1.340949179059101715, 0.9498145873395215100 ) ) ;
#7879=FACE_OUTER_BOUND ( 'NONE', #39209, .T. ) ;
#7880=CARTESIAN_POINT ( 'NONE',  ( 0.1802244519888198671, -0.9569834302806377035, 0.4667502891730959114 ) ) ;
#7884=EDGE_CURVE ( 'NONE', #27951, #15118, #36334, .T. ) ;
#7886=CARTESIAN_POINT ( 'NONE',  ( 0.1663702205777965182, -0.6275672944780111839, 0.5698197300990445191 ) ) ;
#7891=CARTESIAN_POINT ( 'NONE',  ( 0.1316017208954911588, -1.248059642665102942, 0.5182417262812423209 ) ) ;
#7892=CARTESIAN_POINT ( 'NONE',  ( 0.6170741104697204937, -1.294989041298300947, 0.6128831306409553425 ) ) ;
#7894=EDGE_CURVE ( 'NONE', #38375, #29074, #24900, .T. ) ;
#7897=B_SPLINE_CURVE_WITH_KNOTS ( 'NONE', 3,
 ( #16793, #22569, #13086, #35099 ),
 .UNSPECIFIED., .F., .F.,
 ( 4, 4 ),
 ( 3.165573288030121783E-17, 0.0002659535996674141744 ),
 .UNSPECIFIED. ) ;
#7901=CARTESIAN_POINT ( 'NONE',  ( 0.4692393356387120074, -1.241113899949852550, 0.5778994956701821728 ) ) ;
#7904=VERTEX_POINT ( 'NONE', #12744 ) ;
#7905=CARTESIAN_POINT ( 'NONE',  ( 0.4530287582269867386, -1.054472822262606968, 0.7183272867302393783 ) ) ;
#7907=CARTESIAN_POINT ( 'NONE',  ( 0.4001462373468676614, -1.136645747884092783, 0.4743659635294404930 ) ) ;
#7910=CARTESIAN_POINT ( 'NONE',  ( 0.1275181119306449395, -0.9857185180080264564, 0.6886633007003241103 ) ) ;
#7911=ORIENTED_EDGE ( 'NONE', *, *, #18438, .T. ) ;
#7916=CARTESIAN_POINT ( 'NONE',  ( 0.4738421150388607006, -1.247722671731417821, 0.6281918974308814407 ) ) ;
#7919=CARTESIAN_POINT ( 'NONE',  ( 0.1991581284650917050, -0.9215239498232444815, 0.3071336240427082753 ) ) ;
#7920=ORIENTED_EDGE ( 'NONE', *, *, #27560, .F. ) ;
#7925=CARTESIAN_POINT ( 'NONE',  ( 0.4122251433979338686, -1.572231246218684264, 0.7147155659639160552 ) ) ;
#7926=CARTESIAN_POINT ( 'NONE',  ( 0.08908196101633601705, -0.5887339626514037638, 0.07194673905522250279 ) ) ;
#7931=ORIENTED_EDGE ( 'NONE', *, *, #39069, .T. ) ;
#7934=CARTESIAN_POINT ( 'NONE',  ( 0.1193505310152233323, -0.5488392675763952289, 0.1457185332388695187 ) ) ;
#7935=ORIENTED_EDGE ( 'NONE', *, *, #4932, .T. ) ;
#7936=CARTESIAN_POINT ( 'NONE',  ( 0.3120958685407360100, -1.764432100645553891, 0.5326512185289294932 ) ) ;
#7938=AXIS2_PLACEMENT_3D ( 'NONE', #37184, #18882, #15587 ) ;
#7940=CARTESIAN_POINT ( 'NONE',  ( 0.2251050016842718604, -1.237046649890439554, 0.5037622129130751025 ) ) ;
#7943=B_SPLINE_CURVE_WITH_KNOTS ( 'NONE', 3,
 ( #21547, #6073, #15352, #34067 ),
 .UNSPECIFIED., .F., .F.,
 ( 4, 4 ),
 ( 0.003748439525988024514, 0.004404120170952528258 ),
 .UNSPECIFIED. ) ;
#7945=CARTESIAN_POINT ( 'NONE',  ( 0.4910703360858987843, -1.094828989692585575, 0.8654809858424608038 ) ) ;
#7953=CARTESIAN_POINT ( 'NONE',  ( 0.5650875398404070493, -1.618990993344825435, 0.5674743467620558812 ) ) ;
#7956=CARTESIAN_POINT ( 'NONE',  ( 0.3098984767712536503, -1.765718780359063267, 0.5682417262808785452 ) ) ;
#7964=CARTESIAN_POINT ( 'NONE',  ( 0.4412150601155225282, -1.069325677854658041, 0.5182417262812423209 ) ) ;
#7969=CARTESIAN_POINT ( 'NONE',  ( 0.4165761542997364897, -1.741708882820427906, 0.5182417262812423209 ) ) ;
#7972=CARTESIAN_POINT ( 'NONE',  ( 0.4551179479963137764, -1.228091501103429461, 0.7657079515373070855 ) ) ;
#7974=ORIENTED_EDGE ( 'NONE', *, *, #241, .T. ) ;
#7975=CARTESIAN_POINT ( 'NONE',  ( 0.2067623920994063613, -0.8133810345767992223, 0.3693416354660131184 ) ) ;
#7977=ORIENTED_EDGE ( 'NONE', *, *, #13758, .F. ) ;
#7979=CARTESIAN_POINT ( 'NONE',  ( 0.02381802225809039400, -0.5521116243553858549, 0.2426350268205515748 ) ) ;
#7980=CARTESIAN_POINT ( 'NONE',  ( 0.7047269641172427823, -1.495525204603480596, 0.5167404914704131214 ) ) ;
#7981=CARTESIAN_POINT ( 'NONE',  ( 0.1768421950620408245, -0.4866590717709783354, 0.03254264443430439357 ) ) ;
#7982=CARTESIAN_POINT ( 'NONE',  ( 0.4091335057472371695, -1.131547141905885789, 0.4177417262808780229 ) ) ;
#7987=CARTESIAN_POINT ( 'NONE',  ( 0.1788443422962208706, -1.264928261278998711, 0.4182417262808777458 ) ) ;
#7989=CARTESIAN_POINT ( 'NONE',  ( 0.2682412565687398165, -1.183332610994965117, 0.7361391146594850055 ) ) ;
#7995=CARTESIAN_POINT ( 'NONE',  ( 0.2770095578784259605, -1.024149721892290810, 0.6102448670827070876 ) ) ;
#7999=PLANE ( 'NONE',  #2109 ) ;
#8006=CARTESIAN_POINT ( 'NONE',  ( 0.03041512172134077860, -1.119424412222147502, 0.6647272771665519997 ) ) ;
#8007=CARTESIAN_POINT ( 'NONE',  ( 0.3737684249951603865, -1.152107638635602171, 0.5492107935990235834 ) ) ;
#8010=CARTESIAN_POINT ( 'NONE',  ( 0.01207743823765780947, -0.4534980189049991339, 0.03415917635198321284 ) ) ;
#8016=CARTESIAN_POINT ( 'NONE',  ( 0.1889207857526494783, -0.5233380428592805389, 0.2298431039531494136 ) ) ;
#8020=CARTESIAN_POINT ( 'NONE',  ( 0.1345170253128575577, -0.5648217707619066497, 0.2174971669814429742 ) ) ;
#8021=CARTESIAN_POINT ( 'NONE',  ( -0.001494616128554601903, -0.8154047748197732481, 0.04990360719771039233 ) ) ;
#8024=CARTESIAN_POINT ( 'NONE',  ( 0.3416247111477876963, -1.170278351459675514, 0.4404859988295342088 ) ) ;
#8028=CARTESIAN_POINT ( 'NONE',  ( 0.2651531704851615157, -1.635780466096735219, 0.7914256539850866856 ) ) ;
#8034=CARTESIAN_POINT ( 'NONE',  ( 0.5479385918970316460, -1.628670924725093005, 0.5682417262808785452 ) ) ;
#8037=CARTESIAN_POINT ( 'NONE',  ( 0.08509544147734100783, -0.8123111742434817595, 0.1457185332388680477 ) ) ;
#8038=CARTESIAN_POINT ( 'NONE',  ( 0.05658279881179609228, -1.054191643581903426, 0.7314510373715901181 ) ) ;
#8040=CARTESIAN_POINT ( 'NONE',  ( 0.1392922804453227692, -0.7568856236203271859, 0.5828328295004829851 ) ) ;
#8041=CARTESIAN_POINT ( 'NONE',  ( 0.1161639400603292072, -0.5516103353077059790, 0.1797328180798098418 ) ) ;
#8042=CARTESIAN_POINT ( 'NONE',  ( 0.06217409799684354282, -1.272787436899851521, 0.6404467018060111538 ) ) ;
#8044=CARTESIAN_POINT ( 'NONE',  ( 0.06086249397365642300, -1.332142734742585821, 0.5449151288494504808 ) ) ;
#8046=CARTESIAN_POINT ( 'NONE',  ( 0.3862110256088813198, -1.731934476144515456, 0.4282538419479027803 ) ) ;
#8050=FACE_OUTER_BOUND ( 'NONE', #39718, .T. ) ;
#8051=CARTESIAN_POINT ( 'NONE',  ( 0.4367417526623164625, -1.230582192281711507, 0.5840196524529203126 ) ) ;
#8054=CARTESIAN_POINT ( 'NONE',  ( -0.002083146443013336215, -0.8967360763018585867, 0.1624439089914547774 ) ) ;
#8055=CARTESIAN_POINT ( 'NONE',  ( 0.2957689212018802527, -0.9454471935599602084, 0.5654756054326123271 ) ) ;
#8058=CARTESIAN_POINT ( 'NONE',  ( 0.2366026829857577063, -0.6283501033379368383, 0.5457308484972661633 ) ) ;
#8068=CARTESIAN_POINT ( 'NONE',  ( 0.08940845291349239221, -0.9873426107426247489, 0.8215244533732848353 ) ) ;
#8071=DIRECTION ( 'NONE',  ( 0.4999551463232372317, -0.8660512985181135770, 0.000000000000000000 ) ) ;
#8072=EDGE_LOOP ( 'NONE', ( #10156, #32032, #20482, #6645 ) ) ;
#8074=CARTESIAN_POINT ( 'NONE',  ( 0.5932568134822767680, -1.254512724160953940, 0.6928994325643027530 ) ) ;
#8078=ORIENTED_EDGE ( 'NONE', *, *, #36279, .F. ) ;
#8079=CARTESIAN_POINT ( 'NONE',  ( 0.06486042810549992599, -1.341249661891149803, 0.5682417262808776570 ) ) ;
#8082=CIRCLE ( 'NONE', #19901, 0.01000000000000002796 ) ;
#8086=CARTESIAN_POINT ( 'NONE',  ( 0.1263335340626541570, -0.7187389189354154162, 0.4672226359719474642 ) ) ;
#8088=CARTESIAN_POINT ( 'NONE',  ( 0.2933737728020890945, -1.643668813008566598, 0.9134582784372499153 ) ) ;
#8090=CARTESIAN_POINT ( 'NONE',  ( 0.1001591510775032695, -0.5752251226639683024, 0.2680392064541395891 ) ) ;
#8091=CARTESIAN_POINT ( 'NONE',  ( 0.2660355233482954440, -1.634181185541991210, 0.8113338639931253482 ) ) ;
#8092=CARTESIAN_POINT ( 'NONE',  ( 0.3178512907186139547, -1.645949601790900774, 0.6057417262800831592 ) ) ;
#8093=CARTESIAN_POINT ( 'NONE',  ( 0.04790779036325637508, -0.9421369883270767076, 0.2396295160170733851 ) ) ;
#8095=EDGE_LOOP ( 'NONE', ( #18921, #32820, #12196, #2534, #38687 ) ) ;
#8097=CARTESIAN_POINT ( 'NONE',  ( 0.1927624843354359963, -0.4933326792414792772, 0.2922951691234880189 ) ) ;
#8101=CARTESIAN_POINT ( 'NONE',  ( 0.07852099631351548703, -1.320155556401022334, 0.4758808093597276523 ) ) ;
#8103=CARTESIAN_POINT ( 'NONE',  ( 0.1093271622263137233, -1.419650973723309173, 0.5472839097051169777 ) ) ;
#8104=CARTESIAN_POINT ( 'NONE',  ( 0.3219050788564604137, -0.8784703629548025194, 0.6443316309767920247 ) ) ;
#8109=EDGE_CURVE ( 'NONE', #2485, #9135, #34876, .T. ) ;
#8110=CARTESIAN_POINT ( 'NONE',  ( 0.4330554116054934899, -1.226567635015945568, 0.6177703434090197065 ) ) ;
#8117=ORIENTED_EDGE ( 'NONE', *, *, #15028, .T. ) ;
#8118=CARTESIAN_POINT ( 'NONE',  ( 0.2909422066436382348, -0.9047456369702350232, 0.5718823244560541363 ) ) ;
#8120=FACE_OUTER_BOUND ( 'NONE', #3058, .T. ) ;
#8121=EDGE_CURVE ( 'NONE', #38403, #21612, #30938, .T. ) ;
#8123=CARTESIAN_POINT ( 'NONE',  ( 0.07727056149180543121, -0.9554077429465727134, 0.6485806625480800003 ) ) ;
#8124=ORIENTED_EDGE ( 'NONE', *, *, #22222, .T. ) ;
#8125=DIRECTION ( 'NONE',  ( 0.0001066307966871704452, -1.551735798909009237E-06, -0.9999999943137325431 ) ) ;
#8130=CARTESIAN_POINT ( 'NONE',  ( 0.3962101050479742703, -1.143265633725505159, 0.6995449155040951439 ) ) ;
#8135=CARTESIAN_POINT ( 'NONE',  ( 1.480025787077754007, -0.6872203660140440151, 0.1457185332388702959 ) ) ;
#8138=CARTESIAN_POINT ( 'NONE',  ( 0.06179390496056682419, -0.5638175360510637724, 0.2559820944390198694 ) ) ;
#8140=CARTESIAN_POINT ( 'NONE',  ( 0.08737269751878998236, -0.6956646054673948365, 0.02271064067933706646 ) ) ;
#8146=CARTESIAN_POINT ( 'NONE',  ( 0.5632903408051906924, -1.466070610373608529, 0.7198323889707046730 ) ) ;
#8155=CARTESIAN_POINT ( 'NONE',  ( 0.2036159742448276078, -1.249513165191289632, 0.4424631886055492291 ) ) ;
#8159=CARTESIAN_POINT ( 'NONE',  ( 0.3900547927747317067, -0.9231895138380423749, 0.8021268779562266138 ) ) ;
#8165=CARTESIAN_POINT ( 'NONE',  ( 0.5963566829781479228, -1.601993569060106148, 0.5937315688595193874 ) ) ;
#8166=CARTESIAN_POINT ( 'NONE',  ( 0.6909971427696186552, -1.441959902340269384, 0.5038514719706568279 ) ) ;
#8169=CARTESIAN_POINT ( 'NONE',  ( 0.3165986513250982903, -1.745708308064116920, 0.7545403346239585307 ) ) ;
#8173=CARTESIAN_POINT ( 'NONE',  ( 0.1585823774922599239, -1.275097463791165175, 0.5547567935354530411 ) ) ;
#8174=CARTESIAN_POINT ( 'NONE',  ( 0.4751248519516730884, -1.681100737592190031, 0.5628962907142390781 ) ) ;
#8175=AXIS2_PLACEMENT_3D ( 'NONE', #40227, #2800, #21544 ) ;
#8179=CARTESIAN_POINT ( 'NONE',  ( 0.4110292600630488513, -1.110406119314346407, 0.6168944177148723007 ) ) ;
#8181=CARTESIAN_POINT ( 'NONE',  ( 0.05560027925352286488, -1.335209592177159843, 0.5707417262808780478 ) ) ;
#8185=CARTESIAN_POINT ( 'NONE',  ( 0.5140872677725584206, -1.316639973194089430, 0.6836467266521880637 ) ) ;
#8187=EDGE_LOOP ( 'NONE', ( #4930, #17730, #26931, #18355 ) ) ;
#8188=CARTESIAN_POINT ( 'NONE',  ( 0.1897950977212392309, -0.7957416484119633759, 0.2611131357175326961 ) ) ;
#8190=ORIENTED_EDGE ( 'NONE', *, *, #5731, .T. ) ;
#8193=CARTESIAN_POINT ( 'NONE',  ( 0.3216690679530037622, -1.512854433007727595, 0.8542683157091821577 ) ) ;
#8195=CARTESIAN_POINT ( 'NONE',  ( 0.6967942517794997181, -1.491337617863137455, 0.4846308184134556218 ) ) ;
#8196=CARTESIAN_POINT ( 'NONE',  ( 0.1147432612534843299, -0.4767836783747688711, 0.02771918083247308998 ) ) ;
#8203=CARTESIAN_POINT ( 'NONE',  ( 0.2494758918748508081, -1.148756062240769094, 0.7454965398781205899 ) ) ;
#8209=DIRECTION ( 'NONE',  ( 0.4999551463232372317, -0.8660512985181135770, 0.000000000000000000 ) ) ;
#8211=CARTESIAN_POINT ( 'NONE',  ( 0.3582174290906561254, -1.160725967328684050, 0.4391212506391878323 ) ) ;
#8216=CARTESIAN_POINT ( 'NONE',  ( 0.06487940854082643871, -1.341257406870441482, 0.5704520789807075998 ) ) ;
#8219=DIRECTION ( 'NONE',  ( -0.08441620754382399283, 0.8288655086680465356, -0.5530423785248094193 ) ) ;
#8221=CARTESIAN_POINT ( 'NONE',  ( 1.547079322592971316E-05, -0.5132440025857009092, -0.04957435040516270514 ) ) ;
#8224=CARTESIAN_POINT ( 'NONE',  ( 0.01078865671634213208, -0.5493393610439523123, 0.4732676844958878526 ) ) ;
#8227=VERTEX_POINT ( 'NONE', #7574 ) ;
#8228=CARTESIAN_POINT ( 'NONE',  ( 0.1822455911001416018, -0.4993161093247819315, 0.08306801194993664039 ) ) ;
#8232=CARTESIAN_POINT ( 'NONE',  ( 0.008756164835982942901, -0.6361421079842972670, -0.004039510205650067784 ) ) ;
#8236=CARTESIAN_POINT ( 'NONE',  ( 0.3029314534210234000, -0.8887505455264903542, 0.8055725980740405801 ) ) ;
#8238=ADVANCED_FACE ( 'NONE', ( #17046 ), #1400, .T. ) ;
#8244=EDGE_CURVE ( 'NONE', #36413, #31881, #11242, .T. ) ;
#8246=CARTESIAN_POINT ( 'NONE',  ( 0.5654596793231598806, -1.618818539163461301, 0.5682417262808788783 ) ) ;
#8250=CARTESIAN_POINT ( 'NONE',  ( 0.01172053995184539968, -0.7041130843534951778, -0.1131832977452343625 ) ) ;
#8252=CARTESIAN_POINT ( 'NONE',  ( 0.02390224293416483292, -0.9197127835399234730, 0.5774128202788778585 ) ) ;
#8253=CARTESIAN_POINT ( 'NONE',  ( 0.1429797709452751697, -0.7177769904828193992, 0.5286191414039091985 ) ) ;
#8254=CARTESIAN_POINT ( 'NONE',  ( 0.1854231476496841502, -0.8287896031818428044, 0.1136188594679051200 ) ) ;
#8256=DIRECTION ( 'NONE',  ( 0.4999551463232382309, -0.8660512985181127998, 1.639108796198564242E-15 ) ) ;
#8262=CARTESIAN_POINT ( 'NONE',  ( 0.3951584779506375211, -1.106112822567272280, 0.6036734362241392704 ) ) ;
#8263=CARTESIAN_POINT ( 'NONE',  ( 0.4374457586934000219, -1.230173854262892830, 0.5848115461677827476 ) ) ;
#8268=CARTESIAN_POINT ( 'NONE',  ( 0.003124719664520433666, -0.5686731593868930013, 0.1115160683991335139 ) ) ;
#8269=CARTESIAN_POINT ( 'NONE',  ( 0.4929465528686915454, -1.082715557938388029, 0.5653634300333020279 ) ) ;
#8270=CARTESIAN_POINT ( 'NONE',  ( 0.06486303625374841009, -1.341253824744560452, 0.5682723891644412273 ) ) ;
#8272=CARTESIAN_POINT ( 'NONE',  ( 0.6100913662829361428, -1.289225211610094401, 0.8693105457786516332 ) ) ;
#8281=VERTEX_POINT ( 'NONE', #10882 ) ;
#8283=CARTESIAN_POINT ( 'NONE',  ( 0.01410851223904770191, -0.6557637843359752639, 0.5002397451194796618 ) ) ;
#8284=CARTESIAN_POINT ( 'NONE',  ( 0.1294052168131209490, -0.5750714970858038511, 0.2516657636888773864 ) ) ;
#8285=CARTESIAN_POINT ( 'NONE',  ( 0.3361824506367084853, -1.634927130874744172, 0.4198097592826174340 ) ) ;
#8288=CARTESIAN_POINT ( 'NONE',  ( 0.3296415583488681023, -1.757109584657895907, 0.4726979017080325529 ) ) ;
#8289=CARTESIAN_POINT ( 'NONE',  ( 0.2968044078846433509, -0.7977486025825716309, 0.6363905851602879027 ) ) ;
#8295=CARTESIAN_POINT ( 'NONE',  ( 0.2899202446100145880, -1.199999382632172207, 0.4182417262798592827 ) ) ;
#8301=CARTESIAN_POINT ( 'NONE',  ( 0.1024053258065399929, -0.7484833377281776556, 0.3519811350192522670 ) ) ;
#8302=CARTESIAN_POINT ( 'NONE',  ( 0.1137005432816620976, -0.9903671524150755578, 0.9280563831205882463 ) ) ;
#8303=CARTESIAN_POINT ( 'NONE',  ( 0.1413657729933081586, -0.7268754190988079289, 0.5433663266485807553 ) ) ;
#8304=CARTESIAN_POINT ( 'NONE',  ( 0.3291103594116518427, -1.757007705610827086, 0.4729914256106402259 ) ) ;
#8306=CARTESIAN_POINT ( 'NONE',  ( 0.09713336615736777035, -1.305095304553262947, 0.5932891525630709095 ) ) ;
#8311=CARTESIAN_POINT ( 'NONE',  ( 0.3960999722200455042, -0.9602260210612366675, 0.7467566221574177820 ) ) ;
#8313=DIRECTION ( 'NONE',  ( 0.4999551463232372317, -0.8660512985181135770, 0.000000000000000000 ) ) ;
#8314=CARTESIAN_POINT ( 'NONE',  ( 0.4687176343584499305, -1.116552776705967531, 0.5688755853127047679 ) ) ;
#8315=DIRECTION ( 'NONE',  ( 1.000000000000000000, 0.000000000000000000, 0.000000000000000000 ) ) ;
#8318=CARTESIAN_POINT ( 'NONE',  ( 0.3132663380321701885, -1.175085214117265187, 0.5020501538770495431 ) ) ;
#8319=CARTESIAN_POINT ( 'NONE',  ( 0.6161168803315352216, -1.293011444959033973, 0.6214722141784767562 ) ) ;
#8332=CARTESIAN_POINT ( 'NONE',  ( 0.3247324306352935563, -1.759421949583405365, 0.4854534786567430427 ) ) ;
#8334=CARTESIAN_POINT ( 'NONE',  ( 0.06214721934179495005, -0.9131463676375551897, 0.5762997311010702450 ) ) ;
#8335=VERTEX_POINT ( 'NONE', #27120 ) ;
#8336=CARTESIAN_POINT ( 'NONE',  ( 0.1614573949321077284, -0.7569534866611321577, 0.1932149833450299559 ) ) ;
#8340=CARTESIAN_POINT ( 'NONE',  ( 0.4143713219839447182, -1.164911342593115240, 0.6919132719734564230 ) ) ;
#8342=DIRECTION ( 'NONE',  ( -0.9750333724971924632, 0.000000000000000000, -0.2220583763715098247 ) ) ;
#8343=EDGE_CURVE ( 'NONE', #17938, #27730, #31736, .T. ) ;
#8347=CARTESIAN_POINT ( 'NONE',  ( 0.08099778489142739346, -1.320264099216433173, 0.5551538849635637707 ) ) ;
#8350=CARTESIAN_POINT ( 'NONE',  ( 0.4352560923565332307, -1.548119695606142265, 0.7308037930344200017 ) ) ;
#8351=CARTESIAN_POINT ( 'NONE',  ( 0.06739980034908768514, -0.6389769636022399890, 0.005946806555783851894 ) ) ;
#8357=CARTESIAN_POINT ( 'NONE',  ( 0.5739587120820951460, -1.480387852324690057, 0.6855574093161642679 ) ) ;
#8358=CARTESIAN_POINT ( 'NONE',  ( 0.3352639066339355711, -1.762270631036203516, 0.5634487449406784254 ) ) ;
#8360=CARTESIAN_POINT ( 'NONE',  ( 0.6435666421574203211, -1.544684378243342593, 0.4182417262808776903 ) ) ;
#8361=CARTESIAN_POINT ( 'NONE',  ( 0.2053975955868210246, -1.248453031607742458, 0.4579970562924251531 ) ) ;
#8364=CARTESIAN_POINT ( 'NONE',  ( 0.2064087850599171381, -0.5517209573913892662, 0.4235422224703019323 ) ) ;
#8365=CARTESIAN_POINT ( 'NONE',  ( 0.07473354200822579507, -1.325658353975272208, 0.4791244499874081075 ) ) ;
#8369=CARTESIAN_POINT ( 'NONE',  ( 0.6275535865577528405, -1.582657856101383098, 0.6191178097732258356 ) ) ;
#8370=CARTESIAN_POINT ( 'NONE',  ( 0.5943505786846313699, -1.599619272918265445, 0.4280844162099405881 ) ) ;
#8372=EDGE_CURVE ( 'NONE', #31015, #23886, #29795, .T. ) ;
#8374=CARTESIAN_POINT ( 'NONE',  ( 0.1587139193017044758, -1.140357826010188314, 1.006504499293092714 ) ) ;
#8376=CARTESIAN_POINT ( 'NONE',  ( 0.1457989028442929769, -1.282480442862664161, 0.5557458682560576513 ) ) ;
#8377=CARTESIAN_POINT ( 'NONE',  ( 0.3048570497350418518, -1.756853555320991189, 0.5694442476137144826 ) ) ;
#8378=B_SPLINE_SURFACE_WITH_KNOTS ( 'NONE', 3, 3, ( 
 ( #20394, #14215, #29450, #35613, #20815, #4945, #20200, #4136, #29249, #7823, #26575, #39308, #38897, #32725, #7414, #1292, #20605, #16702, #26783, #13613, #23296, #19992, #36018, #23503, #29645, #11329, #32922, #4345, #36213, #16907, #4732, #26363, #10725, #35822, #1487, #7635, #23899, #4532, #17097, #14005, #39114, #10942, #14402, #17302, #29856, #11129, #23688, #8028, #33136, #17511, #30060, #1890, #26965, #21204, #37243, #5760, #18116, #9244, #27180, #15029, #18318, #17695, #30860, #11738, #21429, #15224, #30241, #33741, #24295, #39710, #24110, #27579, #24498 ),
 ( #11547, #33333, #5552, #2290, #11933, #2071, #14608, #5954, #27991, #2682, #36634, #34145, #39920, #30670, #2489, #8438, #8631, #40105, #27782, #40320, #21004, #24712, #9059, #21621, #8850, #18514, #33524, #12147, #15440, #33960, #5333, #37030, #31069, #2889, #40530, #17895, #5142, #12350, #24908, #37432, #30462, #14829, #27396, #36817, #22646, #31285, #28986, #25935, #25515, #850, #13360, #3097, #9458, #470, #16259, #6979, #28598, #6560, #32082, #16054, #19550, #28187, #28387, #28796, #656, #34960, #52, #25710, #6768, #38241, #18939, #19137, #10072 ),
 ( #19346, #6165, #31884, #256, #9860, #3702, #18728, #9670, #12753, #15640, #12544, #3494, #12967, #3889, #25099, #21820, #37638, #31474, #37855, #31676, #22432, #34753, #3281, #35176, #22037, #38047, #22239, #13146, #16443, #38456, #25315, #34351, #34562, #6371, #15836, #33088, #36170, #26525, #1441, #4084, #16653, #13572, #29202, #7165, #1846, #1062, #17054, #17254, #10674, #13955, #30016, #38653, #35774, #23248, #39065, #35564, #10471, #29407, #26138, #16865, #22856, #26736, #14361, #26925, #35375, #39266, #20555, #14168, #10891, #20354, #7363, #23039, #10291 ),
 ( #19940, #1252, #19733, #11089, #32266, #32474, #4300, #23649, #4897, #7979, #23463, #32875, #13754, #26319, #38845, #17463, #7584, #20159, #32687, #35979, #4492, #4685, #29600, #7785, #29808, #1649, #15175, #2837, #36983, #36375, #17852, #20766, #30621, #18069, #24250, #5902, #2446, #33289, #30817, #39662, #14983, #30202, #8193, #15389, #36772, #5098, #18464, #2033, #33482, #8585, #21160, #11283, #9017, #27345, #31017, #39458, #23850, #27131, #17656, #14564, #11499, #24062, #36589, #39875, #2638, #11884, #33690, #8391, #20962, #5504, #24450, #5288, #8804 ),
 ( #27732, #27537, #18275, #30414, #2245, #40058, #14784, #21382, #33918, #11695, #5717, #40267, #12103, #24669, #37197, #21578, #34100, #22591, #419, #37386, #28747, #34510, #12695, #25258, #21767, #3237, #37800, #22382, #25468, #34301, #19291, #3650, #9619, #16212, #6108, #9405, #18675, #38002, #25049, #12310, #25662, #609, #31835, #15599, #22193, #31238, #9811, #27946, #34708, #10, #15997, #15783, #13102, #12913, #6513, #3835, #3054, #19085, #34909, #24866, #6717, #6320, #38196, #28145, #21982, #28333, #18893, #12492, #37582, #31624, #3439, #10021, #31431 ),
 ( #204, #28544, #35122, #9199, #6926, #19498, #32028, #40484, #25880, #17204, #22984, #1201, #13704, #10234, #32425, #26271, #10842, #13898, #22803, #7739, #32823, #38788, #4629, #35325, #38603, #7115, #26470, #13522, #800, #14119, #29749, #20303, #4034, #10620, #19681, #39006, #16392, #23195, #29144, #4443, #1592, #26691, #32216, #35719, #10422, #1010, #17005, #39224, #11044, #7925, #35931, #20502, #26084, #19888, #35503, #29548, #7532, #23417, #23604, #32638, #36118, #16599, #1386, #33034, #28933, #7311, #20107, #13307, #38398, #4247, #16815, #29359, #36935 ),
 ( #12051, #36731, #26879, #8747, #5053, #8539, #36319, #14320, #21532, #2190, #1804, #24609, #8138, #39609, #30364, #14729, #17410, #15123, #33440, #37147, #8959, #4838, #33246, #39411, #20715, #17614, #29970, #11229, #23801, #30161, #21109, #1988, #14511, #27077, #11445, #24207, #40013, #30766, #11648, #27296, #27681, #39824, #2585, #24011, #36538, #11836, #24396, #18010, #8350, #21325, #30571, #33862, #20920, #33637, #5665, #5248, #5450, #17801, #2396, #14933, #40216, #27489, #18220, #34857, #9767, #25205, #12866, #40627, #34052, #31386, #3001, #3387, #147 ),
 ( #9352, #3191, #22148, #6272, #15549, #6666, #2790, #18846, #21931, #15731, #34458, #28281, #37527, #12640, #15338, #37748, #9570, #16167, #19242, #34664, #6467, #27894, #40431, #37338, #12259, #30964, #25615, #24816, #19037, #362, #31568, #15944, #13064, #21713, #28488, #25427, #37956, #18626, #34247, #12443, #9150, #24996, #5850, #22336, #38146, #9970, #18411, #31784, #3598, #28704, #568, #6059, #31183, #28099, #26645, #23361, #38558, #14069, #6873, #26223, #4195, #16959, #16550, #10381, #16354, #19642, #38960, #39176, #20053, #19448, #959, #3798, #13658 ),
 ( #38745, #28889, #13850, #22749, #10571, #10789, #750, #3987, #13255, #32586, #32176, #31986, #20259, #35882, #26423, #10180, #7262, #25826, #4401, #22540, #16762, #35276, #23145, #7694, #32781, #38345, #19836, #29093, #7071, #35674, #4582, #17154, #35067, #1343, #13469, #26036, #22944, #35461, #7476, #32371, #29503, #29703, #1549, #29310, #1158, #36690, #33806, #11604, #26837, #30308, #27243, #14886, #33395, #39366, #23559, #2346, #11791, #30722, #27445, #11186, #39555, #39774, #24349, #20449, #18168, #15081, #14674, #2543, #27635, #32983, #23746, #2135, #5397 ),
 ( #21270, #11389, #11001, #36077, #7877, #36268, #4790, #1761, #14273, #17364, #29919, #23960, #39970, #24166, #36489, #8090, #20666, #5202, #8496, #33200, #21060, #30114, #17960, #5005, #17572, #8303, #1945, #14461, #27028, #17756, #33587, #8691, #20874, #30519, #36883, #5612, #15500, #37483, #28238, #12400, #9104, #313, #8907, #24954, #28054, #9304, #40580, #21882, #2949, #34411, #21484, #31344, #18793, #22290, #25377, #15687, #3149, #6226, #9722, #102, #37910, #5809, #6010, #6419, #34619, #12599, #18368, #3332, #25158, #15895, #37290, #37698, #28439 ),
 ( #9521, #24561, #22097, #18575, #18987, #30915, #34199, #31519, #31133, #34005, #2739, #12818, #34805, #6609, #15284, #40165, #37092, #21670, #19190, #31729, #3549, #16118, #11995, #27843, #40382, #12207, #24767, #25990, #3940, #38514, #32137, #10345, #38097, #19786, #7218, #10736, #13809, #4143, #32326, #22487, #35012, #31941, #6825, #25569, #20212, #19407, #35424, #35624, #29045, #16713, #7648, #16314, #13415, #913, #29259, #13206, #28849, #7035, #3761, #35234, #525, #4354, #32737, #4544, #13020, #16915, #38908, #32536, #1111, #38707, #25777, #709, #28656 ),
 ( #13619, #29460, #38296, #26184, #23311, #10527, #10128, #23098, #7428, #1304, #22906, #22703, #9916, #20004, #26379, #19604, #35835, #16502, #4958, #33926, #18472, #26591, #24873, #21779, #21389, #37395, #9207, #39129, #4743, #36990, #12110, #2846, #24457, #14991, #24676, #15183, #23515, #9024, #34107, #27544, #5912, #36030, #39320, #7834, #27740, #14228, #1502, #15395, #31024, #21585, #17314, #2454, #10953, #40276, #17109, #11894, #29871, #5726, #27953, #40492, #20405, #40065, #11140, #1710, #18281, #12318, #34308, #29658, #37204, #14016, #26793, #20616, #23699 ),
 ( #32938, #36227, #30825, #8810, #8041, #33152, #18076, #30629, #2645, #22599, #10243, #3659, #3063, #25267, #28153, #38010, #25475, #31634, #13314, #9820, #17, #38206, #6328, #22391, #37593, #15607, #22811, #3449, #12503, #25886, #9414, #211, #16007, #28553, #18684, #16400, #34715, #38405, #6118, #31245, #34518, #25059, #21992, #18902, #31439, #3246, #6521, #10028, #19300, #426, #15793, #28343, #12923, #31842, #12705, #16219, #37809, #616, #9627, #22199, #19094, #34919, #6725, #28756, #13110, #25671, #3844, #35131, #6933, #19506, #32036, #28941, #806 ),
 ( #7934, #29976, #7746, #4042, #36125, #1209, #20116, #32646, #29153, #10630, #1018, #32223, #26888, #13528, #1396, #1600, #35727, #26478, #14326, #22991, #4450, #7540, #39013, #19895, #35513, #13711, #26094, #26279, #7122, #11052, #39418, #11237, #19689, #23611, #4845, #39231, #10849, #4637, #32431, #38609, #35333, #20509, #23203, #16605, #10431, #23423, #17014, #29757, #29367, #29555, #7318, #4256, #33043, #16822, #32832, #38797, #13905, #35940, #20309, #17213, #14127, #1811, #26698, #17418, #15131, #24021, #14943, #14518, #33251, #40443, #21119, #20722, #30972 ),
 ( #8967, #30581, #8547, #34060, #18019, #21542, #30169, #30372, #30776, #18229, #36943, #1997, #27692, #8757, #40225, #20926, #33648, #12060, #27903, #40021, #5061, #21334, #2798, #5860, #11844, #27084, #24622, #37156, #27495, #2593, #2198, #23811, #5458, #33447, #33870, #2404, #17621, #36328, #36738, #5254, #24409, #39619, #11452, #18417, #15346, #5675, #36546, #8146, #14739, #8357, #17811, #27304, #39833, #11654, #24214, #3397, #6068, #25434, #9774, #155, #22347, #18635, #37537, #9157, #15740, #18853, #12650, #31396, #28290, #6282, #25212, #21722, #9579 ),
 ( #34670, #22156, #34254, #31192, #3010, #15558, #28106, #13072, #40634, #37758, #12876, #3198, #6477, #576, #12453, #19045, #31577, #15952, #25004, #9360, #21940, #34467, #28498, #12266, #34864, #25623, #24823, #372, #6673, #16175, #19252, #37965, #31792, #3609, #28713, #37347, #9090, #24333, #40565, #33377, #11979, #30707, #2722, #2330, #36860, #2117, #5380, #24751, #12384, #5795, #5180, #27431, #30284, #40148, #27619, #33788, #15484, #24544, #14651, #40361, #8479, #37074, #39755, #17734, #24939, #5595, #27220, #28037, #11587, #14870, #18153, #2529, #20854 ),
 ( #5993, #24149, #39955, #15268, #27824, #21466, #36671, #12191, #33990, #37273, #17942, #15067, #21656, #8284, #8893, #21040, #18353, #33565, #34183, #30900, #30499, #18559, #31114, #2929, #11775, #8676, #21252, #34789, #6405, #6807, #3533, #31327, #13398, #9706, #18972, #16098, #6206, #18775, #10112, #6593, #31925, #34998, #3133, #28835, #13187, #19174, #25757, #15673, #31505, #28220, #19388, #34602, #21866, #35218, #38282, #693, #25143, #22275, #87, #3743, #37467, #31715, #9501, #25553, #22685, #7019, #12581, #28640, #3314, #22079, #38082, #19584, #32120 ),
 ( #16297, #15878, #37682, #896, #3924, #12797, #29027, #34393, #511, #13005, #16482, #28425, #25360, #298, #37895, #9287, #9900, #22471, #22889, #4337, #7202, #17089, #4524, #10718, #33129, #29638, #19768, #17294, #26167, #1479, #16692, #35408, #1881, #23289, #32306, #4937, #29239, #19983, #35812, #7626, #38497, #36207, #13790, #17504, #30053, #25972, #13605, #4126, #1096, #38690, #10327, #10507, #26357, #29849, #39106, #20193, #23078, #35604, #32718, #10932, #7405, #23495, #16898, #20388, #32515, #29440, #38887, #1284, #13997, #26569, #36011, #7817, #23681 ),
 ( #32915, #4725, #1689, #14207, #26773, #39302, #11122, #20596, #8020, #25387, #9927, #28665, #22496, #16126, #35022, #22107, #38108, #22915, #6833, #10353, #18997, #19199, #19612, #7043, #25785, #31530, #16513, #38307, #29053, #9729, #19414, #923, #16723, #28858, #34626, #10139, #32335, #38521, #717, #3344, #13428, #25999, #3768, #32145, #31740, #12606, #31949, #22299, #22711, #16321, #6427, #29270, #25578, #34815, #13218, #15902, #28448, #4156, #35243, #7229, #37706, #35431, #3558, #3952, #19798, #321, #533, #25166, #9528, #12826, #37919, #6620, #13030 ) ),
 .UNSPECIFIED., .F., .F., .F.,
 ( 4, 3, 3, 3, 3, 3, 4 ),
 ( 4, 3, 3, 3, 3, 3, 3, 3, 3, 3, 3, 3, 3, 3, 3, 3, 3, 3, 3, 3, 3, 3, 3, 3, 4 ),
 ( 0.01801207478348941515, 0.2164687590774609371, 0.4149254433714324453, 0.6133821276654038979, 0.7126104698123896242, 0.7622246408858825983, 0.8118388119593754615 ),
 ( 2.187425721392353805E-15, 0.01572090919976749240, 0.03144181839953279906, 0.04716272759929809877, 0.05502318219918075209, 0.06288363679906340542, 0.09432545519859400485, 0.1257672735981246182, 0.1886509103971858448, 0.2515345471962470714, 0.3773018207943694691, 0.5030690943924919223, 0.6288363679906143755, 0.6917200047896755466, 0.7546036415887367177, 0.8174872783877979998, 0.8803709151868591709, 0.9432545519859203420, 0.9746963703854509831, 0.9904172795852163036, 0.9982777341850990194, 0.9992602910100844005, 1.000242847835069782, 1.002207961485040322, 1.006138188784981624 ),
 .UNSPECIFIED. ) ;
#8381=CARTESIAN_POINT ( 'NONE',  ( 0.3965913301904479549, -1.111811593118468222, 0.6217369508112342569 ) ) ;
#8383=CARTESIAN_POINT ( 'NONE',  ( 0.5289571426068226945, -1.341546719958805367, 0.6404369235087098433 ) ) ;
#8386=CARTESIAN_POINT ( 'NONE',  ( 0.5123549971852071616, -1.116020584419624928, 0.5891410297636010540 ) ) ;
#8391=CARTESIAN_POINT ( 'NONE',  ( 0.3559890658834663490, -1.622350306201388648, 0.5721008954271108449 ) ) ;
#8392=CARTESIAN_POINT ( 'NONE',  ( 0.7062469264261600488, -1.498219618710284307, 0.5157970235707075579 ) ) ;
#8393=CARTESIAN_POINT ( 'NONE',  ( 0.1883394337541199892, -0.5195054202416713451, 0.1487585982833818932 ) ) ;
#8394=CYLINDRICAL_SURFACE ( 'NONE', #35241, 0.03749999999977545601 ) ;
#8399=CARTESIAN_POINT ( 'NONE',  ( 0.4679778500672936992, -1.237826332153874942, 0.6057417262809768888 ) ) ;
#8402=CARTESIAN_POINT ( 'NONE',  ( 0.1620457668995331502, -0.9696402434604897147, 0.6787910925089855052 ) ) ;
#8408=CARTESIAN_POINT ( 'NONE',  ( 0.3700970165061411854, -1.093180069723885151, 0.6366904215209722162 ) ) ;
#8412=CARTESIAN_POINT ( 'NONE',  ( 0.008926059106093127415, -1.005466151381485762, 0.5191422350400326513 ) ) ;
#8414=CARTESIAN_POINT ( 'NONE',  ( 0.4598481105376261979, -1.136922751769048112, 0.4503496864651998499 ) ) ;
#8420=CARTESIAN_POINT ( 'NONE',  ( 0.0004848065072079743576, -0.4386563779232509064, 0.1504137895485508913 ) ) ;
#8422=CARTESIAN_POINT ( 'NONE',  ( 0.09031319398383846897, -0.9021502138935498794, 0.8729315218264226406 ) ) ;
#8423=B_SPLINE_CURVE_WITH_KNOTS ( 'NONE', 3,
 ( #1528, #35861, #11367, #4562 ),
 .UNSPECIFIED., .F., .F.,
 ( 4, 4 ),
 ( 0.01056310462781991956, 0.01080186441643053545 ),
 .UNSPECIFIED. ) ;
#8427=CARTESIAN_POINT ( 'NONE',  ( 0.1876095839365586326, -1.270310460104812966, 0.4182417262808778013 ) ) ;
#8433=CARTESIAN_POINT ( 'NONE',  ( 0.007143729570262430731, -0.7929765756790790876, 0.02764597234640707793 ) ) ;
#8434=ORIENTED_EDGE ( 'NONE', *, *, #4618, .T. ) ;
#8435=ORIENTED_EDGE ( 'NONE', *, *, #28525, .T. ) ;
#8438=CARTESIAN_POINT ( 'NONE',  ( 2.342671343675246831E-07, -0.5622830454464696759, 0.2845663875592439052 ) ) ;
#8440=CARTESIAN_POINT ( 'NONE',  ( 0.1187585920567054698, -1.268575696611346837, 0.6205308943225873453 ) ) ;
#8445=VERTEX_POINT ( 'NONE', #38835 ) ;
#8446=CARTESIAN_POINT ( 'NONE',  ( 0.01136143083286298566, -0.9375195846693863411, 0.07874446343318208807 ) ) ;
#8447=CARTESIAN_POINT ( 'NONE',  ( 0.04816613662790503875, -1.016162693040883580, 0.7049299541483310394 ) ) ;
#8448=EDGE_CURVE ( 'NONE', #11376, #38403, #390, .T. ) ;
#8449=CARTESIAN_POINT ( 'NONE',  ( 0.2433285908094565408, -0.9051221626985026525, 0.7049880737946966347 ) ) ;
#8450=CARTESIAN_POINT ( 'NONE',  ( 0.1873786129353195162, -0.6949979828772413493, 0.03410752346106595695 ) ) ;
#8454=CARTESIAN_POINT ( 'NONE',  ( 0.3985710665783231410, -1.718231302922667902, 0.4257489112140997456 ) ) ;
#8455=ADVANCED_FACE ( 'NONE', ( #24438 ), #24655, .T. ) ;
#8459=CARTESIAN_POINT ( 'NONE',  ( 0.4602167293986741958, -1.115147919679363220, 0.5809538542335968003 ) ) ;
#8460=CARTESIAN_POINT ( 'NONE',  ( 0.4358858445580117702, -1.231077702336109247, 0.5834295217759662977 ) ) ;
#8462=B_SPLINE_CURVE_WITH_KNOTS ( 'NONE', 3,
 ( #3019, #2600, #18642, #12274, #37354, #21127, #12459, #9166, #31202, #15139, #25013, #27701, #12068, #5867, #37546, #30378, #9367, #33654 ),
 .UNSPECIFIED., .F., .F.,
 ( 4, 2, 2, 2, 2, 2, 2, 2, 4 ),
 ( 0.006166307077309264237, 0.006694450257964496345, 0.007222593438619729321, 0.007750736619274962297, 0.008278879799930194405, 0.008807022980585426514, 0.009335166161240658622, 0.009863309341895892465, 0.01039145252255112457 ),
 .UNSPECIFIED. ) ;
#8464=CARTESIAN_POINT ( 'NONE',  ( -8.537024980200822558E-17, -0.6872203660140405734, 0.09557912180100291977 ) ) ;
#8465=CARTESIAN_POINT ( 'NONE',  ( 0.3924682913416943086, -1.027586590250060272, 0.6289202682814357681 ) ) ;
#8466=CARTESIAN_POINT ( 'NONE',  ( 0.03203312987340298235, -0.9921091887597466297, 0.6716006140561699977 ) ) ;
#8468=CARTESIAN_POINT ( 'NONE',  ( 0.4910703360858987843, -1.094828989692585575, 0.8654809858424608038 ) ) ;
#8469=ADVANCED_FACE ( 'NONE', ( #15161 ), #36971, .T. ) ;
#8473=FACE_OUTER_BOUND ( 'NONE', #13616, .T. ) ;
#8478=CARTESIAN_POINT ( 'NONE',  ( 0.1655410750827681077, -1.289410180641110459, 0.9375906627650165692 ) ) ;
#8479=CARTESIAN_POINT ( 'NONE',  ( 0.5879879495906505937, -1.491234220313641057, 0.5743657966556454664 ) ) ;
#8483=CARTESIAN_POINT ( 'NONE',  ( 0.6161168803315352216, -1.293011444959033973, 0.6214722141784767562 ) ) ;
#8493=DIRECTION ( 'NONE',  ( 0.9998941247116547304, -0.01455087607601020412, 0.0001066420868422379633 ) ) ;
#8494=CARTESIAN_POINT ( 'NONE',  ( 0.09018131941781912242, -0.7099448699386352590, 0.2428910566028353035 ) ) ;
#8495=CARTESIAN_POINT ( 'NONE',  ( 0.3049302094162430476, -1.696219588324320959, 0.8439175857698040240 ) ) ;
#8496=CARTESIAN_POINT ( 'NONE',  ( 0.1049909493019218765, -0.6021604844197550044, 0.3340894142283440393 ) ) ;
#8497=CARTESIAN_POINT ( 'NONE',  ( -0.0001978441549465614934, -0.7095828240749427751, -0.02101536200760643555 ) ) ;
#8498=CARTESIAN_POINT ( 'NONE',  ( 0.1712463865401376573, -1.267487284506117140, 0.5682417262808779901 ) ) ;
#8499=ORIENTED_EDGE ( 'NONE', *, *, #8517, .T. ) ;
#8502=DIRECTION ( 'NONE',  ( -0.7798479508145914618, 0.000000000000000000, -0.6259689877384361223 ) ) ;
#8503=B_SPLINE_CURVE_WITH_KNOTS ( 'NONE', 3,
 ( #8092, #14072, #17367, #32588, #1345, #35676, #11003, #39368, #36079, #14463, #38962, #23363 ),
 .UNSPECIFIED., .F., .F.,
 ( 4, 2, 2, 2, 2, 4 ),
 ( 0.000000000000000000, 0.0001072734482993500222, 0.0002145468965987000444, 0.0004290937931974111476, 0.0008581875863948205604, 0.001716375172789631580 ),
 .UNSPECIFIED. ) ;
#8504=CARTESIAN_POINT ( 'NONE',  ( 0.5757129296766062554, -1.349865815820367354, 0.8829375841553319670 ) ) ;
#8505=EDGE_CURVE ( 'NONE', #40153, #39497, #16511, .T. ) ;
#8509=FACE_OUTER_BOUND ( 'NONE', #22704, .T. ) ;
#8511=CARTESIAN_POINT ( 'NONE',  ( 0.3208732210860777423, -1.182420994350418697, 0.5690449570999311923 ) ) ;
#8512=CARTESIAN_POINT ( 'NONE',  ( 0.2495280903959155583, -0.7823963870098056272, 0.5160991521645093005 ) ) ;
#8514=( BOUNDED_SURFACE ( )  B_SPLINE_SURFACE ( 3, 2, ( 
 ( #20580, #35797, #1273 ),
 ( #33314, #13978, #17672 ),
 ( #29832, #7804, #33109 ),
 ( #26551, #38869, #20180 ),
 ( #17075, #4921, #29622 ),
 ( #39091, #17277, #4710 ),
 ( #5120, #14193, #23482 ),
 ( #32899, #26758, #39286 ),
 ( #11109, #17488, #11522 ),
 ( #5307, #8606, #40081 ),
 ( #27155, #24888, #2470 ),
 ( #18703, #2267, #36611 ),
 ( #17874, #31262, #20983 ),
 ( #18490, #27759, #11909 ),
 ( #8414, #37006, #40292 ),
 ( #12124, #33717, #9039 ),
 ( #21182, #15004, #5530 ),
 ( #30440, #8827, #5741 ),
 ( #14808, #14587, #24085 ),
 ( #30649, #24473, #2659 ),
 ( #24274, #21406, #15199 ),
 ( #15412, #18094, #33941 ),
 ( #33500, #27559, #18298 ),
 ( #24690, #27371, #5926 ),
 ( #30837, #31045, #39896 ),
 ( #11716, #21794, #39686 ),
 ( #34327, #6139, #36797 ),
 ( #37221, #21601, #40508 ),
 ( #34124, #37412, #2864 ),
 ( #27969, #12331, #9222 ) ),
 .UNSPECIFIED., .F., .F., .T. ) 
 B_SPLINE_SURFACE_WITH_KNOTS ( ( 4, 2, 2, 2, 2, 2, 2, 2, 2, 2, 2, 2, 2, 2, 4 ),
 ( 3, 3 ),
 ( -3.469446951953614189E-18, 0.0008451783626492559258, 0.001267767543973885623, 0.001690356725298515321, 0.002112945906623145235, 0.002535535087947774716, 0.002958124269272404197, 0.003380713450597034112, 0.003803302631921664026, 0.004225891813246293940, 0.004648480994570923855, 0.005071070175895552902, 0.005493659357220181949, 0.005916248538544811864, 0.006761426901194071692 ),
 ( 0.000000000000000000, 1.000000000000000000 ),
 .UNSPECIFIED. ) 
 GEOMETRIC_REPRESENTATION_ITEM ( )  RATIONAL_B_SPLINE_SURFACE ( (
 ( 1.000000000000000000, 0.7062849495007544887, 1.000000000000000000),
 ( 1.000000000000000000, 0.7227129208496203550, 1.000000000000000000),
 ( 1.000000000000000000, 0.7446039768329009156, 1.000000000000000000),
 ( 1.000000000000000000, 0.7785882448431576952, 1.000000000000000000),
 ( 1.000000000000000000, 0.7899748008720065551, 1.000000000000000000),
 ( 1.000000000000000000, 0.8124594432436503810, 1.000000000000000000),
 ( 1.000000000000000000, 0.8236310436141200952, 1.000000000000000000),
 ( 1.000000000000000000, 0.8448283019538158634, 1.000000000000000000),
 ( 1.000000000000000000, 0.8549254312217464680, 1.000000000000000000),
 ( 1.000000000000000000, 0.8740472546363526885, 1.000000000000000000),
 ( 1.000000000000000000, 0.8831075751990844491, 1.000000000000000000),
 ( 1.000000000000000000, 0.8995851049065786142, 1.000000000000000000),
 ( 1.000000000000000000, 0.9070756499137949680, 1.000000000000000000),
 ( 1.000000000000000000, 0.9205552158185307254, 1.000000000000000000),
 ( 1.000000000000000000, 0.9265890096043063462, 1.000000000000000000),
 ( 1.000000000000000000, 0.9367297899379105619, 1.000000000000000000),
 ( 1.000000000000000000, 0.9408642172682338822, 1.000000000000000000),
 ( 1.000000000000000000, 0.9471737341364497853, 1.000000000000000000),
 ( 1.000000000000000000, 0.9493269720088893804, 1.000000000000000000),
 ( 1.000000000000000000, 0.9513457469809029066, 1.000000000000000000),
 ( 1.000000000000000000, 0.9512623927072865193, 1.000000000000000000),
 ( 1.000000000000000000, 0.9488501058180722758, 1.000000000000000000),
 ( 1.000000000000000000, 0.9465153709087239520, 1.000000000000000000),
 ( 1.000000000000000000, 0.9398721796748563673, 1.000000000000000000),
 ( 1.000000000000000000, 0.9355047118274805173, 1.000000000000000000),
 ( 1.000000000000000000, 0.9250133594824604399, 1.000000000000000000),
 ( 1.000000000000000000, 0.9189219428161754522, 1.000000000000000000),
 ( 1.000000000000000000, 0.8981866250659263917, 1.000000000000000000),
 ( 1.000000000000000000, 0.8810974021035897774, 1.000000000000000000),
 ( 1.000000000000000000, 0.8619304930065656567, 1.000000000000000000) ) ) 
 REPRESENTATION_ITEM ( '' )  SURFACE ( )  );
#8517=EDGE_CURVE ( 'NONE', #40111, #2424, #36838, .T. ) ;
#8522=CARTESIAN_POINT ( 'NONE',  ( 0.3405654008276560174, -0.9375483805025445205, 0.6383954687273779571 ) ) ;
#8525=CARTESIAN_POINT ( 'NONE',  ( 0.009566731965422575409, -0.8481436005400048161, 0.2526215923527056484 ) ) ;
#8530=CARTESIAN_POINT ( 'NONE',  ( 0.4410195951477819398, -1.197182411727151008, 0.6593086987560837775 ) ) ;
#8532=CARTESIAN_POINT ( 'NONE',  ( 0.001662780879258194885, -0.4326592981238366886, 0.1457185332388686305 ) ) ;
#8533=B_SPLINE_CURVE_WITH_KNOTS ( 'NONE', 3,
 ( #3767, #37705, #109, #3154, #3342, #9926 ),
 .UNSPECIFIED., .F., .F.,
 ( 4, 2, 4 ),
 ( 0.000000000000000000, 0.5000000000000000000, 1.000000000000000000 ),
 .UNSPECIFIED. ) ;
#8535=ORIENTED_EDGE ( 'NONE', *, *, #28330, .F. ) ;
#8539=CARTESIAN_POINT ( 'NONE',  ( 0.06051550865496472392, -0.5443424548793918127, 0.1927890781605659798 ) ) ;
#8541=CARTESIAN_POINT ( 'NONE',  ( 0.1994847130146940317, -0.7607898051193093814, 0.3264396457034328125 ) ) ;
#8545=ORIENTED_EDGE ( 'NONE', *, *, #25766, .T. ) ;
#8547=CARTESIAN_POINT ( 'NONE',  ( 0.1223843250744573868, -0.5500287403895844918, 0.1616903350415000440 ) ) ;
#8548=CARTESIAN_POINT ( 'NONE',  ( 0.6256947331227940001, -1.595527352996821469, 0.6076831429631934789 ) ) ;
#8551=CARTESIAN_POINT ( 'NONE',  ( 0.2211220101159939722, -1.227820234045938097, 0.5209104070613070903 ) ) ;
#8555=CARTESIAN_POINT ( 'NONE',  ( 0.4624512237511245738, -1.047046041135732741, 0.8530670246638676346 ) ) ;
#8558=CARTESIAN_POINT ( 'NONE',  ( 0.006240228873519562680, -0.9884989829865254984, 0.4718170318920712480 ) ) ;
#8561=CARTESIAN_POINT ( 'NONE',  ( 0.5824768036646325031, -1.621001158744945991, 0.5712635245953084917 ) ) ;
#8563=CARTESIAN_POINT ( 'NONE',  ( 0.5953197980378833742, -1.599064723402610300, 0.4311035055375501135 ) ) ;
#8565=CARTESIAN_POINT ( 'NONE',  ( 0.1802725749815597966, -0.5022333234960129067, 0.1376211838849571434 ) ) ;
#8568=CARTESIAN_POINT ( 'NONE',  ( 0.3432581181243943846, -1.758429828403793138, 0.5770599949894790193 ) ) ;
#8571=CARTESIAN_POINT ( 'NONE',  ( 0.3318240906244541710, -1.171642975870005543, 0.5913302545968384116 ) ) ;
#8574=CARTESIAN_POINT ( 'NONE',  ( 0.4120243698460513970, -1.164832338238820819, 0.7510118434071767490 ) ) ;
#8577=ORIENTED_EDGE ( 'NONE', *, *, #17315, .T. ) ;
#8578=CARTESIAN_POINT ( 'NONE',  ( 0.5089221226418110255, -1.111225213825750568, 0.6024461477417591970 ) ) ;
#8579=EDGE_LOOP ( 'NONE', ( #31410, #35164, #38763, #29943 ) ) ;
#8580=FACE_OUTER_BOUND ( 'NONE', #39100, .T. ) ;
#8581=ORIENTED_EDGE ( 'NONE', *, *, #22276, .T. ) ;
#8585=CARTESIAN_POINT ( 'NONE',  ( 0.3566523005335134333, -1.604465007536034049, 0.7245065946462900808 ) ) ;
#8587=CARTESIAN_POINT ( 'NONE',  ( 0.1139193472829358872, -0.5653918311555475862, -0.06223708083321360246 ) ) ;
#8593=CARTESIAN_POINT ( 'NONE',  ( 0.3040981744558501898, -0.9753306080842758519, 0.5622688203834439458 ) ) ;
#8595=DIRECTION ( 'NONE',  ( 0.4999551463232372317, -0.8660512985181134660, 0.000000000000000000 ) ) ;
#8597=CARTESIAN_POINT ( 'NONE',  ( 0.2879064663585326755, -1.217751227854929841, 0.7176035333459224175 ) ) ;
#8601=CARTESIAN_POINT ( 'NONE',  ( 0.07043814880410684265, -1.334972480813831242, 0.5056242588139928662 ) ) ;
#8602=CARTESIAN_POINT ( 'NONE',  ( 0.6465835049539362389, -1.539613817736340318, 0.4182417262808776903 ) ) ;
#8606=CARTESIAN_POINT ( 'NONE',  ( 0.4264195861673160115, -1.139367626797110900, 0.4357676993674804988 ) ) ;
#8608=CARTESIAN_POINT ( 'NONE',  ( 0.5565975663448354815, -1.184644286187108708, 0.6057417262809814407 ) ) ;
#8611=CARTESIAN_POINT ( 'NONE',  ( 0.0003124531501750084676, -0.4743565691596361433, 0.01672823577956931637 ) ) ;
#8618=EDGE_CURVE ( 'NONE', #37794, #849, #37632, .T. ) ;
#8625=CARTESIAN_POINT ( 'NONE',  ( 0.009902733472184338873, -0.5495308982465882952, 0.06817473810473409501 ) ) ;
#8631=CARTESIAN_POINT ( 'NONE',  ( 0.0008771832397133621367, -0.5718434724294755300, 0.3100202370988239808 ) ) ;
#8633=CARTESIAN_POINT ( 'NONE',  ( 0.1171568423075159127, -1.261316438396035355, 0.6037076130698849630 ) ) ;
#8634=DIRECTION ( 'NONE',  ( 0.4999551463232372317, -0.8660512985181135770, 0.000000000000000000 ) ) ;
#8637=CARTESIAN_POINT ( 'NONE',  ( 0.7093866102592447653, -1.464446360347554155, 0.5673451516581958787 ) ) ;
#8640=CARTESIAN_POINT ( 'NONE',  ( 0.3965913301904470112, -1.111811593118468666, 0.6217369508112339238 ) ) ;
#8641=CARTESIAN_POINT ( 'NONE',  ( 0.1109049718729727962, -0.9286333055842151962, 0.1410250186500828229 ) ) ;
#8643=CARTESIAN_POINT ( 'NONE',  ( 0.2297829359340678446, -0.8828613649094588789, 0.6895610511698265777 ) ) ;
#8645=CARTESIAN_POINT ( 'NONE',  ( 0.1853695079015652281, -0.8324104521289150682, 0.1224972303491578957 ) ) ;
#8650=AXIS2_PLACEMENT_3D ( 'NONE', #13687, #26452, #10406 ) ;
#8652=CARTESIAN_POINT ( 'NONE',  ( 0.3891948688262691358, -1.730102521992781694, 0.4274210666962675598 ) ) ;
#8656=CARTESIAN_POINT ( 'NONE',  ( 0.4007660105564045949, -1.129975317395211620, 0.6051902615802887686 ) ) ;
#8661=CARTESIAN_POINT ( 'NONE',  ( 3.304294434668030104E-05, -0.6893515101347650331, 0.1975634471597359221 ) ) ;
#8662=CARTESIAN_POINT ( 'NONE',  ( 0.05855645742600570219, -1.102688816132245009, 0.7515070308652079811 ) ) ;
#8664=CARTESIAN_POINT ( 'NONE',  ( 0.2690787404081327883, -0.7149439305734058836, 0.6099944544563858928 ) ) ;
#8665=VECTOR ( 'NONE', #1023, 39.37007874015748854 ) ;
#8667=EDGE_CURVE ( 'NONE', #11702, #25265, #6233, .T. ) ;
#8673=CARTESIAN_POINT ( 'NONE',  ( 0.1160506195841335408, -1.088369628471243633, 0.8769193895170159792 ) ) ;
#8674=VECTOR ( 'NONE', #8125, 39.37007874015748143 ) ;
#8676=CARTESIAN_POINT ( 'NONE',  ( 0.1751938157831150200, -0.7243946344483128685, 0.5279096736120190148 ) ) ;
#8677=CARTESIAN_POINT ( 'NONE',  ( 0.2225889308918536924, -1.238345268919997855, 0.5682417262808776570 ) ) ;
#8678=ORIENTED_EDGE ( 'NONE', *, *, #325, .T. ) ;
#8680=CARTESIAN_POINT ( 'NONE',  ( 0.2097017171917790468, -0.6397877375661684685, 0.3875311123790295409 ) ) ;
#8683=CARTESIAN_POINT ( 'NONE',  ( 0.5514545221111827322, -1.194714523076736423, 0.8193424885052650319 ) ) ;
#8689=CARTESIAN_POINT ( 'NONE',  ( 0.1482573209055756402, -0.8073945103406793278, 0.5257187345872705864 ) ) ;
#8690=CARTESIAN_POINT ( 'NONE',  ( 0.3111309942001374562, -1.709659708352874619, 0.8393873792776631593 ) ) ;
#8691=CARTESIAN_POINT ( 'NONE',  ( 0.2632880871822030899, -1.020987797972919164, 0.7882303987144065882 ) ) ;
#8693=CARTESIAN_POINT ( 'NONE',  ( 0.002149636668525627126, -0.5209811123354256557, 0.1235383891433055742 ) ) ;
#8695=CARTESIAN_POINT ( 'NONE',  ( 0.05041038597642048119, -1.271665433281254032, 0.6452718344857854005 ) ) ;
#8701=CARTESIAN_POINT ( 'NONE',  ( 0.4281045213691702656, -0.9891014172330019338, 0.8333036199592755988 ) ) ;
#8704=AXIS2_PLACEMENT_3D ( 'NONE', #5691, #26714, #5476 ) ;
#8707=CARTESIAN_POINT ( 'NONE',  ( 0.3663975874019596568, -1.157438136726378186, 0.4269148889825730708 ) ) ;
#8708=CARTESIAN_POINT ( 'NONE',  ( 0.2714277091601389746, -1.671900126436688838, 0.5222435141121624103 ) ) ;
#8709=CARTESIAN_POINT ( 'NONE',  ( 0.3256425937109617141, -1.179684785606091468, 0.5587805044134809274 ) ) ;
#8710=CARTESIAN_POINT ( 'NONE',  ( 0.5136166297679740644, -1.127695158652323615, 0.6751074532211280843 ) ) ;
#8711=B_SPLINE_SURFACE_WITH_KNOTS ( 'NONE', 5, 5, ( 
 ( #8181, #4883, #7349, #39048, #1835, #23233 ),
 ( #17243, #35761, #1240, #35968, #20756, #7572 ),
 ( #29396, #26915, #7774, #14155, #19925, #39445 ),
 ( #26725, #39254, #11077, #23637, #11272, #36157 ),
 ( #35549, #23839, #33278, #5085, #30191, #2021 ),
 ( #26126, #4287, #32674, #17044, #10459, #23025 ) ),
 .UNSPECIFIED., .F., .F., .F.,
 ( 6, 6 ),
 ( 6, 6 ),
 ( -6.477000000001651436, 6.477000000001639002 ),
 ( -2.080605796196421498, 4.396394203803585476 ),
 .UNSPECIFIED. ) ;
#8719=VERTEX_POINT ( 'NONE', #29134 ) ;
#8720=CARTESIAN_POINT ( 'NONE',  ( 0.3605448558321485697, -1.159604706203796631, 0.5182417262812284431 ) ) ;
#8727=CARTESIAN_POINT ( 'NONE',  ( 0.02924548582525025170, -0.9126776490762169569, 0.5652727012340077462 ) ) ;
#8728=ORIENTED_EDGE ( 'NONE', *, *, #27890, .T. ) ;
#8730=CARTESIAN_POINT ( 'NONE',  ( 0.4830258349640542126, -1.691802070263692004, 0.5182417262812423209 ) ) ;
#8734=CARTESIAN_POINT ( 'NONE',  ( 0.7435985525077578595, -1.513373960891965186, 0.6163350003740883931 ) ) ;
#8737=CARTESIAN_POINT ( 'NONE',  ( 0.4514811354680951516, -1.211986655109367650, 0.6466260521952869045 ) ) ;
#8739=CARTESIAN_POINT ( 'NONE',  ( 0.2200519516156196342, -1.355113298751763562, 0.5481991913389544502 ) ) ;
#8747=CARTESIAN_POINT ( 'NONE',  ( 0.06045611542974323876, -0.5406557321920382186, 0.1728691795844525259 ) ) ;
#8755=EDGE_CURVE ( 'NONE', #35264, #20946, #18994, .T. ) ;
#8757=CARTESIAN_POINT ( 'NONE',  ( 0.1234749398008549298, -0.5742850910011407795, 0.2528056413081115616 ) ) ;
#8758=CARTESIAN_POINT ( 'NONE',  ( 0.4452028689750809343, -1.684051297054903307, 0.4425228722054742603 ) ) ;
#8759=CARTESIAN_POINT ( 'NONE',  ( 0.4069049488313739027, -1.594104043689183570, 0.6057417262804756231 ) ) ;
#8763=CARTESIAN_POINT ( 'NONE',  ( 0.2277099777986371920, -1.235451102848944993, 0.5588482542077454207 ) ) ;
#8767=CARTESIAN_POINT ( 'NONE',  ( 0.6207796129641102167, -1.305782781463471265, 0.8357864796646383709 ) ) ;
#8771=CARTESIAN_POINT ( 'NONE',  ( 0.007114566881182543719, -0.9829610562604936819, 0.4921441418150904190 ) ) ;
#8774=CARTESIAN_POINT ( 'NONE',  ( 0.5704542012684959973, -1.616399117461207569, 0.5772614208947250969 ) ) ;
#8785=EDGE_CURVE ( 'NONE', #17955, #24067, #31623, .T. ) ;
#8788=CARTESIAN_POINT ( 'NONE',  ( 0.3311563363071323152, -1.162429047844745877, 0.5776872415141406369 ) ) ;
#8790=B_SPLINE_CURVE_WITH_KNOTS ( 'NONE', 5,
 ( #21843, #34582, #3111, #8872, #6184, #15655 ),
 .UNSPECIFIED., .F., .F.,
 ( 6, 6 ),
 ( 0.2521360130142110134, 0.5291905289985323613 ),
 .UNSPECIFIED. ) ;
#8793=CARTESIAN_POINT ( 'NONE',  ( 0.4594999264872952072, -1.231639012166720004, 0.7236424862120242052 ) ) ;
#8796=CARTESIAN_POINT ( 'NONE',  ( 0.3793958449840821867, -1.004087596663555848, 0.6383754926613092184 ) ) ;
#8804=CARTESIAN_POINT ( 'NONE',  ( 0.3552119812245919106, -1.622044444526105522, 0.5608365975959591632 ) ) ;
#8806=CARTESIAN_POINT ( 'NONE',  ( 0.1120118048860820614, -0.8483571591711281945, -0.03450342869453253136 ) ) ;
#8809=CARTESIAN_POINT ( 'NONE',  ( 0.4020964902746486658, -1.115374752730860841, 0.6163322898183211107 ) ) ;
#8810=CARTESIAN_POINT ( 'NONE',  ( 0.1161887176043710779, -0.5502801146938044452, 0.1708140022945554004 ) ) ;
#8819=CARTESIAN_POINT ( 'NONE',  ( 0.6540709664215760277, -1.593060928864740156, 0.5182417262812423209 ) ) ;
#8820=CARTESIAN_POINT ( 'NONE',  ( 0.3927915226382389657, -1.715293516864650147, 0.5707417262808793801 ) ) ;
#8821=FACE_OUTER_BOUND ( 'NONE', #26825, .T. ) ;
#8822=CARTESIAN_POINT ( 'NONE',  ( 0.4265404446467185307, -1.123912635142109817, 0.5182417262812248904 ) ) ;
#8823=CARTESIAN_POINT ( 'NONE',  ( 0.04695358122948785351, -1.249483587492180581, 0.6552810377283075915 ) ) ;
#8827=CARTESIAN_POINT ( 'NONE',  ( 0.4741765585715493336, -1.132356602107696952, 0.4721259381520144793 ) ) ;
#8828=FACE_OUTER_BOUND ( 'NONE', #3711, .T. ) ;
#8830=TOROIDAL_SURFACE ( 'NONE', #14084, 0.08249999999977555842, 0.01000000000000000021 ) ;
#8833=CARTESIAN_POINT ( 'NONE',  ( 0.0001146438086225802652, -0.5834251000296799550, -0.08070232224184867298 ) ) ;
#8834=CARTESIAN_POINT ( 'NONE',  ( 0.3298351036060790387, -1.757032636962086114, 0.4723056884894215046 ) ) ;
#8838=EDGE_LOOP ( 'NONE', ( #7911, #33436, #17846, #37577 ) ) ;
#8839=VERTEX_POINT ( 'NONE', #23785 ) ;
#8845=CARTESIAN_POINT ( 'NONE',  ( 0.001993913723218970323, -0.5355225131288038343, 0.09668841071476408366 ) ) ;
#8846=ORIENTED_EDGE ( 'NONE', *, *, #14959, .F. ) ;
#8849=VERTEX_POINT ( 'NONE', #35710 ) ;
#8850=CARTESIAN_POINT ( 'NONE',  ( 0.02433822063067445085, -0.7066234909068694892, 0.5546226239478463382 ) ) ;
#8851=CARTESIAN_POINT ( 'NONE',  ( 0.3168552283135301351, -1.073657105286919267, 0.7402218143473522360 ) ) ;
#8852=CARTESIAN_POINT ( 'NONE',  ( 0.1260969926168152566, -1.253913687407651967, 0.6054891446326211568 ) ) ;
#8853=CARTESIAN_POINT ( 'NONE',  ( 0.3727806007709784097, -1.152479425862310558, 0.4884953832116078476 ) ) ;
#8856=CARTESIAN_POINT ( 'NONE',  ( 0.7055834023472599137, -1.451092590515833392, 0.5677234696916273471 ) ) ;
#8864=CARTESIAN_POINT ( 'NONE',  ( 0.3717445303674562496, -1.104844584519105943, 0.7786008353294959772 ) ) ;
#8868=CARTESIAN_POINT ( 'NONE',  ( 0.3191045316042666613, -1.760553544078689026, 0.5737075626876623202 ) ) ;
#8869=CARTESIAN_POINT ( 'NONE',  ( 0.3891894383937726243, -1.723671533896645958, 0.4268439981611141243 ) ) ;
#8872=CARTESIAN_POINT ( 'NONE',  ( 0.07405242469529096927, -1.324323623009547202, 0.5682417262808779901 ) ) ;
#8873=CARTESIAN_POINT ( 'NONE',  ( 0.3119220788584739501, -1.019769644837810185, 0.7484519766187490708 ) ) ;
#8874=CARTESIAN_POINT ( 'NONE',  ( 0.4247042268939170140, -1.110871729138690256, 0.6103025838679678738 ) ) ;
#8879=CARTESIAN_POINT ( 'NONE',  ( 0.003338613830247910610, -0.5117837562375455729, 0.3073580953312808339 ) ) ;
#8880=CARTESIAN_POINT ( 'NONE',  ( 0.04797482002446179505, -1.049455964310542777, 0.7276413311358312930 ) ) ;
#8882=CARTESIAN_POINT ( 'NONE',  ( 0.4378619693737221819, -1.010538247186560268, 0.8194577876302902020 ) ) ;
#8884=CARTESIAN_POINT ( 'NONE',  ( 0.7038410752055113129, -1.517571454057699443, 0.5632464140165025501 ) ) ;
#8886=EDGE_CURVE ( 'NONE', #29074, #10339, #15054, .T. ) ;
#8892=CARTESIAN_POINT ( 'NONE',  ( 0.2628895756871428291, -1.634670359451999788, 0.7935051471341527662 ) ) ;
#8893=CARTESIAN_POINT ( 'NONE',  ( 0.1296612367934588672, -0.5770376283328382261, 0.2571717286738921526 ) ) ;
#8894=LINE ( 'NONE', #21657, #15179 ) ;
#8897=CARTESIAN_POINT ( 'NONE',  ( 0.5890075386511577360, -1.247786712317649815, 0.6995832148063678702 ) ) ;
#8900=CARTESIAN_POINT ( 'NONE',  ( 0.2381337884976891806, -0.6974119706843676658, 0.5054819936770663658 ) ) ;
#8905=CARTESIAN_POINT ( 'NONE',  ( 0.09981923470275097521, -0.7260083312159106850, 0.3343492273789105407 ) ) ;
#8907=CARTESIAN_POINT ( 'NONE',  ( 0.4725026279546233332, -1.434192584178236807, 0.8017224222965745328 ) ) ;
#8909=CARTESIAN_POINT ( 'NONE',  ( -0.001900788452498577497, -0.8469055337045260368, 0.09163843197140913999 ) ) ;
#8910=CARTESIAN_POINT ( 'NONE',  ( 0.01623329718145851558, -0.9477957671793985073, 0.2415891105782959902 ) ) ;
#8911=ORIENTED_EDGE ( 'NONE', *, *, #39899, .T. ) ;
#8914=CARTESIAN_POINT ( 'NONE',  ( 0.5545352172160372684, -1.200673110126019294, 0.8790629059729889727 ) ) ;
#8920=CARTESIAN_POINT ( 'NONE',  ( 0.000000000000000000, 0.000000000000000000, 0.000000000000000000 ) ) ;
#8926=CARTESIAN_POINT ( 'NONE',  ( 0.3511079287476749355, -1.164805985122749465, 0.4335040596137047508 ) ) ;
#8927=CARTESIAN_POINT ( 'NONE',  ( 0.5083828713348212958, -1.120917766412646177, 0.6786323191735850191 ) ) ;
#8933=ADVANCED_FACE ( 'NONE', ( #40419 ), #14291, .T. ) ;
#8937=CARTESIAN_POINT ( 'NONE',  ( 0.6841302653033145553, -1.411212316466117223, 0.6057417262805112612 ) ) ;
#8941=CARTESIAN_POINT ( 'NONE',  ( 0.1447739588591331894, -1.157841457446613598, 0.7566199150856840472 ) ) ;
#8948=B_SPLINE_CURVE_WITH_KNOTS ( 'NONE', 3,
 ( #8640, #33967, #17703, #30250, #11556, #39930, #5562, #11746, #18325, #2080, #37039, #36828, #40113, #14618, #21213, #30680 ),
 .UNSPECIFIED., .F., .F.,
 ( 4, 2, 2, 2, 2, 2, 2, 4 ),
 ( 0.000000000000000000, 0.0004030402500546790201, 0.0008060805001093580401, 0.001209120750164036952, 0.001612161000218716080, 0.002418241500328066531, 0.002821281750382742624, 0.003224322000437419150 ),
 .UNSPECIFIED. ) ;
#8952=CARTESIAN_POINT ( 'NONE',  ( 0.2325871439873127555, -1.347985720369676121, 0.5231355526079688456 ) ) ;
#8956=CARTESIAN_POINT ( 'NONE',  ( 0.1774005755516563920, -0.7643112578446873417, 0.6237371788150407603 ) ) ;
#8958=CARTESIAN_POINT ( 'NONE',  ( 0.6777607415330073604, -1.552933800012288978, 0.6113354315870481726 ) ) ;
#8959=CARTESIAN_POINT ( 'NONE',  ( 0.07091372799986922493, -0.6193112222544570056, 0.3868635014313515641 ) ) ;
#8961=CARTESIAN_POINT ( 'NONE',  ( 0.5532300872722170082, -1.623494116491306594, 0.5181769067174267773 ) ) ;
#8967=CARTESIAN_POINT ( 'NONE',  ( 0.1224514167073170595, -0.5493860373880040671, 0.1457185332388692411 ) ) ;
#8968=CARTESIAN_POINT ( 'NONE',  ( 0.4547198050419078430, -1.678377057945577677, 0.4517409696548269071 ) ) ;
#8969=DIRECTION ( 'NONE',  ( 1.060606950627616897E-16, 6.122684696619992497E-17, 1.000000000000000000 ) ) ;
#8972=FACE_OUTER_BOUND ( 'NONE', #17415, .T. ) ;
#8978=CARTESIAN_POINT ( 'NONE',  ( 0.4897931935426230177, -1.095389100717072850, 0.8439147301884563079 ) ) ;
#8980=CARTESIAN_POINT ( 'NONE',  ( 0.02467386667972750608, -1.028554209509673578, 0.5662612265361036679 ) ) ;
#8986=CARTESIAN_POINT ( 'NONE',  ( 0.1401418647927308025, -0.8661219404098066121, 0.4927111136368755306 ) ) ;
#8987=CARTESIAN_POINT ( 'NONE',  ( 0.2669858372074024322, -1.675026322382315191, 0.5720923781018742993 ) ) ;
#8995=CARTESIAN_POINT ( 'NONE',  ( 0.6554648208145406052, -1.536877632280804873, 0.4182417262808777458 ) ) ;
#8997=ADVANCED_FACE ( 'NONE', ( #2388, #30564 ), #36532, .F. ) ;
#9002=CARTESIAN_POINT ( 'NONE',  ( 0.3917146490717380303, -1.113158088163010095, 0.6227922109902478409 ) ) ;
#9003=CARTESIAN_POINT ( 'NONE',  ( 0.1892549258828873926, -0.8411929458066104148, 0.2428197129412378030 ) ) ;
#9005=CARTESIAN_POINT ( 'NONE',  ( 0.4381095118996915505, -1.199720832187643582, 0.7206127906299513164 ) ) ;
#9008=CARTESIAN_POINT ( 'NONE',  ( 0.3877041582795131003, -1.010062466692070560, 0.6423187497268529889 ) ) ;
#9017=CARTESIAN_POINT ( 'NONE',  ( 0.3594954150521289526, -1.619161029595283186, 0.6519928337199429880 ) ) ;
#9018=CARTESIAN_POINT ( 'NONE',  ( 0.06505414422235179794, -0.8155846679102959351, 0.07151615054459180276 ) ) ;
#9019=CARTESIAN_POINT ( 'NONE',  ( 0.1753879760477817240, -0.8109860937599424613, -0.04834239174515909954 ) ) ;
#9023=CARTESIAN_POINT ( 'NONE',  ( 0.3090203544014926140, -0.9165002773570758432, 0.5981876956776405185 ) ) ;
#9024=CARTESIAN_POINT ( 'NONE',  ( 0.4408853310126066849, -1.325034971439371212, 0.8326428173140825173 ) ) ;
#9025=ORIENTED_EDGE ( 'NONE', *, *, #7894, .F. ) ;
#9031=B_SPLINE_CURVE_WITH_KNOTS ( 'NONE', 3,
 ( #21486, #5399, #2951, #18577, #8909, #24168, #17962, #30522, #27447, #2347, #24351, #15502, #33589, #34007, #18170, #8497, #27637, #5811, #6012, #15286, #18370, #36692, #28056, #21062, #34201, #39972, #11793, #30724, #30917, #21672, #36885, #8693, #24769, #21272 ),
 .UNSPECIFIED., .F., .F.,
 ( 4, 2, 2, 2, 2, 2, 2, 2, 2, 2, 2, 2, 2, 2, 2, 2, 4 ),
 ( 0.000000000000000000, 0.0008327512041488100087, 0.001665502408297620017, 0.002498253612446430568, 0.003331004816595241336, 0.004163756020744051670, 0.004996507224892862871, 0.005829258429041673205, 0.006662009633190484406, 0.007494760837339294740, 0.008327512041488103339, 0.009160263245636913673, 0.009993014449785724007, 0.01082576565393453434, 0.01165851685808334294, 0.01249126806223215327, 0.01332401926638096534 ),
 .UNSPECIFIED. ) ;
#9034=CARTESIAN_POINT ( 'NONE',  ( 0.5696125550597064269, -1.613556559779221189, 0.4687417262808790674 ) ) ;
#9037=CARTESIAN_POINT ( 'NONE',  ( 0.2073812095156316870, -1.204313567361931847, 0.5182417262812423209 ) ) ;
#9039=CARTESIAN_POINT ( 'NONE',  ( 0.4635148750433638609, -1.130672306621219647, 0.4607556654368962779 ) ) ;
#9040=CARTESIAN_POINT ( 'NONE',  ( 0.4374219344798826459, -1.230185402379724069, 0.5856983068965044836 ) ) ;
#9042=CARTESIAN_POINT ( 'NONE',  ( 0.01266180416972241714, -0.9102398499036795654, 0.5581420674395337622 ) ) ;
#9043=CARTESIAN_POINT ( 'NONE',  ( 0.2616322387702281205, -1.678013124025769187, 0.5382687897764735219 ) ) ;
#9045=CARTESIAN_POINT ( 'NONE',  ( 0.5971614065082352374, -1.461417804984935342, 0.6057417262805111502 ) ) ;
#9047=ORIENTED_EDGE ( 'NONE', *, *, #11263, .F. ) ;
#9059=CARTESIAN_POINT ( 'NONE',  ( 0.01298442562731116044, -0.6517174416560403971, 0.4734301074441944479 ) ) ;
#9060=CARTESIAN_POINT ( 'NONE',  ( 0.2984382882072237897, -1.047452999410511065, 0.7351907297634064919 ) ) ;
#9061=CARTESIAN_POINT ( 'NONE',  ( 0.6047538891612445067, -1.605163873594933843, 0.4396382108053981108 ) ) ;
#9062=CARTESIAN_POINT ( 'NONE',  ( 0.6065946466975035145, -1.478929314905678361, 0.5636733106534758120 ) ) ;
#9070=CARTESIAN_POINT ( 'NONE',  ( 0.4914180550386734736, -1.285646375261855878, 0.7919587470386610928 ) ) ;
#9073=CARTESIAN_POINT ( 'NONE',  ( 0.03757742148941851240, -0.6212996915455626379, 0.6062798531290721771 ) ) ;
#9074=B_SPLINE_CURVE_WITH_KNOTS ( 'NONE', 5,
 ( #8246, #8034, #14615, #27185, #18121, #40110 ),
 .UNSPECIFIED., .F., .F.,
 ( 6, 6 ),
 ( 5.240850777407929151, 7.803531517424560526 ),
 .UNSPECIFIED. ) ;
#9076=CARTESIAN_POINT ( 'NONE',  ( 0.6586645934826005355, -1.563799363216411331, 0.4177417262808784670 ) ) ;
#9079=DIRECTION ( 'NONE',  ( -0.4999551463232372317, 0.8660512985181134660, -0.000000000000000000 ) ) ;
#9080=CARTESIAN_POINT ( 'NONE',  ( 0.2039603895705197623, -1.429414345016513765, 0.9236325154956378514 ) ) ;
#9081=CARTESIAN_POINT ( 'NONE',  ( 0.05019192336334400012, -1.073493884431249601, 0.7323994023816953192 ) ) ;
#9083=CARTESIAN_POINT ( 'NONE',  ( 0.2173028089842584942, -0.6047810126270140030, 0.4525757583899530645 ) ) ;
#9084=CARTESIAN_POINT ( 'NONE',  ( 0.6699292074404745723, -1.569526485364062474, 0.6071573546319919412 ) ) ;
#9089=CARTESIAN_POINT ( 'NONE',  ( 0.2675992341663611107, -1.614841384873237917, 0.8159387862359652743 ) ) ;
#9090=CARTESIAN_POINT ( 'NONE',  ( 0.4552858789809595685, -1.287359980045181151, 0.8227995234754879039 ) ) ;
#9093=CARTESIAN_POINT ( 'NONE',  ( 0.5367554652047751285, -1.159747519872984300, 0.6504567231333411303 ) ) ;
#9102=CARTESIAN_POINT ( 'NONE',  ( 0.08673251224761270584, -0.7254629984980496271, 0.1796334135243346508 ) ) ;
#9103=CARTESIAN_POINT ( 'NONE',  ( 0.3048570497350419073, -1.756853555320991189, 0.5694442476137213660 ) ) ;
#9104=CARTESIAN_POINT ( 'NONE',  ( 0.4529273117239071000, -1.400119990640080081, 0.8223471911486823771 ) ) ;
#9107=CARTESIAN_POINT ( 'NONE',  ( 0.01573875648097932539, -0.9458718438695528086, 0.1964948750599073701 ) ) ;
#9109=CARTESIAN_POINT ( 'NONE',  ( 0.4624513059194432230, -1.677210534090505245, 0.5769224047549080803 ) ) ;
#9110=CARTESIAN_POINT ( 'NONE',  ( 0.5352968706694352097, -1.169515972850764696, 0.8775555985942493642 ) ) ;
#9115=CARTESIAN_POINT ( 'NONE',  ( 0.3948505749649401375, -1.157343825677206617, 0.4182417262808778013 ) ) ;
#9117=FACE_OUTER_BOUND ( 'NONE', #16352, .T. ) ;
#9118=CARTESIAN_POINT ( 'NONE',  ( 0.4452807512755668218, -1.047893410216382382, 0.6910429845488149647 ) ) ;
#9122=CARTESIAN_POINT ( 'NONE',  ( 0.5611322101011324559, -1.505499452099228641, 0.5480364229397299836 ) ) ;
#9125=ORIENTED_EDGE ( 'NONE', *, *, #10763, .T. ) ;
#9127=CARTESIAN_POINT ( 'NONE',  ( 0.2142458193968007074, -0.9048875576697104073, 0.6439300487045382937 ) ) ;
#9130=CARTESIAN_POINT ( 'NONE',  ( 0.1722800781603322229, -1.380285231960554526, 0.5936621141595983531 ) ) ;
#9135=VERTEX_POINT ( 'NONE', #34453 ) ;
#9137=CARTESIAN_POINT ( 'NONE',  ( 0.7308477326836637644, -1.487300591783543124, 0.7156276807793737760 ) ) ;
#9139=EDGE_CURVE ( 'NONE', #17741, #38533, #36870, .T. ) ;
#9142=CARTESIAN_POINT ( 'NONE',  ( 0.1826134026666640375, -1.261648033191452578, 0.4282186462236585722 ) ) ;
#9147=CARTESIAN_POINT ( 'NONE',  ( 0.1136507236048572705, -0.6373588427272240953, 0.4267424632662121242 ) ) ;
#9150=CARTESIAN_POINT ( 'NONE',  ( 0.4048501170226769807, -1.424128732296970234, 0.8405605425542692632 ) ) ;
#9151=DIRECTION ( 'NONE',  ( 0.4996194577002578407, -0.8662449985352299597, 0.000000000000000000 ) ) ;
#9152=CARTESIAN_POINT ( 'NONE',  ( 0.5596723329040782513, -1.621442011146171369, 0.5567257723923959567 ) ) ;
#9153=CARTESIAN_POINT ( 'NONE',  ( 0.06875593408321428734, -1.327476523378791962, 0.5532905004612894695 ) ) ;
#9157=CARTESIAN_POINT ( 'NONE',  ( 0.5809008504126312866, -1.495258029342362072, 0.5730765960790278335 ) ) ;
#9158=CARTESIAN_POINT ( 'NONE',  ( 0.4838384605851756559, -1.673620472881901300, 0.5087549739108570002 ) ) ;
#9161=VERTEX_POINT ( 'NONE', #6866 ) ;
#9165=CARTESIAN_POINT ( 'NONE',  ( 0.2181682312481163233, -1.239626545742103181, 0.5655726110498544568 ) ) ;
#9166=CARTESIAN_POINT ( 'NONE',  ( 0.2259476328985426941, -1.236619376729935382, 0.4746024408792181570 ) ) ;
#9167=B_SPLINE_CURVE_WITH_KNOTS ( 'NONE', 3,
 ( #35092, #6689, #16185, #19469, #28726, #32002, #3209, #15754, #587, #22561, #16369, #28304, #28908, #13279, #21737, #174, #34271, #31208 ),
 .UNSPECIFIED., .F., .F.,
 ( 4, 2, 2, 2, 2, 2, 2, 2, 4 ),
 ( 0.000000000000000000, 0.0007544293770661929764, 0.001508858754132385953, 0.002263288131198578929, 0.003017717508264771906, 0.003772146885330964882, 0.004526576262397157858, 0.005281005639463353003, 0.006035435016529549015 ),
 .UNSPECIFIED. ) ;
#9168=CARTESIAN_POINT ( 'NONE',  ( 0.4805300281521128203, -1.080349003257709439, 0.8405881438443104647 ) ) ;
#9173=CARTESIAN_POINT ( 'NONE',  ( 0.1268788240767347308, -0.8367918140873071842, 0.4559310628402723498 ) ) ;
#9174=CARTESIAN_POINT ( 'NONE',  ( 0.2623454991891604471, -1.677609158577047621, 0.5446184138564792443 ) ) ;
#9176=ORIENTED_EDGE ( 'NONE', *, *, #382, .F. ) ;
#9179=CARTESIAN_POINT ( 'NONE',  ( 0.6583193209383879640, -1.530332598402602828, 0.4182417262808776903 ) ) ;
#9182=ORIENTED_EDGE ( 'NONE', *, *, #20222, .F. ) ;
#9185=CARTESIAN_POINT ( 'NONE',  ( 0.3780793312557618191, -1.119558780295859535, 0.6237031023607847446 ) ) ;
#9189=CARTESIAN_POINT ( 'NONE',  ( 0.4177594668114605336, -1.172467419432972724, 0.7388445284618762043 ) ) ;
#9192=CARTESIAN_POINT ( 'NONE',  ( 0.1960870051948097048, -0.8771803234346856604, 0.3014997781122282783 ) ) ;
#9199=CARTESIAN_POINT ( 'NONE',  ( 0.04802694997680392180, -0.5385102852490685210, 0.1733495709028375353 ) ) ;
#9201=CARTESIAN_POINT ( 'NONE',  ( 0.1864532405559393979, -0.6659192699994888054, -0.02049162290020863433 ) ) ;
#9206=CARTESIAN_POINT ( 'NONE',  ( 0.3804416727307123880, -1.009541828604827218, 0.6200734748803748975 ) ) ;
#9207=CARTESIAN_POINT ( 'NONE',  ( 0.1648809095896444921, -0.7520497700267493313, 0.5690099980341608576 ) ) ;
#9218=CARTESIAN_POINT ( 'NONE',  ( 0.4136294883733862005, -1.694877849074643672, 0.4182417262808776903 ) ) ;
#9219=CARTESIAN_POINT ( 'NONE',  ( 0.06824055730039223222, -1.289945330482348496, 0.6789996349980699231 ) ) ;
#9221=CARTESIAN_POINT ( 'NONE',  ( 0.4613690144166702201, -1.065390048215762997, 0.6270275320092995042 ) ) ;
#9222=CARTESIAN_POINT ( 'NONE',  ( 0.4611807422268464074, -1.110735627432217765, 0.5647948193072632739 ) ) ;
#9225=CARTESIAN_POINT ( 'NONE',  ( 0.01933088760290150449, -0.9443470376599968352, 0.6102586483404766060 ) ) ;
#9229=CARTESIAN_POINT ( 'NONE',  ( 0.5960504044690355663, -1.458754575269462395, 0.6057417262805163682 ) ) ;
#9234=ORIENTED_EDGE ( 'NONE', *, *, #30894, .F. ) ;
#9238=CARTESIAN_POINT ( 'NONE',  ( 0.5185735850971436856, -1.328908583238292973, 0.7912473624542825101 ) ) ;
#9244=CARTESIAN_POINT ( 'NONE',  ( 0.2678708459125263008, -1.675617809333246777, 0.5935539999434353842 ) ) ;
#9246=CARTESIAN_POINT ( 'NONE',  ( 0.1039318284443993545, -1.302570566043166123, 0.5899279477117637116 ) ) ;
#9251=ORIENTED_EDGE ( 'NONE', *, *, #18862, .T. ) ;
#9254=DIRECTION ( 'NONE',  ( 0.01455087615875040596, 0.9998941303973200023, 0.000000000000000000 ) ) ;
#9256=CARTESIAN_POINT ( 'NONE',  ( 0.4745478738625271697, -1.259349835786171878, 0.7951441819683597867 ) ) ;
#9257=CARTESIAN_POINT ( 'NONE',  ( 0.1309676594288840534, -0.8283632510577545460, 0.2782064429851813236 ) ) ;
#9258=DIRECTION ( 'NONE',  ( -0.4999551463232372317, 0.8660512985181135770, -0.000000000000000000 ) ) ;
#9262=CARTESIAN_POINT ( 'NONE',  ( 0.02831927448914906692, -0.5730460782701279898, 0.5331832225423767113 ) ) ;
#9263=ADVANCED_FACE ( 'NONE', ( #30513 ), #33802, .F. ) ;
#9264=CARTESIAN_POINT ( 'NONE',  ( 0.3891097478030026147, -1.721120859245148571, 0.4231916600392490180 ) ) ;
#9266=CARTESIAN_POINT ( 'NONE',  ( 0.3931005117246323399, -1.715828765679402679, 0.3667417262808779777 ) ) ;
#9268=CARTESIAN_POINT ( 'NONE',  ( 0.3900778056733008592, -1.134510399567245864, 0.7523592440643727119 ) ) ;
#9274=CARTESIAN_POINT ( 'NONE',  ( 0.1053607631531530836, -1.334516741563384068, 0.7095644064326338540 ) ) ;
#9276=CARTESIAN_POINT ( 'NONE',  ( 0.3446155261768803491, -0.8529094429884808148, 0.7348996499020890028 ) ) ;
#9279=CARTESIAN_POINT ( 'NONE',  ( 0.6750313905811581305, -1.555737387944355454, 0.6033254075622310753 ) ) ;
#9282=VERTEX_POINT ( 'NONE', #15077 ) ;
#9284=CARTESIAN_POINT ( 'NONE',  ( 0.2351328385853270198, -1.513397575123461403, 0.9164249233862159505 ) ) ;
#9287=CARTESIAN_POINT ( 'NONE',  ( 0.1330058442311542188, -0.5794291578589204628, 0.2619875031982849545 ) ) ;
#9289=ORIENTED_EDGE ( 'NONE', *, *, #38942, .F. ) ;
#9290=CARTESIAN_POINT ( 'NONE',  ( 0.5544140612800516621, -1.190962001057203956, 0.5445415982692776158 ) ) ;
#9293=CARTESIAN_POINT ( 'NONE',  ( 0.2006703192425639271, -0.5962780551271036344, 0.3430129484740815360 ) ) ;
#9297=DIRECTION ( 'NONE',  ( 1.060606950627616897E-16, 6.122684696619992497E-17, 1.000000000000000000 ) ) ;
#9302=CARTESIAN_POINT ( 'NONE',  ( 0.1086040402818805040, -0.7941143328802063861, 0.3875077444786869107 ) ) ;
#9304=CARTESIAN_POINT ( 'NONE',  ( 0.4971617628130152178, -1.474698883450294540, 0.7633393513624641136 ) ) ;
#9309=CARTESIAN_POINT ( 'NONE',  ( 0.4341036163735219611, -1.690926254025340691, 0.4262558845157656262 ) ) ;
#9310=CARTESIAN_POINT ( 'NONE',  ( 0.7139080051254665937, -1.458177603278905332, 0.7675176523170569309 ) ) ;
#9311=CARTESIAN_POINT ( 'NONE',  ( 0.1084341599040759135, -1.414529908605170361, 0.5685197021117063265 ) ) ;
#9314=EDGE_CURVE ( 'NONE', #33860, #28462, #33698, .T. ) ;
#9317=CARTESIAN_POINT ( 'NONE',  ( 0.006005486288604863949, -0.9514584861060970677, 0.4879672165010910390 ) ) ;
#9318=CARTESIAN_POINT ( 'NONE',  ( 0.4820398931871337500, -1.088803207145679242, 0.6894399345265510570 ) ) ;
#9321=CIRCLE ( 'NONE', #28403, 0.009999999999999944697 ) ;
#9325=CARTESIAN_POINT ( 'NONE',  ( 0.3893819225029191422, -1.720935294021423978, 0.4231407362055625843 ) ) ;
#9327=ORIENTED_EDGE ( 'NONE', *, *, #12922, .F. ) ;
#9328=CARTESIAN_POINT ( 'NONE',  ( 0.4062230848227149638, -1.145582794160931117, 0.4248905050063955802 ) ) ;
#9330=CARTESIAN_POINT ( 'NONE',  ( 0.08670662847365112613, -0.7414284123014263095, 0.03488965029717239208 ) ) ;
#9333=CARTESIAN_POINT ( 'NONE',  ( 0.1141547338916006765, -1.221815644227830511, 0.7539337555814515923 ) ) ;
#9334=ORIENTED_EDGE ( 'NONE', *, *, #19321, .F. ) ;
#9338=CARTESIAN_POINT ( 'NONE',  ( 0.4039331521932674751, -1.711434328629108714, 0.5182417262808777236 ) ) ;
#9344=CARTESIAN_POINT ( 'NONE',  ( 0.1266021694322588542, -1.239399129679921829, 0.5182417262812423209 ) ) ;
#9346=CARTESIAN_POINT ( 'NONE',  ( 0.1044857023475970897, -0.6151305603489410911, 0.3740774240993971489 ) ) ;
#9352=CARTESIAN_POINT ( 'NONE',  ( 0.07283724563382382167, -0.5406377204022615457, 0.1457185332388694354 ) ) ;
#9354=CARTESIAN_POINT ( 'NONE',  ( 0.5680507681239298501, -1.626009195392588591, 0.5004993007562670293 ) ) ;
#9356=CARTESIAN_POINT ( 'NONE',  ( 0.1853092822385233873, -0.9263384658431096375, 0.3280667635356543377 ) ) ;
#9360=CARTESIAN_POINT ( 'NONE',  ( 0.1341053683801476104, -0.6137581712303235015, 0.3478286551500012203 ) ) ;
#9361=CARTESIAN_POINT ( 'NONE',  ( 0.4284705980304526207, -1.706026416638912746, 0.4298431576648689689 ) ) ;
#9367=CARTESIAN_POINT ( 'NONE',  ( 0.2257333548162994141, -1.236570967228644680, 0.5622049477089006153 ) ) ;
#9369=CARTESIAN_POINT ( 'NONE',  ( 0.6804297327399058126, -1.407484794882680745, 0.5682417262808783232 ) ) ;
#9371=CARTESIAN_POINT ( 'NONE',  ( 0.05844749783569043455, -1.323029004274733689, 0.5991599809669244658 ) ) ;
#9376=CARTESIAN_POINT ( 'NONE',  ( 0.1559984031573804775, -0.8964835598961180541, 0.5757252305435468509 ) ) ;
#9393=CARTESIAN_POINT ( 'NONE',  ( 0.3460543618422604051, -1.756493685445453146, 0.4557286970618524280 ) ) ;
#9396=CARTESIAN_POINT ( 'NONE',  ( 0.3852795338934388858, -1.129116621630487760, 0.7334296061308062109 ) ) ;
#9399=CARTESIAN_POINT ( 'NONE',  ( 0.4927016384402401195, -1.082581181811578697, 0.5750743434332348247 ) ) ;
#9404=VERTEX_POINT ( 'NONE', #16112 ) ;
#9405=CARTESIAN_POINT ( 'NONE',  ( 0.2720344517543004104, -1.310141966359744004, 0.9014112804584356597 ) ) ;
#9407=CARTESIAN_POINT ( 'NONE',  ( 0.1846989274142681881, -0.8380492819789600034, 0.07482513216622958818 ) ) ;
#9413=CARTESIAN_POINT ( 'NONE',  ( 0.4231691825188668710, -1.033889518165662436, 0.6356716544661608070 ) ) ;
#9414=CARTESIAN_POINT ( 'NONE',  ( 0.2607777723285606419, -0.9519272446484895456, 0.7368745005339746301 ) ) ;
#9416=CARTESIAN_POINT ( 'NONE',  ( 0.1872737887141963653, -0.7022237677290258384, 0.03102906701263268355 ) ) ;
#9432=CARTESIAN_POINT ( 'NONE',  ( 0.4835150722484384267, -1.077540828773440484, 0.6059843185820091849 ) ) ;
#9435=CARTESIAN_POINT ( 'NONE',  ( 0.5465059510172681767, -1.167163004870445331, 0.6057417262810063097 ) ) ;
#9437=CARTESIAN_POINT ( 'NONE',  ( 0.002166586416275674380, -0.8510908774931603693, 0.4206164911499951642 ) ) ;
#9445=ADVANCED_FACE ( 'NONE', ( #18788 ), #24522, .T. ) ;
#9446=LINE ( 'NONE', #7153, #38760 ) ;
#9452=VERTEX_POINT ( 'NONE', #9717 ) ;
#9458=CARTESIAN_POINT ( 'NONE',  ( 0.3014272484937131624, -1.653539857075366326, 0.6572327318754673797 ) ) ;
#9460=CARTESIAN_POINT ( 'NONE',  ( 0.1892549258828873926, -0.8411929458066104148, 0.2428197129412378030 ) ) ;
#9462=CARTESIAN_POINT ( 'NONE',  ( 0.01212422548420533965, -0.4367320064996455531, 0.07838015645872611903 ) ) ;
#9470=CARTESIAN_POINT ( 'NONE',  ( 0.5925686224617396913, -1.450288384180856038, 0.6546787349964396929 ) ) ;
#9471=CARTESIAN_POINT ( 'NONE',  ( 0.1340157750494070377, -0.8309105032810858438, 0.3116155039148025274 ) ) ;
#9474=CARTESIAN_POINT ( 'NONE',  ( 0.3240187991416175750, -1.728356536110253971, 0.7856525166496111101 ) ) ;
#9476=DIRECTION ( 'NONE',  ( -0.8660512985181177958, -0.4999551463232295712, 0.000000000000000000 ) ) ;
#9478=CARTESIAN_POINT ( 'NONE',  ( 0.07954574449638877887, -1.328936272382664097, 0.4736275662433468425 ) ) ;
#9480=CARTESIAN_POINT ( 'NONE',  ( 0.4108705347506164118, -1.163082222544741917, 0.7368721330335714637 ) ) ;
#9488=CARTESIAN_POINT ( 'NONE',  ( 0.1069896402632359023, -1.343652384576294212, 0.7022810525467199083 ) ) ;
#9495=EDGE_CURVE ( 'NONE', #15275, #5559, #4702, .T. ) ;
#9499=CARTESIAN_POINT ( 'NONE',  ( 0.2695576056624507943, -1.654889899364205608, 0.7708593280864846076 ) ) ;
#9501=CARTESIAN_POINT ( 'NONE',  ( 0.5949489883904641729, -1.487197279388327686, 0.5733659136327053929 ) ) ;
#9504=EDGE_CURVE ( 'NONE', #15275, #38229, #10618, .T. ) ;
#9506=CARTESIAN_POINT ( 'NONE',  ( 0.4340563226180833012, -1.025953197730038458, 0.7364845616659437821 ) ) ;
#9509=CARTESIAN_POINT ( 'NONE',  ( 0.2043052629501167783, -0.6086048778238046797, 0.3675695283820143433 ) ) ;
#9518=CARTESIAN_POINT ( 'NONE',  ( 0.08587344643816560708, -0.7676835104866827075, 0.1818131584873270978 ) ) ;
#9520=DIRECTION ( 'NONE',  ( 0.8660512985181133550, 0.4999551463232370652, 0.000000000000000000 ) ) ;
#9521=CARTESIAN_POINT ( 'NONE',  ( 0.1038461025547568750, -0.5461054185183505938, 0.1457185332388694909 ) ) ;
#9524=VERTEX_POINT ( 'NONE', #38093 ) ;
#9525=CARTESIAN_POINT ( 'NONE',  ( 0.4279390326040263259, -1.697518787232198179, 0.6054493271085924500 ) ) ;
#9526=CARTESIAN_POINT ( 'NONE',  ( 0.6984602154402382856, -1.438837821160460217, 0.5667713030031571453 ) ) ;
#9528=CARTESIAN_POINT ( 'NONE',  ( 0.6088374871291468704, -1.478988480944025241, 0.5690365700181255759 ) ) ;
#9533=CARTESIAN_POINT ( 'NONE',  ( 0.4091335057472371695, -1.131547141905885789, 0.4177417262808780229 ) ) ;
#9537=CARTESIAN_POINT ( 'NONE',  ( 0.05992090360963518020, -1.332693131100006312, 0.5739722883257112329 ) ) ;
#9538=CARTESIAN_POINT ( 'NONE',  ( 0.2974794542262550467, -0.9002722561939086043, 0.5860092920552725237 ) ) ;
#9544=CARTESIAN_POINT ( 'NONE',  ( 0.4903692945236159395, -1.545726006398236985, 0.5613691942562457626 ) ) ;
#9550=CARTESIAN_POINT ( 'NONE',  ( 0.6179353394495009644, -1.299228382567916285, 0.5682417262808779901 ) ) ;
#9551=CARTESIAN_POINT ( 'NONE',  ( 0.1851279770616925946, -0.8484560160152216923, 0.1977347518530706560 ) ) ;
#9553=CARTESIAN_POINT ( 'NONE',  ( 0.3453377680718429099, -1.749458763706847497, 0.4498113177182618272 ) ) ;
#9554=CARTESIAN_POINT ( 'NONE',  ( 0.1730569967620999294, -1.381888235275370080, 0.5814882153268127185 ) ) ;
#9557=FACE_OUTER_BOUND ( 'NONE', #8579, .T. ) ;
#9558=CARTESIAN_POINT ( 'NONE',  ( 0.08146015332400738385, -1.318321297778865864, 0.4704503523288164346 ) ) ;
#9566=CARTESIAN_POINT ( 'NONE',  ( 0.09266809627140198957, -0.6152261176636174556, 0.2439027869080791222 ) ) ;
#9570=CARTESIAN_POINT ( 'NONE',  ( 0.07625856036271293215, -0.5806278947743503949, 0.2951979850929375426 ) ) ;
#9574=CARTESIAN_POINT ( 'NONE',  ( 0.1875000000000003331, -0.9151275355372965326, 0.1457185332388701848 ) ) ;
#9578=CARTESIAN_POINT ( 'NONE',  ( 0.1153529736793553612, -0.4467512060742309665, 0.1565319484199297895 ) ) ;
#9579=CARTESIAN_POINT ( 'NONE',  ( 0.5802862917196511816, -1.495087218360813042, 0.5610704458703436037 ) ) ;
#9583=CARTESIAN_POINT ( 'NONE',  ( 0.06923712653936904549, -0.5400029222721455247, 0.1457185332388703236 ) ) ;
#9585=CARTESIAN_POINT ( 'NONE',  ( 0.2968044078846433509, -0.7977486025825716309, 0.6363905851602879027 ) ) ;
#9587=CARTESIAN_POINT ( 'NONE',  ( 0.02584783977369822794, -1.092114942298472169, 0.6499590385907687562 ) ) ;
#9591=CARTESIAN_POINT ( 'NONE',  ( 0.3918182118607624331, -1.107073211027153725, 0.6042946153017959565 ) ) ;
#9592=CARTESIAN_POINT ( 'NONE',  ( 0.08435616334553369677, -0.8469091540353979042, 0.3709842075955784857 ) ) ;
#9599=CARTESIAN_POINT ( 'NONE',  ( 0.6544078563150441674, -1.544269123161570390, 0.4241055859090137603 ) ) ;
#9602=CIRCLE ( 'NONE', #33935, 0.1012268159172230869 ) ;
#9605=( BOUNDED_SURFACE ( )  B_SPLINE_SURFACE ( 3, 2, ( 
 ( #33193, #29697, #20047 ),
 ( #36482, #8295, #7688 ),
 ( #26417, #30107, #35665 ),
 ( #20252, #36261, #20867 ) ),
 .UNSPECIFIED., .F., .F., .T. ) 
 B_SPLINE_SURFACE_WITH_KNOTS ( ( 4, 4 ),
 ( 3, 3 ),
 ( 7.502679033599690683E-16, 0.004712633340305917920 ),
 ( 0.000000000000000000, 1.000000000000000000 ),
 .UNSPECIFIED. ) 
 GEOMETRIC_REPRESENTATION_ITEM ( )  RATIONAL_B_SPLINE_SURFACE ( (
 ( 1.000000000000000000, 0.7064740011956678334, 1.000000000000000000),
 ( 1.000000000000000000, 0.7068967119107782970, 1.000000000000000000),
 ( 1.000000000000000000, 0.7076183925776566852, 1.000000000000000000),
 ( 1.000000000000000000, 0.7079223141425841082, 1.000000000000000000) ) ) 
 REPRESENTATION_ITEM ( '' )  SURFACE ( )  );
#9606=CARTESIAN_POINT ( 'NONE',  ( 0.2950576522027442139, -1.312148821418196443, 0.5683580896351703160 ) ) ;
#9609=CARTESIAN_POINT ( 'NONE',  ( 0.3940236569407176148, -1.140246238217890840, 0.7425364925414594808 ) ) ;
#9610=CARTESIAN_POINT ( 'NONE',  ( 0.2614468074032732514, -0.7584085742687330933, 0.1932256475537141860 ) ) ;
#9612=CARTESIAN_POINT ( 'NONE',  ( 0.4871018846440973715, -1.079508789421436799, 0.5988988590622403851 ) ) ;
#9617=B_SPLINE_CURVE_WITH_KNOTS ( 'NONE', 3,
 ( #22570, #34688, #19511, #3819, #32201, #4015, #12471, #28915, #38377, #780, #25644, #38174, #25236, #31412, #28126, #13286, #3416, #25026, #37558, #35100, #9792, #6493, #15975, #21962 ),
 .UNSPECIFIED., .F., .F.,
 ( 4, 2, 2, 2, 2, 2, 2, 2, 2, 2, 2, 4 ),
 ( 3.541895844777533420E-16, 0.001886868708433897144, 0.002830303062650669967, 0.003773737416867442140, 0.005660606125300986918, 0.006604040479517757356, 0.007547474833734527794, 0.008490909187951298231, 0.009434343542168068669, 0.01132121225060160261, 0.01320808095903513654, 0.01509494966746866874 ),
 .UNSPECIFIED. ) ;
#9618=ORIENTED_EDGE ( 'NONE', *, *, #820, .F. ) ;
#9619=CARTESIAN_POINT ( 'NONE',  ( 0.1999031773436300563, -1.118309514668103466, 0.8646612173229440979 ) ) ;
#9620=CARTESIAN_POINT ( 'NONE',  ( 0.08622878581753390392, -0.7696919062817791923, 0.05383970079421885463 ) ) ;
#9621=CARTESIAN_POINT ( 'NONE',  ( 0.1755124995118596265, -0.7841637173364213176, -0.06301638288098621032 ) ) ;
#9626=CARTESIAN_POINT ( 'NONE',  ( 0.1266021694322588542, -1.239399129679921829, 0.5182417262812423209 ) ) ;
#9627=CARTESIAN_POINT ( 'NONE',  ( 0.5674053191207506508, -1.503247083075981205, 0.5820947328701803203 ) ) ;
#9629=CARTESIAN_POINT ( 'NONE',  ( 0.01251651876921019806, -0.9543982913104013255, 0.3144092334379698372 ) ) ;
#9636=CARTESIAN_POINT ( 'NONE',  ( 0.1185062575666918222, -1.414355497448371413, 0.4982023605334466865 ) ) ;
#9640=CARTESIAN_POINT ( 'NONE',  ( 0.1037868704622257193, -1.285705572052544543, 0.6122442384440756058 ) ) ;
#9643=CARTESIAN_POINT ( 'NONE',  ( 0.1133199752903892021, -1.408071044610375466, 0.6174663899997400174 ) ) ;
#9646=CARTESIAN_POINT ( 'NONE',  ( 0.3238203105384647174, -0.9899218032796638367, 0.5856430185708639824 ) ) ;
#9647=CARTESIAN_POINT ( 'NONE',  ( 0.3190393728410141350, -1.171751842138375244, 0.4809317249889470958 ) ) ;
#9648=CARTESIAN_POINT ( 'NONE',  ( 0.5435131371594662530, -1.168890700092135804, 0.6057417262810184111 ) ) ;
#9650=CARTESIAN_POINT ( 'NONE',  ( 0.02591418161326580066, -1.064383994110095877, 0.6545759956939124491 ) ) ;
#9651=CARTESIAN_POINT ( 'NONE',  ( -8.431455208089989601E-05, -0.7678062237554516001, -0.09016270909632642661 ) ) ;
#9652=CARTESIAN_POINT ( 'NONE',  ( 0.6790301733516745930, -1.437036692487801526, 0.4793159731800502588 ) ) ;
#9658=ORIENTED_EDGE ( 'NONE', *, *, #37555, .T. ) ;
#9661=CARTESIAN_POINT ( 'NONE',  ( 0.6164308040309282033, -1.473203056481420692, 0.5449326099368130283 ) ) ;
#9662=B_SPLINE_CURVE_WITH_KNOTS ( 'NONE', 3,
 ( #23483, #24086, #17875, #37007, #36193, #8007, #30650, #33718, #36402, #27561 ),
 .UNSPECIFIED., .F., .F.,
 ( 4, 2, 2, 2, 4 ),
 ( 0.0001365264101772900964, 0.0006734250193805398814, 0.001210323628583789531, 0.001747222237787039289, 0.002284120846990289264 ),
 .UNSPECIFIED. ) ;
#9667=CARTESIAN_POINT ( 'NONE',  ( 0.2028766461682649236, -0.6553055420477189585, 0.3449445657290035050 ) ) ;
#9670=CARTESIAN_POINT ( 'NONE',  ( 0.01099302296002880285, -0.5422623884125030713, 0.2194225212593840790 ) ) ;
#9671=CARTESIAN_POINT ( 'NONE',  ( 0.2498278802431492807, -0.9843056470458266816, 0.7020538874898170079 ) ) ;
#9672=CARTESIAN_POINT ( 'NONE',  ( 0.07975072596342917819, -1.320959035748987098, 0.5731222016746064796 ) ) ;
#9674=CARTESIAN_POINT ( 'NONE',  ( 0.1870989724938920962, -0.8266995537623093027, -0.08446770797961487831 ) ) ;
#9677=ADVANCED_FACE ( 'NONE', ( #29650 ), #16567, .T. ) ;
#9678=FACE_OUTER_BOUND ( 'NONE', #8187, .T. ) ;
#9679=ORIENTED_EDGE ( 'NONE', *, *, #14080, .T. ) ;
#9683=CARTESIAN_POINT ( 'NONE',  ( 0.1856930765046928833, -0.8391312611259635901, 0.1792070938244055278 ) ) ;
#9685=CARTESIAN_POINT ( 'NONE',  ( 0.5611967014548586707, -1.396901917415622973, 0.7440408781994463094 ) ) ;
#9686=CARTESIAN_POINT ( 'NONE',  ( 0.1483787585013065236, -0.8436283734347517216, 0.4121418770343379112 ) ) ;
#9687=CARTESIAN_POINT ( 'NONE',  ( 0.2658650419925461250, -1.607106637764143420, 0.8265052428267256612 ) ) ;
#9688=CARTESIAN_POINT ( 'NONE',  ( 0.3253107118822870514, -1.742078995693881138, 0.7432966274578529653 ) ) ;
#9690=CARTESIAN_POINT ( 'NONE',  ( 0.07734939284328633258, -1.330214815144483698, 0.4791517717473012805 ) ) ;
#9691=CARTESIAN_POINT ( 'NONE',  ( 0.1850732001874748345, -0.8229804149772106392, 0.1457185332388700183 ) ) ;
#9696=CARTESIAN_POINT ( 'NONE',  ( 0.002083146443013456344, -0.4777046557262296100, 0.09357736723029726200 ) ) ;
#9700=CARTESIAN_POINT ( 'NONE',  ( 0.6817109428167473784, -1.507712782526625883, 0.4506074055298545655 ) ) ;
#9705=CARTESIAN_POINT ( 'NONE',  ( 0.1911888169624559319, -1.364106057445899856, 0.9496954658188896392 ) ) ;
#9706=CARTESIAN_POINT ( 'NONE',  ( 0.3701761278964109114, -1.124337411362599015, 0.8051996703508850217 ) ) ;
#9707=CARTESIAN_POINT ( 'NONE',  ( 0.3577715969228448256, -1.744183799078588226, 0.4401225512775638338 ) ) ;
#9716=EDGE_CURVE ( 'NONE', #8839, #3591, #2239, .T. ) ;
#9717=CARTESIAN_POINT ( 'NONE',  ( 0.1802350563441833808, -0.5022327775090948965, 0.1477559389858786043 ) ) ;
#9720=CARTESIAN_POINT ( 'NONE',  ( 0.1691926429880553362, -0.8469287021894142953, 0.5696781129675587696 ) ) ;
#9722=CARTESIAN_POINT ( 'NONE',  ( 0.5257712170263993956, -1.526907663539789572, 0.5830379435895678419 ) ) ;
#9726=CARTESIAN_POINT ( 'NONE',  ( 0.4395714512744828273, -1.702217766737038174, 0.6022144385477095074 ) ) ;
#9727=CARTESIAN_POINT ( 'NONE',  ( 0.6399309177019067985, -1.482104228856624406, 0.8013445891425567957 ) ) ;
#9728=CARTESIAN_POINT ( 'NONE',  ( 0.08016251834805442067, -1.309203902574839207, 0.5631135398343307674 ) ) ;
#9729=CARTESIAN_POINT ( 'NONE',  ( 0.2558199171275122308, -0.8856984187707415135, 0.6867119623177011523 ) ) ;
#9731=EDGE_CURVE ( 'NONE', #23498, #2485, #26799, .T. ) ;
#9735=EDGE_CURVE ( 'NONE', #34794, #35264, #9074, .T. ) ;
#9738=CARTESIAN_POINT ( 'NONE',  ( 0.2017226021742919428, -0.8083333955854449249, 0.3447374551949819454 ) ) ;
#9743=ORIENTED_EDGE ( 'NONE', *, *, #21070, .T. ) ;
#9744=CARTESIAN_POINT ( 'NONE',  ( 0.4322485342602996883, -1.579783117282272720, 0.5939163760578864970 ) ) ;
#9746=CARTESIAN_POINT ( 'NONE',  ( 0.08536139700232568683, -0.8064920420962284897, 0.1131592819080732837 ) ) ;
#9749=CARTESIAN_POINT ( 'NONE',  ( 0.1402368025282916819, -1.302452809619852436, 0.7172172189790673169 ) ) ;
#9757=CARTESIAN_POINT ( 'NONE',  ( 0.6011812487780853198, -1.595544227086114653, 0.4276680258713908001 ) ) ;
#9763=ORIENTED_EDGE ( 'NONE', *, *, #1920, .T. ) ;
#9764=CARTESIAN_POINT ( 'NONE',  ( 0.09001134929717277688, -0.6059489090321513727, 0.1642870258393102911 ) ) ;
#9765=ORIENTED_EDGE ( 'NONE', *, *, #37029, .T. ) ;
#9766=CARTESIAN_POINT ( 'NONE',  ( 0.01053196809506632727, -0.5372589727095348211, 0.4763883693587342427 ) ) ;
#9767=CARTESIAN_POINT ( 'NONE',  ( 0.4417054119102772902, -1.573775560800656059, 0.5739987501060517250 ) ) ;
#9768=CARTESIAN_POINT ( 'NONE',  ( 0.003322744920643190894, -0.5573345580546938960, 0.2952108599035634939 ) ) ;
#9769=CARTESIAN_POINT ( 'NONE',  ( 0.1987206965304505746, -1.209313118825164235, 0.5182417262812423209 ) ) ;
#9770=CARTESIAN_POINT ( 'NONE',  ( 0.005974780502986185536, -0.8455926682250717308, 0.1923417552807378805 ) ) ;
#9771=CARTESIAN_POINT ( 'NONE',  ( 0.1804200693113137133, -0.9232518763482380209, 0.2929062103565514552 ) ) ;
#9774=CARTESIAN_POINT ( 'NONE',  ( 0.5813445478835994606, -1.495260542201000131, 0.5817699383783053735 ) ) ;
#9779=CARTESIAN_POINT ( 'NONE',  ( 0.07240097019314004068, -0.5694418211797861451, 0.2666026808772828938 ) ) ;
#9782=CARTESIAN_POINT ( 'NONE',  ( 0.5969179818652998737, -1.265625243575819514, 0.7915741918176316672 ) ) ;
#9783=CARTESIAN_POINT ( 'NONE',  ( 0.4516518293581444632, -1.119247471017704942, 0.5164366663489963205 ) ) ;
#9784=CARTESIAN_POINT ( 'NONE',  ( 0.05499745022826314084, -1.300966059534855113, 0.6243749980364792229 ) ) ;
#9789=CARTESIAN_POINT ( 'NONE',  ( 0.6954966302589218330, -1.498494318102867595, 0.4775031782631350974 ) ) ;
#9792=CARTESIAN_POINT ( 'NONE',  ( 0.3877735588591806337, -1.128227633100496785, 0.7844172370806664629 ) ) ;
#9793=CARTESIAN_POINT ( 'NONE',  ( 0.6672745098620159743, -1.495646976912385906, 0.4226893254941921363 ) ) ;
#9798=DIRECTION ( 'NONE',  ( 0.8660512985181126888, 0.4999551463232384529, 0.000000000000000000 ) ) ;
#9801=CARTESIAN_POINT ( 'NONE',  ( 0.4865325576204800884, -1.269899856794043824, 0.6586424791840079784 ) ) ;
#9804=CARTESIAN_POINT ( 'NONE',  ( 0.5779297624755960205, -1.623152544610868109, 0.5629341535590222101 ) ) ;
#9805=CARTESIAN_POINT ( 'NONE',  ( 0.4003901567941702822, -1.031933045472551269, 0.6312919426632347397 ) ) ;
#9808=CARTESIAN_POINT ( 'NONE',  ( -0.002282498291095993656, -0.8555267327002353817, 0.1457185332388701293 ) ) ;
#9811=CARTESIAN_POINT ( 'NONE',  ( 0.3728324473123414973, -1.558310038709751710, 0.7835862474759246465 ) ) ;
#9812=CARTESIAN_POINT ( 'NONE',  ( 0.08541475502865693292, -0.8049639420879202145, 0.1080243483262872811 ) ) ;
#9815=B_SPLINE_CURVE_WITH_KNOTS ( 'NONE', 3,
 ( #39077, #10904, #23474, #4502, #32697, #32887 ),
 .UNSPECIFIED., .F., .F.,
 ( 4, 2, 4 ),
 ( 0.000000000000000000, 0.0006158527847097438647, 0.001231705569419487729 ),
 .UNSPECIFIED. ) ;
#9820=CARTESIAN_POINT ( 'NONE',  ( 0.1252239888084831498, -0.6131032844985105923, 0.3504799705789324871 ) ) ;
#9822=CARTESIAN_POINT ( 'NONE',  ( 0.07014435923140931173, -1.325199841737229711, 0.5075297796643253312 ) ) ;
#9825=CARTESIAN_POINT ( 'NONE',  ( 0.1863335705363715067, -0.7656576722580051841, 0.1913830803212247800 ) ) ;
#9827=CARTESIAN_POINT ( 'NONE',  ( 0.3311983384110263606, -1.753850171096680288, 0.5836116394440121757 ) ) ;
#9836=CARTESIAN_POINT ( 'NONE',  ( 0.4765072543226545609, -1.073695880004174930, 0.6154142099768207252 ) ) ;
#9842=CARTESIAN_POINT ( 'NONE',  ( -0.001733054258001554731, -0.9004704535694999512, 0.2409329515054920989 ) ) ;
#9845=CARTESIAN_POINT ( 'NONE',  ( 0.2798936374030868146, -1.205716238392265938, 0.4282426334535158197 ) ) ;
#9846=ORIENTED_EDGE ( 'NONE', *, *, #19209, .T. ) ;
#9847=ORIENTED_EDGE ( 'NONE', *, *, #16933, .T. ) ;
#9852=FACE_OUTER_BOUND ( 'NONE', #35185, .T. ) ;
#9853=AXIS2_PLACEMENT_3D ( 'NONE', #27983, #6552, #25309 ) ;
#9856=EDGE_LOOP ( 'NONE', ( #40091, #27230, #3657, #27388 ) ) ;
#9858=ORIENTED_EDGE ( 'NONE', *, *, #36821, .F. ) ;
#9860=CARTESIAN_POINT ( 'NONE',  ( 0.01082649148626377289, -0.5336901187179717843, 0.1852521559336037515 ) ) ;
#9861=DIRECTION ( 'NONE',  ( 0.9998941247116546194, -0.01455087607601020239, 0.0001066420868422379362 ) ) ;
#9863=CARTESIAN_POINT ( 'NONE',  ( 0.3187641638634979291, -1.760284878867078184, 0.5597302103697513465 ) ) ;
#9865=CARTESIAN_POINT ( 'NONE',  ( 0.4173132459375102354, -1.699444977922911493, 0.4182417262808778013 ) ) ;
#9867=EDGE_LOOP ( 'NONE', ( #21690, #37799, #22902, #35009 ) ) ;
#9869=CARTESIAN_POINT ( 'NONE',  ( 0.2267725030444622258, -0.9370487796004768333, 0.4246761745800142762 ) ) ;
#9871=CARTESIAN_POINT ( 'NONE',  ( 0.5903457776621824360, -1.446032249997192265, 0.6697935441370801435 ) ) ;
#9873=CARTESIAN_POINT ( 'NONE',  ( 0.03743290345340095221, -0.7527584146679924260, 0.6138086348110104451 ) ) ;
#9874=CARTESIAN_POINT ( 'NONE',  ( 0.4811037392677499636, -1.175372539374476277, 0.4182417262808778013 ) ) ;
#9875=CARTESIAN_POINT ( 'NONE',  ( 0.001519927481451859626, -0.8472461526284917888, 0.1457185332388711008 ) ) ;
#9882=CARTESIAN_POINT ( 'NONE',  ( -0.0004424791507732630863, -0.9367167129038177498, 0.1813186842804689336 ) ) ;
#9884=CARTESIAN_POINT ( 'NONE',  ( 0.3165986513250982903, -1.745708308064116920, 0.7545403346239585307 ) ) ;
#9891=ADVANCED_FACE ( 'NONE', ( #9678 ), #18754, .T. ) ;
#9896=CARTESIAN_POINT ( 'NONE',  ( 0.1950037666476622522, -0.5640115203604925131, 0.3061966258278945863 ) ) ;
#9899=CARTESIAN_POINT ( 'NONE',  ( 0.2664135068126231021, -1.673169779535225166, 0.5456938477760421291 ) ) ;
#9900=CARTESIAN_POINT ( 'NONE',  ( 0.1341641613487604967, -0.5874067381197118909, 0.2837651016474003196 ) ) ;
#9906=CARTESIAN_POINT ( 'NONE',  ( 0.6623042051160524801, -1.539866302937538789, 0.7062118603361370317 ) ) ;
#9913=CARTESIAN_POINT ( 'NONE',  ( 0.08963489136116924161, -0.7509102906732701976, 0.2481878857498304447 ) ) ;
#9914=CARTESIAN_POINT ( 'NONE',  ( 0.08990536851188021816, -0.5646295468556834507, 0.1408780685345830397 ) ) ;
#9916=CARTESIAN_POINT ( 'NONE',  ( 0.1114640335818673916, -0.5707303086454891261, 0.2491850945404860684 ) ) ;
#9919=AXIS2_PLACEMENT_3D ( 'NONE', #11076, #23636, #36155 ) ;
#9920=CARTESIAN_POINT ( 'NONE',  ( 0.7207144797668179059, -1.477263269554723202, 0.5687618070419677707 ) ) ;
#9923=CARTESIAN_POINT ( 'NONE',  ( 0.3164126684801325529, -1.761786144345217187, 0.5684815686975395188 ) ) ;
#9924=CARTESIAN_POINT ( 'NONE',  ( 0.6757026422043570513, -1.393510729029532547, 0.7334196951842761880 ) ) ;
#9926=CARTESIAN_POINT ( 'NONE',  ( 0.5654596793231598806, -1.618818539163461301, 0.5682417262808788783 ) ) ;
#9927=CARTESIAN_POINT ( 'NONE',  ( 0.1349510429637978681, -0.5701812554335998762, 0.2338515878604368881 ) ) ;
#9930=CARTESIAN_POINT ( 'NONE',  ( 0.3207148961678939481, -1.182401600646133089, 0.3667417262808778111 ) ) ;
#9933=CARTESIAN_POINT ( 'NONE',  ( 0.4975638555224211612, -1.097967759515461550, 0.6244301767862630026 ) ) ;
#9939=CARTESIAN_POINT ( 'NONE',  ( 0.6054889487767985967, -1.479703267939684874, 0.5856070495615782745 ) ) ;
#9947=CARTESIAN_POINT ( 'NONE',  ( 0.002938675265522861478, -0.5479465208063443171, 0.2683199588513891509 ) ) ;
#9948=AXIS2_PLACEMENT_3D ( 'NONE', #34394, #37683, #12798 ) ;
#9951=CARTESIAN_POINT ( 'NONE',  ( 0.4094665197507286747, -1.132124008075320098, 0.5707417262808780478 ) ) ;
#9952=CARTESIAN_POINT ( 'NONE',  ( 0.002782022538515906661, -0.9412645402768823333, 0.6116066270186392151 ) ) ;
#9961=B_SPLINE_CURVE_WITH_KNOTS ( 'NONE', 3,
 ( #33865, #30367, #24399, #27684 ),
 .UNSPECIFIED., .F., .F.,
 ( 4, 4 ),
 ( 0.000000000000000000, 0.0002238335178989935437 ),
 .UNSPECIFIED. ) ;
#9964=CARTESIAN_POINT ( 'NONE',  ( 0.2486235419350810716, -1.344789659884683797, 1.171751475820631105 ) ) ;
#9967=CARTESIAN_POINT ( 'NONE',  ( 0.09572618302809746127, -0.6249641250925348501, 0.2872090638444997901 ) ) ;
#9968=B_SPLINE_CURVE_WITH_KNOTS ( 'NONE', 3,
 ( #11351, #5166, #8263, #36238, #8051, #39737, #8460, #15052, #20630, #17327 ),
 .UNSPECIFIED., .F., .F.,
 ( 4, 3, 3, 4 ),
 ( 0.000000000000000000, 4.304601007142825036E-05, 8.690714465717732273E-05, 0.0001096645486937237969 ),
 .UNSPECIFIED. ) ;
#9969=CARTESIAN_POINT ( 'NONE',  ( 0.02524471160769579600, -0.6279797553945640765, 0.5994203574518347510 ) ) ;
#9970=CARTESIAN_POINT ( 'NONE',  ( 0.4456035407152363348, -1.502374677390132529, 0.7781194087335665532 ) ) ;
#9971=CARTESIAN_POINT ( 'NONE',  ( 0.04598863217031589484, -0.8257334846043561383, 0.7092904895903023865 ) ) ;
#9973=CARTESIAN_POINT ( 'NONE',  ( 0.01227139476065501611, -0.8747808039168644134, 0.4454182558007432347 ) ) ;
#9974=CARTESIAN_POINT ( 'NONE',  ( 0.1718750000000003053, -0.9178826446108661052, 0.1457185332388701848 ) ) ;
#9977=LINE ( 'NONE', #153, #33773 ) ;
#9981=AXIS2_PLACEMENT_3D ( 'NONE', #7891, #23161, #13862 ) ;
#9984=DIRECTION ( 'NONE',  ( 0.8660512985181136880, 0.4999551463232367876, 0.000000000000000000 ) ) ;
#9985=CARTESIAN_POINT ( 'NONE',  ( 0.3136035985995381248, -0.8251737266935038617, 0.6634070228338775355 ) ) ;
#9987=CARTESIAN_POINT ( 'NONE',  ( 0.4839838468137014904, -1.192129550890687062, 0.4021087476649028991 ) ) ;
#9988=CARTESIAN_POINT ( 'NONE',  ( 0.04078634645975903056, -1.210087468311284553, 0.6658561005973028246 ) ) ;
#9993=CARTESIAN_POINT ( 'NONE',  ( 0.2939503495491210816, -1.005253864439647371, 0.7192296934484712079 ) ) ;
#10000=CARTESIAN_POINT ( 'NONE',  ( 0.06444297064315794576, -0.8352831487901670737, 0.1457185332388703236 ) ) ;
#10001=CARTESIAN_POINT ( 'NONE',  ( 0.08609945990018005868, -1.325383490889678662, 0.4606874596949692147 ) ) ;
#10007=CARTESIAN_POINT ( 'NONE',  ( 0.1818182084070924798, -0.5169919523671798745, 0.2198248585042891778 ) ) ;
#10012=CARTESIAN_POINT ( 'NONE',  ( 0.4433349170228174652, -1.204176679204282729, 0.6897527930916858008 ) ) ;
#10014=CARTESIAN_POINT ( 'NONE',  ( 0.4862843069642890925, -1.079060212656593798, 0.6007065101366493298 ) ) ;
#10015=ORIENTED_EDGE ( 'NONE', *, *, #28089, .T. ) ;
#10018=CARTESIAN_POINT ( 'NONE',  ( 0.007861457232516730342, -0.8999816549950413469, 0.5065308129498107270 ) ) ;
#10021=CARTESIAN_POINT ( 'NONE',  ( 0.3845294810406492680, -1.605350533059137108, 0.5636378812280004036 ) ) ;
#10022=CARTESIAN_POINT ( 'NONE',  ( 0.06448134467046603979, -0.8354324776869207492, 0.1387861693055511825 ) ) ;
#10023=CARTESIAN_POINT ( 'NONE',  ( 0.1940093581540119627, -0.6292132035201315476, 0.3231077534996323886 ) ) ;
#10028=CARTESIAN_POINT ( 'NONE',  ( 0.5500379755161437512, -1.473456634498119699, 0.7231298284428128165 ) ) ;
#10034=CARTESIAN_POINT ( 'NONE',  ( 0.08556124454896821274, -1.317821213116421308, 0.4727606578195797660 ) ) ;
#10038=CARTESIAN_POINT ( 'NONE',  ( 0.7255563027409094312, -1.477976514587821422, 0.7347025679090390948 ) ) ;
#10040=VECTOR ( 'NONE', #3815, 39.37007874015748143 ) ;
#10042=CARTESIAN_POINT ( 'NONE',  ( 0.1157337385916143990, -1.413492129114879203, 0.5950113313978990792 ) ) ;
#10048=CARTESIAN_POINT ( 'NONE',  ( 0.7185393139234729221, -1.479621239843056157, 0.4933132820244564565 ) ) ;
#10050=CARTESIAN_POINT ( 'NONE',  ( 0.4952488905928924545, -1.196841907270136174, 0.4182417262808778013 ) ) ;
#10053=CARTESIAN_POINT ( 'NONE',  ( 0.02199361096923483153, -0.8343928545013460374, 0.5934276300867008525 ) ) ;
#10054=CARTESIAN_POINT ( 'NONE',  ( 1.543663729362214677E-05, -0.6714880032592078773, -0.1033492426826144589 ) ) ;
#10058=ORIENTED_EDGE ( 'NONE', *, *, #13758, .T. ) ;
#10062=DIRECTION ( 'NONE',  ( -0.8660512985181119117, -0.4999551463232398962, 0.000000000000000000 ) ) ;
#10064=CARTESIAN_POINT ( 'NONE',  ( 0.3297457498401996645, -1.032296429229499823, 0.7921737166615708814 ) ) ;
#10066=ORIENTED_EDGE ( 'NONE', *, *, #495, .T. ) ;
#10067=EDGE_LOOP ( 'NONE', ( #17297, #27015, #16823 ) ) ;
#10072=CARTESIAN_POINT ( 'NONE',  ( 0.2962541062570004380, -1.656293626468827274, 0.5607359955346605807 ) ) ;
#10073=CARTESIAN_POINT ( 'NONE',  ( 0.6560486628413821908, -1.555476615240107829, 0.4279073640907943843 ) ) ;
#10076=CARTESIAN_POINT ( 'NONE',  ( 0.01185910703655305813, -0.5726836470825711345, -0.08659834197632501618 ) ) ;
#10081=CARTESIAN_POINT ( 'NONE',  ( 0.1862146387795068081, -0.9153544180079368209, 0.1468049697877028548 ) ) ;
#10082=AXIS2_PLACEMENT_3D ( 'NONE', #22457, #22262, #34983 ) ;
#10084=CARTESIAN_POINT ( 'NONE',  ( 0.6080545645982834424, -1.479187156349330623, 0.6099109919555032455 ) ) ;
#10086=CARTESIAN_POINT ( 'NONE',  ( 0.2434517139947088293, -1.036255305955214867, 0.7293849779716305992 ) ) ;
#10097=CARTESIAN_POINT ( 'NONE',  ( 0.3149693831142335032, -1.765269515322325899, 0.6420921437412323574 ) ) ;
#10098=CARTESIAN_POINT ( 'NONE',  ( 0.1115667700604296847, -1.368744839739478580, 0.6778201501234852877 ) ) ;
#10111=CARTESIAN_POINT ( 'NONE',  ( 0.2621369394866731595, -1.686413516690222547, 0.5356639672823564347 ) ) ;
#10112=CARTESIAN_POINT ( 'NONE',  ( 0.4883354474493797337, -1.330538578445629838, 0.8129148094954937731 ) ) ;
#10113=CARTESIAN_POINT ( 'NONE',  ( 0.5474085822752589037, -1.175693918439151942, 0.6018262437559286360 ) ) ;
#10114=EDGE_LOOP ( 'NONE', ( #15584, #28586, #16191, #10373, #2822, #29524, #10174, #29207, #34993 ) ) ;
#10124=CARTESIAN_POINT ( 'NONE',  ( 0.1716662052826025409, -0.8629998118152951703, 0.5713517472061939717 ) ) ;
#10126=CARTESIAN_POINT ( 'NONE',  ( 0.08990536851188150880, -0.5646295468556827846, 0.1446695161202934954 ) ) ;
#10128=CARTESIAN_POINT ( 'NONE',  ( 0.1101907795074059532, -0.5552708166754189989, 0.1999101508315398457 ) ) ;
#10132=FACE_OUTER_BOUND ( 'NONE', #12095, .T. ) ;
#10135=CARTESIAN_POINT ( 'NONE',  ( 0.7414302106162510286, -1.507121135501449771, 0.6614796144117841559 ) ) ;
#10139=CARTESIAN_POINT ( 'NONE',  ( 0.4435146130966207134, -1.231926360794060260, 0.8199172986756667614 ) ) ;
#10141=CARTESIAN_POINT ( 'NONE',  ( -1.882535413755627890E-05, -0.9357343916592213429, 0.06558131283649058785 ) ) ;
#10144=CARTESIAN_POINT ( 'NONE',  ( 1.365923996832131609E-16, -0.9481888444201345134, 0.1139263443108001761 ) ) ;
#10145=CARTESIAN_POINT ( 'NONE',  ( 0.1897950977212392309, -0.7957416484119633759, 0.2611131357175326961 ) ) ;
#10147=DIRECTION ( 'NONE',  ( 0.4999551463232372317, -0.8660512985181135770, 0.000000000000000000 ) ) ;
#10151=AXIS2_PLACEMENT_3D ( 'NONE', #34256, #15133, #27497 ) ;
#10156=ORIENTED_EDGE ( 'NONE', *, *, #5244, .T. ) ;
#10157=CARTESIAN_POINT ( 'NONE',  ( 0.4328515195334204368, -1.579414682775934109, 0.5917285476992683035 ) ) ;
#10159=CARTESIAN_POINT ( 'NONE',  ( 0.01065772415598345742, -0.5389421826269154003, 0.2091342918453681088 ) ) ;
#10164=CARTESIAN_POINT ( 'NONE',  ( 0.6566606523871314494, -1.361328185136354119, 0.7219929986176217840 ) ) ;
#10169=VERTEX_POINT ( 'NONE', #13067 ) ;
#10172=B_SPLINE_CURVE_WITH_KNOTS ( 'NONE', 3,
 ( #1086, #35594, #16287, #13173, #4111, #28825 ),
 .UNSPECIFIED., .F., .F.,
 ( 4, 2, 4 ),
 ( 2.453269466693398698E-18, 0.0006420322884310510243, 0.001284064576862099447 ),
 .UNSPECIFIED. ) ;
#10174=ORIENTED_EDGE ( 'NONE', *, *, #17544, .T. ) ;
#10175=CARTESIAN_POINT ( 'NONE',  ( -2.086568639411206917E-17, -0.4716478265891163035, 0.3521378080009727185 ) ) ;
#10177=CARTESIAN_POINT ( 'NONE',  ( 0.1670460928285160684, -0.7847983796158649605, 0.5835955661026850372 ) ) ;
#10178=ADVANCED_FACE ( 'NONE', ( #19246 ), #36287, .F. ) ;
#10179=CARTESIAN_POINT ( 'NONE',  ( 0.01324987932754901482, -0.4603397457172120344, 0.2948093344987445241 ) ) ;
#10180=CARTESIAN_POINT ( 'NONE',  ( 0.08793790621863624424, -0.5736368938888692925, 0.2699646086827657832 ) ) ;
#10181=CARTESIAN_POINT ( 'NONE',  ( 0.06517940379945762197, -0.9109053406753262472, 0.7832400949722142514 ) ) ;
#10183=CARTESIAN_POINT ( 'NONE',  ( 0.1026215434209815508, -1.318872523977856259, 0.7205090641466329604 ) ) ;
#10184=CARTESIAN_POINT ( 'NONE',  ( 0.4548150350199454128, -1.105354657904179305, 0.5758811255889696445 ) ) ;
#10190=CARTESIAN_POINT ( 'NONE',  ( 0.3818955917259486132, -1.608577936064920832, 0.5280597390133632274 ) ) ;
#10191=CARTESIAN_POINT ( 'NONE',  ( 0.1153473914419797103, -0.4465972332940850720, 0.1475347861288875961 ) ) ;
#10200=CARTESIAN_POINT ( 'NONE',  ( 0.6326847266287998206, -1.322366380368365180, 0.7606069447649664861 ) ) ;
#10203=CARTESIAN_POINT ( 'NONE',  ( 0.06367953181181854050, -1.330828220450373855, 0.6041689818902572506 ) ) ;
#10207=ORIENTED_EDGE ( 'NONE', *, *, #25563, .T. ) ;
#10208=CARTESIAN_POINT ( 'NONE',  ( 0.2218534108553797402, -0.9537299479064303975, 0.6731843348530399673 ) ) ;
#10212=CARTESIAN_POINT ( 'NONE',  ( 0.4115766028365042128, -1.733048369835246794, 0.5182417262812423209 ) ) ;
#10213=CARTESIAN_POINT ( 'NONE',  ( 0.2535025136047072691, -0.9395968292722070014, 0.7008665722193688774 ) ) ;
#10215=CARTESIAN_POINT ( 'NONE',  ( 0.1581650021276240492, -1.285700486175305635, 0.4182417262808778013 ) ) ;
#10217=CARTESIAN_POINT ( 'NONE',  ( 0.08853488529544603636, -0.8965169086451082459, 0.5508734361391500745 ) ) ;
#10224=CARTESIAN_POINT ( 'NONE',  ( 0.4885442780260524920, -1.272859572036962650, 0.6135294268981799082 ) ) ;
#10227=CARTESIAN_POINT ( 'NONE',  ( 0.4508097189255980131, -1.059596525805123202, 0.6314750327306427602 ) ) ;
#10234=CARTESIAN_POINT ( 'NONE',  ( 0.04942251982096398932, -0.5642247362408411293, 0.2638688747701836146 ) ) ;
#10235=CARTESIAN_POINT ( 'NONE',  ( 0.08519720172272383929, -0.8101245899050438792, 0.1318208758437162953 ) ) ;
#10241=CARTESIAN_POINT ( 'NONE',  ( 0.3258695488805244955, -1.294614862064145333, 0.5703292412207198181 ) ) ;
#10243=CARTESIAN_POINT ( 'NONE',  ( 0.1169372607101707567, -0.5676260265568476848, 0.2368506474140012752 ) ) ;
#10248=EDGE_CURVE ( 'NONE', #12740, #11030, #29690, .T. ) ;
#10249=CARTESIAN_POINT ( 'NONE',  ( 0.2739720158966007513, -1.679698321540450845, 0.5182417262812423209 ) ) ;
#10251=CARTESIAN_POINT ( 'NONE',  ( 0.08642651716623081515, -0.7265462466526347862, 0.1036714726766719968 ) ) ;
#10257=CARTESIAN_POINT ( 'NONE',  ( 0.3193593568291898666, -1.759991732705063150, 0.5682417262808788783 ) ) ;
#10258=EDGE_CURVE ( 'NONE', #14931, #37238, #13294, .T. ) ;
#10259=CARTESIAN_POINT ( 'NONE',  ( 0.06146611576415164646, -1.320267390396500318, 0.5069306018158911131 ) ) ;
#10263=B_SPLINE_CURVE_WITH_KNOTS ( 'NONE', 3,
 ( #16257, #3700, #31674, #37853, #13356, #6557, #31472, #3279, #28385, #15834, #22035, #16649, #9667, #31882, #32080, #22643, #19135, #34958 ),
 .UNSPECIFIED., .F., .F.,
 ( 4, 2, 2, 2, 2, 2, 2, 2, 4 ),
 ( 0.001064266670126195764, 0.001883953749284820664, 0.002703640828443445564, 0.003523327907602070465, 0.004343014986760694932, 0.005162702065919320266, 0.005982389145077945600, 0.006802076224236569199, 0.007621763303395194533 ),
 .UNSPECIFIED. ) ;
#10267=CARTESIAN_POINT ( 'NONE',  ( 0.1850176395162889120, -0.7468748968588784232, -0.01500765167341262980 ) ) ;
#10268=CARTESIAN_POINT ( 'NONE',  ( 0.4627917923195704608, -1.215609717498142173, 0.4882610493429819787 ) ) ;
#10271=CARTESIAN_POINT ( 'NONE',  ( 0.003124719664520368614, -0.5686731593868924461, 0.1457185332388688526 ) ) ;
#10272=CARTESIAN_POINT ( 'NONE',  ( -5.779841274449564311E-05, -0.7442380360777858250, -0.09691552782533552346 ) ) ;
#10281=DIRECTION ( 'NONE',  ( 0.01455087615875041117, 0.9998941303973198913, 0.000000000000000000 ) ) ;
#10282=CARTESIAN_POINT ( 'NONE',  ( 0.5314776938657069794, -1.347789272887517820, 0.7454713222889900459 ) ) ;
#10285=CARTESIAN_POINT ( 'NONE',  ( 0.3778447279644155388, -0.9516834458091659732, 0.7020028943473471950 ) ) ;
#10289=CARTESIAN_POINT ( 'NONE',  ( 0.5654596793231598806, -1.618818539163461301, 0.5682417262808788783 ) ) ;
#10291=CARTESIAN_POINT ( 'NONE',  ( 0.3260790593237656299, -1.638809186220848257, 0.5607896681960787832 ) ) ;
#10292=CARTESIAN_POINT ( 'NONE',  ( 0.6147754885679747039, -1.587842851228911556, 0.4306178729423159601 ) ) ;
#10300=CARTESIAN_POINT ( 'NONE',  ( 0.3211164138312800898, -1.297326394713050890, 0.5856983068966360451 ) ) ;
#10301=AXIS2_PLACEMENT_3D ( 'NONE', #25589, #6841, #16330 ) ;
#10302=CARTESIAN_POINT ( 'NONE',  ( 0.2342238878248118772, -0.8684236987200721902, 0.4577198892158801935 ) ) ;
#10304=FACE_OUTER_BOUND ( 'NONE', #10661, .T. ) ;
#10305=CARTESIAN_POINT ( 'NONE',  ( 0.1220082445362224849, -0.8490970766526738656, 0.4167849038607836509 ) ) ;
#10307=CARTESIAN_POINT ( 'NONE',  ( 0.4904112910084882371, -1.188461936721588064, 0.4182417262808778013 ) ) ;
#10309=CARTESIAN_POINT ( 'NONE',  ( 0.1901695884098246192, -0.5023773489605839471, 0.1477569985384105666 ) ) ;
#10313=CIRCLE ( 'NONE', #33285, 0.09249999999977555343 ) ;
#10316=CARTESIAN_POINT ( 'NONE',  ( 0.1782715084618822221, -0.4916008192336085991, 0.1361683654214305150 ) ) ;
#10319=CARTESIAN_POINT ( 'NONE',  ( 0.4840003331797737562, -1.673488358279072941, 0.5079737477917150024 ) ) ;
#10323=CIRCLE ( 'NONE', #23470, 0.009999999999999960310 ) ;
#10326=CARTESIAN_POINT ( 'NONE',  ( 0.2705736468062067690, -1.683571660621278943, 0.6651229586412615857 ) ) ;
#10327=CARTESIAN_POINT ( 'NONE',  ( 0.5984989131615597868, -1.474188139544028608, 0.6628805706823384103 ) ) ;
#10328=CARTESIAN_POINT ( 'NONE',  ( 0.5860257985473389386, -1.592810714289445650, 0.4182417262808776903 ) ) ;
#10333=ORIENTED_EDGE ( 'NONE', *, *, #2937, .F. ) ;
#10338=CARTESIAN_POINT ( 'NONE',  ( 0.002922335949518027436, -0.5275076572294762345, 0.04185307883324664718 ) ) ;
#10339=VERTEX_POINT ( 'NONE', #7431 ) ;
#10341=CARTESIAN_POINT ( 'NONE',  ( 0.1015825433511447218, -0.8064352114398918303, 0.3490809539757221969 ) ) ;
#10343=CARTESIAN_POINT ( 'NONE',  ( 0.08990669076543263138, -0.5646496350939130826, 0.1479540721674596493 ) ) ;
#10345=CARTESIAN_POINT ( 'NONE',  ( 0.2720353181507955131, -1.018083045546113841, 0.7834435089220197490 ) ) ;
#10347=CARTESIAN_POINT ( 'NONE',  ( 0.05665256868255191119, -1.234311085492082016, 0.6576315090042377243 ) ) ;
#10348=CARTESIAN_POINT ( 'NONE',  ( 0.6064149006458688929, -1.480831751486391568, 0.5848188689676782070 ) ) ;
#10350=CARTESIAN_POINT ( 'NONE',  ( 0.3558981752617644823, -1.739539538141937847, 0.5952128432464615093 ) ) ;
#10353=CARTESIAN_POINT ( 'NONE',  ( 0.1434142660641894162, -0.6144585306666423552, 0.3449574928712252908 ) ) ;
#10354=CARTESIAN_POINT ( 'NONE',  ( -1.069831502984013885E-05, -0.8266740528552610767, -0.07503813273732132250 ) ) ;
#10355=CARTESIAN_POINT ( 'NONE',  ( 0.008166896316263525663, -0.6975401206106399687, -0.01226723980950392666 ) ) ;
#10357=CARTESIAN_POINT ( 'NONE',  ( 0.1172021019593823543, -1.233981478044366087, 0.8520562743190572830 ) ) ;
#10358=CARTESIAN_POINT ( 'NONE',  ( 0.3223305689799217388, -0.9241512680936796453, 0.6167986945225242268 ) ) ;
#10360=EDGE_CURVE ( 'NONE', #38179, #799, #38910, .T. ) ;
#10363=ORIENTED_EDGE ( 'NONE', *, *, #13715, .T. ) ;
#10365=CARTESIAN_POINT ( 'NONE',  ( 0.002296835029420861689, -0.5198933010532014176, 0.1443450864220853225 ) ) ;
#10366=CARTESIAN_POINT ( 'NONE',  ( 0.1331762155611039000, -1.278701992196867199, 0.4313405395425053412 ) ) ;
#10369=CARTESIAN_POINT ( 'NONE',  ( 0.6804297327399058126, -1.407484794882680745, 0.5682417262808783232 ) ) ;
#10372=CARTESIAN_POINT ( 'NONE',  ( 0.5022839945508311699, -1.192782407697791980, 0.4224083929475445642 ) ) ;
#10373=ORIENTED_EDGE ( 'NONE', *, *, #26993, .T. ) ;
#10378=CARTESIAN_POINT ( 'NONE',  ( 2.760432932221084055E-19, -0.4262518876079539609, 0.1943948295682533245 ) ) ;
#10379=CARTESIAN_POINT ( 'NONE',  ( 0.1335488240444889507, -0.7306454402582662766, 0.4913411250300099842 ) ) ;
#10381=CARTESIAN_POINT ( 'NONE',  ( 0.4697899360850255612, -1.558003200582610326, 0.5742671668342153035 ) ) ;
#10383=CARTESIAN_POINT ( 'NONE',  ( 0.3634331063870702705, -1.729372196318228028, 0.4280548696313287715 ) ) ;
#10384=CARTESIAN_POINT ( 'NONE',  ( 0.2369787301659028733, -1.147573247486365133, 0.6457685179108213491 ) ) ;
#10387=CARTESIAN_POINT ( 'NONE',  ( 0.1945367592390488398, -0.5021430848050445483, 0.3156752544587705933 ) ) ;
#10392=CARTESIAN_POINT ( 'NONE',  ( 0.4929832608774247782, -1.104425667152665991, 0.8058332650092189242 ) ) ;
#10393=CARTESIAN_POINT ( 'NONE',  ( 0.4561342652787643281, -1.116728573584468975, 0.5428924009958523422 ) ) ;
#10394=CARTESIAN_POINT ( 'NONE',  ( 0.008743562632478048963, -0.8600815613495956802, 0.3724168526861249551 ) ) ;
#10397=CARTESIAN_POINT ( 'NONE',  ( 0.3483176199711587318, -1.078699710109881194, 0.7396318397321306470 ) ) ;
#10404=CARTESIAN_POINT ( 'NONE',  ( 0.09079604095656999829, -0.5753325755772371597, 0.2071909514994974000 ) ) ;
#10406=DIRECTION ( 'NONE',  ( -1.000000000000000000, 0.000000000000000000, 0.000000000000000000 ) ) ;
#10408=ADVANCED_FACE ( 'NONE', ( #30475, #24308 ), #17524, .T. ) ;
#10409=CARTESIAN_POINT ( 'NONE',  ( 0.2164536357353635254, -1.200268718222536224, 0.7409067871576232589 ) ) ;
#10415=CARTESIAN_POINT ( 'NONE',  ( 0.4636748301137948447, -1.234986657158876122, 0.6895902313637624070 ) ) ;
#10417=CARTESIAN_POINT ( 'NONE',  ( 0.3174184176267917934, -1.762933076790991205, 0.5319023928053214778 ) ) ;
#10419=ORIENTED_EDGE ( 'NONE', *, *, #1875, .F. ) ;
#10422=CARTESIAN_POINT ( 'NONE',  ( 0.3875215993302730810, -1.517830918838856569, 0.8094752223628088883 ) ) ;
#10423=ADVANCED_FACE ( 'NONE', ( #2304 ), #14845, .T. ) ;
#10424=CARTESIAN_POINT ( 'NONE',  ( 0.08604873559162301566, -0.7971672130737051942, 0.05183853996302047878 ) ) ;
#10425=CARTESIAN_POINT ( 'NONE',  ( 0.1961281144780854524, -0.6676453483071772554, 0.3322964415046538722 ) ) ;
#10426=CARTESIAN_POINT ( 'NONE',  ( 0.1817694849310280136, -1.261899108304536110, 0.5084384546551340422 ) ) ;
#10430=CARTESIAN_POINT ( 'NONE',  ( 0.3325245471243513107, -1.290768314560045038, 0.5729784808290850906 ) ) ;
#10431=CARTESIAN_POINT ( 'NONE',  ( 0.5346825410386824018, -1.439718025093458920, 0.7637196853476909686 ) ) ;
#10438=CARTESIAN_POINT ( 'NONE',  ( 0.3845449968151027353, -1.722577193482669022, 0.6193603067054115341 ) ) ;
#10439=B_SPLINE_CURVE_WITH_KNOTS ( 'NONE', 3,
 ( #24782, #27257, #39786, #24176 ),
 .UNSPECIFIED., .F., .F.,
 ( 4, 4 ),
 ( 1.748223473168675632E-18, 0.0009765734425980529369 ),
 .UNSPECIFIED. ) ;
#10440=CARTESIAN_POINT ( 'NONE',  ( 0.6100913662829361428, -1.289225211610094401, 0.8693105457786516332 ) ) ;
#10446=CARTESIAN_POINT ( 'NONE',  ( 0.1839464713631710491, -0.5494516881424977850, 0.02732684068011371689 ) ) ;
#10450=CARTESIAN_POINT ( 'NONE',  ( 0.02242113575389428556, -0.7151737931810984161, 0.5646644402375310401 ) ) ;
#10458=ORIENTED_EDGE ( 'NONE', *, *, #7180, .T. ) ;
#10459=CARTESIAN_POINT ( 'NONE',  ( 0.4970758107849645446, -1.079867600816170059, 0.3667417262808778666 ) ) ;
#10461=CARTESIAN_POINT ( 'NONE',  ( 0.3728661538533184494, -1.740126085018506963, 0.4331033444688550116 ) ) ;
#10463=CARTESIAN_POINT ( 'NONE',  ( 0.4707424504419197020, -1.251593692541077107, 0.7595398601079852430 ) ) ;
#10464=CARTESIAN_POINT ( 'NONE',  ( 0.5935794547855036685, -1.611332463636045764, 0.4487275098415936525 ) ) ;
#10466=CARTESIAN_POINT ( 'NONE',  ( 0.2256328605772283669, -0.7491591359250245885, 0.4461645245400559512 ) ) ;
#10471=CARTESIAN_POINT ( 'NONE',  ( 0.3289079490030120123, -1.639352849464426498, 0.6015274726064920863 ) ) ;
#10472=EDGE_CURVE ( 'NONE', #2281, #35264, #1747, .T. ) ;
#10475=CARTESIAN_POINT ( 'NONE',  ( 0.1438681892407857876, -1.284094082863941111, 0.3157417262808777658 ) ) ;
#10479=CARTESIAN_POINT ( 'NONE',  ( 0.5447018010467034044, -1.168331122704159286, 0.5148643787740219135 ) ) ;
#10480=CARTESIAN_POINT ( 'NONE',  ( 0.1866070744275658277, -0.9155653071574156865, 0.1780381001982239975 ) ) ;
#10484=CARTESIAN_POINT ( 'NONE',  ( 0.1573455698924841606, -0.8938959663910659437, 0.5707458213001018743 ) ) ;
#10485=CARTESIAN_POINT ( 'NONE',  ( 0.1058066437981236146, -1.050304887260346876, 0.8576506362211480106 ) ) ;
#10486=CARTESIAN_POINT ( 'NONE',  ( 0.4905684254636979436, -1.178471512614451822, 0.4182417262808778013 ) ) ;
#10490=DIRECTION ( 'NONE',  ( -0.01254811300245605755, -0.8659344938869285579, -0.4999999971568663826 ) ) ;
#10493=CARTESIAN_POINT ( 'NONE',  ( 0.01387309669645373639, -1.022410628767960405, 0.5763875663499552493 ) ) ;
#10495=CARTESIAN_POINT ( 'NONE',  ( 0.1084311124255188524, -1.402644867855400657, 0.6343705678861770725 ) ) ;
#10497=CARTESIAN_POINT ( 'NONE',  ( 0.4719957491900099722, -1.679875000564180709, 0.4688966813032011682 ) ) ;
#10502=ORIENTED_EDGE ( 'NONE', *, *, #6998, .T. ) ;
#10507=CARTESIAN_POINT ( 'NONE',  ( 0.6007894471599048991, -1.477974513124123312, 0.6406838331186633928 ) ) ;
#10513=VERTEX_POINT ( 'NONE', #33755 ) ;
#10521=CARTESIAN_POINT ( 'NONE',  ( 0.002762111618723705336, -0.9534082139883239826, -0.1178596299512794793 ) ) ;
#10525=CARTESIAN_POINT ( 'NONE',  ( 0.1845623500247081106, -0.8903488908324218576, 0.5922637714853882240 ) ) ;
#10526=CARTESIAN_POINT ( 'NONE',  ( 0.06924657340766243729, -0.5400045880099085815, 0.1370866209488758869 ) ) ;
#10527=CARTESIAN_POINT ( 'NONE',  ( 0.1100840907954307585, -0.5526133480759019001, 0.1897287169192503620 ) ) ;
#10529=CARTESIAN_POINT ( 'NONE',  ( 0.03468330715085447130, -1.089634729100930954, 0.6338593068032741806 ) ) ;
#10532=CIRCLE ( 'NONE', #21053, 0.03749999999977545601 ) ;
#10533=CARTESIAN_POINT ( 'NONE',  ( 0.3379905402051226471, -1.761107921090772299, 0.5690149188013547965 ) ) ;
#10535=FACE_OUTER_BOUND ( 'NONE', #10555, .T. ) ;
#10539=CARTESIAN_POINT ( 'NONE',  ( -0.0003095478128742020006, -0.9052138808146785731, 0.02354638163038534626 ) ) ;
#10540=CARTESIAN_POINT ( 'NONE',  ( 0.5171109296076384920, -1.359203088151551331, 0.7981695906224013370 ) ) ;
#10541=CARTESIAN_POINT ( 'NONE',  ( 0.4970758107849645446, -1.079867600816170059, 0.3667417262808778666 ) ) ;
#10543=CARTESIAN_POINT ( 'NONE',  ( 0.1172025164431036715, -1.392648223243311723, 0.6963985612953286219 ) ) ;
#10544=CARTESIAN_POINT ( 'NONE',  ( 0.3630793090018165636, -0.9924503543686107321, 0.6290125294248597454 ) ) ;
#10546=EDGE_CURVE ( 'NONE', #13556, #27730, #5157, .T. ) ;
#10547=B_SPLINE_CURVE_WITH_KNOTS ( 'NONE', 3,
 ( #36112, #10613, #1381, #17608, #4621, #14503, #4831, #17402, #39001, #7732 ),
 .UNSPECIFIED., .F., .F.,
 ( 4, 2, 2, 2, 4 ),
 ( 0.000000000000000000, 0.0005419198834577468185, 0.001083839766915493637, 0.001625759650373240564, 0.002167679533830987274 ),
 .UNSPECIFIED. ) ;
#10549=DIRECTION ( 'NONE',  ( -0.1766035691529960483, -0.1934850654821817784, 0.9650775662079078554 ) ) ;
#10550=VERTEX_POINT ( 'NONE', #5348 ) ;
#10552=CARTESIAN_POINT ( 'NONE',  ( 0.002514036842440564665, -0.5353143163907467805, 0.2306785804606524271 ) ) ;
#10555=EDGE_LOOP ( 'NONE', ( #19403, #12144, #19236, #7723 ) ) ;
#10557=CARTESIAN_POINT ( 'NONE',  ( 0.1895831464430141888, -0.5047047246472139426, 0.1503823323309240734 ) ) ;
#10568=CARTESIAN_POINT ( 'NONE',  ( 0.5457411013609096972, -1.645686818912574179, 0.8576316932085735756 ) ) ;
#10569=CARTESIAN_POINT ( 'NONE',  ( 0.1145849041649253802, -0.6984622373509431492, 0.4166132103181554580 ) ) ;
#10570=CARTESIAN_POINT ( 'NONE',  ( 0.06413938869033396217, -0.7427754723600979991, 0.7547169867245954178 ) ) ;
#10571=CARTESIAN_POINT ( 'NONE',  ( 0.08541776836348415058, -0.5463775883488639629, 0.1813289453475219748 ) ) ;
#10574=CARTESIAN_POINT ( 'NONE',  ( 0.1986024623659905786, -1.088350075686307816, 0.6415510412962815989 ) ) ;
#10579=CARTESIAN_POINT ( 'NONE',  ( 0.1899112346947867958, -0.5366114675534041645, 0.1755787374122024513 ) ) ;
#10580=DIRECTION ( 'NONE',  ( 0.9998941247116546194, -0.01455087607601020412, 0.0001066420868422379362 ) ) ;
#10587=CARTESIAN_POINT ( 'NONE',  ( 0.4865355734717750624, -1.097175741254786452, 0.7494200075675998551 ) ) ;
#10589=CARTESIAN_POINT ( 'NONE',  ( 0.4933430811445716491, -1.186754567874577226, 0.4151382928142203221 ) ) ;
#10590=CARTESIAN_POINT ( 'NONE',  ( -0.002362956560267360107, -0.8470628361959046115, 0.1913124104053905150 ) ) ;
#10594=CARTESIAN_POINT ( 'NONE',  ( 0.3247155104185332486, -1.295292661530707878, 0.4306002955320518133 ) ) ;
#10595=CARTESIAN_POINT ( 'NONE',  ( 0.4065905862282702676, -1.156565771161806921, 0.7145884245918578959 ) ) ;
#10602=CARTESIAN_POINT ( 'NONE',  ( 0.4209449764515663106, -1.127703425338436372, 0.4919882752232563328 ) ) ;
#10603=CIRCLE ( 'NONE', #15870, 0.01000000000000002970 ) ;
#10604=CARTESIAN_POINT ( 'NONE',  ( 0.05856722883986545392, -0.8414967731140865492, 0.2843716283219245855 ) ) ;
#10605=ORIENTED_EDGE ( 'NONE', *, *, #40072, .T. ) ;
#10610=CARTESIAN_POINT ( 'NONE',  ( 0.4340920373745369432, -1.192938021670690407, 0.7091433560946051040 ) ) ;
#10613=CARTESIAN_POINT ( 'NONE',  ( 0.5346239700487379620, -1.154911596989372846, 0.5682481700188124485 ) ) ;
#10614=CARTESIAN_POINT ( 'NONE',  ( 0.2370370725713593918, -0.9423068241879761775, 0.4501375130042485906 ) ) ;
#10618=CIRCLE ( 'NONE', #21145, 0.04749999999977550652 ) ;
#10620=CARTESIAN_POINT ( 'NONE',  ( 0.2438426133570002763, -1.175331807871637269, 0.8706532464808368621 ) ) ;
#10621=CARTESIAN_POINT ( 'NONE',  ( 0.06797573035266660235, -0.5960914377309097789, 0.02939662547896050929 ) ) ;
#10622=CARTESIAN_POINT ( 'NONE',  ( 0.2018363294977822686, -0.7308029772144113423, 0.3390199763628233831 ) ) ;
#10624=ORIENTED_EDGE ( 'NONE', *, *, #33012, .F. ) ;
#10630=CARTESIAN_POINT ( 'NONE',  ( 0.1197446008095364028, -0.5662179169742945772, 0.2308386541185581120 ) ) ;
#10633=B_SPLINE_CURVE_WITH_KNOTS ( 'NONE', 3,
 ( #13782, #10706, #1680, #30223, #17494, #14197, #26348, #23280, #39292, #30046 ),
 .UNSPECIFIED., .F., .F.,
 ( 4, 2, 2, 2, 4 ),
 ( 3.469446951953614189E-18, 0.0005277335017653989350, 0.001055467003530794401, 0.001583200505296189758, 0.002110934007061585332 ),
 .UNSPECIFIED. ) ;
#10635=CARTESIAN_POINT ( 'NONE',  ( 0.2087112741175610464, -1.246538662281911236, 0.4623142537311495381 ) ) ;
#10640=CARTESIAN_POINT ( 'NONE',  ( 0.5573545814012507149, -1.203739305690170402, 0.8778060520269345135 ) ) ;
#10645=DIRECTION ( 'NONE',  ( -0.1166888840060208155, -0.08018547039157027101, -0.9899262571967228919 ) ) ;
#10647=CARTESIAN_POINT ( 'NONE',  ( 0.1849961625554341071, -0.7276430976136223361, -0.02180148029977278454 ) ) ;
#10648=CARTESIAN_POINT ( 'NONE',  ( 0.4168377001686644490, -1.242140235433856432, 0.4952185744155029323 ) ) ;
#10649=CARTESIAN_POINT ( 'NONE',  ( 0.1077840105943417282, -1.313547665849942314, 0.4360032343016825851 ) ) ;
#10654=CARTESIAN_POINT ( 'NONE',  ( 0.2890670123411187564, -1.729633309587475187, 0.5682417262808785452 ) ) ;
#10660=ORIENTED_EDGE ( 'NONE', *, *, #24826, .T. ) ;
#10661=EDGE_LOOP ( 'NONE', ( #7974, #5010, #18673, #15892, #21618, #4252, #23234 ) ) ;
#10666=CARTESIAN_POINT ( 'NONE',  ( 0.4760599958747125937, -1.259643329453308924, 0.7570774943031273185 ) ) ;
#10669=CARTESIAN_POINT ( 'NONE',  ( 0.3146548270004942971, -0.9167534899940792403, 0.6079632372063322743 ) ) ;
#10672=CARTESIAN_POINT ( 'NONE',  ( 0.3229289876128840775, -1.169687821100875658, 0.5631135379446852163 ) ) ;
#10673=ORIENTED_EDGE ( 'NONE', *, *, #8244, .T. ) ;
#10674=CARTESIAN_POINT ( 'NONE',  ( 0.3255049925932525512, -1.611144953433153448, 0.7534810049541833532 ) ) ;
#10679=ORIENTED_EDGE ( 'NONE', *, *, #23113, .T. ) ;
#10680=EDGE_CURVE ( 'NONE', #23498, #1496, #28724, .T. ) ;
#10681=CARTESIAN_POINT ( 'NONE',  ( 0.5446972779418673971, -1.168323287519652975, 0.4762509439642684250 ) ) ;
#10684=ADVANCED_FACE ( 'NONE', ( #21634 ), #12018, .T. ) ;
#10687=CARTESIAN_POINT ( 'NONE',  ( 0.1170610741652670789, -0.8436375311889402484, 0.3825169963771947179 ) ) ;
#10688=CARTESIAN_POINT ( 'NONE',  ( 0.01061034631529937829, -0.5352819679159596111, 0.1926328805739365713 ) ) ;
#10696=CARTESIAN_POINT ( 'NONE',  ( 0.6059510396320981762, -1.580958211694154292, 0.4182417262808776348 ) ) ;
#10697=CONICAL_SURFACE ( 'NONE', #5417, 0.1762268159172233339, 0.7853981633974500554 ) ;
#10699=CARTESIAN_POINT ( 'NONE',  ( 0.2722331219925429036, -1.671874623808670135, 0.4849083929475441201 ) ) ;
#10701=CARTESIAN_POINT ( 'NONE',  ( 0.06481251280142887039, -1.340178673227269801, 0.5794969380269323622 ) ) ;
#10706=CARTESIAN_POINT ( 'NONE',  ( 0.3985218788515150212, -1.105145776744873798, 0.6030479543138400622 ) ) ;
#10708=CARTESIAN_POINT ( 'NONE',  ( 0.3102026568030923914, -1.754211112397273009, 0.6570273542612804496 ) ) ;
#10714=CARTESIAN_POINT ( 'NONE',  ( 0.1772270119712388292, -0.4894770652708761438, 0.1265226523157877703 ) ) ;
#10715=ORIENTED_EDGE ( 'NONE', *, *, #36036, .F. ) ;
#10718=CARTESIAN_POINT ( 'NONE',  ( 0.1601225296750040661, -0.6765572740170349153, 0.4594829422558849852 ) ) ;
#10719=VERTEX_POINT ( 'NONE', #18914 ) ;
#10723=CARTESIAN_POINT ( 'NONE',  ( 0.1220110744298638639, -0.4984167407757109647, 0.3414028199781711792 ) ) ;
#10725=CARTESIAN_POINT ( 'NONE',  ( 0.1226099275768244429, -1.148810827165510862, 0.9082586858799801544 ) ) ;
#10727=CARTESIAN_POINT ( 'NONE',  ( 0.1676546834103173622, -1.385519403818823436, 0.5281503411795812619 ) ) ;
#10730=CARTESIAN_POINT ( 'NONE',  ( 0.001778485958989725092, -0.5275076572294763455, -0.01138449076159588590 ) ) ;
#10733=CARTESIAN_POINT ( 'NONE',  ( 0.1318732271430533010, -0.8550887030632243757, 0.4701083376385029045 ) ) ;
#10735=CARTESIAN_POINT ( 'NONE',  ( 0.07151319716137326254, -0.5632038019116255567, 0.2489596798534031985 ) ) ;
#10736=CARTESIAN_POINT ( 'NONE',  ( 0.3901811030578707373, -1.256540976566071333, 0.8456182275435326634 ) ) ;
#10738=CARTESIAN_POINT ( 'NONE',  ( 0.3865586847035667462, -1.614704152518654512, 0.5182417262812423209 ) ) ;
#10739=CARTESIAN_POINT ( 'NONE',  ( 0.6504330680646749352, -1.464154268620814880, 0.4118863462905618111 ) ) ;
#10742=CARTESIAN_POINT ( 'NONE',  ( 0.3373037064751163716, -1.749770764905459242, 0.5760335165290267900 ) ) ;
#10745=CARTESIAN_POINT ( 'NONE',  ( 0.06829362261317843685, -1.326848020601397504, 0.5207672198342441217 ) ) ;
#10746=AXIS2_PLACEMENT_3D ( 'NONE', #19532, #13734, #34176 ) ;
#10749=CARTESIAN_POINT ( 'NONE',  ( 0.01146630784979661005, -0.8949520681090487040, -0.009824401211993303087 ) ) ;
#10750=CARTESIAN_POINT ( 'NONE',  ( 0.4693814222616094489, -1.280284924017013770, 0.8165702439546136393 ) ) ;
#10752=EDGE_CURVE ( 'NONE', #356, #12111, #21859, .T. ) ;
#10755=CARTESIAN_POINT ( 'NONE',  ( 0.07582666994630285484, -1.068917391567854036, 0.8049195030047635591 ) ) ;
#10757=CARTESIAN_POINT ( 'NONE',  ( 0.4928237909781065240, -1.082648202709539431, 0.5731206881285608734 ) ) ;
#10759=CARTESIAN_POINT ( 'NONE',  ( 0.3508337187165347926, -0.8535322721259723799, 0.7608596062780633718 ) ) ;
#10763=EDGE_CURVE ( 'NONE', #14, #32251, #223, .T. ) ;
#10764=CARTESIAN_POINT ( 'NONE',  ( 0.3768783096114511344, -1.720370743462839025, 0.4222122349756194382 ) ) ;
#10765=CARTESIAN_POINT ( 'NONE',  ( 0.3061479062650170335, -1.759180248854478101, 0.5686207101516911333 ) ) ;
#10767=ORIENTED_EDGE ( 'NONE', *, *, #9716, .F. ) ;
#10769=CARTESIAN_POINT ( 'NONE',  ( 0.003257547668126477714, -0.5625981998575959597, 0.2841698052623323201 ) ) ;
#10772=CARTESIAN_POINT ( 'NONE',  ( 0.06319106323617752763, -1.336233308022867217, 0.5682657828639668951 ) ) ;
#10773=CARTESIAN_POINT ( 'NONE',  ( 0.4107733320947055122, -0.9780847931859447675, 0.7674390821536307694 ) ) ;
#10785=CARTESIAN_POINT ( 'NONE',  ( 0.009263959265383548899, -0.5910811120922173645, 0.02017480025628250878 ) ) ;
#10786=CARTESIAN_POINT ( 'NONE',  ( 0.1529695162128977548, -0.7869584365478802246, 0.5431710472807829149 ) ) ;
#10788=CARTESIAN_POINT ( 'NONE',  ( 0.1454824607866254671, -1.106208088005755208, 0.9808573752210623109 ) ) ;
#10789=CARTESIAN_POINT ( 'NONE',  ( 0.08551960242419305580, -0.5485164467215365436, 0.1912689294972731158 ) ) ;
#10791=CARTESIAN_POINT ( 'NONE',  ( 0.2661871413848379553, -1.687809284679251620, 0.5876828195007447464 ) ) ;
#10793=CARTESIAN_POINT ( 'NONE',  ( 0.1684731838197772724, -0.9467412257359250072, 0.4230012374223513505 ) ) ;
#10796=CARTESIAN_POINT ( 'NONE',  ( 0.3460582752528997830, -1.629311570083116889, 0.5557434574143875761 ) ) ;
#10797=CARTESIAN_POINT ( 'NONE',  ( 0.1190390134088109841, -0.4827176764154528787, 0.3011203263016439813 ) ) ;
#10805=CARTESIAN_POINT ( 'NONE',  ( 0.5008076730341156635, -1.117067070538257489, 0.7495569431474730093 ) ) ;
#10806=AXIS2_PLACEMENT_3D ( 'NONE', #18049, #6090, #5698 ) ;
#10809=CARTESIAN_POINT ( 'NONE',  ( 0.02715706672027885099, -0.9320027591207687978, 0.6014473777329288895 ) ) ;
#10813=CARTESIAN_POINT ( 'NONE',  ( 0.2636704545280705303, -1.001036816892615811, 0.7140474771236937634 ) ) ;
#10816=CARTESIAN_POINT ( 'NONE',  ( 0.5741497723391727481, -1.420869068547097269, 0.6057417262805909752 ) ) ;
#10817=( BOUNDED_SURFACE ( )  B_SPLINE_SURFACE ( 3, 2, ( 
 ( #22795, #3830, #35497 ),
 ( #3644, #6710, #31616 ),
 ( #25462, #16594, #32211 ),
 ( #15990, #19675, #25873 ),
 ( #16206, #4240, #38187 ),
 ( #10417, #13698, #29138 ) ),
 .UNSPECIFIED., .F., .F., .F. ) 
 B_SPLINE_SURFACE_WITH_KNOTS ( ( 4, 2, 4 ),
 ( 3, 3 ),
 ( 3.903127820947815962E-18, 0.0005634672180686404065, 0.001126934436137276910 ),
 ( 0.000000000000000000, 1.000000000000000000 ),
 .UNSPECIFIED. ) 
 GEOMETRIC_REPRESENTATION_ITEM ( )  RATIONAL_B_SPLINE_SURFACE ( (
 ( 1.000000000000000000, 0.9544113358811391334, 1.000000000000000000),
 ( 1.000000000000000000, 0.9558699249329746239, 1.000000000000000000),
 ( 1.000000000000000000, 0.9497853595015035566, 1.000000000000000000),
 ( 1.000000000000000000, 0.9203877932839388265, 1.000000000000000000),
 ( 1.000000000000000000, 0.8974056080853995976, 1.000000000000000000),
 ( 1.000000000000000000, 0.8602827799847387880, 1.000000000000000000) ) ) 
 REPRESENTATION_ITEM ( '' )  SURFACE ( )  );
#10824=CARTESIAN_POINT ( 'NONE',  ( 0.03202889392918464168, -0.8409986250695942189, 0.1806008807001980021 ) ) ;
#10825=EDGE_LOOP ( 'NONE', ( #14058, #26726 ) ) ;
#10828=CARTESIAN_POINT ( 'NONE',  ( 0.4152335211599790799, -1.084324332244355205, 0.5182417262812423209 ) ) ;
#10830=AXIS2_PLACEMENT_3D ( 'NONE', #33744, #8634, #27785 ) ;
#10831=CARTESIAN_POINT ( 'NONE',  ( 0.4450023961560361507, -1.208088614032591490, 0.7033065338990315274 ) ) ;
#10832=CARTESIAN_POINT ( 'NONE',  ( 0.4124787977826392948, -1.129720521516186960, 0.5352010793853081427 ) ) ;
#10836=CIRCLE ( 'NONE', #4271, 0.04749999999977543713 ) ;
#10842=CARTESIAN_POINT ( 'NONE',  ( 0.05093431041759328981, -0.5776221905076182050, 0.2999712174261540132 ) ) ;
#10843=CARTESIAN_POINT ( 'NONE',  ( 0.06891712773961738980, -0.5465723661966604974, 0.1009469152245711515 ) ) ;
#10845=CARTESIAN_POINT ( 'NONE',  ( 0.1700813958898667599, -1.268695326050480299, 0.4882188859375907741 ) ) ;
#10849=CARTESIAN_POINT ( 'NONE',  ( 0.4441618370914984237, -1.292678418814498187, 0.8278337041136846208 ) ) ;
#10854=B_SPLINE_CURVE_WITH_KNOTS ( 'NONE', 3,
 ( #32042, #9825, #37815, #29159, #22996, #16826, #13532, #22397, #13115, #13319, #35518, #34720, #32437, #29372 ),
 .UNSPECIFIED., .F., .F.,
 ( 4, 2, 2, 2, 2, 2, 4 ),
 ( 0.002220865337158942510, 0.002866522892504111235, 0.003512180447849279526, 0.003835009225521858467, 0.004157838003194438276, 0.004480666780867017217, 0.004803495558539596158 ),
 .UNSPECIFIED. ) ;
#10855=CARTESIAN_POINT ( 'NONE',  ( 0.1856343102545933432, -1.259872755799225086, 0.4406686558725164127 ) ) ;
#10856=CARTESIAN_POINT ( 'NONE',  ( 0.07006815180908280982, -1.315301596572416631, 0.5080907171456734428 ) ) ;
#10858=CARTESIAN_POINT ( 'NONE',  ( 0.4504805333218593333, -1.026900667268108469, 0.8467065612799143937 ) ) ;
#10859=FACE_OUTER_BOUND ( 'NONE', #36716, .T. ) ;
#10860=CARTESIAN_POINT ( 'NONE',  ( 0.07973371882703013391, -1.320969072382258913, 0.5669061587800955371 ) ) ;
#10872=LINE ( 'NONE', #29997, #25221 ) ;
#10877=B_SPLINE_CURVE_WITH_KNOTS ( 'NONE', 3,
 ( #34926, #6731, #19308, #31850 ),
 .UNSPECIFIED., .F., .F.,
 ( 4, 4 ),
 ( 5.151976560715283563E-05, 0.0009056307464049973130 ),
 .UNSPECIFIED. ) ;
#10882=CARTESIAN_POINT ( 'NONE',  ( 0.3754387176203204946, -1.765456752270669449, 0.5182417262812423209 ) ) ;
#10884=CARTESIAN_POINT ( 'NONE',  ( 0.5546139119538038287, -1.386769227612277611, 0.6118514161299568599 ) ) ;
#10887=CARTESIAN_POINT ( 'NONE',  ( 0.4609105641225965111, -1.064890115380353386, 0.6919706562625183022 ) ) ;
#10891=CARTESIAN_POINT ( 'NONE',  ( 0.3267929376468292069, -1.639096506223164829, 0.5708619501093183946 ) ) ;
#10892=CARTESIAN_POINT ( 'NONE',  ( 0.6579944548887032285, -1.543696042244296462, 0.4299453908671848068 ) ) ;
#10893=CARTESIAN_POINT ( 'NONE',  ( 0.1880883187714730009, -0.5243002637854453640, 0.1042455497702089173 ) ) ;
#10894=CARTESIAN_POINT ( 'NONE',  ( 0.4090604450045443596, -1.131420581850358653, 0.3667417262808778666 ) ) ;
#10897=CIRCLE ( 'NONE', #29307, 0.02500000000000004996 ) ;
#10901=EDGE_CURVE ( 'NONE', #3626, #40153, #12487, .T. ) ;
#10902=CARTESIAN_POINT ( 'NONE',  ( 0.3754333920846802952, -1.248282022732751351, 0.6420704804048268377 ) ) ;
#10904=CARTESIAN_POINT ( 'NONE',  ( 0.5891906343740130891, -1.485326646281273089, 0.6398249741016610592 ) ) ;
#10907=CIRCLE ( 'NONE', #39151, 0.009999999999999998473 ) ;
#10912=CARTESIAN_POINT ( 'NONE',  ( 0.4368279861776801498, -1.677667223885810577, 0.4282417262809075087 ) ) ;
#10914=CARTESIAN_POINT ( 'NONE',  ( 0.02646712690499511758, -1.095781990028246833, 0.6523102692877094100 ) ) ;
#10916=DIRECTION ( 'NONE',  ( 0.000000000000000000, 0.5550234895931941415, 0.8318346746798871427 ) ) ;
#10919=CARTESIAN_POINT ( 'NONE',  ( 0.2213055653232768594, -1.375750682257318447, 1.025040830464602815 ) ) ;
#10926=CARTESIAN_POINT ( 'NONE',  ( 0.1791081599780166012, -0.4927798373357311079, 0.1046006427271031491 ) ) ;
#10929=LINE ( 'NONE', #36626, #15141 ) ;
#10932=CARTESIAN_POINT ( 'NONE',  ( 0.6022170153251571456, -1.483150505077808878, 0.5777505789966421723 ) ) ;
#10934=CARTESIAN_POINT ( 'NONE',  ( -0.001802072477946061032, -0.8317662731473794979, 0.07689373464280477299 ) ) ;
#10939=CARTESIAN_POINT ( 'NONE',  ( 0.1411908422770818405, -0.5631842745024300267, 0.4719898812008860300 ) ) ;
#10942=CARTESIAN_POINT ( 'NONE',  ( 0.2363740895084206761, -1.537497096284702103, 0.8974013143058253705 ) ) ;
#10948=ORIENTED_EDGE ( 'NONE', *, *, #29215, .F. ) ;
#10950=CARTESIAN_POINT ( 'NONE',  ( 0.09328054744289671074, -0.8198616939459991704, 0.2909628914676452016 ) ) ;
#10951=CARTESIAN_POINT ( 'NONE',  ( 0.06913471046454594537, -1.118970164930346733, 0.7557088715074291585 ) ) ;
#10952=CARTESIAN_POINT ( 'NONE',  ( 0.1445232641043270594, -0.7452533224692177161, 0.5265950822232948747 ) ) ;
#10953=CARTESIAN_POINT ( 'NONE',  ( 0.5536391078438838154, -1.507869940163521827, 0.6342902233424858593 ) ) ;
#10954=CARTESIAN_POINT ( 'NONE',  ( 0.06005323737745657531, -1.257861521318574205, 0.6484451051230492036 ) ) ;
#10957=CARTESIAN_POINT ( 'NONE',  ( 0.5446874837152237969, -1.168306321392260649, 0.4290006342139815465 ) ) ;
#10961=CARTESIAN_POINT ( 'NONE',  ( 0.06747690200237689562, -1.330070943150472917, 0.5060650602545671006 ) ) ;
#10964=CARTESIAN_POINT ( 'NONE',  ( -0.0001419198701252090346, -0.8132405810867952001, -0.06941372320109172322 ) ) ;
#10965=CARTESIAN_POINT ( 'NONE',  ( 0.5655345595830957306, -1.445718534125680410, 0.7372501758031703156 ) ) ;
#10967=LENGTH_MEASURE_WITH_UNIT ( LENGTH_MEASURE( 0.02539999999999999897 ), #38919 );
#10968=CARTESIAN_POINT ( 'NONE',  ( 0.006846968701975976630, -0.8130952999835362460, 0.04930517669358801952 ) ) ;
#10969=B_SPLINE_CURVE_WITH_KNOTS ( 'NONE', 3,
 ( #38359, #37971, #22351, #22766, #32188, #34869 ),
 .UNSPECIFIED., .F., .F.,
 ( 4, 2, 4 ),
 ( 0.0001296384739227541844, 0.002096621291417103024, 0.004063604108911452080 ),
 .UNSPECIFIED. ) ;
#10972=CARTESIAN_POINT ( 'NONE',  ( 0.02760435326350026836, -0.9850525496912549972, 0.6581503728771671557 ) ) ;
#10973=CARTESIAN_POINT ( 'NONE',  ( 0.2060221519102763132, -0.8840977030479291177, 0.3560353928791143985 ) ) ;
#10975=CARTESIAN_POINT ( 'NONE',  ( 0.2064087850599171381, -0.5517209573913892662, 0.4235422224703019323 ) ) ;
#10977=CARTESIAN_POINT ( 'NONE',  ( 0.3048327051194437698, -1.756855311985219936, 0.5690458522854572321 ) ) ;
#10981=CARTESIAN_POINT ( 'NONE',  ( 0.1023069199889618808, -1.037162491060638736, 0.8507079986674529470 ) ) ;
#10989=CARTESIAN_POINT ( 'NONE',  ( 0.6761418372287171241, -1.395094899906518471, 0.6557117145240808354 ) ) ;
#10999=CARTESIAN_POINT ( 'NONE',  ( 0.08878836246962278078, -0.6867776948031327766, 0.2056562767453794516 ) ) ;
#11000=CARTESIAN_POINT ( 'NONE',  ( 0.2852911188406123122, -1.556753723687055224, 0.9829980583461535026 ) ) ;
#11001=CARTESIAN_POINT ( 'NONE',  ( 0.09766204791072935487, -0.5457031429471165263, 0.1623845927645223841 ) ) ;
#11002=CARTESIAN_POINT ( 'NONE',  ( 0.2650451966282841298, -1.687516040838051845, 0.5730406266932795978 ) ) ;
#11003=CARTESIAN_POINT ( 'NONE',  ( 0.3116047323306956884, -1.649437158552430338, 0.5948350866965763650 ) ) ;
#11004=ADVANCED_FACE ( 'NONE', ( #11855 ), #3461, .T. ) ;
#11005=CARTESIAN_POINT ( 'NONE',  ( 0.04706940247297254631, -0.9403352153122209733, 0.1954608171380558534 ) ) ;
#11008=B_SPLINE_CURVE_WITH_KNOTS ( 'NONE', 3,
 ( #30115, #1946, #36691, #33808 ),
 .UNSPECIFIED., .F., .F.,
 ( 4, 4 ),
 ( 0.0006408076469776195555, 0.0007877951202762262500 ),
 .UNSPECIFIED. ) ;
#11009=ADVANCED_FACE ( 'NONE', ( #27506 ), #17170, .T. ) ;
#11010=CARTESIAN_POINT ( 'NONE',  ( 0.2178843723336029436, -0.5744936670103212295, 0.4629775832872777830 ) ) ;
#11011=B_SPLINE_CURVE_WITH_KNOTS ( 'NONE', 3,
 ( #19794, #23105, #22911, #3947 ),
 .UNSPECIFIED., .F., .F.,
 ( 4, 4 ),
 ( 0.000000000000000000, 0.0004498717961012255943 ),
 .UNSPECIFIED. ) ;
#11016=CARTESIAN_POINT ( 'NONE',  ( 0.1909052096321314784, -0.5854118129141068216, 0.1777712087850742972 ) ) ;
#11019=CARTESIAN_POINT ( 'NONE',  ( 0.3297273269827796782, -1.292423171921244895, 0.4805102893914065532 ) ) ;
#11025=CARTESIAN_POINT ( 'NONE',  ( 0.4640588441595929203, -1.068323083224587577, 0.7162715700772641636 ) ) ;
#11028=CARTESIAN_POINT ( 'NONE',  ( 0.4139226612333222199, -1.128928040977267511, 0.5474757255584167259 ) ) ;
#11029=CARTESIAN_POINT ( 'NONE',  ( 0.2774637254902345140, -1.318135075689816249, 0.6011524605781312092 ) ) ;
#11030=VERTEX_POINT ( 'NONE', #16570 ) ;
#11035=CARTESIAN_POINT ( 'NONE',  ( 0.3647626819780801499, -1.106519030682488802, 0.7096260846467223882 ) ) ;
#11037=CARTESIAN_POINT ( 'NONE',  ( 0.5670576198622274688, -1.627347961110953367, 0.5260709129414246066 ) ) ;
#11044=CARTESIAN_POINT ( 'NONE',  ( 0.4083779858257735040, -1.563267192213793511, 0.7363480300735880668 ) ) ;
#11045=CARTESIAN_POINT ( 'NONE',  ( 0.08836802265519826116, -0.6144346768691744121, 0.02127763492959088010 ) ) ;
#11052=CARTESIAN_POINT ( 'NONE',  ( 0.2359862434256725650, -0.8906993715589636151, 0.6977976417879780957 ) ) ;
#11058=CARTESIAN_POINT ( 'NONE',  ( 0.1806433941755341832, -1.251233634640312120, 0.4406669043849698597 ) ) ;
#11060=CARTESIAN_POINT ( 'NONE',  ( 0.6638964227572436982, -1.375154404986101531, 0.8002223753517787586 ) ) ;
#11067=CARTESIAN_POINT ( 'NONE',  ( 0.002083146443013456344, -0.4777046557262296100, 0.09357736723029726200 ) ) ;
#11069=CARTESIAN_POINT ( 'NONE',  ( 0.4226000438817392180, -1.709616762427842218, 0.4282184315516496809 ) ) ;
#11070=ADVANCED_FACE ( 'NONE', ( #38759 ), #33997, .T. ) ;
#11071=CARTESIAN_POINT ( 'NONE',  ( 0.5975349495741208994, -1.597363011650178688, 0.4182417262808776903 ) ) ;
#11076=CARTESIAN_POINT ( 'NONE',  ( 0.6540709664215760277, -1.593060928864740156, 0.5182417262812423209 ) ) ;
#11077=CARTESIAN_POINT ( 'NONE',  ( 0.3208715077212234701, -1.182672892261233732, 0.4687417262808780127 ) ) ;
#11081=CARTESIAN_POINT ( 'NONE',  ( 0.5095464092883764673, -1.311269877878546763, 0.7328776202162170517 ) ) ;
#11084=CARTESIAN_POINT ( 'NONE',  ( 0.2122887247597850247, -0.8188226314918697346, 0.3927370908608381339 ) ) ;
#11088=ORIENTED_EDGE ( 'NONE', *, *, #14788, .F. ) ;
#11089=CARTESIAN_POINT ( 'NONE',  ( 0.02322197787115687709, -0.5342335529176228670, 0.1743862541488195861 ) ) ;
#11090=CARTESIAN_POINT ( 'NONE',  ( 0.7077821646032427250, -1.503511044123807316, 0.5489718279396991196 ) ) ;
#11091=CARTESIAN_POINT ( 'NONE',  ( 0.1764183673576233957, -0.5463805283139606672, -0.03610222269428862291 ) ) ;
#11092=CARTESIAN_POINT ( 'NONE',  ( 0.2319960710055803677, -1.232736008543062090, 0.4687417262808780127 ) ) ;
#11096=CARTESIAN_POINT ( 'NONE',  ( 0.1598324831679015234, -1.276895193453223776, 0.4182417262808777458 ) ) ;
#11098=CARTESIAN_POINT ( 'NONE',  ( 0.3313744226343967036, -1.290158028341789276, 0.5896145059446814551 ) ) ;
#11102=B_SPLINE_CURVE_WITH_KNOTS ( 'NONE', 3,
 ( #21336, #8759, #24024, #14741 ),
 .UNSPECIFIED., .F., .F.,
 ( 4, 4 ),
 ( 0.005101096601136854980, 0.009027368544441125020 ),
 .UNSPECIFIED. ) ;
#11103=CARTESIAN_POINT ( 'NONE',  ( 0.3965913301904470112, -1.111811593118468666, 0.6217369508112339238 ) ) ;
#11109=CARTESIAN_POINT ( 'NONE',  ( 0.4186431762316955019, -1.143068542649264163, 0.4275947501741096946 ) ) ;
#11110=CARTESIAN_POINT ( 'NONE',  ( 0.1770675091758397157, -0.4892248890959581820, 0.1433326821102208493 ) ) ;
#11113=CARTESIAN_POINT ( 'NONE',  ( 0.01212774845371318924, -0.4356706518047467891, 0.08239804974011019634 ) ) ;
#11115=CARTESIAN_POINT ( 'NONE',  ( 0.1352158960584371739, -1.069175309996540202, 0.9661058881916898544 ) ) ;
#11122=CARTESIAN_POINT ( 'NONE',  ( 0.1344413119357726061, -0.5591674697507452718, 0.1973459964408592893 ) ) ;
#11124=CARTESIAN_POINT ( 'NONE',  ( 0.008064696880236928156, -0.7084159389384210304, -0.01121069830473241102 ) ) ;
#11127=CARTESIAN_POINT ( 'NONE',  ( 0.1175045378272833174, -0.4723384530406989912, 0.2724513898149077962 ) ) ;
#11128=EDGE_LOOP ( 'NONE', ( #36596, #14043, #27018, #29708, #2278, #34838, #12622, #27395 ) ) ;
#11129=CARTESIAN_POINT ( 'NONE',  ( 0.2573325307069851409, -1.608293788183657869, 0.8328901382586275659 ) ) ;
#11131=CARTESIAN_POINT ( 'NONE',  ( 0.2101924623511064461, -1.233948830739026503, 0.5631135211526988593 ) ) ;
#11135=EDGE_LOOP ( 'NONE', ( #3480, #30869, #34920, #84, #28329 ) ) ;
#11138=CARTESIAN_POINT ( 'NONE',  ( 0.08480723791494081121, -1.210854647815037932, 0.7609210295126361823 ) ) ;
#11139=CARTESIAN_POINT ( 'NONE',  ( 0.1531589382160408741, -0.7640739595342987966, 0.5488755516528662781 ) ) ;
#11140=CARTESIAN_POINT ( 'NONE',  ( 0.5530210029615032497, -1.511195326521239224, 0.5738729771428068283 ) ) ;
#11142=CARTESIAN_POINT ( 'NONE',  ( 0.6030593677082874970, -1.482073155342621851, 0.6044986214589193052 ) ) ;
#11145=CARTESIAN_POINT ( 'NONE',  ( 0.6983789749627276056, -1.438823976843206509, 0.5652110266803307415 ) ) ;
#11151=CARTESIAN_POINT ( 'NONE',  ( 0.4075835738538290398, -1.123965384694001868, 0.6035659867371363507 ) ) ;
#11152=CARTESIAN_POINT ( 'NONE',  ( 0.3279590963379148683, -1.123159558159656957, 0.5182417262812423209 ) ) ;
#11156=CARTESIAN_POINT ( 'NONE',  ( 0.004343411016521666126, -0.7362306918419727619, 0.3916307744012189618 ) ) ;
#11157=CARTESIAN_POINT ( 'NONE',  ( 0.4928690250500026293, -1.082673021089655574, 0.5721439028494731405 ) ) ;
#11159=CARTESIAN_POINT ( 'NONE',  ( 0.2723301224276278298, -0.7044396210649886969, 0.6356112240561296867 ) ) ;
#11162=( BOUNDED_SURFACE ( )  B_SPLINE_SURFACE ( 3, 2, ( 
 ( #28400, #27588, #12158 ),
 ( #40114, #2690, #37251 ),
 ( #24916, #11945, #12553 ),
 ( #37443, #24508, #18126 ) ),
 .UNSPECIFIED., .F., .F., .F. ) 
 B_SPLINE_SURFACE_WITH_KNOTS ( ( 4, 4 ),
 ( 3, 3 ),
 ( 2.764715539838036307E-18, 0.001173839118112707421 ),
 ( 0.000000000000000000, 1.000000000000000000 ),
 .UNSPECIFIED. ) 
 GEOMETRIC_REPRESENTATION_ITEM ( )  RATIONAL_B_SPLINE_SURFACE ( (
 ( 1.000000000000000000, 0.9157534740979349497, 1.000000000000000000),
 ( 1.000000000000000000, 0.9253442540293808083, 1.000000000000000000),
 ( 1.000000000000000000, 0.9341318845569276386, 1.000000000000000000),
 ( 1.000000000000000000, 0.9411999499705258065, 1.000000000000000000) ) ) 
 REPRESENTATION_ITEM ( '' )  SURFACE ( )  );
#11163=EDGE_CURVE ( 'NONE', #26173, #7249, #36545, .T. ) ;
#11167=CARTESIAN_POINT ( 'NONE',  ( 0.1740866738651369872, -1.306816224518804415, 0.9481330771635244625 ) ) ;
#11168=CARTESIAN_POINT ( 'NONE',  ( 0.1099539500251690283, -1.292169261604334540, 0.4406931972238851691 ) ) ;
#11170=VERTEX_POINT ( 'NONE', #38873 ) ;
#11172=CARTESIAN_POINT ( 'NONE',  ( 0.1906247196645202702, -0.5843772811062371009, 0.1457185332388696020 ) ) ;
#11183=CARTESIAN_POINT ( 'NONE',  ( 0.08952804818007449594, -0.6881766246006204568, 0.2235799437253089272 ) ) ;
#11184=CARTESIAN_POINT ( 'NONE',  ( 0.2100130340724439826, -1.285393126011718623, 1.028891139539269250 ) ) ;
#11185=CIRCLE ( 'NONE', #34174, 0.01000000000000001582 ) ;
#11186=CARTESIAN_POINT ( 'NONE',  ( 0.4978489536914548208, -1.542573269935797686, 0.5796211865037168565 ) ) ;
#11187=CARTESIAN_POINT ( 'NONE',  ( 0.1953104519840635767, -1.377916898911103472, 0.9490300120740665646 ) ) ;
#11189=CARTESIAN_POINT ( 'NONE',  ( 0.2751433273660585099, -1.204544342693914860, 0.5922316713047012238 ) ) ;
#11193=CARTESIAN_POINT ( 'NONE',  ( 0.2048162548087716639, -0.6103794925887051637, 0.3711584868840494544 ) ) ;
#11202=CARTESIAN_POINT ( 'NONE',  ( 0.3578995607061009054, -0.9255625346965836719, 0.6844156867609741957 ) ) ;
#11212=CARTESIAN_POINT ( 'NONE',  ( 0.3510880644213571489, -0.9448783719387029434, 0.6508378404258201577 ) ) ;
#11214=CARTESIAN_POINT ( 'NONE',  ( 0.3979671137871990116, -1.137957823998669848, 0.4904217454224647499 ) ) ;
#11215=CARTESIAN_POINT ( 'NONE',  ( 0.1897997141002692179, -1.273939956134424234, 0.7173303927998203600 ) ) ;
#11221=CARTESIAN_POINT ( 'NONE',  ( 0.4684633558679283660, -1.238878407153067851, 0.5960060519205929719 ) ) ;
#11224=CARTESIAN_POINT ( 'NONE',  ( 0.2296032268162506162, -0.9382281285954664485, 0.4302797228108481420 ) ) ;
#11229=CARTESIAN_POINT ( 'NONE',  ( 0.1184242373551691735, -0.7868154500338676582, 0.6262615020233922580 ) ) ;
#11230=CARTESIAN_POINT ( 'NONE',  ( 0.06842540263846834392, -0.5687803859286276742, 0.05749882982346820465 ) ) ;
#11232=CARTESIAN_POINT ( 'NONE',  ( 0.1826048122412617103, -1.261403426677984108, 0.5133468128926989005 ) ) ;
#11233=ORIENTED_EDGE ( 'NONE', *, *, #24141, .T. ) ;
#11237=CARTESIAN_POINT ( 'NONE',  ( 0.2939024926760947509, -1.010691472418420389, 0.7713339393085973938 ) ) ;
#11242=CIRCLE ( 'NONE', #2032, 0.08249999999977555842 ) ;
#11245=CARTESIAN_POINT ( 'NONE',  ( 0.2343801618657880559, -1.231732140494844030, 0.5084283139525508366 ) ) ;
#11250=CARTESIAN_POINT ( 'NONE',  ( 0.6859459673519229250, -1.411154268469613227, 0.7682993476293730195 ) ) ;
#11253=ADVANCED_FACE ( 'NONE', ( #30221 ), #39290, .F. ) ;
#11255=VECTOR ( 'NONE', #20306, 39.37007874015748143 ) ;
#11259=CARTESIAN_POINT ( 'NONE',  ( 0.08344352785338075840, -1.320654673502084098, 0.4605903863189703684 ) ) ;
#11261=CARTESIAN_POINT ( 'NONE',  ( 0.04961935711675592720, -0.7636540146707464505, 0.7296111229395446651 ) ) ;
#11263=EDGE_CURVE ( 'NONE', #16305, #20093, #24495, .T. ) ;
#11272=CARTESIAN_POINT ( 'NONE',  ( 0.3207148961678939481, -1.182401600646133089, 0.3667417262808778111 ) ) ;
#11273=DIRECTION ( 'NONE',  ( 0.4999551463232372317, -0.8660512985181135770, 0.000000000000000000 ) ) ;
#11275=CARTESIAN_POINT ( 'NONE',  ( 0.5335270692236984136, -1.350917419745129466, 0.6007964825855031110 ) ) ;
#11278=CARTESIAN_POINT ( 'NONE',  ( 0.4926052497631904226, -1.101322287461897975, 0.6863075852112333619 ) ) ;
#11283=CARTESIAN_POINT ( 'NONE',  ( 0.3592589994864452962, -1.616760386158514251, 0.6673211502991388544 ) ) ;
#11284=CARTESIAN_POINT ( 'NONE',  ( 0.6826933326075008690, -1.509735114952027724, 0.4536807863530596396 ) ) ;
#11286=CARTESIAN_POINT ( 'NONE',  ( 0.3211756810167746834, -1.183199798883805887, 0.5707417262808780478 ) ) ;
#11292=CARTESIAN_POINT ( 'NONE',  ( 0.1695210371906753222, -0.9850032004317544887, 0.6936202826021303780 ) ) ;
#11297=ADVANCED_FACE ( 'NONE', ( #27158 ), #26947, .T. ) ;
#11303=CARTESIAN_POINT ( 'NONE',  ( 0.3465569301755319076, -1.167400393090313404, 0.4215427493204025877 ) ) ;
#11308=CARTESIAN_POINT ( 'NONE',  ( 0.06380145895344221940, -1.331679772128220751, 0.6026722500081351797 ) ) ;
#11310=DIRECTION ( 'NONE',  ( -0.8660512985181132439, -0.4999551463232376758, 0.000000000000000000 ) ) ;
#11311=CARTESIAN_POINT ( 'NONE',  ( 0.0002784714592843559058, -0.4877735126986449954, -0.003907027868444597034 ) ) ;
#11313=CARTESIAN_POINT ( 'NONE',  ( 0.07697101544015785834, -0.8504277950014116350, 0.8348144624976774342 ) ) ;
#11317=CARTESIAN_POINT ( 'NONE',  ( 0.1799893395252018524, -0.5084901828474633900, 0.2372766076402116897 ) ) ;
#11322=CARTESIAN_POINT ( 'NONE',  ( 0.0004130725403994839557, -0.6456490322605723531, -0.008477622837938958433 ) ) ;
#11325=CARTESIAN_POINT ( 'NONE',  ( 0.1445495956827405892, -0.5724930378805425102, 0.4876118625187007560 ) ) ;
#11326=AXIS2_PLACEMENT_3D ( 'NONE', #11561, #33537, #39934 ) ;
#11327=ORIENTED_EDGE ( 'NONE', *, *, #34266, .T. ) ;
#11329=CARTESIAN_POINT ( 'NONE',  ( 0.01631055661851274138, -0.7363905679946652905, 0.6008399523819771826 ) ) ;
#11332=DIRECTION ( 'NONE',  ( 0.4999551463232371762, -0.8660512985181134660, 0.000000000000000000 ) ) ;
#11339=CARTESIAN_POINT ( 'NONE',  ( 0.1187488235998804681, -1.413962359561577786, 0.5741705506523664404 ) ) ;
#11340=B_SPLINE_SURFACE_WITH_KNOTS ( 'NONE', 3, 3, ( 
 ( #5847, #33632, #12048, #5445, #24606, #15334, #8956, #30567, #2393, #21528, #18408, #27891, #12255, #37334, #9147, #21710, #9346, #19446, #28277, #19235, #18843, #37524, #3985, #25423, #24993, #35274, #31383, #22145, #31779, #12635, #22535, #40623, #15938, #7069 ),
 ( #21926, #19640, #13254, #34660, #6268, #31984, #13060, #3796, #12439, #6661, #144, #6463, #34455, #358, #28096, #3187, #12862, #15728, #37953, #25201, #35062, #9967, #38343, #37744, #9566, #19033, #31564, #3382, #565, #22746, #28483, #9764, #22333, #32174 ),
 ( #34853, #28887, #3594, #16163, #28700, #25612, #38143, #16351, #10177, #6870, #25822, #748, #10379, #8086, #1759, #10569, #35458, #20447, #1545, #32981, #956, #35880, #16760, #35670, #22942, #29501, #33198, #13467, #1340, #7260, #13848, #19834, #23557, #39174 ),
 ( #26421, #7692, #13656, #32368, #38956, #26835, #38743, #7473, #4192, #4786, #10786, #23359, #38556, #17361, #26033, #20257, #32583, #17152, #32778, #7873, #4580, #29701, #29308, #14066, #26643, #14271, #11183, #10999, #26221, #1155, #23143, #20051, #4399, #16956 ),
 ( #36075, #29917, #39364, #23743, #36266, #20663, #16548, #29089, #5003, #39968, #17753, #33804, #37089, #11789, #21266, #11385, #2737, #30306, #5609, #8905, #40378, #21481, #27240, #27633, #27443, #8494, #39772, #18166, #30516, #40163, #34002, #30720, #5807, #5200 ),
 ( #33585, #39552, #14884, #18366, #2344, #23957, #1943, #24164, #27026, #36881, #24346, #8689, #12205, #2541, #36487, #30912, #2133, #15079, #8301, #14458, #21668, #11993, #20872, #24764, #14669, #24557, #15282, #27839, #37286, #33393, #9102, #11602, #17569, #30112 ),
 ( #36688, #21058, #5395, #17956, #15685, #34803, #18985, #16114, #38095, #9720, #22485, #34407, #19188, #16311, #6606, #21880, #15893, #6417, #22288, #28437, #6223, #6008, #25567, #35010, #13201, #9913, #18791, #22095, #31728, #6822, #2947, #707, #38294, #37907 ),
 ( #31129, #25774, #24952, #28236, #3545, #31342, #28654, #18573, #34618, #10124, #34196, #15498, #12397, #28052, #40577, #523, #37480, #9302, #31517, #19404, #3147, #31939, #3759, #28846, #99, #12596, #3329, #13016, #25156, #37695, #9518, #310, #12816, #25375 ),
 ( #32324, #13411, #25987, #38705, #35831, #17311, #39317, #911, #10525, #1705, #22700, #38906, #36027, #29865, #7644, #32134, #3937, #20208, #32934, #10341, #16499, #23095, #20000, #17106, #35621, #14225, #38512, #23512, #32533, #39125, #29043, #4141, #22903, #32733 ),
 ( #29457, #19601, #16709, #16913, #26791, #35422, #7423, #4352, #26375, #7216, #19782, #1302, #13807, #23307, #10733, #14013, #4539, #29654, #29255, #1499, #26585, #7831, #35232, #10950, #1109, #13617, #26181, #20402, #4740, #7033, #2689, #30069, #17905, #8037 ) ),
 .UNSPECIFIED., .F., .F., .F.,
 ( 4, 3, 3, 4 ),
 ( 4, 3, 3, 3, 3, 3, 3, 3, 3, 3, 3, 4 ),
 ( 0.2088659071706846226, 0.5009378285833450128, 0.6469737892896751941, 0.7930097499960053753 ),
 ( 0.3645345204366292058, 0.4439677053820508812, 0.5234008903274726121, 0.6028340752728943430, 0.6822672602183160739, 0.7617004451637376938, 0.8411336301091594247, 0.8808502225818702902, 0.9205668150545811557, 0.9602834075272920211, 0.9801417037636475094, 1.000000000000002887 ),
 .UNSPECIFIED. ) ;
#11341=CARTESIAN_POINT ( 'NONE',  ( 0.1139667446832752368, -0.6485154308321814387, 0.4297538792301814903 ) ) ;
#11342=CARTESIAN_POINT ( 'NONE',  ( 0.1871628350115532857, -0.7098502299333919741, 0.03075682391282563016 ) ) ;
#11348=DIRECTION ( 'NONE',  ( 0.9998941247116546194, -0.01455087607601020239, 0.0001066420868422379362 ) ) ;
#11351=CARTESIAN_POINT ( 'NONE',  ( 0.4380553862277722921, -1.229819722584721164, 0.5856983068965045947 ) ) ;
#11352=B_SPLINE_CURVE_WITH_KNOTS ( 'NONE', 3,
 ( #1279, #4331, #16684, #16893, #25351, #37888, #25966, #6585, #26163, #38491, #35402, #7195, #9700, #38683, #19763, #16091 ),
 .UNSPECIFIED., .F., .F.,
 ( 4, 2, 2, 2, 2, 2, 2, 4 ),
 ( 4.646041361794957016E-06, 0.0005830979320143057703, 0.001161549822666816615, 0.001740001713319327351, 0.002318453603971838521, 0.002896905494624349257, 0.003475357385276859994, 0.004632261166581898813 ),
 .UNSPECIFIED. ) ;
#11353=B_SPLINE_CURVE_WITH_KNOTS ( 'NONE', 3,
 ( #23600, #36115, #5050, #32635 ),
 .UNSPECIFIED., .F., .F.,
 ( 4, 4 ),
 ( 0.000000000000000000, 0.004359680035278114957 ),
 .UNSPECIFIED. ) ;
#11354=AXIS2_PLACEMENT_3D ( 'NONE', #39518, #11348, #23919 ) ;
#11356=CARTESIAN_POINT ( 'NONE',  ( 0.1835308262027276760, -1.352961526709849149, 0.9396307682827382823 ) ) ;
#11357=CARTESIAN_POINT ( 'NONE',  ( 0.4045633573398161875, -1.022308794230461171, 0.6485999566564401020 ) ) ;
#11360=CARTESIAN_POINT ( 'NONE',  ( 0.2978499211271074532, -0.7548715063715667473, 0.6844903506759184575 ) ) ;
#11363=DIRECTION ( 'NONE',  ( -0.8660512985181135770, -0.4999551463232371207, 0.000000000000000000 ) ) ;
#11367=CARTESIAN_POINT ( 'NONE',  ( 0.3211013594029290541, -1.758905195063801052, 0.5654687988106404939 ) ) ;
#11368=CARTESIAN_POINT ( 'NONE',  ( 0.01305698674251137489, -0.5857752844667294401, 0.3380397419882886223 ) ) ;
#11369=CARTESIAN_POINT ( 'NONE',  ( 0.3191806098734731312, -1.644742521496082688, 0.4260382800181419238 ) ) ;
#11374=CARTESIAN_POINT ( 'NONE',  ( 0.5308880977089266429, -1.160028955924689242, 0.7442320808281387423 ) ) ;
#11376=VERTEX_POINT ( 'NONE', #39479 ) ;
#11379=DIRECTION ( 'NONE',  ( 0.000000000000000000, 1.000000000000000000, 7.931692224083225994E-17 ) ) ;
#11385=CARTESIAN_POINT ( 'NONE',  ( 0.1177726229696089005, -0.7519543602322694698, 0.4275972577093408722 ) ) ;
#11387=CARTESIAN_POINT ( 'NONE',  ( 0.2968214893875291693, -1.658325148620396261, 0.8976394753983624186 ) ) ;
#11389=CARTESIAN_POINT ( 'NONE',  ( 0.09764433117057016998, -0.5450118788951328064, 0.1538195766994619462 ) ) ;
#11390=CARTESIAN_POINT ( 'NONE',  ( 0.1139096195112916099, -0.5666989323863135253, -0.06299521055917528534 ) ) ;
#11392=CARTESIAN_POINT ( 'NONE',  ( 0.05396242693373293209, -1.112133054815703348, 0.6504500721729179480 ) ) ;
#11396=CARTESIAN_POINT ( 'NONE',  ( 0.5894480801153691996, -1.254546968075577418, 0.8139536464034254903 ) ) ;
#11398=CARTESIAN_POINT ( 'NONE',  ( 0.3690965330173307524, -1.099411688709415413, 0.5182417262812423209 ) ) ;
#11399=( GEOMETRIC_REPRESENTATION_CONTEXT ( 3 ) GLOBAL_UNCERTAINTY_ASSIGNED_CONTEXT ( ( #15737 ) ) GLOBAL_UNIT_ASSIGNED_CONTEXT ( ( #1126, #26195, #23112 ) ) REPRESENTATION_CONTEXT ( 'NONE', 'WORKASPACE' ) );
#11401=CARTESIAN_POINT ( 'NONE',  ( 0.4688079631758284016, -1.116561345930851656, 0.5688791344137259509 ) ) ;
#11406=CARTESIAN_POINT ( 'NONE',  ( 0.3154536323005096010, -1.185489152943391078, 0.5575863575408869233 ) ) ;
#11407=CARTESIAN_POINT ( 'NONE',  ( 0.5932568134822767680, -1.254512724160953940, 0.6928994325643027530 ) ) ;
#11413=EDGE_LOOP ( 'NONE', ( #6229, #20805, #4090, #27575, #29339, #17836, #34399, #31270 ) ) ;
#11419=ORIENTED_EDGE ( 'NONE', *, *, #26350, .T. ) ;
#11421=CARTESIAN_POINT ( 'NONE',  ( 0.4125455718730863808, -1.129683035667270685, 0.5355335411479252850 ) ) ;
#11424=CARTESIAN_POINT ( 'NONE',  ( 0.1284780417918266471, -1.109535762947133186, 0.7509360102231731338 ) ) ;
#11429=CARTESIAN_POINT ( 'NONE',  ( 0.4138729472876766513, -1.128955312352843965, 0.5470489658417444501 ) ) ;
#11431=B_SPLINE_CURVE_WITH_KNOTS ( 'NONE', 3,
 ( #3180, #31768, #3372, #12629 ),
 .UNSPECIFIED., .F., .F.,
 ( 4, 4 ),
 ( 0.000000000000000000, 0.0008608482128229501219 ),
 .UNSPECIFIED. ) ;
#11434=CARTESIAN_POINT ( 'NONE',  ( 0.4531756115490733205, -1.216278074989430635, 0.6647715044327879852 ) ) ;
#11442=CARTESIAN_POINT ( 'NONE',  ( 0.3704697912810962501, -1.166474544107111377, 0.4182417262808778013 ) ) ;
#11443=ORIENTED_EDGE ( 'NONE', *, *, #14031, .T. ) ;
#11445=CARTESIAN_POINT ( 'NONE',  ( 0.2896156192559988241, -1.230497722748672418, 0.8765274707950017063 ) ) ;
#11446=CARTESIAN_POINT ( 'NONE',  ( 0.6803372715343216637, -1.562881934859470245, 0.6028921635761279596 ) ) ;
#11447=CARTESIAN_POINT ( 'NONE',  ( 0.1991979404706940571, -0.7475258006208684858, 0.3239363664478491778 ) ) ;
#11448=CARTESIAN_POINT ( 'NONE',  ( 0.5727661025814071438, -1.498384876352202744, 0.4882842553274438502 ) ) ;
#11452=CARTESIAN_POINT ( 'NONE',  ( 0.5221487387134132740, -1.408661551139909429, 0.7843041425632609753 ) ) ;
#11453=EDGE_LOOP ( 'NONE', ( #35259, #6973, #34959, #14222, #16256, #10624 ) ) ;
#11454=CARTESIAN_POINT ( 'NONE',  ( 0.5882251369675207675, -1.618009200102772382, 0.5801761169464535461 ) ) ;
#11459=CARTESIAN_POINT ( 'NONE',  ( 0.6465835049539245816, -1.539613817736331658, 0.4182417262808776903 ) ) ;
#11461=CARTESIAN_POINT ( 'NONE',  ( 0.2117005958754011041, -1.244844897664459271, 0.4511303960385213974 ) ) ;
#11462=CARTESIAN_POINT ( 'NONE',  ( 0.006146411395858588159, -0.5280326101355133916, 0.1457225173264089235 ) ) ;
#11465=CARTESIAN_POINT ( 'NONE',  ( 0.6930531720067659718, -1.422936651082730375, 0.7544454077531311809 ) ) ;
#11468=CARTESIAN_POINT ( 'NONE',  ( -2.194511862571855274E-05, -0.9481927139366428392, 0.1457185332388704346 ) ) ;
#11472=CARTESIAN_POINT ( 'NONE',  ( 0.5908959048872449715, -1.601544548465861473, 0.4282886817583849703 ) ) ;
#11474=CARTESIAN_POINT ( 'NONE',  ( 0.3165138724069220255, -1.757609964495261190, 0.6990733182572979043 ) ) ;
#11476=CARTESIAN_POINT ( 'NONE',  ( 0.1817330915907873212, -1.261857734097182160, 0.5280675647135233408 ) ) ;
#11477=CARTESIAN_POINT ( 'NONE',  ( 0.3048336326901729953, -1.756854950747158473, 0.5690634040337300137 ) ) ;
#11483=CIRCLE ( 'NONE', #16740, 0.1012268159172230869 ) ;
#11484=CARTESIAN_POINT ( 'NONE',  ( 0.3279422950026300576, -1.178402953498526751, 0.5630877674954837264 ) ) ;
#11486=CARTESIAN_POINT ( 'NONE',  ( 0.06923712653936904549, -0.5400029222721455247, 0.1457185332388703236 ) ) ;
#11489=CARTESIAN_POINT ( 'NONE',  ( 0.3793388072559690793, -1.119460787698140392, 0.7530470861100434510 ) ) ;
#11492=CARTESIAN_POINT ( 'NONE',  ( 0.5043207191046787941, -1.105492587439252494, 0.6133613128836958861 ) ) ;
#11499=CARTESIAN_POINT ( 'NONE',  ( 0.3563569779892122313, -1.622467549537393694, 0.5771720492809274683 ) ) ;
#11500=CARTESIAN_POINT ( 'NONE',  ( 0.6968370183900322035, -1.494039123299786942, 0.4851329554411836775 ) ) ;
#11508=CARTESIAN_POINT ( 'NONE',  ( 0.2944674956371818308, -1.228845936351069978, 0.7080622490502053168 ) ) ;
#11516=CARTESIAN_POINT ( 'NONE',  ( 0.6586645934826005355, -1.563799363216411331, 0.4177417262808784670 ) ) ;
#11519=CARTESIAN_POINT ( 'NONE',  ( 0.05963972588713747913, -1.330888851906829595, 0.5826259623951950406 ) ) ;
#11522=CARTESIAN_POINT ( 'NONE',  ( 0.4157784994257035516, -1.135080422749356943, 0.4335792570559673931 ) ) ;
#11523=CARTESIAN_POINT ( 'NONE',  ( 0.4668905103052730654, -1.236430484539588592, 0.6057417262809813296 ) ) ;
#11525=CARTESIAN_POINT ( 'NONE',  ( 0.6952357793749982529, -1.543270793921424744, 0.4282417262808777547 ) ) ;
#11526=CARTESIAN_POINT ( 'NONE',  ( 0.01192210659473974012, -0.5278220828877545623, -0.05896525035967064426 ) ) ;
#11532=CARTESIAN_POINT ( 'NONE',  ( 0.1931842209117922704, -0.5499223536180041227, 0.2739543758472387514 ) ) ;
#11536=EDGE_CURVE ( 'NONE', #35372, #243, #36070, .T. ) ;
#11539=CARTESIAN_POINT ( 'NONE',  ( 0.0008024698624184804785, -0.6024510043979661722, 0.0006787156188479290470 ) ) ;
#11543=B_SPLINE_CURVE_WITH_KNOTS ( 'NONE', 3,
 ( #18100, #14386, #40298, #12131, #15012, #37226 ),
 .UNSPECIFIED., .F., .F.,
 ( 4, 2, 4 ),
 ( 0.000000000000000000, 0.0005867836345122920015, 0.001173567269024584003 ),
 .UNSPECIFIED. ) ;
#11545=CARTESIAN_POINT ( 'NONE',  ( 0.1156883557706581828, -0.4553337736917355549, 0.2193215644107081586 ) ) ;
#11547=CARTESIAN_POINT ( 'NONE',  ( -0.001584010976415602514, -0.5275152449236483188, 0.1457185332388696297 ) ) ;
#11549=CARTESIAN_POINT ( 'NONE',  ( 0.1353747033919373288, -1.277178147914981965, 0.6051480509469141511 ) ) ;
#11556=CARTESIAN_POINT ( 'NONE',  ( 0.3727794023048966454, -1.123217151053685692, 0.6232678702655031211 ) ) ;
#11558=CARTESIAN_POINT ( 'NONE',  ( 0.1187265588701445079, -1.410790600435402720, 0.5974809741846841549 ) ) ;
#11559=CARTESIAN_POINT ( 'NONE',  ( 0.09010370433594069861, -0.5674124104709881156, 0.1743615206353293645 ) ) ;
#11560=CARTESIAN_POINT ( 'NONE',  ( 0.1870560818649253665, -0.7171819408363133697, 0.03132522962495347396 ) ) ;
#11561=CARTESIAN_POINT ( 'NONE',  ( 0.4165761542997364897, -1.741708882820427906, 0.5182417262812423209 ) ) ;
#11564=FACE_OUTER_BOUND ( 'NONE', #25977, .T. ) ;
#11565=EDGE_CURVE ( 'NONE', #18202, #39770, #13939, .T. ) ;
#11569=CARTESIAN_POINT ( 'NONE',  ( 0.4036829562542670335, -1.110694686686239496, 0.6196874900528862584 ) ) ;
#11574=CARTESIAN_POINT ( 'NONE',  ( 0.2385638199407473237, -1.468035130309864655, 0.9857930272948494110 ) ) ;
#11575=CARTESIAN_POINT ( 'NONE',  ( 0.4646871136015383597, -1.067210575163276776, 0.6251146133038130159 ) ) ;
#11576=CARTESIAN_POINT ( 'NONE',  ( 0.0004231800003877070619, -0.8698522374252537492, 0.3712277156174843551 ) ) ;
#11578=CARTESIAN_POINT ( 'NONE',  ( 0.6551261771431925451, -1.361944467462807395, 0.8444247977208539924 ) ) ;
#11584=CARTESIAN_POINT ( 'NONE',  ( -0.002063022417946163214, -0.8810992990880223141, 0.1457185332388702959 ) ) ;
#11585=CARTESIAN_POINT ( 'NONE',  ( 0.08896364796864351943, -1.020649669505796053, 0.8448254586460793858 ) ) ;
#11587=CARTESIAN_POINT ( 'NONE',  ( 0.5877158659771946070, -1.491177997581171644, 0.5692036392475393614 ) ) ;
#11591=CARTESIAN_POINT ( 'NONE',  ( 0.3418186750811026964, -0.8703758711135023418, 0.7017026408156415984 ) ) ;
#11596=CARTESIAN_POINT ( 'NONE',  ( 0.5785166455485266646, -1.495798471460381140, 0.5520824867764277943 ) ) ;
#11598=CARTESIAN_POINT ( 'NONE',  ( 0.4958908375534706869, -1.219525668783798977, 0.6057417262809816627 ) ) ;
#11602=CARTESIAN_POINT ( 'NONE',  ( 0.08647347352317601155, -0.7251180098799488993, 0.1691244536827258838 ) ) ;
#11603=CARTESIAN_POINT ( 'NONE',  ( 0.3025690150559682823, -1.684573983455480706, 0.8624521912671884172 ) ) ;
#11604=CARTESIAN_POINT ( 'NONE',  ( 0.4841033199777585172, -1.510029708904473189, 0.7391567888139168874 ) ) ;
#11607=CARTESIAN_POINT ( 'NONE',  ( 0.1701719723773303661, -1.263281085629067269, 0.5928467369345694626 ) ) ;
#11612=CARTESIAN_POINT ( 'NONE',  ( 0.5360489703051245503, -1.170555442393250933, 0.8194398345008427897 ) ) ;
#11618=CARTESIAN_POINT ( 'NONE',  ( 0.4065932041851623713, -1.147918556006411350, 0.4182417262808777458 ) ) ;
#11620=CARTESIAN_POINT ( 'NONE',  ( 0.3125015783326245966, -1.187070760913759626, 0.4876403188951574097 ) ) ;
#11622=CARTESIAN_POINT ( 'NONE',  ( 0.5556047631917466756, -1.190343314783628870, 0.5823040822259395455 ) ) ;
#11629=CARTESIAN_POINT ( 'NONE',  ( 0.6062642334505776720, -1.480048462320248559, 0.5555565214026880749 ) ) ;
#11630=EDGE_LOOP ( 'NONE', ( #37525, #8117, #16554, #39645, #25697, #37242, #35818 ) ) ;
#11631=CARTESIAN_POINT ( 'NONE',  ( 0.4696555196854587666, -1.075282885199456251, 0.7143639487365693874 ) ) ;
#11634=CARTESIAN_POINT ( 'NONE',  ( 0.2129387079736155819, -1.324090063805845929, 0.6635512456264479608 ) ) ;
#11640=CARTESIAN_POINT ( 'NONE',  ( 0.3900902991962562072, -1.136166487165251704, 0.6916372837714432897 ) ) ;
#11644=ORIENTED_EDGE ( 'NONE', *, *, #34421, .F. ) ;
#11645=DIRECTION ( 'NONE',  ( -0.4999551463232372317, 0.8660512985181135770, -0.000000000000000000 ) ) ;
#11647=CARTESIAN_POINT ( 'NONE',  ( 0.1904741123364903921, -0.6407273034312881421, 0.05501147976861575639 ) ) ;
#11648=CARTESIAN_POINT ( 'NONE',  ( 0.3606268415227102397, -1.392835293988391232, 0.8657824657960605519 ) ) ;
#11650=CARTESIAN_POINT ( 'NONE',  ( 0.1927077495703349297, -0.8180328145591141409, 0.2791508387892266407 ) ) ;
#11651=CARTESIAN_POINT ( 'NONE',  ( 0.6952084031009919673, -1.569313059414498612, 0.5182417262812423209 ) ) ;
#11654=CARTESIAN_POINT ( 'NONE',  ( 0.5817635102457460183, -1.493441422541048613, 0.6192858208287552735 ) ) ;
#11660=CARTESIAN_POINT ( 'NONE',  ( 0.2197619200132477080, -1.239992638468456310, 0.5547062449803537021 ) ) ;
#11662=CARTESIAN_POINT ( 'NONE',  ( 0.4904112910084666432, -1.188461936721600720, 0.4182417262808778013 ) ) ;
#11663=CARTESIAN_POINT ( 'NONE',  ( 0.4199384557880279645, -0.9749410087210258480, 0.8268343460595501959 ) ) ;
#11669=DIRECTION ( 'NONE',  ( 0.4999551463232372317, -0.8660512985181134660, 0.000000000000000000 ) ) ;
#11670=CARTESIAN_POINT ( 'NONE',  ( 0.5775994654647633730, -1.623302777163974309, 0.5622733483718397318 ) ) ;
#11674=CARTESIAN_POINT ( 'NONE',  ( 0.1805970051927620057, -0.5031265787226441022, 0.1274127068463872803 ) ) ;
#11678=B_SPLINE_SURFACE_WITH_KNOTS ( 'NONE', 5, 5, ( 
 ( #24132, #33546, #17918, #30482, #2311, #21844 ),
 ( #37051, #37259, #30692, #18337, #9266, #14851 ),
 ( #2512, #30882, #24315, #36839, #21226, #33764 ),
 ( #24521, #5973, #30262, #27803, #40339, #31090 ),
 ( #2909, #12168, #24730, #9076, #21640, #15462 ),
 ( #28011, #12367, #24923, #37450, #489, #13164 ) ),
 .UNSPECIFIED., .F., .F., .F.,
 ( 6, 6 ),
 ( 6, 6 ),
 ( -6.477000000001651436, 6.477000000001640778 ),
 ( -2.080605796196440593, 4.396394203803596135 ),
 .UNSPECIFIED. ) ;
#11679=ORIENTED_EDGE ( 'NONE', *, *, #22873, .F. ) ;
#11682=ORIENTED_EDGE ( 'NONE', *, *, #11263, .T. ) ;
#11683=CARTESIAN_POINT ( 'NONE',  ( -19685.04193433331602, 285.7890798983738136, -1.951739244310253252 ) ) ;
#11686=CARTESIAN_POINT ( 'NONE',  ( 0.5211427556806288441, -1.328754734744161503, 0.6184543104854637319 ) ) ;
#11689=CARTESIAN_POINT ( 'NONE',  ( 0.5127940875192875669, -1.116701596374397587, 0.5863938561526392812 ) ) ;
#11695=CARTESIAN_POINT ( 'NONE',  ( 0.03624043082992319670, -0.5539225501819573516, 0.2410209412657329242 ) ) ;
#11696=CARTESIAN_POINT ( 'NONE',  ( 0.7001105832783358629, -1.490154023927230620, 0.4954520656533412670 ) ) ;
#11697=FACE_OUTER_BOUND ( 'NONE', #28880, .T. ) ;
#11701=CARTESIAN_POINT ( 'NONE',  ( 0.4091989031083814732, -1.120218831783651225, 0.6059596497380331792 ) ) ;
#11702=VERTEX_POINT ( 'NONE', #28776 ) ;
#11705=CARTESIAN_POINT ( 'NONE',  ( 0.2618259362272229440, -1.171708162254243346, 0.7401477599866793655 ) ) ;
#11706=CYLINDRICAL_SURFACE ( 'NONE', #4056, 0.03749999999977557397 ) ;
#11708=DIRECTION ( 'NONE',  ( 0.8733930460526325712, 0.4870160029269101076, 1.225071845210601238E-12 ) ) ;
#11711=CARTESIAN_POINT ( 'NONE',  ( 0.3665423450487189094, -1.157372158458239930, 0.4269203576084827367 ) ) ;
#11716=CARTESIAN_POINT ( 'NONE',  ( 0.4853835224616649957, -1.121831837822684363, 0.5320487966727919238 ) ) ;
#11718=CARTESIAN_POINT ( 'NONE',  ( 0.4669913346123752418, -1.236372280561029768, 0.6057417262809813296 ) ) ;
#11719=AXIS2_PLACEMENT_3D ( 'NONE', #4584, #20261, #7479 ) ;
#11721=CARTESIAN_POINT ( 'NONE',  ( 0.0003234651869381446995, -0.4702172293755216281, 0.02383708635093780698 ) ) ;
#11723=CARTESIAN_POINT ( 'NONE',  ( 0.01853211186653049014, -0.5933771545062531683, 0.5476569912671933604 ) ) ;
#11729=VERTEX_POINT ( 'NONE', #19709 ) ;
#11738=CARTESIAN_POINT ( 'NONE',  ( 0.2665790487942257814, -1.675396594968343589, 0.5762402978905174500 ) ) ;
#11740=CARTESIAN_POINT ( 'NONE',  ( 0.1548133193268841079, -1.266291356060329942, 0.6052138703867981917 ) ) ;
#11741=CARTESIAN_POINT ( 'NONE',  ( 0.3924513946351673721, -1.141110873382124913, 0.4807468720547258823 ) ) ;
#11746=CARTESIAN_POINT ( 'NONE',  ( 0.3546663891935897261, -1.141357238359193227, 0.6167818336462109752 ) ) ;
#11748=CARTESIAN_POINT ( 'NONE',  ( 0.2963953263377933633, -0.9883368321787951993, 0.7520588641002025065 ) ) ;
#11749=CARTESIAN_POINT ( 'NONE',  ( 0.1862608185035845298, -0.7716910769734633968, 0.05026386998840438880 ) ) ;
#11758=CARTESIAN_POINT ( 'NONE',  ( 0.4438204728424792744, -1.112778709206400540, 0.5971037950205706490 ) ) ;
#11761=ADVANCED_FACE ( 'NONE', ( #14342 ), #13205, .T. ) ;
#11763=CARTESIAN_POINT ( 'NONE',  ( 0.02434420200121316033, -0.6484821100597173427, 0.5849520929678148073 ) ) ;
#11766=CARTESIAN_POINT ( 'NONE',  ( 0.6005716857727874114, -1.273429356927226364, 0.8451723082856259506 ) ) ;
#11772=CARTESIAN_POINT ( 'NONE',  ( 0.02531197093827743799, -0.7324061903732035361, 0.5907467694136248060 ) ) ;
#11775=CARTESIAN_POINT ( 'NONE',  ( 0.1660212896393471194, -0.7004965508887009973, 0.4943758604162845627 ) ) ;
#11780=CARTESIAN_POINT ( 'NONE',  ( 0.3136035985995381248, -0.8251737266935038617, 0.6634070228338775355 ) ) ;
#11785=DIRECTION ( 'NONE',  ( -0.8660512985181135770, -0.4999551463232371207, 0.000000000000000000 ) ) ;
#11788=ORIENTED_EDGE ( 'NONE', *, *, #38315, .F. ) ;
#11789=CARTESIAN_POINT ( 'NONE',  ( 0.1308037668030993250, -0.7698811990532283822, 0.4769619041194265163 ) ) ;
#11791=CARTESIAN_POINT ( 'NONE',  ( 0.4986356724744993030, -1.542411423100964685, 0.5955585433317269750 ) ) ;
#11792=CARTESIAN_POINT ( 'NONE',  ( 0.3387747544451191195, -1.750987805599188762, 0.4530632734751737778 ) ) ;
#11793=CARTESIAN_POINT ( 'NONE',  ( 0.001416521061405088058, -0.5542609177154461664, 0.04326317503830075240 ) ) ;
#11794=CARTESIAN_POINT ( 'NONE',  ( 0.03379672557156814666, -1.165057834625447430, 0.6664856670883784195 ) ) ;
#11798=CARTESIAN_POINT ( 'NONE',  ( 0.5942568569871560236, -1.385430782096122915, 0.8695712771822926568 ) ) ;
#11799=CARTESIAN_POINT ( 'NONE',  ( 0.4686299618660970667, -1.116544485314582058, 0.5688522617922341373 ) ) ;
#11801=CARTESIAN_POINT ( 'NONE',  ( 0.3791158569359883712, -1.152399346284787240, 0.4250371444196747728 ) ) ;
#11802=FACE_OUTER_BOUND ( 'NONE', #34541, .T. ) ;
#11804=CARTESIAN_POINT ( 'NONE',  ( 0.3187440932968347851, -1.183579951292570431, 0.5368940269945723376 ) ) ;
#11805=CARTESIAN_POINT ( 'NONE',  ( 0.5416676161616581497, -1.167047932790743037, 0.6420073683128293407 ) ) ;
#11808=CARTESIAN_POINT ( 'NONE',  ( 0.6280011288705396044, -1.582389882725783403, 0.6191887264445070649 ) ) ;
#11810=DIRECTION ( 'NONE',  ( 0.8660512985181125778, 0.4999551463232387860, 0.000000000000000000 ) ) ;
#11818=CARTESIAN_POINT ( 'NONE',  ( 0.06533280422175168078, -0.9217453127808572511, 0.5945887534868308233 ) ) ;
#11823=CARTESIAN_POINT ( 'NONE',  ( 0.3048982267989297501, -1.756746414302344350, 0.5594309555313059512 ) ) ;
#11826=CARTESIAN_POINT ( 'NONE',  ( 0.3392040500280487647, -1.075138255607900994, 0.7131914377028192309 ) ) ;
#11829=CARTESIAN_POINT ( 'NONE',  ( -0.0003416957584554876381, -0.9395563572588278012, 0.1457085237891919405 ) ) ;
#11832=EDGE_LOOP ( 'NONE', ( #28186, #9334, #4677, #26353 ) ) ;
#11835=CARTESIAN_POINT ( 'NONE',  ( 0.1854056692992981370, -0.7337134285967986669, 0.008518417185872215538 ) ) ;
#11836=CARTESIAN_POINT ( 'NONE',  ( 0.4195515592568131447, -1.516513744509174977, 0.7855708791636160093 ) ) ;
#11838=CARTESIAN_POINT ( 'NONE',  ( 0.5835029919942696930, -1.605605060618692459, 0.4537850722327775865 ) ) ;
#11839=CARTESIAN_POINT ( 'NONE',  ( 0.4148946963616447769, -1.144346411133103869, 0.4245081400086456180 ) ) ;
#11844=CARTESIAN_POINT ( 'NONE',  ( 0.1594335956643706809, -0.7007958973334156294, 0.4972769676686734641 ) ) ;
#11845=CARTESIAN_POINT ( 'NONE',  ( 0.4829940418909406952, -1.675148570078003551, 0.5372820393660157068 ) ) ;
#11848=CARTESIAN_POINT ( 'NONE',  ( 0.4861231359011924380, -1.648611998150725899, 0.4182417262808776348 ) ) ;
#11852=CARTESIAN_POINT ( 'NONE',  ( 0.1927903040881008279, -0.5292341811144671837, 0.2767179517167643321 ) ) ;
#11855=FACE_OUTER_BOUND ( 'NONE', #13881, .T. ) ;
#11859=CARTESIAN_POINT ( 'NONE',  ( 0.3222810527215910770, -1.758570551863011922, 0.4849083929475442867 ) ) ;
#11862=ORIENTED_EDGE ( 'NONE', *, *, #28072, .T. ) ;
#11868=CARTESIAN_POINT ( 'NONE',  ( 0.3998620935691252209, -1.132090473766684147, 0.6053150776564959479 ) ) ;
#11871=CARTESIAN_POINT ( 'NONE',  ( 0.4683334428778225811, -1.244683268694764422, 0.7181273297428137914 ) ) ;
#11875=CARTESIAN_POINT ( 'NONE',  ( 0.4598226378601848463, -1.064312249210862982, 0.6507415875188953258 ) ) ;
#11884=CARTESIAN_POINT ( 'NONE',  ( 0.3561347686598763107, -1.622407662918015525, 0.5742129511320137603 ) ) ;
#11885=CARTESIAN_POINT ( 'NONE',  ( 0.3609773110263161389, -1.159644750248734590, 0.4285221785616858958 ) ) ;
#11886=CARTESIAN_POINT ( 'NONE',  ( 0.1866284055609182813, -0.6442149268503359894, -0.01633133720890060300 ) ) ;
#11892=CARTESIAN_POINT ( 'NONE',  ( 0.4952507122378954074, -1.106196709240402587, 0.6973901343829200794 ) ) ;
#11893=EDGE_CURVE ( 'NONE', #8227, #34098, #38978, .T. ) ;
#11894=CARTESIAN_POINT ( 'NONE',  ( 0.5540806847553930714, -1.510732556792533376, 0.6006766572140512794 ) ) ;
#11900=CARTESIAN_POINT ( 'NONE',  ( 0.4284886185654731561, -1.682582563036773227, 0.4182417262808776903 ) ) ;
#11901=CARTESIAN_POINT ( 'NONE',  ( 0.4787764723021453728, -1.660223331282874915, 0.4687417262808790119 ) ) ;
#11909=CARTESIAN_POINT ( 'NONE',  ( 0.4521395518622611243, -1.131665481844795540, 0.4506733450461792301 ) ) ;
#11910=AXIS2_PLACEMENT_3D ( 'NONE', #33701, #2648, #37207 ) ;
#11915=CARTESIAN_POINT ( 'NONE',  ( 6.932235465596841962E-06, -0.5784058487176239050, -0.09163823625527117711 ) ) ;
#11920=EDGE_LOOP ( 'NONE', ( #16341, #35660, #3270, #21045, #34599, #36806 ) ) ;
#11922=CARTESIAN_POINT ( 'NONE',  ( 0.2411830127710683502, -1.239411202381304644, 0.4182417262808778013 ) ) ;
#11923=VERTEX_POINT ( 'NONE', #26062 ) ;
#11926=CARTESIAN_POINT ( 'NONE',  ( 0.002241505894149531299, -0.5197024079959072784, 0.1379092258170560858 ) ) ;
#11929=ORIENTED_EDGE ( 'NONE', *, *, #7465, .F. ) ;
#11933=CARTESIAN_POINT ( 'NONE',  ( -0.001587914043712823457, -0.5315844267872958939, 0.1859523187655416077 ) ) ;
#11934=CARTESIAN_POINT ( 'NONE',  ( 0.08206746009357554494, -0.8455242767393098546, 0.3585407082876929663 ) ) ;
#11935=CARTESIAN_POINT ( 'NONE',  ( 0.1930470874137825976, -1.251549148891850205, 0.5897281480909083440 ) ) ;
#11944=CARTESIAN_POINT ( 'NONE',  ( 0.01173648626945268322, -0.6872203660140956405, -0.1131804859792006068 ) ) ;
#11945=CARTESIAN_POINT ( 'NONE',  ( 0.3527394985022780372, -1.741207400137176897, 0.4357698812951643075 ) ) ;
#11947=CARTESIAN_POINT ( 'NONE',  ( 0.5242754061866402582, -1.337501420007544795, 0.7785695029743999740 ) ) ;
#11948=AXIS2_PLACEMENT_3D ( 'NONE', #6604, #25154, #521 ) ;
#11953=CARTESIAN_POINT ( 'NONE',  ( 0.3114014046812714209, -1.661719107297196407, 0.8995554786316910523 ) ) ;
#11954=CARTESIAN_POINT ( 'NONE',  ( 0.4073028344303278314, -1.718531852617160682, 0.4257392557717242232 ) ) ;
#11957=FACE_OUTER_BOUND ( 'NONE', #5208, .T. ) ;
#11958=CARTESIAN_POINT ( 'NONE',  ( 0.3918182118607623221, -1.107073211027153725, 0.6042946153017959565 ) ) ;
#11963=CARTESIAN_POINT ( 'NONE',  ( 0.2912354967743938094, -1.730409171686111414, 0.5958501190287942562 ) ) ;
#11964=B_SPLINE_CURVE_WITH_KNOTS ( 'NONE', 3,
 ( #40524, #12345, #34553, #5547 ),
 .UNSPECIFIED., .F., .F.,
 ( 4, 4 ),
 ( 1.245646092707955119E-09, 0.0005051110321922458674 ),
 .UNSPECIFIED. ) ;
#11965=CARTESIAN_POINT ( 'NONE',  ( 0.04274323293624435194, -0.9931624692768277196, 0.6843196792473072998 ) ) ;
#11967=CARTESIAN_POINT ( 'NONE',  ( 0.7145247768745858208, -1.460049439684881323, 0.6872404240164239342 ) ) ;
#11968=AXIS2_PLACEMENT_3D ( 'NONE', #24515, #9258, #34580 ) ;
#11969=CARTESIAN_POINT ( 'NONE',  ( 0.7054299102235100927, -1.513544197856392826, 0.5664287308913636965 ) ) ;
#11977=CARTESIAN_POINT ( 'NONE',  ( 0.2619807479409076434, -1.590845703386517096, 0.8456310547791294763 ) ) ;
#11979=CARTESIAN_POINT ( 'NONE',  ( 0.5070218031793033431, -1.372995523392680273, 0.8015102820899869807 ) ) ;
#11982=CARTESIAN_POINT ( 'NONE',  ( 0.6149708076787919753, -1.290796914294373154, 0.6294291921256529587 ) ) ;
#11984=ORIENTED_EDGE ( 'NONE', *, *, #16729, .F. ) ;
#11985=CARTESIAN_POINT ( 'NONE',  ( 0.6985364634159124675, -1.438850461896725275, 0.5682400285031795617 ) ) ;
#11993=CARTESIAN_POINT ( 'NONE',  ( 0.09613268118642956384, -0.7396151843482207111, 0.3087118449850515534 ) ) ;
#11994=CARTESIAN_POINT ( 'NONE',  ( 0.3253043410525603418, -1.741901272161220149, 0.7439933838227589247 ) ) ;
#11995=CARTESIAN_POINT ( 'NONE',  ( 0.1241130014567568551, -0.6538280912446031712, 0.4339932856162626029 ) ) ;
#11998=CARTESIAN_POINT ( 'NONE',  ( 0.002016835409016338402, -0.9611306028646753319, 0.3504772518132928116 ) ) ;
#12004=CARTESIAN_POINT ( 'NONE',  ( 0.6448553937467123021, -1.345730860570678589, 0.8527667722720939647 ) ) ;
#12013=CARTESIAN_POINT ( 'NONE',  ( 0.3740960844805631957, -1.108072201694596526, 0.5182417262812423209 ) ) ;
#12016=CARTESIAN_POINT ( 'NONE',  ( 0.3412847681102941233, -1.170475593325866592, 0.4399642596021446916 ) ) ;
#12017=CARTESIAN_POINT ( 'NONE',  ( 0.2256328605772283669, -0.7491591359250245885, 0.4461645245400559512 ) ) ;
#12018=B_SPLINE_SURFACE_WITH_KNOTS ( 'NONE', 3, 3, ( 
 ( #34579, #28404, #18746, #31299, #9257, #9471, #40541, #31689, #9686, #671, #6384, #28007, #19362, #3511, #16066, #64, #6572, #31487, #3294, #12768, #28614, #5967, #18528, #2903, #21838, #484, #15651, #3108, #272, #25330, #12980, #31899, #22253, #28200, #22445, #25531, #34975, #3718, #7176, #32280, #19744, #26149, #29821, #865, #38471, #7595, #32485, #20363, #1659, #4695, #32696, #17267 ),
 ( #26331, #1264, #6994, #35576, #13372, #25946, #13584, #10687, #10305, #32886, #25724, #38257, #22869, #29212, #4098, #38855, #10484, #16665, #1074, #38664, #23260, #35386, #35784, #7795, #20170, #23049, #29417, #10086, #13766, #22658, #4501, #17064, #35193, #39076, #19564, #29610, #4311, #7377, #1452, #32094, #13967, #19953, #26539, #3902, #10902, #16458, #23473, #35988, #29000, #16877, #5517, #39887 ),
 ( #26934, #24261, #30210, #14370, #23658, #17862, #17474, #2459, #39467, #33301, #36599, #30427, #2255, #2041, #30028, #18080, #5108, #27143, #36784, #21170, #26746, #1855, #8402, #11292, #14573, #23863, #27548, #20972, #33704, #30633, #36387, #14181, #8203, #39673, #11705, #7989, #4906, #14794, #8597, #11508, #36180, #27358, #20777, #17663, #24073, #33490, #14995, #20568, #39275, #11098, #33099, #5297 ),
 ( #29345, #19667, #4018, #29953, #10604, #14303, #23399, #989, #16797, #7513, #32204, #1373, #29530, #13880, #10217, #20092, #35310, #16582, #29130, #13505, #26069, #22968, #7910, #38586, #16990, #22785, #26257, #23178, #1790, #39208, #35916, #26454, #33016, #14100, #10409, #38773, #35489, #26674, #13689, #7295, #29731, #26865, #19871, #38992, #32408, #4231, #7098, #1188, #11029, #35706, #32621, #23586 ),
 ( #4431, #10824, #7722, #20289, #32809, #4611, #36104, #4821, #20481, #17187, #1577, #17393, #17600, #33425, #33230, #8334, #11818, #5232, #21093, #8123, #30144, #23781, #5834, #5647, #14492, #27060, #39590, #11424, #36299, #8941, #39997, #15320, #36522, #33618, #20698, #27275, #39394, #23994, #11215, #34032, #5038, #30341, #1973, #11634, #20903, #17785, #2172, #24192, #30554, #14712, #39808, #36715 ),
 ( #21305, #24379, #30947, #8525, #5428, #21517, #18201, #30751, #17994, #36915, #2375, #14918, #27472, #2570, #8727, #18394, #33845, #15105, #27666, #40198, #12032, #24594, #37128, #2771, #38129, #34647, #28084, #552, #37732, #3581, #34231, #9333, #34441, #21914, #28265, #31969, #2982, #40612, #9749, #6448, #22520, #3786, #6857, #34836, #19435, #25600, #27877, #28469, #3367, #9130, #9554, #15532 ),
 ( #12847, #12428, #35045, #40414, #12240, #24978, #31372, #6257, #344, #12624, #18828, #3176, #130, #25408, #37511, #37939, #9952, #22320, #25188, #31550, #24802, #15922, #37321, #15717, #22131, #19019, #6647, #19221, #31761, #21697, #16147, #28685, #13048, #6041, #18609, #31169, #19109, #22007, #31856, #16412, #12722, #32235, #22405, #22616, #37827, #28955, #38024, #9643, #34532, #10042, #28358, #4054 ) ),
 .UNSPECIFIED., .F., .F., .F.,
 ( 4, 3, 4 ),
 ( 4, 3, 3, 3, 3, 3, 3, 3, 3, 3, 3, 3, 3, 3, 3, 3, 3, 4 ),
 ( 0.2346985215076158870, 0.6110997835933865696, 0.9875010456791571967 ),
 ( -7.634747961624772664E-15, 0.1249999999999946293, 0.2499999999999968914, 0.3749999999999991673, 0.4375000000000003331, 0.5000000000000014433, 0.5625000000000026645, 0.6250000000000037748, 0.6875000000000048850, 0.7500000000000059952, 0.8125000000000071054, 0.8437500000000076605, 0.8750000000000082157, 0.9062500000000087708, 0.9375000000000093259, 0.9687500000000098810, 0.9843750000000102141, 1.000000000000010436 ),
 .UNSPECIFIED. ) ;
#12028=CIRCLE ( 'NONE', #31733, 0.09249999999977555343 ) ;
#12029=CARTESIAN_POINT ( 'NONE',  ( 0.08829612734217157088, -0.8123682747727402065, 0.2531801848959081558 ) ) ;
#12032=CARTESIAN_POINT ( 'NONE',  ( 0.04854223356900850411, -0.9826572199518598394, 0.6756526958422652829 ) ) ;
#12044=CARTESIAN_POINT ( 'NONE',  ( 0.1637585665034339832, -0.5994899851647166322, 0.1022936816274461203 ) ) ;
#12047=ADVANCED_FACE ( 'NONE', ( #28308 ), #16189, .T. ) ;
#12048=CARTESIAN_POINT ( 'NONE',  ( 0.2271594253415122056, -0.8546831118382453019, 0.7084329392384713930 ) ) ;
#12050=CARTESIAN_POINT ( 'NONE',  ( 0.7053410326410682885, -1.513865973459305625, 0.5669051209305092653 ) ) ;
#12051=CARTESIAN_POINT ( 'NONE',  ( 0.06043370286545070302, -0.5384506411558260819, 0.1457185332388693799 ) ) ;
#12052=CARTESIAN_POINT ( 'NONE',  ( 0.07444041171459701844, -1.335750591677182575, 0.5458585244681498638 ) ) ;
#12053=CARTESIAN_POINT ( 'NONE',  ( 0.5670943157340239127, -1.614800677630997772, 0.4626854145028929111 ) ) ;
#12056=EDGE_LOOP ( 'NONE', ( #23812, #91, #9763, #3991 ) ) ;
#12060=CARTESIAN_POINT ( 'NONE',  ( 0.1268547004962813363, -0.5950674506041877532, 0.3072773567659817240 ) ) ;
#12061=CARTESIAN_POINT ( 'NONE',  ( 0.4828783412368256589, -1.662196317011951807, 0.4845646038109067133 ) ) ;
#12062=CARTESIAN_POINT ( 'NONE',  ( 0.3069771088456038077, -1.146818725534535233, 0.5182417262812423209 ) ) ;
#12065=CARTESIAN_POINT ( 'NONE',  ( 0.2347586836304188518, -1.231494575820371917, 0.5212298410651946545 ) ) ;
#12068=CARTESIAN_POINT ( 'NONE',  ( 0.2347703329119436577, -1.231486961704138405, 0.5219302041182221075 ) ) ;
#12069=CARTESIAN_POINT ( 'NONE',  ( 0.6802496923668470696, -1.403733334520502973, 0.6188728273484885856 ) ) ;
#12073=CARTESIAN_POINT ( 'NONE',  ( 0.01055723141996775354, -1.003148971495586350, 0.5413436042764798728 ) ) ;
#12076=CARTESIAN_POINT ( 'NONE',  ( 0.5799012421785839644, -1.622272342335922879, 0.5669080035957854147 ) ) ;
#12087=CARTESIAN_POINT ( 'NONE',  ( 0.3625003971738279263, -1.132488407015356247, 0.6206807596827853546 ) ) ;
#12091=CARTESIAN_POINT ( 'NONE',  ( 0.5234610746152311700, -1.331927276539631499, 0.6628694543310861276 ) ) ;
#12094=CARTESIAN_POINT ( 'NONE',  ( 0.5108734140540642787, -1.113869616463002643, 0.5959577563698095215 ) ) ;
#12095=EDGE_LOOP ( 'NONE', ( #549, #29315, #34050, #25648, #3750, #3747 ) ) ;
#12101=ORIENTED_EDGE ( 'NONE', *, *, #34374, .F. ) ;
#12103=CARTESIAN_POINT ( 'NONE',  ( 0.03676551872540411575, -0.5603456902706456244, 0.2596414817900425942 ) ) ;
#12105=CARTESIAN_POINT ( 'NONE',  ( 0.1122718071269267481, -0.8163803874974441266, -0.05810663026781571344 ) ) ;
#12109=CARTESIAN_POINT ( 'NONE',  ( 0.3704445633776799474, -1.093428063567875475, 0.6364787831697373832 ) ) ;
#12110=CARTESIAN_POINT ( 'NONE',  ( 0.2524445808839146377, -0.9543908899680845215, 0.7414919205053484008 ) ) ;
#12111=VERTEX_POINT ( 'NONE', #31409 ) ;
#12119=CARTESIAN_POINT ( 'NONE',  ( 0.008263909818985001182, -0.6872203660130532521, -0.01225013371141639093 ) ) ;
#12121=CARTESIAN_POINT ( 'NONE',  ( 0.05889106705834949718, -1.326084810051836982, 0.5931655932887337501 ) ) ;
#12124=CARTESIAN_POINT ( 'NONE',  ( 0.4673670683790682734, -1.135785369362879216, 0.4578920774821071960 ) ) ;
#12125=CARTESIAN_POINT ( 'NONE',  ( 0.4957950520941065697, -1.219580963930161133, 0.6057417262809816627 ) ) ;
#12129=CARTESIAN_POINT ( 'NONE',  ( 0.009238630504655715933, -0.9704941665429688280, 0.5327612241319219510 ) ) ;
#12130=CARTESIAN_POINT ( 'NONE',  ( 0.2717989554234621075, -1.672126109062499477, 0.4863275332560569875 ) ) ;
#12131=CARTESIAN_POINT ( 'NONE',  ( 0.3122991364858720975, -1.758414243292331536, 0.5144673742672133399 ) ) ;
#12133=VECTOR ( 'NONE', #6231, 39.37007874015748854 ) ;
#12143=ORIENTED_EDGE ( 'NONE', *, *, #22555, .T. ) ;
#12144=ORIENTED_EDGE ( 'NONE', *, *, #38312, .F. ) ;
#12147=CARTESIAN_POINT ( 'NONE',  ( 0.04546828490520857941, -0.7968594640744619539, 0.6630748410649087710 ) ) ;
#12149=CARTESIAN_POINT ( 'NONE',  ( 0.1164557078696717290, -1.290608969205410350, 0.5990493494779465244 ) ) ;
#12158=CARTESIAN_POINT ( 'NONE',  ( 0.3768783096114196596, -1.720370743462857899, 0.4222122349756300963 ) ) ;
#12160=VECTOR ( 'NONE', #15314, 39.37007874015748143 ) ;
#12161=CARTESIAN_POINT ( 'NONE',  ( 0.5010280360125842769, -1.301577949779766818, 0.8062107694647361322 ) ) ;
#12162=DIRECTION ( 'NONE',  ( 0.4999551463232371762, -0.8660512985181134660, 0.000000000000000000 ) ) ;
#12168=CARTESIAN_POINT ( 'NONE',  ( 0.6588957223800396834, -1.564199738096486714, 0.5197417262808792238 ) ) ;
#12173=CARTESIAN_POINT ( 'NONE',  ( -8.537024980200822558E-17, -0.6872203660140400183, 0.1290053960929137267 ) ) ;
#12174=B_SPLINE_CURVE_WITH_KNOTS ( 'NONE', 1,
 ( #4371, #23712 ),
 .UNSPECIFIED., .F., .F.,
 ( 2, 2 ),
 ( 0.000000000000000000, 1.000000000000000000 ),
 .UNSPECIFIED. ) ;
#12175=CARTESIAN_POINT ( 'NONE',  ( 0.06410545231634277863, -1.149572297890252059, 0.7543797106542713404 ) ) ;
#12178=CARTESIAN_POINT ( 'NONE',  ( 0.2320929863655918080, -0.6391054805530269611, 0.5101375161162777783 ) ) ;
#12190=CARTESIAN_POINT ( 'NONE',  ( 0.2291492867289149638, -1.472603918266135903, 0.9192788838655852057 ) ) ;
#12191=CARTESIAN_POINT ( 'NONE',  ( 0.1282480831355250206, -0.5607311205846683411, 0.2079606190596378357 ) ) ;
#12195=CARTESIAN_POINT ( 'NONE',  ( 0.5553494029534283838, -1.189621637772522389, 0.5881472999875582142 ) ) ;
#12196=ORIENTED_EDGE ( 'NONE', *, *, #21805, .F. ) ;
#12198=CARTESIAN_POINT ( 'NONE',  ( 0.6991393458465392508, -1.438784036003081246, 0.5823241596405769327 ) ) ;
#12203=CARTESIAN_POINT ( 'NONE',  ( 0.3098980262120963891, -1.765718015157915710, 0.5682965708553142647 ) ) ;
#12205=CARTESIAN_POINT ( 'NONE',  ( 0.1402790378157611761, -0.7973165635238237403, 0.5029188386495354601 ) ) ;
#12206=CARTESIAN_POINT ( 'NONE',  ( 0.3098600959331583304, -1.724931092596566851, 0.7848886570988899969 ) ) ;
#12207=CARTESIAN_POINT ( 'NONE',  ( 0.1481794566618464815, -0.7263954259819791481, 0.5403200226437546716 ) ) ;
#12210=CARTESIAN_POINT ( 'NONE',  ( 0.02729138952952809422, -0.9928868837826979599, 0.4957075431573730318 ) ) ;
#12213=VECTOR ( 'NONE', #36926, 39.37007874015748143 ) ;
#12214=CARTESIAN_POINT ( 'NONE',  ( 0.4297110609522239999, -1.008900777665432846, 0.7743681538882086768 ) ) ;
#12224=CARTESIAN_POINT ( 'NONE',  ( 0.4661750196922136991, -1.070732324447800421, 0.6917658376937553255 ) ) ;
#12225=EDGE_CURVE ( 'NONE', #755, #26173, #37507, .T. ) ;
#12230=CARTESIAN_POINT ( 'NONE',  ( 0.4026370839150509306, -1.708716391613837704, 0.4182417262808776903 ) ) ;
#12236=CARTESIAN_POINT ( 'NONE',  ( 0.08964054516919921223, -0.5683534925436617424, 0.1144277174209273190 ) ) ;
#12240=CARTESIAN_POINT ( 'NONE',  ( -0.01390182309215610978, -0.8546603537104834336, 0.2908326285636944619 ) ) ;
#12243=CARTESIAN_POINT ( 'NONE',  ( 0.3061198483567182382, -1.759173221084211702, 0.5682343826784257423 ) ) ;
#12247=CARTESIAN_POINT ( 'NONE',  ( 0.7394099696849650849, -1.503374687208528737, 0.6698237402283935271 ) ) ;
#12255=CARTESIAN_POINT ( 'NONE',  ( 0.1256500344729209739, -0.6634235672001109752, 0.4782051305092041571 ) ) ;
#12259=CARTESIAN_POINT ( 'NONE',  ( 0.1060801343968929555, -0.7029796262605895185, 0.5196367930449407035 ) ) ;
#12261=CARTESIAN_POINT ( 'NONE',  ( 0.5546727557022121946, -1.622188815229450576, 0.4987667657539088251 ) ) ;
#12262=CARTESIAN_POINT ( 'NONE',  ( 0.5022839945508311699, -1.192782407697791980, 0.4224083929475445642 ) ) ;
#12266=CARTESIAN_POINT ( 'NONE',  ( 0.1536443843255308750, -0.6766421297890219400, 0.4621652830613652840 ) ) ;
#12267=EDGE_CURVE ( 'NONE', #6859, #2486, #5605, .T. ) ;
#12268=CARTESIAN_POINT ( 'NONE',  ( 0.4843194246718440232, -1.673553810144886578, 0.5158839267268513495 ) ) ;
#12272=CARTESIAN_POINT ( 'NONE',  ( 0.5860257985473268372, -1.592810714289452312, 0.4182417262808775793 ) ) ;
#12274=CARTESIAN_POINT ( 'NONE',  ( 0.2034338387653989444, -1.249618221326741496, 0.4422361201100588057 ) ) ;
#12276=CARTESIAN_POINT ( 'NONE',  ( 0.2320929863655918080, -0.6391054805530269611, 0.5101375161162777783 ) ) ;
#12283=CARTESIAN_POINT ( 'NONE',  ( 0.3792246514435647642, -1.152363445361852756, 0.4250283846459516623 ) ) ;
#12290=CARTESIAN_POINT ( 'NONE',  ( 0.6609374024770126033, -1.531375946314106562, 0.4235895360073886895 ) ) ;
#12291=CARTESIAN_POINT ( 'NONE',  ( 0.3775892182204781400, -1.738445149920042843, 0.6053742338740327744 ) ) ;
#12294=CARTESIAN_POINT ( 'NONE',  ( 0.3305685589621363274, -1.177413511476334218, 0.5677266399387778106 ) ) ;
#12295=CARTESIAN_POINT ( 'NONE',  ( 0.3356575430205383515, -1.760770474539644415, 0.4707318425698279740 ) ) ;
#12297=CARTESIAN_POINT ( 'NONE',  ( 0.4789118146089810790, -1.259265696533273360, 0.6923424817665398967 ) ) ;
#12301=CARTESIAN_POINT ( 'NONE',  ( 0.4373890596466497582, -1.046786911024660593, 0.6537231983888873721 ) ) ;
#12304=EDGE_CURVE ( 'NONE', #17350, #11030, #18363, .T. ) ;
#12306=CARTESIAN_POINT ( 'NONE',  ( 0.1025208718600092855, -1.387521180747156135, 0.6451533902090165196 ) ) ;
#12308=VERTEX_POINT ( 'NONE', #36710 ) ;
#12310=CARTESIAN_POINT ( 'NONE',  ( 0.3226986062199907468, -1.438512784532514743, 0.8769455027070669484 ) ) ;
#12312=CARTESIAN_POINT ( 'NONE',  ( 0.1850717614292713420, -0.8146629789669863619, 0.03779116257895110548 ) ) ;
#12317=CARTESIAN_POINT ( 'NONE',  ( 0.4278511620221643330, -1.036794873576569742, 0.6363761450469351821 ) ) ;
#12318=CARTESIAN_POINT ( 'NONE',  ( 0.5529345759058228449, -1.511181546743121329, 0.5724623201282376117 ) ) ;
#12323=FACE_OUTER_BOUND ( 'NONE', #8838, .T. ) ;
#12325=FACE_OUTER_BOUND ( 'NONE', #28885, .T. ) ;
#12326=CARTESIAN_POINT ( 'NONE',  ( 0.4250974642402614578, -1.123820390179259832, 0.5291520644862812706 ) ) ;
#12327=CARTESIAN_POINT ( 'NONE',  ( 0.07208523036626358904, -1.310649742666034401, 0.6665797303350883274 ) ) ;
#12330=CARTESIAN_POINT ( 'NONE',  ( 0.4912263342062789806, -1.081771733098906729, 0.5857582446664630904 ) ) ;
#12331=CARTESIAN_POINT ( 'NONE',  ( 0.4630246609694094739, -1.116058605367935774, 0.5664886635214763100 ) ) ;
#12332=CARTESIAN_POINT ( 'NONE',  ( 0.4480287403985907524, -1.224062292566040044, 0.5856983068965044836 ) ) ;
#12334=CARTESIAN_POINT ( 'NONE',  ( -0.001163483333746527255, -0.8281092574587937127, 0.3345003353200291518 ) ) ;
#12335=CARTESIAN_POINT ( 'NONE',  ( 0.3314668577237731006, -1.779294220870033971, 0.5182417262812423209 ) ) ;
#12345=CARTESIAN_POINT ( 'NONE',  ( 0.6048371382129751339, -1.480131487591726192, 0.5922871325631168249 ) ) ;
#12350=CARTESIAN_POINT ( 'NONE',  ( 0.2323486294662862328, -1.426838467342053773, 0.9230749924135009943 ) ) ;
#12351=CARTESIAN_POINT ( 'NONE',  ( 0.3896040541115246003, -1.173367793883531629, 0.7095735600779148333 ) ) ;
#12352=CARTESIAN_POINT ( 'NONE',  ( 0.08147730132796977831, -1.319048655531604330, 0.5775129287537744682 ) ) ;
#12356=CARTESIAN_POINT ( 'NONE',  ( 0.4000099798367661164, -1.704638381955401183, 0.4182417262808776903 ) ) ;
#12357=EDGE_LOOP ( 'NONE', ( #39591, #35936, #28263, #6055 ) ) ;
#12358=ORIENTED_EDGE ( 'NONE', *, *, #28398, .F. ) ;
#12362=CARTESIAN_POINT ( 'NONE',  ( 0.1885535751052127285, -0.8341734923249479738, 0.6205604111359355191 ) ) ;
#12365=CARTESIAN_POINT ( 'NONE',  ( 0.01223674427371603327, -0.4317327575158859121, 0.1899612123909241723 ) ) ;
#12366=CARTESIAN_POINT ( 'NONE',  ( 0.4228356896103982465, -1.238666721341417754, 0.5481991966187728105 ) ) ;
#12367=CARTESIAN_POINT ( 'NONE',  ( 0.7471901070607220863, -1.513130089782565468, 0.5197417262808792238 ) ) ;
#12368=CARTESIAN_POINT ( 'NONE',  ( 0.3619468766189660736, -1.093412635382523090, 0.7620081947267545175 ) ) ;
#12372=CARTESIAN_POINT ( 'NONE',  ( 0.3053298862878815467, -1.679825167650452089, 0.8905181393053133165 ) ) ;
#12373=CARTESIAN_POINT ( 'NONE',  ( 0.07334890854203197919, -1.206402556078998822, 0.7552868396345799873 ) ) ;
#12375=CARTESIAN_POINT ( 'NONE',  ( 0.3938123320717736853, -0.9371650893754340794, 0.7866333354397343491 ) ) ;
#12376=B_SPLINE_CURVE_WITH_KNOTS ( 'NONE', 3,
 ( #5935, #18500, #3084, #6353, #37620, #18925, #22023, #21804, #34545, #12530, #2275, #2871, #39904, #34334, #40300, #31053 ),
 .UNSPECIFIED., .F., .F.,
 ( 4, 2, 2, 2, 2, 2, 2, 4 ),
 ( 0.002977951493358393584, 0.003350111319365625326, 0.003722271145372857068, 0.004094430971380088810, 0.004466590797387320552, 0.004838750623394552294, 0.005210910449401784036, 0.005955230101416240582 ),
 .UNSPECIFIED. ) ;
#12383=CARTESIAN_POINT ( 'NONE',  ( 0.2364914840723867095, -1.527680518818696376, 0.9000837182161988137 ) ) ;
#12384=CARTESIAN_POINT ( 'NONE',  ( 0.5753449303846843721, -1.469417681867138725, 0.7012099257484931680 ) ) ;
#12387=CARTESIAN_POINT ( 'NONE',  ( 0.2195574306699510647, -0.7404155031343288007, 0.4240249586596535059 ) ) ;
#12389=ORIENTED_EDGE ( 'NONE', *, *, #16792, .T. ) ;
#12393=CARTESIAN_POINT ( 'NONE',  ( 0.3187641638634980401, -1.760284878867077962, 0.5597302103697523457 ) ) ;
#12397=CARTESIAN_POINT ( 'NONE',  ( 0.1440972951654591883, -0.8326116813828831065, 0.5086132051937420906 ) ) ;
#12400=CARTESIAN_POINT ( 'NONE',  ( 0.4416766012272996811, -1.379493900532093198, 0.8297147258887590526 ) ) ;
#12406=CARTESIAN_POINT ( 'NONE',  ( 0.4192448355688633832, -1.702263579849587760, 0.6182028396105488932 ) ) ;
#12407=CARTESIAN_POINT ( 'NONE',  ( 0.6672510479475136647, -1.560290543660546092, 0.6093665759723777553 ) ) ;
#12408=EDGE_CURVE ( 'NONE', #2424, #4246, #16397, .T. ) ;
#12409=CARTESIAN_POINT ( 'NONE',  ( 0.1186103394390872201, -1.414144848331978510, 0.5683298932114988489 ) ) ;
#12411=( CONVERSION_BASED_UNIT ( 'INCH', #21072 ) LENGTH_UNIT ( ) NAMED_UNIT ( #19419 ) );
#12414=CARTESIAN_POINT ( 'NONE',  ( 0.003421962176364201202, -0.9701471101739370662, 0.4009549150280219965 ) ) ;
#12415=CARTESIAN_POINT ( 'NONE',  ( 0.5484966004669556972, -1.177603726185705080, 0.6257892858931851654 ) ) ;
#12417=CARTESIAN_POINT ( 'NONE',  ( 0.5919221460426853376, -1.604281172822828783, 0.6022512693985722088 ) ) ;
#12420=CARTESIAN_POINT ( 'NONE',  ( 0.3967672410070270383, -1.715978560527550378, 0.4221337113864314095 ) ) ;
#12423=CARTESIAN_POINT ( 'NONE',  ( 0.4341915061220629757, -1.587206619470876268, 0.5182417262812423209 ) ) ;
#12425=CARTESIAN_POINT ( 'NONE',  ( 0.1442713433645926024, -0.8486712127012279172, 0.5110818735405668889 ) ) ;
#12428=CARTESIAN_POINT ( 'NONE',  ( -0.01502126383153270378, -0.8492948373293983666, 0.1816685507761301444 ) ) ;
#12436=CARTESIAN_POINT ( 'NONE',  ( 0.1731685197160121870, -1.267101063757091861, 0.4261332338546713339 ) ) ;
#12439=CARTESIAN_POINT ( 'NONE',  ( 0.1625622452632755621, -0.7569282882511942923, 0.5806955612166369018 ) ) ;
#12442=CARTESIAN_POINT ( 'NONE',  ( 0.6672263256168233791, -1.559577713309469038, 0.6159734170043378310 ) ) ;
#12443=CARTESIAN_POINT ( 'NONE',  ( 0.3944496393030803016, -1.402754858333492338, 0.8483264674520886173 ) ) ;
#12451=CARTESIAN_POINT ( 'NONE',  ( 0.1153471661799269632, -0.4465907051537382211, 0.1385946963835902879 ) ) ;
#12453=CARTESIAN_POINT ( 'NONE',  ( 0.1266980462273043506, -0.5766536709655731840, 0.2577630623947261834 ) ) ;
#12454=CARTESIAN_POINT ( 'NONE',  ( 0.4655920101359526941, -1.672100886989639656, 0.4503321976353596989 ) ) ;
#12456=LINE ( 'NONE', #2597, #27745 ) ;
#12459=CARTESIAN_POINT ( 'NONE',  ( 0.2198287030041630452, -1.240152648543706881, 0.4626484354544510569 ) ) ;
#12460=CARTESIAN_POINT ( 'NONE',  ( 0.5405998635167484911, -1.177347015163466182, 0.8538091603066587654 ) ) ;
#12463=CARTESIAN_POINT ( 'NONE',  ( 0.05294255105929539240, -1.287813536604528686, 0.6347874768812761248 ) ) ;
#12470=CARTESIAN_POINT ( 'NONE',  ( 0.3216048373150969253, -1.652200788492672823, 0.5182417262812423209 ) ) ;
#12471=CARTESIAN_POINT ( 'NONE',  ( 0.5709871546789997421, -1.412948679733850410, 0.7285269761084822715 ) ) ;
#12481=CARTESIAN_POINT ( 'NONE',  ( 0.4936674894353650922, -1.281362546945149505, 0.6421980442539246825 ) ) ;
#12483=CARTESIAN_POINT ( 'NONE',  ( 0.07006815180908280982, -1.315301596572416631, 0.5080907171456734428 ) ) ;
#12484=CARTESIAN_POINT ( 'NONE',  ( 0.4434061351937851336, -1.055534433944394390, 0.6333734109485414931 ) ) ;
#12487=B_SPLINE_CURVE_WITH_KNOTS ( 'NONE', 3,
 ( #35529, #35951, #26111, #17027, #10860, #29169 ),
 .UNSPECIFIED., .F., .F.,
 ( 4, 2, 4 ),
 ( 0.000000000000000000, 0.5000000000000000000, 1.000000000000000000 ),
 .UNSPECIFIED. ) ;
#12488=CARTESIAN_POINT ( 'NONE',  ( 0.1048591973540500683, -1.410537849644770025, 0.5682417262808777680 ) ) ;
#12490=EDGE_CURVE ( 'NONE', #32251, #15168, #16678, .T. ) ;
#12492=CARTESIAN_POINT ( 'NONE',  ( 0.3850832117555434420, -1.605563056493195750, 0.5719009434103851097 ) ) ;
#12493=CARTESIAN_POINT ( 'NONE',  ( 0.06660359447752162154, -0.7066512958380626319, -0.0009978780739624637606 ) ) ;
#12494=CARTESIAN_POINT ( 'NONE',  ( 0.1868996193594879007, -0.6130910221644165770, -0.004499342026776794248 ) ) ;
#12495=CARTESIAN_POINT ( 'NONE',  ( 0.06870814706323993826, -0.5548752703722420465, 0.08030761319108148388 ) ) ;
#12501=CARTESIAN_POINT ( 'NONE',  ( 0.4649110479086845382, -1.060769885487067965, 0.6308327102990411994 ) ) ;
#12503=CARTESIAN_POINT ( 'NONE',  ( 0.2053702793495189582, -0.8326540434915299382, 0.6524417661613786112 ) ) ;
#12505=CARTESIAN_POINT ( 'NONE',  ( 0.01128677947712186484, -0.9461986806730106059, 0.1457185332388702959 ) ) ;
#12512=CARTESIAN_POINT ( 'NONE',  ( 0.4271456124369221174, -1.696040845303949940, 0.4245472146382419654 ) ) ;
#12513=DIRECTION ( 'NONE',  ( -0.8660512985181135770, -0.4999551463232371207, 0.000000000000000000 ) ) ;
#12514=CARTESIAN_POINT ( 'NONE',  ( 0.1014370313544829955, -1.288984516341279196, 0.6101567855675421592 ) ) ;
#12515=ADVANCED_FACE ( 'NONE', ( #29287 ), #36643, .T. ) ;
#12520=CARTESIAN_POINT ( 'NONE',  ( 0.4897881687547872565, -1.080982661159355818, 0.5914788577480112330 ) ) ;
#12522=CARTESIAN_POINT ( 'NONE',  ( 0.3504057387187116679, -1.153664717295437070, 0.4422128889498895266 ) ) ;
#12523=CARTESIAN_POINT ( 'NONE',  ( 0.06486471661944531730, -1.341257090703712240, 0.5604528108220497851 ) ) ;
#12524=B_SPLINE_CURVE_WITH_KNOTS ( 'NONE', 3,
 ( #24477, #6748, #34737, #19326, #38031, #31867, #25497, #3683, #31459, #13129, #638, #4066, #7146, #38226, #25693, #15817, #28370, #25298, #236, #19713, #10054, #22624, #32243, #10272, #25912, #9651, #16242, #12732, #3871, #22021, #22834, #28780, #37838, #6542, #16631, #22219, #35160, #16032, #19118, #6959, #13339, #29177, #38432 ),
 .UNSPECIFIED., .F., .F.,
 ( 4, 2, 2, 2, 2, 2, 2, 2, 2, 2, 2, 2, 2, 1, 2, 2, 2, 2, 2, 2, 2, 4 ),
 ( 0.000000000000000000, 0.001251999155498175918, 0.002503998310996351836, 0.003129997888745439036, 0.003755997466494526670, 0.005007996621992698467, 0.006259995777490869398, 0.006885995355239957899, 0.007511994932989045533, 0.008763994088487214729, 0.01001599324398538479, 0.01126799239948355659, 0.01189399197723264162, 0.01251999155498172665, 0.01314599113273081515, 0.01377199071047990019, 0.01502398986597806851, 0.01627598902147623858, 0.01752798817697440517, 0.01815398775472349194, 0.01877998733247257523, 0.02003198648797073489 ),
 .UNSPECIFIED. ) ;
#12526=CARTESIAN_POINT ( 'NONE',  ( 0.1877024697326355740, -1.541847387273544756, 0.6461194557730155497 ) ) ;
#12527=CARTESIAN_POINT ( 'NONE',  ( 0.3453377680719361131, -1.749458763706787545, 0.4498113177181523037 ) ) ;
#12528=CARTESIAN_POINT ( 'NONE',  ( 0.6522089892707538805, -1.452491178199303956, 0.4224083929475448973 ) ) ;
#12530=CARTESIAN_POINT ( 'NONE',  ( 0.3545136070857681787, -1.624373116762336755, 0.4807375746916207615 ) ) ;
#12538=CARTESIAN_POINT ( 'NONE',  ( 0.5762847659421821422, -1.421719372835159589, 0.7207317226011845657 ) ) ;
#12542=CYLINDRICAL_SURFACE ( 'NONE', #26462, 0.03749999999977554621 ) ;
#12544=CARTESIAN_POINT ( 'NONE',  ( 0.01152972583212505224, -0.5524291824619802505, 0.2505810646121844343 ) ) ;
#12552=CARTESIAN_POINT ( 'NONE',  ( 0.1850410792612997846, -0.8547936666690651997, 0.1477569985384105389 ) ) ;
#12553=CARTESIAN_POINT ( 'NONE',  ( 0.3505769137777456912, -1.738054031222972862, 0.4360220170068370704 ) ) ;
#12555=CARTESIAN_POINT ( 'NONE',  ( 0.2867526321560044944, -0.9860951448986656764, 0.7283370995064215592 ) ) ;
#12557=CARTESIAN_POINT ( 'NONE',  ( 0.2735777270575741604, -1.648034364121254036, 0.7523254439293706186 ) ) ;
#12558=CARTESIAN_POINT ( 'NONE',  ( 0.3224542088160151643, -1.759949008389460223, 0.6236646122038994600 ) ) ;
#12570=CARTESIAN_POINT ( 'NONE',  ( 0.09482598954113068135, -1.341677941020415377, 0.6974875476592315993 ) ) ;
#12572=CARTESIAN_POINT ( 'NONE',  ( 0.6712941330769894854, -1.387165532388958678, 0.7909734157804186871 ) ) ;
#12574=CARTESIAN_POINT ( 'NONE',  ( 0.6803383295583191881, -1.562882757458972982, 0.6028934748675488509 ) ) ;
#12577=ORIENTED_EDGE ( 'NONE', *, *, #23579, .T. ) ;
#12579=CARTESIAN_POINT ( 'NONE',  ( 0.2649388293739690647, -1.647471256193353994, 0.7673347028883034104 ) ) ;
#12581=CARTESIAN_POINT ( 'NONE',  ( 0.5948448836580337851, -1.487180068494697860, 0.5714582431182474442 ) ) ;
#12582=FACE_OUTER_BOUND ( 'NONE', #1633, .T. ) ;
#12583=ORIENTED_EDGE ( 'NONE', *, *, #14510, .T. ) ;
#12584=CARTESIAN_POINT ( 'NONE',  ( 0.5555567715531690709, -1.190973094708358992, 0.5709149340790615756 ) ) ;
#12586=VERTEX_POINT ( 'NONE', #37462 ) ;
#12587=CARTESIAN_POINT ( 'NONE',  ( 0.3155498261607609933, -0.8427994992563406784, 0.6561175494744075909 ) ) ;
#12593=CIRCLE ( 'NONE', #8650, 0.01000000000000002970 ) ;
#12596=CARTESIAN_POINT ( 'NONE',  ( 0.08944029709302749043, -0.7717967997121178980, 0.2508382323318106844 ) ) ;
#12598=CARTESIAN_POINT ( 'NONE',  ( 0.4115766028365042128, -1.733048369835246794, 0.5182417262812423209 ) ) ;
#12599=CARTESIAN_POINT ( 'NONE',  ( 0.5251744434789910043, -1.526859942859090324, 0.5727264815542076892 ) ) ;
#12603=CARTESIAN_POINT ( 'NONE',  ( 0.4581770189839536878, -1.680087630256094755, 0.5962093605133977903 ) ) ;
#12604=CARTESIAN_POINT ( 'NONE',  ( 0.6989095468901158625, -1.435512049448604444, 0.6261787951156853049 ) ) ;
#12605=DIRECTION ( 'NONE',  ( 0.8660512985181126888, 0.4999551463232384529, 0.000000000000000000 ) ) ;
#12606=CARTESIAN_POINT ( 'NONE',  ( 0.5750439247535107379, -1.432704706222420521, 0.7403086931740429089 ) ) ;
#12609=CARTESIAN_POINT ( 'NONE',  ( 0.2679554415261233280, -1.674078903935640517, 0.5221304914950548604 ) ) ;
#12610=FACE_OUTER_BOUND ( 'NONE', #32459, .T. ) ;
#12611=CARTESIAN_POINT ( 'NONE',  ( 0.2467813525974754951, -0.8519813862200177335, 0.4954293255957377684 ) ) ;
#12621=CARTESIAN_POINT ( 'NONE',  ( 0.08510361377861434817, -0.8106636051554854117, 0.1454306519311501233 ) ) ;
#12622=ORIENTED_EDGE ( 'NONE', *, *, #33570, .F. ) ;
#12623=CARTESIAN_POINT ( 'NONE',  ( 0.4970758107849645446, -1.079867600816170059, 0.3667417262808778666 ) ) ;
#12624=CARTESIAN_POINT ( 'NONE',  ( -0.007649408449226275004, -0.8869281924019897234, 0.4775367515392046069 ) ) ;
#12629=CARTESIAN_POINT ( 'NONE',  ( 0.3259879919982042185, -1.767950897709266611, 0.5312986935552648227 ) ) ;
#12635=CARTESIAN_POINT ( 'NONE',  ( 0.09015709819048388363, -0.5643440796219489908, 0.1782129044586291677 ) ) ;
#12637=VERTEX_POINT ( 'NONE', #31319 ) ;
#12640=CARTESIAN_POINT ( 'NONE',  ( 0.07460218941637257462, -0.5676562956907557078, 0.2601178745213920673 ) ) ;
#12641=ADVANCED_FACE ( 'NONE', ( #6961 ), #2923, .T. ) ;
#12643=CARTESIAN_POINT ( 'NONE',  ( 0.5558855420699814198, -1.622948660481935423, 0.5440994406646009196 ) ) ;
#12644=CARTESIAN_POINT ( 'NONE',  ( 0.006145725594649042133, -0.8471966322199038224, 0.2388777800840232446 ) ) ;
#12645=CARTESIAN_POINT ( 'NONE',  ( 0.3349327071708561587, -0.9960187932710996561, 0.5970633004496839202 ) ) ;
#12649=CARTESIAN_POINT ( 'NONE',  ( 0.1897125635009227207, -0.5340696856102284951, 0.1480337217182641774 ) ) ;
#12650=CARTESIAN_POINT ( 'NONE',  ( 0.5808183205011048234, -1.495242300261638402, 0.5715967477096820515 ) ) ;
#12655=CARTESIAN_POINT ( 'NONE',  ( 0.4937576479559093179, -1.320126057825392607, 0.8099836062144650795 ) ) ;
#12657=CARTESIAN_POINT ( 'NONE',  ( 0.4077406957728484382, -0.9605384586880818532, 0.7982698588713066368 ) ) ;
#12659=CARTESIAN_POINT ( 'NONE',  ( 0.04514759861635499888, -1.211207050343567238, 0.6773524313334282621 ) ) ;
#12664=CARTESIAN_POINT ( 'NONE',  ( 0.06443582809897516195, -0.8352844082134175396, 0.1913173570483421015 ) ) ;
#12675=CARTESIAN_POINT ( 'NONE',  ( 0.6521185033023405575, -1.542907011849279364, 0.4182417262808776348 ) ) ;
#12684=CARTESIAN_POINT ( 'NONE',  ( 0.2594029906281075104, -1.332806731452343962, 0.4172623082385037430 ) ) ;
#12685=CARTESIAN_POINT ( 'NONE',  ( 0.4469231120930088896, -1.683251538248273338, 0.4316885541138326121 ) ) ;
#12687=CARTESIAN_POINT ( 'NONE',  ( 0.5110404537384164447, -1.311648276678567093, 0.6104441183122480963 ) ) ;
#12690=CARTESIAN_POINT ( 'NONE',  ( 0.4929465528686921005, -1.082715557938388029, 0.5682417262808779901 ) ) ;
#12695=CARTESIAN_POINT ( 'NONE',  ( 0.05229530933811773336, -0.6522472549805439224, 0.4589227677422883511 ) ) ;
#12697=CARTESIAN_POINT ( 'NONE',  ( 0.06525845452225115251, -0.8048554632036153400, 0.05552589205823528495 ) ) ;
#12698=CARTESIAN_POINT ( 'NONE',  ( 0.1754198919089409725, -0.8045108718813741566, -0.05231893310831398081 ) ) ;
#12699=CARTESIAN_POINT ( 'NONE',  ( 0.06897536523928704533, -0.5446676224100435171, 0.1075395329137426442 ) ) ;
#12702=VERTEX_POINT ( 'NONE', #4069 ) ;
#12704=CARTESIAN_POINT ( 'NONE',  ( 0.4933397991863339715, -1.083186959060361332, 0.5723784735904143828 ) ) ;
#12705=CARTESIAN_POINT ( 'NONE',  ( 0.5679494682189658583, -1.502316997319172565, 0.6067939519441243323 ) ) ;
#12707=CARTESIAN_POINT ( 'NONE',  ( 0.1873953661158407891, -0.6938363853788876989, 0.03552928613571013777 ) ) ;
#12708=CARTESIAN_POINT ( 'NONE',  ( 0.5432513433150938376, -1.169106661975274353, 0.5798782747789370529 ) ) ;
#12715=CARTESIAN_POINT ( 'NONE',  ( 0.08535460625685879765, -0.8121872720543428237, 0.1030692480275667428 ) ) ;
#12719=FACE_OUTER_BOUND ( 'NONE', #16427, .T. ) ;
#12720=CARTESIAN_POINT ( 'NONE',  ( 0.09485889511719647338, -1.298679434850192216, 0.6031548665757355820 ) ) ;
#12722=CARTESIAN_POINT ( 'NONE',  ( 0.09402968441108132402, -1.354797296243051008, 0.6996042430478996987 ) ) ;
#12724=CARTESIAN_POINT ( 'NONE',  ( 0.5941217087312797851, -1.459610275592444273, 0.5526975506195443977 ) ) ;
#12725=CARTESIAN_POINT ( 'NONE',  ( 0.2043866115177667420, -1.364383961788701249, 0.4807399974250947117 ) ) ;
#12726=CARTESIAN_POINT ( 'NONE',  ( 0.06581764578086118922, -1.340728352476674212, 0.5449258910593480776 ) ) ;
#12727=CARTESIAN_POINT ( 'NONE',  ( 0.2637142753222213587, -1.685688650057170390, 0.5655586431828601990 ) ) ;
#12728=ADVANCED_FACE ( 'NONE', ( #5273 ), #35324, .T. ) ;
#12730=B_SPLINE_CURVE_WITH_KNOTS ( 'NONE', 3,
 ( #39677, #35992, #7798, #24079, #36788, #26751, #32889, #14373, #23868, #20975, #26939, #18087, #29824, #27365, #36392, #2260, #4701, #7995, #1667, #36603, #23661, #33307, #39279, #20573, #20783, #8408, #30432, #2045, #14799, #11103 ),
 .UNSPECIFIED., .F., .F.,
 ( 4, 2, 2, 2, 2, 2, 2, 2, 2, 2, 2, 2, 2, 2, 4 ),
 ( -5.999999999967792359E-08, 0.002163189985905394474, 0.004326439971810788591, 0.006489689957716177938, 0.007571314950668870010, 0.008652939943621561214, 0.01081618992952694709, 0.01189781492247964263, 0.01297943991543233817, 0.01406106490838503545, 0.01514268990133772926, 0.01568350239781407876, 0.01622431489429042653, 0.01676512739076677430, 0.01730593988724312207 ),
 .UNSPECIFIED. ) ;
#12731=CARTESIAN_POINT ( 'NONE',  ( 0.1227332031174801358, -1.426450801877330088, 0.6430247681006037164 ) ) ;
#12732=CARTESIAN_POINT ( 'NONE',  ( -0.0001212384970512573110, -0.7977683222466966928, -0.07773302012097864366 ) ) ;
#12734=EDGE_CURVE ( 'NONE', #35767, #35465, #10872, .T. ) ;
#12740=VERTEX_POINT ( 'NONE', #23445 ) ;
#12744=CARTESIAN_POINT ( 'NONE',  ( 0.0004750592482352814579, -0.4386115460793976739, 0.1457185332388683252 ) ) ;
#12746=CARTESIAN_POINT ( 'NONE',  ( 0.4483952930911858648, -1.219233892752134230, 0.8146593353750180011 ) ) ;
#12748=VERTEX_POINT ( 'NONE', #5081 ) ;
#12753=CARTESIAN_POINT ( 'NONE',  ( 0.01112738939452267463, -0.5460437306624825737, 0.2315852079017418352 ) ) ;
#12756=CARTESIAN_POINT ( 'NONE',  ( 0.1026681637763624949, -1.278312822899872581, 0.5960544170339612258 ) ) ;
#12757=CARTESIAN_POINT ( 'NONE',  ( 0.3093710864688895557, -1.763897289999589280, 0.5510299488878679375 ) ) ;
#12758=CARTESIAN_POINT ( 'NONE',  ( 0.1889626679396633202, -0.9196856789278203825, 0.008518417185872219008 ) ) ;
#12763=EDGE_CURVE ( 'NONE', #4342, #30110, #6031, .T. ) ;
#12768=CARTESIAN_POINT ( 'NONE',  ( 0.2076380708292103194, -0.9071444418369396523, 0.6111425315318238516 ) ) ;
#12769=CARTESIAN_POINT ( 'NONE',  ( 0.2715177313894526767, -1.674232447558412495, 0.6134098869104458451 ) ) ;
#12771=CARTESIAN_POINT ( 'NONE',  ( 0.2863795044656264888, -1.560883083107998059, 0.9807757954863742800 ) ) ;
#12790=ADVANCED_FACE ( 'NONE', ( #39441 ), #35754, .F. ) ;
#12792=CARTESIAN_POINT ( 'NONE',  ( 0.1973196604133208854, -0.5903291263510783704, 0.3099102803838563180 ) ) ;
#12793=EDGE_LOOP ( 'NONE', ( #32532, #4561, #27687, #33683 ) ) ;
#12795=CARTESIAN_POINT ( 'NONE',  ( 0.2025468388808826514, -1.402172900482729911, 0.9469506584777290792 ) ) ;
#12797=CARTESIAN_POINT ( 'NONE',  ( 0.1313385724593379156, -0.5561286514583599905, 0.1878675228657155638 ) ) ;
#12798=DIRECTION ( 'NONE',  ( 0.01455087615875007116, 0.9998941303973200023, 0.000000000000000000 ) ) ;
#12800=AXIS2_PLACEMENT_3D ( 'NONE', #1773, #7701, #33209 ) ;
#12801=ORIENTED_EDGE ( 'NONE', *, *, #34263, .T. ) ;
#12809=EDGE_CURVE ( 'NONE', #37238, #24651, #38984, .T. ) ;
#12814=ORIENTED_EDGE ( 'NONE', *, *, #22553, .T. ) ;
#12815=EDGE_CURVE ( 'NONE', #2281, #24994, #30095, .T. ) ;
#12816=CARTESIAN_POINT ( 'NONE',  ( 0.08538299691383845202, -0.7671892257780283941, 0.1589107908280385228 ) ) ;
#12817=VECTOR ( 'NONE', #28562, 39.37007874015748143 ) ;
#12818=CARTESIAN_POINT ( 'NONE',  ( 0.1052052648158661730, -0.5678973627517217571, 0.2443419843495847621 ) ) ;
#12822=CARTESIAN_POINT ( 'NONE',  ( 0.4068922648389373120, -1.709694718896766163, 0.6105211896656776993 ) ) ;
#12823=CARTESIAN_POINT ( 'NONE',  ( 0.7282435738944056380, -1.482681635168590084, 0.7278836751128088256 ) ) ;
#12826=CARTESIAN_POINT ( 'NONE',  ( 0.6087833944362014416, -1.478973828311692884, 0.5678978172759817644 ) ) ;
#12829=CARTESIAN_POINT ( 'NONE',  ( 0.1434010736994648927, -1.283284918233685623, 0.5707417262808780478 ) ) ;
#12832=CARTESIAN_POINT ( 'NONE',  ( 0.05447883519600660307, -1.297772118441766542, 0.6273051521731305424 ) ) ;
#12833=CARTESIAN_POINT ( 'NONE',  ( 0.3071794164948500327, -0.9095699098325729093, 0.5987596725107463547 ) ) ;
#12839=CARTESIAN_POINT ( 'NONE',  ( 0.5845432865795784361, -1.492259592395753121, 0.5476657707439447353 ) ) ;
#12844=CARTESIAN_POINT ( 'NONE',  ( 0.08906878592800504535, -0.5893343340316107293, 0.07116080034756296080 ) ) ;
#12846=CARTESIAN_POINT ( 'NONE',  ( 0.4092450614235220163, -1.131740385117829817, 0.4687417262808780127 ) ) ;
#12847=CARTESIAN_POINT ( 'NONE',  ( -0.01502126383153619404, -0.8492948373293993658, 0.1457185332388695187 ) ) ;
#12849=ORIENTED_EDGE ( 'NONE', *, *, #27890, .F. ) ;
#12858=CARTESIAN_POINT ( 'NONE',  ( 0.01048552245699511248, -0.5296434293125212855, 0.1353013932409117825 ) ) ;
#12862=CARTESIAN_POINT ( 'NONE',  ( 0.1074308231225710453, -0.6537910774608231002, 0.3828935582149098904 ) ) ;
#12866=CARTESIAN_POINT ( 'NONE',  ( 0.4416260615216031638, -1.573751756256522860, 0.5728199209250995905 ) ) ;
#12867=CARTESIAN_POINT ( 'NONE',  ( 0.002594981386083806962, -0.5384102241734924910, 0.2402617689866153317 ) ) ;
#12870=CARTESIAN_POINT ( 'NONE',  ( 0.4073273336764455244, -1.035739235929862723, 0.6333991914734626860 ) ) ;
#12871=CARTESIAN_POINT ( 'NONE',  ( 0.3711011835697567429, -1.742358524620057914, 0.6021863986438362737 ) ) ;
#12875=CARTESIAN_POINT ( 'NONE',  ( 0.1887425661959986067, -0.4595475489851841844, 0.1484827297904532939 ) ) ;
#12876=CARTESIAN_POINT ( 'NONE',  ( 0.1257895988989382596, -0.5688825542510129729, 0.2354356649681056124 ) ) ;
#12878=DIRECTION ( 'NONE',  ( -0.8660512985181135770, -0.4999551463232371207, 0.000000000000000000 ) ) ;
#12880=CARTESIAN_POINT ( 'NONE',  ( 0.5546478408217279110, -1.425212702037291113, 0.7586032485602538511 ) ) ;
#12881=CARTESIAN_POINT ( 'NONE',  ( 0.3047936848243344432, -1.756875962071034580, 0.5682417262361116883 ) ) ;
#12882=CARTESIAN_POINT ( 'NONE',  ( 0.2196261443710258443, -0.6607888217372858142, 0.4354189310569229754 ) ) ;
#12884=CARTESIAN_POINT ( 'NONE',  ( 0.06285925416399532062, -1.277715309600261806, 0.6373717965182834622 ) ) ;
#12889=CARTESIAN_POINT ( 'NONE',  ( 0.1465276397530375918, -0.8893464018661847437, 0.5571063954901773752 ) ) ;
#12891=CARTESIAN_POINT ( 'NONE',  ( 0.6528116166078939964, -1.560548874428574262, 0.4255554162163330822 ) ) ;
#12893=ORIENTED_EDGE ( 'NONE', *, *, #1664, .T. ) ;
#12902=CARTESIAN_POINT ( 'NONE',  ( 0.2230281810701175149, -1.353330874913282855, 0.5685393872860169395 ) ) ;
#12905=CARTESIAN_POINT ( 'NONE',  ( 0.3779407171956395972, -1.119494477781395103, 0.7341046588790626215 ) ) ;
#12908=CARTESIAN_POINT ( 'NONE',  ( 0.4929039159923706559, -1.082692164550193237, 0.5711674032880966756 ) ) ;
#12912=ORIENTED_EDGE ( 'NONE', *, *, #138, .T. ) ;
#12913=CARTESIAN_POINT ( 'NONE',  ( 0.3881114196206040812, -1.604032130030556447, 0.6335681399033196159 ) ) ;
#12914=CARTESIAN_POINT ( 'NONE',  ( 0.08535229771277842714, -0.8275964096657028035, 0.1106497307489484189 ) ) ;
#12915=CARTESIAN_POINT ( 'NONE',  ( 0.1746425353517715717, -0.9069533527181683485, 0.07551361239408968529 ) ) ;
#12916=CARTESIAN_POINT ( 'NONE',  ( 0.08510361377861434817, -0.8106636051554854117, 0.1454306519311501233 ) ) ;
#12920=CARTESIAN_POINT ( 'NONE',  ( 0.4913580909694157950, -1.080994014340969311, 0.5908918996469622043 ) ) ;
#12922=EDGE_CURVE ( 'NONE', #17955, #13190, #33762, .T. ) ;
#12923=CARTESIAN_POINT ( 'NONE',  ( 0.5673951979382229061, -1.499929312403656123, 0.6329649192270386804 ) ) ;
#12937=CARTESIAN_POINT ( 'NONE',  ( 0.6872158423035881203, -1.414036026188038031, 0.8114895833460221697 ) ) ;
#12943=CARTESIAN_POINT ( 'NONE',  ( 0.4579382962256918765, -1.063507731091402952, 0.6287285752299462960 ) ) ;
#12945=CARTESIAN_POINT ( 'NONE',  ( 0.2637479789745994507, -0.6009450727723176788, 0.1023043458361303365 ) ) ;
#12946=CARTESIAN_POINT ( 'NONE',  ( 0.2638409115276085237, -1.685919794262354499, 0.5661884833608360479 ) ) ;
#12949=CARTESIAN_POINT ( 'NONE',  ( 0.1209218709639075517, -1.413449759333152755, 0.6688053819537839173 ) ) ;
#12961=CARTESIAN_POINT ( 'NONE',  ( 0.5692153087590623439, -1.410103658342158894, 0.7339724487708582101 ) ) ;
#12962=CARTESIAN_POINT ( 'NONE',  ( 0.5988734330629296165, -1.608409508104120089, 0.4438041697090711057 ) ) ;
#12965=CARTESIAN_POINT ( 'NONE',  ( 0.5593576702765247211, -1.619265888493739869, 0.4800288912735870550 ) ) ;
#12967=CARTESIAN_POINT ( 'NONE',  ( 0.01188774847410361928, -0.5569381300819099545, 0.2634111891979500353 ) ) ;
#12969=LINE ( 'NONE', #37857, #39262 ) ;
#12970=CARTESIAN_POINT ( 'NONE',  ( 0.3116392842230086835, -1.763036623927715763, 0.5305946302528526948 ) ) ;
#12972=CARTESIAN_POINT ( 'NONE',  ( 0.4125049716505733155, -1.702587279938547082, 0.4182417262808258984 ) ) ;
#12976=CARTESIAN_POINT ( 'NONE',  ( 0.2120302040687593315, -0.9292546879809068239, 0.3755713860025718942 ) ) ;
#12979=CARTESIAN_POINT ( 'NONE',  ( 0.5744677579470482964, -1.463377169234544084, 0.7112240420332721635 ) ) ;
#12980=CARTESIAN_POINT ( 'NONE',  ( 0.3215791306822571305, -1.068485763701718438, 0.7392398419832824086 ) ) ;
#12982=EDGE_CURVE ( 'NONE', #243, #34712, #20790, .T. ) ;
#12987=CARTESIAN_POINT ( 'NONE',  ( 0.3251018894956911320, -1.768268453779731519, 0.5225951996439848202 ) ) ;
#12989=CARTESIAN_POINT ( 'NONE',  ( 0.4553705988804589988, -1.219712494940672132, 0.6659395549564459671 ) ) ;
#12992=CARTESIAN_POINT ( 'NONE',  ( -0.0004431470427073231017, -0.9367128829938298207, 0.1457185332388704069 ) ) ;
#12994=CARTESIAN_POINT ( 'NONE',  ( 0.1143055500903454591, -1.383430755858714445, 0.6590833788586937247 ) ) ;
#13001=CARTESIAN_POINT ( 'NONE',  ( 0.4239279940938358027, -1.134057330594810509, 0.4357807031462634928 ) ) ;
#13003=DIRECTION ( 'NONE',  ( 1.060606950627616897E-16, 6.122684696619992497E-17, 1.000000000000000000 ) ) ;
#13004=CARTESIAN_POINT ( 'NONE',  ( 0.2648844005684549696, -1.672583955634053599, 0.5258809023128611093 ) ) ;
#13005=CARTESIAN_POINT ( 'NONE',  ( 0.1316748077902114011, -0.5679410235953537001, 0.2289183786684796940 ) ) ;
#13010=CARTESIAN_POINT ( 'NONE',  ( 0.6408424734368098896, -1.484124584333256447, 0.7996275517132238608 ) ) ;
#13015=VERTEX_POINT ( 'NONE', #34889 ) ;
#13016=CARTESIAN_POINT ( 'NONE',  ( 0.08709445727914670587, -0.7690269056237728496, 0.2131905848466921494 ) ) ;
#13019=CARTESIAN_POINT ( 'NONE',  ( 0.08990936761270149069, -0.5436479961250832993, 0.1437216542238700934 ) ) ;
#13020=CARTESIAN_POINT ( 'NONE',  ( 0.5390789672074006722, -1.519044896617570473, 0.5730556844385706894 ) ) ;
#13025=EDGE_CURVE ( 'NONE', #20653, #12637, #24727, .T. ) ;
#13027=CARTESIAN_POINT ( 'NONE',  ( 0.6567493722867359107, -1.524089082616542745, 0.7420751960461151597 ) ) ;
#13030=CARTESIAN_POINT ( 'NONE',  ( 0.6084588361978461313, -1.478885940474569782, 0.5610653007198931341 ) ) ;
#13032=CARTESIAN_POINT ( 'NONE',  ( 0.1438070510857625550, -1.283988175806205723, 0.3667417262808778111 ) ) ;
#13034=CARTESIAN_POINT ( 'NONE',  ( 0.07959189571600921997, -1.355556588927695927, 0.6171934786799392336 ) ) ;
#13035=CARTESIAN_POINT ( 'NONE',  ( 0.3637128952805344095, -0.9645059733743139851, 0.6550525653421633843 ) ) ;
#13037=EDGE_CURVE ( 'NONE', #16750, #1246, #15377, .T. ) ;
#13038=B_SPLINE_CURVE_WITH_KNOTS ( 'NONE', 3,
 ( #13514, #6506, #26077, #38596, #22186, #34701 ),
 .UNSPECIFIED., .F., .F.,
 ( 4, 2, 4 ),
 ( 1.734723475976807094E-18, 0.0003588387877355910536, 0.0007176775754711803724 ),
 .UNSPECIFIED. ) ;
#13040=CARTESIAN_POINT ( 'NONE',  ( 0.6931363209573969675, -1.429025764147124677, 0.5740297270470278157 ) ) ;
#13042=EDGE_LOOP ( 'NONE', ( #19647, #10419, #7920, #24483 ) ) ;
#13043=CARTESIAN_POINT ( 'NONE',  ( 0.4326363521158365644, -1.579581225308487324, 0.5961853866131431312 ) ) ;
#13047=CARTESIAN_POINT ( 'NONE',  ( 0.05583995664670776682, -1.335624775257321817, 0.3157417262808777658 ) ) ;
#13048=CARTESIAN_POINT ( 'NONE',  ( 0.07107056164821387578, -1.264508437377509065, 0.7522515875062320001 ) ) ;
#13051=DIRECTION ( 'NONE',  ( -0.8660512985181135770, -0.4999551463232368431, 0.000000000000000000 ) ) ;
#13058=CYLINDRICAL_SURFACE ( 'NONE', #5438, 0.1762268159172277748 ) ;
#13059=VERTEX_POINT ( 'NONE', #1187 ) ;
#13060=CARTESIAN_POINT ( 'NONE',  ( 0.1833618000930513636, -0.7929100317814798959, 0.6245802647066135416 ) ) ;
#13062=ORIENTED_EDGE ( 'NONE', *, *, #8755, .F. ) ;
#13063=CARTESIAN_POINT ( 'NONE',  ( 0.02241053216763305364, -0.5389090406332393002, 0.4746621284997309398 ) ) ;
#13064=CARTESIAN_POINT ( 'NONE',  ( 0.2558668472228415869, -1.097573035806539643, 0.8345594848954058786 ) ) ;
#13067=CARTESIAN_POINT ( 'NONE',  ( 0.4916863479492353806, -1.686802518800459616, 0.5182417262812423209 ) ) ;
#13068=ADVANCED_FACE ( 'NONE', ( #8120 ), #28542, .T. ) ;
#13070=CARTESIAN_POINT ( 'NONE',  ( 0.1153471661800104520, -0.4465907051537530426, 0.1436109887884166880 ) ) ;
#13071=ADVANCED_FACE ( 'NONE', ( #32619 ), #20074, .T. ) ;
#13072=CARTESIAN_POINT ( 'NONE',  ( 0.1252465029946501218, -0.5602642337835891384, 0.2083474642613161176 ) ) ;
#13076=CARTESIAN_POINT ( 'NONE',  ( 0.6448460108028967186, -1.341977515531164844, 0.7437914968157772755 ) ) ;
#13078=CARTESIAN_POINT ( 'NONE',  ( 0.02569018704401261968, -1.113496988582522773, 0.6482248533806770352 ) ) ;
#13082=CARTESIAN_POINT ( 'NONE',  ( 0.3720999503424056720, -1.111552407429487133, 0.7356505582348251693 ) ) ;
#13084=CARTESIAN_POINT ( 'NONE',  ( 0.6995787265782542619, -1.495850124575206275, 0.4894661681568200362 ) ) ;
#13086=CARTESIAN_POINT ( 'NONE',  ( 0.4632309505043279430, -1.114013528690801280, 0.5645935559310804042 ) ) ;
#13089=CARTESIAN_POINT ( 'NONE',  ( 0.08222542156927918622, -1.327483614382551913, 0.4683366274853996702 ) ) ;
#13092=CARTESIAN_POINT ( 'NONE',  ( 0.1514761298305456472, -1.395251342086818447, 0.4173550238117827438 ) ) ;
#13093=CARTESIAN_POINT ( 'NONE',  ( 0.4419048264408250715, -1.686280600454902245, 0.4284299735159858291 ) ) ;
#13095=CARTESIAN_POINT ( 'NONE',  ( 0.4460384620557638624, -1.210965027603213562, 0.7166821082092738049 ) ) ;
#13097=CARTESIAN_POINT ( 'NONE',  ( 0.2709623010280027278, -1.672610760848568967, 0.4891849873696615392 ) ) ;
#13098=CARTESIAN_POINT ( 'NONE',  ( 0.4929465528686918230, -1.082715557938388029, 0.5668025781570900090 ) ) ;
#13100=CARTESIAN_POINT ( 'NONE',  ( 0.07891471443405570496, -1.242007717308747816, 0.7479880969011341030 ) ) ;
#13102=CARTESIAN_POINT ( 'NONE',  ( 0.3881903648927482742, -1.602336578643832166, 0.6494100698158274954 ) ) ;
#13103=CARTESIAN_POINT ( 'NONE',  ( 0.08627532403026182128, -0.7836850491146717390, 0.03808575201433064827 ) ) ;
#13104=CARTESIAN_POINT ( 'NONE',  ( 0.1973196604133173049, -0.5903291263510807019, 0.3099102803838534315 ) ) ;
#13106=ORIENTED_EDGE ( 'NONE', *, *, #1880, .F. ) ;
#13110=CARTESIAN_POINT ( 'NONE',  ( 0.5669110650657969153, -1.503232105430957866, 0.5727642746916661309 ) ) ;
#13115=CARTESIAN_POINT ( 'NONE',  ( 0.1854670398194577796, -0.8253301720469685687, 0.1740524287424448091 ) ) ;
#13116=CARTESIAN_POINT ( 'NONE',  ( 0.08058916068514349051, -1.309220013881624789, 0.4727703015479322590 ) ) ;
#13121=CARTESIAN_POINT ( 'NONE',  ( 0.3214803987143096675, -1.758709516440660092, 0.5682417262808786562 ) ) ;
#13126=CARTESIAN_POINT ( 'NONE',  ( 0.4712007327250372080, -1.210758550387179389, 0.4993402092387030367 ) ) ;
#13128=CARTESIAN_POINT ( 'NONE',  ( 0.2322327485446251394, -1.539891620887370749, 0.8667544471685157959 ) ) ;
#13129=CARTESIAN_POINT ( 'NONE',  ( 0.0002740986199341223918, -0.4896253918872909283, -0.006330435234190400287 ) ) ;
#13132=VERTEX_POINT ( 'NONE', #8332 ) ;
#13138=CARTESIAN_POINT ( 'NONE',  ( 0.6055916563817613785, -1.479479184092913790, 0.5526975506195442867 ) ) ;
#13146=CARTESIAN_POINT ( 'NONE',  ( 0.06022557703969336207, -0.7946678218323519616, 0.6553662645558616662 ) ) ;
#13147=CARTESIAN_POINT ( 'NONE',  ( 0.6241407479001672698, -1.577349794062394173, 0.4194501188810796921 ) ) ;
#13148=CARTESIAN_POINT ( 'NONE',  ( 0.1109092093543055241, -0.9286325583098424818, 0.1457252011008478843 ) ) ;
#13155=CARTESIAN_POINT ( 'NONE',  ( 0.1130167353402539848, -0.9297503534748314813, 0.2195922346210762433 ) ) ;
#13160=CARTESIAN_POINT ( 'NONE',  ( 0.01055999984691518775, -0.5296565616858172065, 0.1504712070062352303 ) ) ;
#13162=CARTESIAN_POINT ( 'NONE',  ( 0.4732168309031719033, -1.158657407058850231, 0.4227107324326277449 ) ) ;
#13163=DIRECTION ( 'NONE',  ( 0.7783639739848380312, 0.6278132875326314366, -1.203114244385168678E-15 ) ) ;
#13164=CARTESIAN_POINT ( 'NONE',  ( 0.7483483892508734359, -1.515136533364971339, 0.3157417262808776548 ) ) ;
#13169=DIRECTION ( 'NONE',  ( 1.060606950627616897E-16, 6.122684696619992497E-17, 1.000000000000000000 ) ) ;
#13170=CARTESIAN_POINT ( 'NONE',  ( 0.1051933607849167424, -1.410369882047322054, 0.5802930348479838907 ) ) ;
#13173=CARTESIAN_POINT ( 'NONE',  ( 0.3683624102916023269, -1.734627145252658709, 0.4304674844703075265 ) ) ;
#13178=EDGE_CURVE ( 'NONE', #17240, #7215, #4849, .T. ) ;
#13182=DIRECTION ( 'NONE',  ( -0.4999551463232372317, 0.8660512985181135770, -0.000000000000000000 ) ) ;
#13184=CARTESIAN_POINT ( 'NONE',  ( 0.1169788285577439829, -1.415237608940837388, 0.5049415650359101448 ) ) ;
#13185=CARTESIAN_POINT ( 'NONE',  ( 0.2675012769506449617, -1.687995237057803743, 0.6051696940006884295 ) ) ;
#13187=CARTESIAN_POINT ( 'NONE',  ( 0.5539760576047348950, -1.429473381317945213, 0.7575193456964278704 ) ) ;
#13190=VERTEX_POINT ( 'NONE', #29950 ) ;
#13199=CARTESIAN_POINT ( 'NONE',  ( -0.004042975624358886508, -0.7404579356088993869, 0.09509064842808988283 ) ) ;
#13201=CARTESIAN_POINT ( 'NONE',  ( 0.09112929967733415793, -0.7529705612394925751, 0.2647947205566859585 ) ) ;
#13203=CARTESIAN_POINT ( 'NONE',  ( 0.5640895105453352931, -1.503407492374277510, 0.5358556994421860287 ) ) ;
#13205=( BOUNDED_SURFACE ( )  B_SPLINE_SURFACE ( 3, 2, ( 
 ( #4275, #26500, #29385 ),
 ( #30184, #11259, #26716 ),
 ( #24038, #26295, #1416 ),
 ( #17035, #20527, #13930 ),
 ( #23828, #7562, #10649 ),
 ( #26905, #23224, #20136 ),
 ( #32664, #16845, #17637 ),
 ( #7337, #4468, #29782 ),
 ( #35956, #19916, #29575 ),
 ( #2014, #32452, #39034 ) ),
 .UNSPECIFIED., .F., .F., .T. ) 
 B_SPLINE_SURFACE_WITH_KNOTS ( ( 4, 2, 2, 2, 4 ),
 ( 3, 3 ),
 ( -5.681219383824043234E-17, 0.0005968317653288563113, 0.001193663530657769435, 0.001790495295986682667, 0.002387327061315595682 ),
 ( 0.000000000000000000, 1.000000000000000000 ),
 .UNSPECIFIED. ) 
 GEOMETRIC_REPRESENTATION_ITEM ( )  RATIONAL_B_SPLINE_SURFACE ( (
 ( 1.000000000000000000, 0.8817574585067788906, 1.000000000000000000),
 ( 1.000000000000000000, 0.8790203634614224271, 1.000000000000000000),
 ( 1.000000000000000000, 0.8757315292216423241, 1.000000000000000000),
 ( 1.000000000000000000, 0.8680526864388360408, 1.000000000000000000),
 ( 1.000000000000000000, 0.8636649569025933726, 1.000000000000000000),
 ( 1.000000000000000000, 0.8542598775336711636, 1.000000000000000000),
 ( 1.000000000000000000, 0.8491049259533275384, 1.000000000000000000),
 ( 1.000000000000000000, 0.8385672512564581460, 1.000000000000000000),
 ( 1.000000000000000000, 0.8331525095424542338, 1.000000000000000000),
 ( 1.000000000000000000, 0.8275829691081207917, 1.000000000000000000) ) ) 
 REPRESENTATION_ITEM ( '' )  SURFACE ( )  );
#13206=CARTESIAN_POINT ( 'NONE',  ( 0.5402709567952270753, -1.518608341991216193, 0.6013252739479361120 ) ) ;
#13211=AXIS2_PLACEMENT_3D ( 'NONE', #3531, #13003, #893 ) ;
#13212=CARTESIAN_POINT ( 'NONE',  ( 0.6726929394684000307, -1.451800111398652282, 0.4506308943308222625 ) ) ;
#13215=CARTESIAN_POINT ( 'NONE',  ( 0.3684487530574376835, -1.732198733335989838, 0.6142793637999888201 ) ) ;
#13216=CARTESIAN_POINT ( 'NONE',  ( 0.6658408180046718750, -1.561543279147396213, 0.5677753029035824683 ) ) ;
#13218=CARTESIAN_POINT ( 'NONE',  ( 0.6097373418327217687, -1.478078193704709387, 0.6043344841116261579 ) ) ;
#13220=CARTESIAN_POINT ( 'NONE',  ( 0.1438681892407857876, -1.284094082863941111, 0.3157417262808777658 ) ) ;
#13222=CARTESIAN_POINT ( 'NONE',  ( 0.004725042054567132541, -0.9785087964782590575, 0.4373990939698282343 ) ) ;
#13223=CARTESIAN_POINT ( 'NONE',  ( 0.4955945803445692133, -1.095919195860131534, 0.6270439991606266972 ) ) ;
#13229=CARTESIAN_POINT ( 'NONE',  ( 0.4619339661384890272, -1.161483764442722277, 0.4182417262808779124 ) ) ;
#13235=B_SPLINE_CURVE_WITH_KNOTS ( 'NONE', 3,
 ( #22665, #4316, #9875, #38478, #34978, #28815 ),
 .UNSPECIFIED., .F., .F.,
 ( 4, 2, 4 ),
 ( 0.000000000000000000, 0.5000000000000000000, 1.000000000000000000 ),
 .UNSPECIFIED. ) ;
#13236=CARTESIAN_POINT ( 'NONE',  ( 0.01057244653857888211, -0.5314355501429048889, 0.1721360658708845914 ) ) ;
#13240=ORIENTED_EDGE ( 'NONE', *, *, #21805, .T. ) ;
#13241=CARTESIAN_POINT ( 'NONE',  ( 0.4093611158985690501, -1.131941421409890403, 0.5197417262808780025 ) ) ;
#13243=CARTESIAN_POINT ( 'NONE',  ( 0.6810725650087121608, -1.407094454800211558, 0.5876998678990568159 ) ) ;
#13250=CARTESIAN_POINT ( 'NONE',  ( 0.5982840689033031012, -1.484634935760666297, 0.5555640900495016909 ) ) ;
#13253=CARTESIAN_POINT ( 'NONE',  ( 0.3373010429313745284, -1.775523145178461659, 0.9104836108820145713 ) ) ;
#13254=CARTESIAN_POINT ( 'NONE',  ( 0.2327882622295160964, -0.8773484716388458837, 0.7033211034437524267 ) ) ;
#13255=CARTESIAN_POINT ( 'NONE',  ( 0.08609365838014089445, -0.5574749707375634689, 0.2233878406577052278 ) ) ;
#13256=EDGE_CURVE ( 'NONE', #1703, #3174, #22234, .T. ) ;
#13258=CARTESIAN_POINT ( 'NONE',  ( 0.1581650021276240492, -1.285700486175305635, 0.4182417262808778013 ) ) ;
#13259=CARTESIAN_POINT ( 'NONE',  ( 0.6012242321195756523, -1.481952306731540103, 0.4817067625245349261 ) ) ;
#13260=CARTESIAN_POINT ( 'NONE',  ( 0.2384528902787253490, -0.9430836346886342092, 0.4549805665859378845 ) ) ;
#13261=ORIENTED_EDGE ( 'NONE', *, *, #24487, .F. ) ;
#13266=CARTESIAN_POINT ( 'NONE',  ( 0.3545313261651519277, -1.624420226475606688, 0.5557399904385574851 ) ) ;
#13271=AXIS2_PLACEMENT_3D ( 'NONE', #39573, #23765, #38974 ) ;
#13273=VECTOR ( 'NONE', #40571, 39.37007874015748143 ) ;
#13275=CARTESIAN_POINT ( 'NONE',  ( 0.3740232550247291066, -0.9210422728154799010, 0.7367171417286558777 ) ) ;
#13276=CARTESIAN_POINT ( 'NONE',  ( 0.4482386148825789340, -1.121187352528194348, 0.5033830347951704365 ) ) ;
#13277=CARTESIAN_POINT ( 'NONE',  ( 0.03938209889053093798, -1.119348185605193224, 0.6511811422115141301 ) ) ;
#13279=CARTESIAN_POINT ( 'NONE',  ( 0.1906988285079815049, -0.7702759449875168363, 0.3037686268896108710 ) ) ;
#13280=EDGE_LOOP ( 'NONE', ( #8846, #18505, #6014, #35403 ) ) ;
#13281=CARTESIAN_POINT ( 'NONE',  ( 0.3011262021662038935, -1.003312458126826012, 0.7429693187443193736 ) ) ;
#13286=CARTESIAN_POINT ( 'NONE',  ( 0.4681011950856142634, -1.249373052585525334, 0.7957081402449762697 ) ) ;
#13290=CARTESIAN_POINT ( 'NONE',  ( 0.1504520142239714753, -1.289994444693127296, 0.4182417262808776903 ) ) ;
#13294=CIRCLE ( 'NONE', #18550, 0.1762268159172233339 ) ;
#13295=VECTOR ( 'NONE', #31455, 39.37007874015748854 ) ;
#13296=CARTESIAN_POINT ( 'NONE',  ( 0.1889603646001475068, -0.5843802352234823694, 0.2966845687057266812 ) ) ;
#13299=CARTESIAN_POINT ( 'NONE',  ( 0.4905433154531526063, -1.277135180857473795, 0.5917710136670832899 ) ) ;
#13302=CARTESIAN_POINT ( 'NONE',  ( 0.4919302148474398173, -1.082157928207513331, 0.5818935738131040258 ) ) ;
#13305=CARTESIAN_POINT ( 'NONE',  ( 0.08883185798063782113, -1.305096067312203401, 0.7226060327209433698 ) ) ;
#13307=CARTESIAN_POINT ( 'NONE',  ( 0.4134850239672457350, -1.589496775099021653, 0.5717027448869763662 ) ) ;
#13309=CARTESIAN_POINT ( 'NONE',  ( 0.1923864837526514660, -0.6113152005538800005, 0.3150246423246629290 ) ) ;
#13313=CARTESIAN_POINT ( 'NONE',  ( 0.3603245586327842864, -1.274710059600435486, 0.5779767968998822392 ) ) ;
#13314=CARTESIAN_POINT ( 'NONE',  ( 0.1231242327260526209, -0.6037900324288171250, 0.3295969312879552526 ) ) ;
#13318=B_SPLINE_CURVE_WITH_KNOTS ( 'NONE', 3,
 ( #22221, #456, #34739, #32066, #25916, #9845, #31869, #6545, #22839, #35542 ),
 .UNSPECIFIED., .F., .F.,
 ( 4, 3, 3, 4 ),
 ( 3.193936382936243481E-15, 0.0005080000155662609419, 0.002540000352560990542, 0.004712884098096298095 ),
 .UNSPECIFIED. ) ;
#13319=CARTESIAN_POINT ( 'NONE',  ( 0.1853834160488257721, -0.8311217846528596853, 0.1678811282091721702 ) ) ;
#13334=CARTESIAN_POINT ( 'NONE',  ( 0.1848746338969347036, -0.6872459287048060528, -0.02854997582304983142 ) ) ;
#13338=CARTESIAN_POINT ( 'NONE',  ( 0.2912354967743938094, -1.730409171686111414, 0.5958501190287942562 ) ) ;
#13339=CARTESIAN_POINT ( 'NONE',  ( -0.0003982523508731287097, -0.9350673170737405782, 0.1130908737492680588 ) ) ;
#13346=VERTEX_POINT ( 'NONE', #8937 ) ;
#13349=CIRCLE ( 'NONE', #29113, 0.08749999999977554899 ) ;
#13350=CARTESIAN_POINT ( 'NONE',  ( 0.4258289169993133561, -1.184892057508847296, 0.7715538982757290665 ) ) ;
#13353=CARTESIAN_POINT ( 'NONE',  ( 0.4594195809631357874, -1.060066247262113182, 0.7450334795338161564 ) ) ;
#13356=CARTESIAN_POINT ( 'NONE',  ( 0.1976682978929888146, -0.7785829950231940577, 0.3156600736487931713 ) ) ;
#13360=CARTESIAN_POINT ( 'NONE',  ( 0.3013866175335212505, -1.646058783738227005, 0.7062181652641160712 ) ) ;
#13362=CARTESIAN_POINT ( 'NONE',  ( 0.1130275343130942994, -0.7030560519982989032, -0.09532014130486921033 ) ) ;
#13363=CARTESIAN_POINT ( 'NONE',  ( 0.3051775095946583360, -1.756515733326251105, 0.5493018342092053086 ) ) ;
#13368=CARTESIAN_POINT ( 'NONE',  ( 0.1859972922984850507, -0.8393112992344217149, 0.1889479090597321054 ) ) ;
#13371=CARTESIAN_POINT ( 'NONE',  ( 0.5951727137181233029, -1.456125169982292800, 0.6236106044506557478 ) ) ;
#13372=CARTESIAN_POINT ( 'NONE',  ( 0.1068110449628701525, -0.8327494205295853380, 0.2803338686668198076 ) ) ;
#13373=CARTESIAN_POINT ( 'NONE',  ( 0.1241306338573257562, -1.117108204751295686, 0.8885289527623265737 ) ) ;
#13375=CARTESIAN_POINT ( 'NONE',  ( 0.4062230848227129099, -1.145582794160925788, 0.4248905050063985778 ) ) ;
#13380=CIRCLE ( 'NONE', #18640, 0.01000000000000003490 ) ;
#13382=CARTESIAN_POINT ( 'NONE',  ( 0.1808993972631122160, -0.4988400884274764024, 0.1169007445746203938 ) ) ;
#13383=CARTESIAN_POINT ( 'NONE',  ( 0.1183428582170880927, -1.407360454669288385, 0.6103212893459412092 ) ) ;
#13395=CARTESIAN_POINT ( 'NONE',  ( 0.4087622015559044253, -1.136016260234564701, 0.4319160579129420752 ) ) ;
#13398=CARTESIAN_POINT ( 'NONE',  ( 0.3387696793961558761, -1.066620522076481947, 0.7898564859712591257 ) ) ;
#13401=VERTEX_POINT ( 'NONE', #15528 ) ;
#13403=CARTESIAN_POINT ( 'NONE',  ( 0.6649543069449874721, -1.548310422546823606, 0.6796974753901866562 ) ) ;
#13406=DIRECTION ( 'NONE',  ( -0.4999551463232372317, 0.8660512985181134660, 0.000000000000000000 ) ) ;
#13409=CARTESIAN_POINT ( 'NONE',  ( -0.001051960901064252297, -0.8469330747986114627, -0.06462206035643724977 ) ) ;
#13411=CARTESIAN_POINT ( 'NONE',  ( 0.2704459367631082412, -0.9896522447148606849, 0.6916254092597398095 ) ) ;
#13415=CARTESIAN_POINT ( 'NONE',  ( 0.5399440942408553212, -1.515719783342790228, 0.6355856557526133876 ) ) ;
#13421=CARTESIAN_POINT ( 'NONE',  ( 0.6686281500267547973, -1.536646776530108838, 0.4440777536512748314 ) ) ;
#13422=CARTESIAN_POINT ( 'NONE',  ( 0.3048570497350418518, -1.756853555320991189, 0.5694442476137144826 ) ) ;
#13425=CIRCLE ( 'NONE', #25231, 0.03749999999977554621 ) ;
#13427=EDGE_CURVE ( 'NONE', #17938, #1703, #2608, .T. ) ;
#13428=CARTESIAN_POINT ( 'NONE',  ( 0.5253354359398262341, -1.363713559762562033, 0.7943058037876152833 ) ) ;
#13430=CARTESIAN_POINT ( 'NONE',  ( -1.465953029183149908E-06, -0.7472984521689456372, -0.1083893734920139823 ) ) ;
#13431=ADVANCED_FACE ( 'NONE', ( #31757 ), #38195, .T. ) ;
#13436=CARTESIAN_POINT ( 'NONE',  ( -0.002083146443013338383, -0.8967360763018588088, 0.1457185332388704624 ) ) ;
#13437=CARTESIAN_POINT ( 'NONE',  ( 0.4864609864856930255, -1.087049186798351608, 0.6366279691173203359 ) ) ;
#13443=CARTESIAN_POINT ( 'NONE',  ( 0.4780517542678584531, -1.172877689127207024, 0.4182417262808778013 ) ) ;
#13448=CARTESIAN_POINT ( 'NONE',  ( 0.4415369156091736302, -1.574510176363862479, 0.6025007236356999529 ) ) ;
#13452=CARTESIAN_POINT ( 'NONE',  ( 0.08522006272954811557, -0.8097442991749735919, 0.1288917670895001755 ) ) ;
#13454=CARTESIAN_POINT ( 'NONE',  ( 0.1437340355044557927, -1.283861693981850349, 0.4177417262808780229 ) ) ;
#13456=CARTESIAN_POINT ( 'NONE',  ( 0.2120163453477715010, -0.5915265038663817254, 0.4276896445164236615 ) ) ;
#13461=ORIENTED_EDGE ( 'NONE', *, *, #1420, .T. ) ;
#13466=CARTESIAN_POINT ( 'NONE',  ( 0.08612155440268152995, -0.6906331012568079908, 0.7711272665534666393 ) ) ;
#13467=CARTESIAN_POINT ( 'NONE',  ( 0.08977666489915449299, -0.6469118995760279045, 0.2018334186708977129 ) ) ;
#13468=CARTESIAN_POINT ( 'NONE',  ( 0.01518662448050903287, -0.4837837598039577136, 0.3562993236613829495 ) ) ;
#13469=CARTESIAN_POINT ( 'NONE',  ( 0.3306407300723779308, -1.212941238661646715, 0.8562008246371364262 ) ) ;
#13472=CARTESIAN_POINT ( 'NONE',  ( 0.08524282091866439148, -1.033473658707478871, 0.5862322604168024309 ) ) ;
#13475=CARTESIAN_POINT ( 'NONE',  ( 0.4000099798367555137, -1.704638381955407400, 0.4282417262808771441 ) ) ;
#13476=CARTESIAN_POINT ( 'NONE',  ( 0.2286386731437905495, -0.6007009410402062155, 0.5044687263126308441 ) ) ;
#13477=AXIS2_PLACEMENT_3D ( 'NONE', #26600, #32333, #7840 ) ;
#13483=B_SPLINE_CURVE_WITH_KNOTS ( 'NONE', 3,
 ( #8427, #11922, #20993, #33513 ),
 .UNSPECIFIED., .F., .F.,
 ( 4, 4 ),
 ( 8.673617379884035472E-19, 0.004712633589911092123 ),
 .UNSPECIFIED. ) ;
#13485=DIRECTION ( 'NONE',  ( -0.4999551463232371762, 0.8660512985181134660, -0.000000000000000000 ) ) ;
#13487=CIRCLE ( 'NONE', #33836, 0.01000000000000002970 ) ;
#13488=CARTESIAN_POINT ( 'NONE',  ( 0.6145270684574122289, -1.293427813764720824, 0.7790094959668801833 ) ) ;
#13489=CARTESIAN_POINT ( 'NONE',  ( 0.4103533436992015671, -1.245885857446504374, 0.5182417262812503145 ) ) ;
#13493=CARTESIAN_POINT ( 'NONE',  ( 0.2755989780306793424, -1.016327101040557901, 0.7228497138915612741 ) ) ;
#13495=CARTESIAN_POINT ( 'NONE',  ( 0.5953303036072959964, -1.457508885835639978, 0.6057417262805095959 ) ) ;
#13505=CARTESIAN_POINT ( 'NONE',  ( 0.1098552746376899730, -0.9433422683584672397, 0.6393798403408993414 ) ) ;
#13508=CARTESIAN_POINT ( 'NONE',  ( 0.3817504269947160078, -1.726033828776056378, 0.4251703030630522018 ) ) ;
#13512=CARTESIAN_POINT ( 'NONE',  ( 0.3846646194939473684, -1.128865715846599560, 0.7236265502079624046 ) ) ;
#13514=CARTESIAN_POINT ( 'NONE',  ( 0.4000099798367660608, -1.704638381955401183, 0.4182417262808776903 ) ) ;
#13522=CARTESIAN_POINT ( 'NONE',  ( 0.1039735380096880463, -0.7886731789469053622, 0.6333316274729952067 ) ) ;
#13523=CARTESIAN_POINT ( 'NONE',  ( 0.06453910615976091170, -0.8346243741771329772, 0.1288229811268807867 ) ) ;
#13524=CARTESIAN_POINT ( 'NONE',  ( 0.2020481313132333201, -0.6875151388636763228, 0.3386544405593424623 ) ) ;
#13525=CARTESIAN_POINT ( 'NONE',  ( 0.1302110173660007697, -1.291756932227970944, 0.4882610538605935413 ) ) ;
#13526=VERTEX_POINT ( 'NONE', #7458 ) ;
#13527=CARTESIAN_POINT ( 'NONE',  ( 0.3264055361853325232, -1.294304910894763072, 0.5706360388247739834 ) ) ;
#13528=CARTESIAN_POINT ( 'NONE',  ( 0.1205771094107126462, -0.5739007583310267169, 0.2533364529363901219 ) ) ;
#13532=CARTESIAN_POINT ( 'NONE',  ( 0.1856180156872625775, -0.8149015557553581646, 0.1814193148890651530 ) ) ;
#13535=CARTESIAN_POINT ( 'NONE',  ( 0.3486350902747559211, -1.743989531435688356, 0.6021158924634461007 ) ) ;
#13536=CARTESIAN_POINT ( 'NONE',  ( 0.08861793153380866095, -0.6435352693684576186, 0.1047593608519658409 ) ) ;
#13538=CARTESIAN_POINT ( 'NONE',  ( 0.6630438016670622270, -1.374754038922163080, 0.8377997132616019638 ) ) ;
#13546=CARTESIAN_POINT ( 'NONE',  ( 0.1847276542582137193, -0.6567261035475721043, -0.02741476136339842176 ) ) ;
#13547=CARTESIAN_POINT ( 'NONE',  ( 0.4470752049162848851, -1.224679863139781721, 0.4807434620714813311 ) ) ;
#13549=CARTESIAN_POINT ( 'NONE',  ( 0.2474040834808491629, -1.657462368044302137, 0.5682417262808785452 ) ) ;
#13551=EDGE_CURVE ( 'NONE', #15736, #27340, #20254, .T. ) ;
#13556=VERTEX_POINT ( 'NONE', #36252 ) ;
#13560=ORIENTED_EDGE ( 'NONE', *, *, #28330, .T. ) ;
#13563=CARTESIAN_POINT ( 'NONE',  ( 0.5249339888458012249, -1.337369657638982634, 0.7530580798306065748 ) ) ;
#13564=CARTESIAN_POINT ( 'NONE',  ( 0.5668224073227418058, -1.626940512309301257, 0.5103467090509832271 ) ) ;
#13565=ORIENTED_EDGE ( 'NONE', *, *, #19810, .F. ) ;
#13566=CARTESIAN_POINT ( 'NONE',  ( 0.4529286794724542986, -1.051290237540063455, 0.7432202178062045084 ) ) ;
#13571=VERTEX_POINT ( 'NONE', #29293 ) ;
#13572=CARTESIAN_POINT ( 'NONE',  ( 0.2891949312394517801, -1.508234465259375767, 0.8769322456029351454 ) ) ;
#13581=CARTESIAN_POINT ( 'NONE',  ( 0.1109049718728864486, -0.9286333055842306283, 0.1449575636331430772 ) ) ;
#13584=CARTESIAN_POINT ( 'NONE',  ( 0.1132625840440346782, -0.8395474731811463087, 0.3484180331796957741 ) ) ;
#13585=CARTESIAN_POINT ( 'NONE',  ( 0.01056122778382778161, -0.5298774523167767425, 0.1553095696234600420 ) ) ;
#13591=CARTESIAN_POINT ( 'NONE',  ( 0.3259879919982042185, -1.767950897709266611, 0.5312986935552648227 ) ) ;
#13595=CARTESIAN_POINT ( 'NONE',  ( 0.1806271871886622193, -0.4979126063066979802, 0.1191298491398793680 ) ) ;
#13600=CARTESIAN_POINT ( 'NONE',  ( 0.2856903115327851239, -1.612432775839717225, 0.9415318914171060261 ) ) ;
#13605=CARTESIAN_POINT ( 'NONE',  ( 0.5764473935400443727, -1.446560465971904463, 0.7291923036817888892 ) ) ;
#13610=CARTESIAN_POINT ( 'NONE',  ( 0.5863399829793073392, -1.370111929318044597, 0.8757726842784098187 ) ) ;
#13613=CARTESIAN_POINT ( 'NONE',  ( -0.007799093721804064433, -0.6030369617549071748, 0.3865317856287898146 ) ) ;
#13615=CARTESIAN_POINT ( 'NONE',  ( -0.002000607657151622348, -0.7404579356088996089, -0.01138449076159512782 ) ) ;
#13616=EDGE_LOOP ( 'NONE', ( #2681, #19331, #27929, #28702 ) ) ;
#13617=CARTESIAN_POINT ( 'NONE',  ( 0.08970085000315114465, -0.8164246713187256477, 0.2562084196594314744 ) ) ;
#13619=CARTESIAN_POINT ( 'NONE',  ( 0.1100478739389431776, -0.5471989581415684922, 0.1457185332388694632 ) ) ;
#13620=CARTESIAN_POINT ( 'NONE',  ( 0.06720200293959881221, -1.311493277772410426, 0.6073410707387120189 ) ) ;
#13623=CARTESIAN_POINT ( 'NONE',  ( 0.3650261032261186700, -1.734273230346309091, 0.6015988091205355381 ) ) ;
#13626=CARTESIAN_POINT ( 'NONE',  ( 0.3135533596100509857, -1.751749968712532635, 0.5597833863612885485 ) ) ;
#13628=CARTESIAN_POINT ( 'NONE',  ( -2.158236442226783958E-06, -0.7557589808029421263, -0.1062375170323252432 ) ) ;
#13629=CARTESIAN_POINT ( 'NONE',  ( 0.06952717988241019498, -0.5442879774309438146, 0.1846901343294024000 ) ) ;
#13630=CARTESIAN_POINT ( 'NONE',  ( 0.007573306818223588845, -0.7572691898189487514, 0.003620172530112310012 ) ) ;
#13632=CARTESIAN_POINT ( 'NONE',  ( 0.01266180416972241714, -0.9102398499036795654, 0.5581420674395337622 ) ) ;
#13633=CARTESIAN_POINT ( 'NONE',  ( 0.4638997371337593156, -1.067608878195758448, 0.6494661525283214054 ) ) ;
#13635=CYLINDRICAL_SURFACE ( 'NONE', #16244, 0.2500000000000000000 ) ;
#13636=CARTESIAN_POINT ( 'NONE',  ( 0.3187814993714178091, -1.760346054620885781, 0.5688112331864385585 ) ) ;
#13638=CARTESIAN_POINT ( 'NONE',  ( 0.4465857567753348523, -1.571616349952935643, 0.6043008826171946124 ) ) ;
#13639=CARTESIAN_POINT ( 'NONE',  ( 0.01075032470689779758, -0.5446343802999467076, 0.2276730487650680257 ) ) ;
#13642=CARTESIAN_POINT ( 'NONE',  ( 0.1859432605888821921, -0.7573098151843028480, 0.1022962920937455361 ) ) ;
#13643=EDGE_CURVE ( 'NONE', #25669, #36006, #24707, .T. ) ;
#13645=CARTESIAN_POINT ( 'NONE',  ( 0.2033263846434442690, -0.5675993867538808857, 0.3776288918835234987 ) ) ;
#13649=CARTESIAN_POINT ( 'NONE',  ( 0.6590705178848084156, -1.601721441849921268, 0.5182417262812423209 ) ) ;
#13654=CARTESIAN_POINT ( 'NONE',  ( 0.3480299946200001715, -1.742528658578555989, 0.5682417262808788783 ) ) ;
#13656=CARTESIAN_POINT ( 'NONE',  ( 0.2421733343592223919, -0.9179996579516339628, 0.6933330327357866141 ) ) ;
#13657=CARTESIAN_POINT ( 'NONE',  ( 0.01846853196186494517, -0.5817156171557603672, 0.5516149763055392397 ) ) ;
#13658=CARTESIAN_POINT ( 'NONE',  ( 0.4689754774150589056, -1.557726810111841775, 0.5609945539710509133 ) ) ;
#13659=CARTESIAN_POINT ( 'NONE',  ( 0.2713590513584660524, -1.676816687660336758, 0.7035140810151785384 ) ) ;
#13661=CARTESIAN_POINT ( 'NONE',  ( 0.2181072496379036219, -0.9917094513883838447, 0.5584457447843073075 ) ) ;
#13665=CARTESIAN_POINT ( 'NONE',  ( 0.1967274779738960033, -0.6939718894208231070, 0.6484394435625246977 ) ) ;
#13674=CARTESIAN_POINT ( 'NONE',  ( 0.3857344834571298509, -0.9392921734164567660, 0.7474990102649032853 ) ) ;
#13675=CARTESIAN_POINT ( 'NONE',  ( 0.4393445808683661413, -1.126265756603593182, 0.4785818640455667961 ) ) ;
#13676=CARTESIAN_POINT ( 'NONE',  ( 0.06846619564075531739, -1.327627092167478873, 0.5756175524039078839 ) ) ;
#13680=CARTESIAN_POINT ( 'NONE',  ( 0.3952148919761621637, -1.141712405902378435, 0.7491518327547966871 ) ) ;
#13681=CARTESIAN_POINT ( 'NONE',  ( 0.2683831008096893567, -1.674238039577110593, 0.5753345947181904840 ) ) ;
#13686=CARTESIAN_POINT ( 'NONE',  ( 0.09000415367089972807, -0.5660392021805559226, 0.1654146037094502697 ) ) ;
#13687=CARTESIAN_POINT ( 'NONE',  ( 0.7255201985491259720, -1.551814629293185366, 0.5182417262812423209 ) ) ;
#13688=CARTESIAN_POINT ( 'NONE',  ( 0.4233039937489216364, -1.123485956316199186, 0.5460366295032810235 ) ) ;
#13689=CARTESIAN_POINT ( 'NONE',  ( 0.2388530902294009883, -1.245845591994676926, 0.7174669630728713887 ) ) ;
#13696=CARTESIAN_POINT ( 'NONE',  ( 0.4637507040111739087, -1.233505390051135242, 0.6717282244380275991 ) ) ;
#13698=CARTESIAN_POINT ( 'NONE',  ( 0.3116392842230071292, -1.763036623927723978, 0.5305946302528894432 ) ) ;
#13704=CARTESIAN_POINT ( 'NONE',  ( 0.04921512002571602068, -0.5620675706429341112, 0.2577714020897228786 ) ) ;
#13705=CARTESIAN_POINT ( 'NONE',  ( 0.08725757351828516972, -0.7039266628255411717, 0.02354379185445030359 ) ) ;
#13706=CARTESIAN_POINT ( 'NONE',  ( 0.2024211440586259347, -0.7203912786704501636, 0.3419443000676659628 ) ) ;
#13708=ORIENTED_EDGE ( 'NONE', *, *, #6447, .F. ) ;
#13711=CARTESIAN_POINT ( 'NONE',  ( 0.1650742144947170698, -0.7251586625020333132, 0.5326188692438563743 ) ) ;
#13715=EDGE_CURVE ( 'NONE', #22890, #8281, #23337, .T. ) ;
#13718=CARTESIAN_POINT ( 'NONE',  ( 0.1991599691044491915, -1.252086681028342863, 0.4385478258677236729 ) ) ;
#13719=CARTESIAN_POINT ( 'NONE',  ( 0.4741105259895962432, -1.670573610379107787, 0.5762220851322598092 ) ) ;
#13721=CARTESIAN_POINT ( 'NONE',  ( 0.7435985525077578595, -1.513373960891965186, 0.6163350003740883931 ) ) ;
#13730=CARTESIAN_POINT ( 'NONE',  ( 0.1023011615166706662, -1.050388104772951969, 0.8771683563204210055 ) ) ;
#13734=DIRECTION ( 'NONE',  ( 0.9998941247116547304, -0.01455087607601020412, 0.0001066420868422379633 ) ) ;
#13741=ORIENTED_EDGE ( 'NONE', *, *, #5635, .T. ) ;
#13744=ADVANCED_FACE ( 'NONE', ( #1271 ), #29868, .T. ) ;
#13745=CARTESIAN_POINT ( 'NONE',  ( 0.5475879855805122487, -1.373140497242092195, 0.6594375008024977447 ) ) ;
#13747=ORIENTED_EDGE ( 'NONE', *, *, #31499, .F. ) ;
#13748=CARTESIAN_POINT ( 'NONE',  ( 0.3465599992496842807, -0.9476710551646405634, 0.6409924101657002993 ) ) ;
#13749=EDGE_CURVE ( 'NONE', #1246, #22420, #6016, .T. ) ;
#13751=VERTEX_POINT ( 'NONE', #4917 ) ;
#13754=CARTESIAN_POINT ( 'NONE',  ( 0.02432663359975386838, -0.5586419101762778450, 0.2615263354939962870 ) ) ;
#13756=CARTESIAN_POINT ( 'NONE',  ( 0.1124368596819388111, -0.7940650780295996913, -0.07060698127412667890 ) ) ;
#13758=EDGE_CURVE ( 'NONE', #20946, #13015, #18052, .T. ) ;
#13762=CARTESIAN_POINT ( 'NONE',  ( 0.2002687484916081118, -0.9229665737500837297, 0.3245110103503117682 ) ) ;
#13766=CARTESIAN_POINT ( 'NONE',  ( 0.2543894466873252158, -1.055563264917066091, 0.7376352696996288927 ) ) ;
#13767=CARTESIAN_POINT ( 'NONE',  ( 0.04703489300812706275, -0.8021760332774975355, 0.6694782157141636603 ) ) ;
#13777=CARTESIAN_POINT ( 'NONE',  ( 0.02521977883247775859, -1.088411770194798178, 0.6474433479578449724 ) ) ;
#13778=CARTESIAN_POINT ( 'NONE',  ( 0.1774972420046788679, -0.4900154790703133423, 0.1409049844863272671 ) ) ;
#13782=CARTESIAN_POINT ( 'NONE',  ( 0.3918182118607624331, -1.107073211027153725, 0.6042946153017959565 ) ) ;
#13786=CARTESIAN_POINT ( 'NONE',  ( 0.1778984696810832766, -0.5443775716742050852, 0.2437360553562945842 ) ) ;
#13788=CARTESIAN_POINT ( 'NONE',  ( 0.2592175946368545092, -1.678678769766079881, 0.5610528864763278944 ) ) ;
#13790=CARTESIAN_POINT ( 'NONE',  ( 0.5409705397755507628, -1.398922715619407064, 0.7775598356702776437 ) ) ;
#13792=ORIENTED_EDGE ( 'NONE', *, *, #14959, .T. ) ;
#13794=VERTEX_POINT ( 'NONE', #31258 ) ;
#13796=CARTESIAN_POINT ( 'NONE',  ( 0.4790210037517146358, -1.178264979292966252, 0.8995276976856623197 ) ) ;
#13797=( BOUNDED_SURFACE ( )  B_SPLINE_SURFACE ( 3, 2, ( 
 ( #8046, #24518, #18334 ),
 ( #8652, #5573, #2090 ),
 ( #36233, #8869, #24128 ),
 ( #20622, #39937, #27411 ),
 ( #36650, #8454, #14418 ),
 ( #11954, #33158, #18133 ),
 ( #33542, #36446, #21223 ),
 ( #5352, #2697, #2507 ),
 ( #21447, #15047, #33974 ),
 ( #15245, #32439, #4262 ) ),
 .UNSPECIFIED., .F., .F., .T. ) 
 B_SPLINE_SURFACE_WITH_KNOTS ( ( 4, 2, 2, 2, 4 ),
 ( 3, 3 ),
 ( 0.0007861888542779920438, 0.001094194827383940163, 0.001402200800489888498, 0.001710206773595836617, 0.002018212746701784736 ),
 ( 0.000000000000000000, 0.6753453643475422208 ),
 .UNSPECIFIED. ) 
 GEOMETRIC_REPRESENTATION_ITEM ( )  RATIONAL_B_SPLINE_SURFACE ( (
 ( 1.000000000000000000, 0.7938099847028182721, 0.8661189114170375625),
 ( 1.000000000000000000, 0.8158720960386478538, 0.8804440448519528228),
 ( 1.000000000000000000, 0.8317178396726564449, 0.8907328331042354552),
 ( 1.000000000000000000, 0.8529323147884961820, 0.9045075884828177593),
 ( 1.000000000000000000, 0.8583035682245675480, 0.9079951931373873020),
 ( 1.000000000000000000, 0.8588125958609250654, 0.9083257095010246474),
 ( 1.000000000000000000, 0.8539403388225746960, 0.9051621078338429882),
 ( 1.000000000000000000, 0.8338631590414414818, 0.8921258088602976866),
 ( 1.000000000000000000, 0.8186530614390943317, 0.8822497514696410192),
 ( 1.000000000000000000, 0.7974297740311802052, 0.8684692741881134825) ) ) 
 REPRESENTATION_ITEM ( '' )  SURFACE ( )  );
#13805=ORIENTED_EDGE ( 'NONE', *, *, #12734, .F. ) ;
#13807=CARTESIAN_POINT ( 'NONE',  ( 0.1487996072293812644, -0.8705227087253726292, 0.5144977190368104081 ) ) ;
#13808=CARTESIAN_POINT ( 'NONE',  ( 0.09004308680322813119, -0.5453319202395334742, 0.1700947645392699159 ) ) ;
#13809=CARTESIAN_POINT ( 'NONE',  ( 0.4164415605102140816, -1.305827022127384884, 0.8402016264797032008 ) ) ;
#13810=CARTESIAN_POINT ( 'NONE',  ( 0.06579623839312427613, -1.299927852201166356, 0.6199554873623526197 ) ) ;
#13812=CARTESIAN_POINT ( 'NONE',  ( 0.6933406572447815552, -1.440653850451423468, 0.5079424769205712620 ) ) ;
#13814=B_SPLINE_CURVE_WITH_KNOTS ( 'NONE', 3,
 ( #9328, #25182, #30745, #34224, #14912, #37124, #27468, #6036, #21907, #18195, #37725, #18603, #34434, #15100, #6252, #31162 ),
 .UNSPECIFIED., .F., .F.,
 ( 4, 2, 2, 2, 2, 2, 2, 4 ),
 ( 0.001520026421036642893, 0.002129310495689869936, 0.002738594570343096547, 0.003347878644996323157, 0.003957162719649550200, 0.004566446794302777244, 0.005175730868956004288, 0.006394299018262457508 ),
 .UNSPECIFIED. ) ;
#13815=CARTESIAN_POINT ( 'NONE',  ( 0.7430335777066456870, -1.516427533338710276, 0.5621624951216923627 ) ) ;
#13816=CARTESIAN_POINT ( 'NONE',  ( 0.06581764578086071737, -1.340728352476673546, 0.5449258910593480776 ) ) ;
#13820=CARTESIAN_POINT ( 'NONE',  ( -0.0002679541628580975484, -0.8872122825745146768, -0.004047411357262368885 ) ) ;
#13821=CARTESIAN_POINT ( 'NONE',  ( 0.5721826821263369389, -1.458777054030341747, 0.7189295076877989521 ) ) ;
#13824=CARTESIAN_POINT ( 'NONE',  ( 0.002166586416275674380, -0.8510908774931603693, 0.4206164911499951642 ) ) ;
#13825=CARTESIAN_POINT ( 'NONE',  ( 0.4927016384402401195, -1.082581181811578697, 0.5750743434332348247 ) ) ;
#13827=CARTESIAN_POINT ( 'NONE',  ( 0.5337404313129848754, -1.165174529015815530, 0.8761190665599410954 ) ) ;
#13829=CARTESIAN_POINT ( 'NONE',  ( 0.3165154177081624387, -1.761756825665560022, 0.5689576620947197627 ) ) ;
#13832=CARTESIAN_POINT ( 'NONE',  ( 0.01055999354154677286, -0.5296565605740106708, 0.1345257393686825065 ) ) ;
#13834=CARTESIAN_POINT ( 'NONE',  ( 0.1251292443316412706, -1.283366339454344196, 0.4333571588881200976 ) ) ;
#13837=CARTESIAN_POINT ( 'NONE',  ( 0.5104750172518451867, -1.131314744720151477, 0.8088526445616294192 ) ) ;
#13839=VERTEX_POINT ( 'NONE', #9037 ) ;
#13848=CARTESIAN_POINT ( 'NONE',  ( 0.08904301877626455419, -0.6451442797342821223, 0.1752162043042217454 ) ) ;
#13849=CARTESIAN_POINT ( 'NONE',  ( 0.2340814018463421020, -1.370659533647821116, 1.031107782677665119 ) ) ;
#13850=CARTESIAN_POINT ( 'NONE',  ( 0.08527833055735040135, -0.5435345793325218056, 0.1626648481634892229 ) ) ;
#13851=CARTESIAN_POINT ( 'NONE',  ( 0.2421782067677001327, -1.538462374013507494, 0.9033803661575985355 ) ) ;
#13853=CARTESIAN_POINT ( 'NONE',  ( 0.3600618142828818646, -1.126602618899190666, 0.6272543034982291932 ) ) ;
#13857=CARTESIAN_POINT ( 'NONE',  ( 0.2438833895742764379, -0.7102944716943135894, 0.5217179281748908215 ) ) ;
#13861=CARTESIAN_POINT ( 'NONE',  ( 0.001520397658112405872, -0.4673780482903918676, 0.1457185332388684362 ) ) ;
#13862=DIRECTION ( 'NONE',  ( 0.8660512985181134660, 0.4999551463232371207, 0.000000000000000000 ) ) ;
#13863=CARTESIAN_POINT ( 'NONE',  ( 0.6177995476601370051, -1.296677486146512681, 0.6035100636680229558 ) ) ;
#13865=CARTESIAN_POINT ( 'NONE',  ( 0.006138594813777389046, -0.8471251931369432331, 0.2368169677984677812 ) ) ;
#13870=CARTESIAN_POINT ( 'NONE',  ( 0.3974715091898353148, -1.183013071782477610, 0.7014967152191310396 ) ) ;
#13873=ORIENTED_EDGE ( 'NONE', *, *, #16230, .T. ) ;
#13874=CARTESIAN_POINT ( 'NONE',  ( 0.5370561722153690543, -1.157568837174978160, 0.6041238513417164224 ) ) ;
#13875=CARTESIAN_POINT ( 'NONE',  ( 0.08989780363036058153, -0.5646359461869331353, 0.1460065308160271857 ) ) ;
#13880=CARTESIAN_POINT ( 'NONE',  ( 0.08519453467371698729, -0.8897552423473668037, 0.5328790022427215556 ) ) ;
#13881=EDGE_LOOP ( 'NONE', ( #33399, #9327, #27667, #15318 ) ) ;
#13888=CARTESIAN_POINT ( 'NONE',  ( 0.4400018551782722831, -1.199590102754184429, 0.6918963007991280056 ) ) ;
#13891=CARTESIAN_POINT ( 'NONE',  ( 0.5680530317233595250, -1.627115649102798045, 0.5337353644224959170 ) ) ;
#13898=CARTESIAN_POINT ( 'NONE',  ( 0.05234297472369140586, -0.5872343478182446841, 0.3233092731135888132 ) ) ;
#13899=CARTESIAN_POINT ( 'NONE',  ( 0.08897024507276897476, -0.5939270582310836044, 0.06544685392209818875 ) ) ;
#13905=CARTESIAN_POINT ( 'NONE',  ( 0.5747667309145861880, -1.499072180388674180, 0.5927272562183352189 ) ) ;
#13910=CARTESIAN_POINT ( 'NONE',  ( 0.6011193747858255554, -1.595581932925110857, 0.4276689662439312478 ) ) ;
#13911=CARTESIAN_POINT ( 'NONE',  ( 0.08570207522761710828, -1.306251794185867565, 0.4630506868879065152 ) ) ;
#13913=CARTESIAN_POINT ( 'NONE',  ( 0.08964573052713356582, -0.6030796524031889483, 0.1052737554848243579 ) ) ;
#13915=ADVANCED_FACE ( 'NONE', ( #17871 ), #8830, .T. ) ;
#13916=CARTESIAN_POINT ( 'NONE',  ( 0.3279357908889724005, -0.8116789304350262579, 0.7312476538325396458 ) ) ;
#13921=ADVANCED_FACE ( 'NONE', ( #33715 ), #30396, .T. ) ;
#13923=EDGE_CURVE ( 'NONE', #6325, #9452, #35455, .T. ) ;
#13926=CARTESIAN_POINT ( 'NONE',  ( 0.2261350199769993075, -1.351787128704465824, 0.4952186049488564445 ) ) ;
#13930=CARTESIAN_POINT ( 'NONE',  ( 0.1016012100809402935, -1.316932346213368854, 0.4414107644021351140 ) ) ;
#13933=CARTESIAN_POINT ( 'NONE',  ( 0.003124719664520466192, -0.5686731593868933343, 0.09441483597926585147 ) ) ;
#13937=CARTESIAN_POINT ( 'NONE',  ( 0.5943325146468168008, -1.599629339932625571, 0.4280854842635419266 ) ) ;
#13939=B_SPLINE_CURVE_WITH_KNOTS ( 'NONE', 3,
 ( #22832, #38222, #19324, #35534, #37834, #12946, #12727, #452, #32061, #25495, #6540, #35351, #19116, #22217 ),
 .UNSPECIFIED., .F., .F.,
 ( 4, 2, 2, 2, 2, 2, 4 ),
 ( 0.000000000000000000, 2.630382555147416532E-05, 5.260765110294833064E-05, 0.0001052153022059013369, 0.0002104306044118009933, 0.0004208612088236007398, 0.0008417224176471900954 ),
 .UNSPECIFIED. ) ;
#13941=ORIENTED_EDGE ( 'NONE', *, *, #36386, .T. ) ;
#13942=CARTESIAN_POINT ( 'NONE',  ( 0.1051168147106792405, -1.410983822109892261, 0.5678361409211155619 ) ) ;
#13943=EDGE_CURVE ( 'NONE', #13132, #19301, #16739, .T. ) ;
#13948=CARTESIAN_POINT ( 'NONE',  ( 0.4421893865606449370, -1.209647901485848109, 0.7918999424850913238 ) ) ;
#13951=CARTESIAN_POINT ( 'NONE',  ( 0.2017226021742919428, -0.8083333955854449249, 0.3447374551949819454 ) ) ;
#13955=CARTESIAN_POINT ( 'NONE',  ( 0.3285372126246737245, -1.620950097204016283, 0.7294768256710487675 ) ) ;
#13956=CARTESIAN_POINT ( 'NONE',  ( 0.6870256655133099022, -1.509029865219357003, 0.4581990961816077568 ) ) ;
#13958=CARTESIAN_POINT ( 'NONE',  ( 0.1581650021276240492, -1.285700486175305413, 0.4282417262808778102 ) ) ;
#13959=VECTOR ( 'NONE', #37050, 39.37007874015748854 ) ;
#13961=ORIENTED_EDGE ( 'NONE', *, *, #34775, .T. ) ;
#13966=CIRCLE ( 'NONE', #30426, 0.04749999999977543713 ) ;
#13967=CARTESIAN_POINT ( 'NONE',  ( 0.3513474575719932047, -1.212688753581547152, 0.6982256170334331102 ) ) ;
#13976=CARTESIAN_POINT ( 'NONE',  ( 0.1876095839365586326, -1.270310460104812966, 0.4182417262808778013 ) ) ;
#13978=CARTESIAN_POINT ( 'NONE',  ( 0.3619206956467402869, -1.158069748661290310, 0.4377863372772762829 ) ) ;
#13981=CARTESIAN_POINT ( 'NONE',  ( 0.7089445223657345752, -1.512404601863501119, 0.5481705145598362305 ) ) ;
#13986=CARTESIAN_POINT ( 'NONE',  ( 0.1975154665785900376, -1.291488013533474755, 1.023236177360688393 ) ) ;
#13993=CARTESIAN_POINT ( 'NONE',  ( 0.1912095264562755359, -0.5378710435959832559, 0.2569485330840456383 ) ) ;
#13997=CARTESIAN_POINT ( 'NONE',  ( 0.6017699220438542662, -1.483087398378163613, 0.5690941353624772159 ) ) ;
#13998=CARTESIAN_POINT ( 'NONE',  ( -0.001435095205611100358, -0.8221821212370526988, 0.04482441723982503318 ) ) ;
#14002=ORIENTED_EDGE ( 'NONE', *, *, #23769, .T. ) ;
#14003=CARTESIAN_POINT ( 'NONE',  ( 0.5780995139542189909, -1.354416361880780073, 0.8813196190093472993 ) ) ;
#14005=CARTESIAN_POINT ( 'NONE',  ( 0.2226433022657542116, -1.491184131797351764, 0.9185802828613613968 ) ) ;
#14013=CARTESIAN_POINT ( 'NONE',  ( 0.1246135125235463964, -0.8485378787666528755, 0.4456728382190667248 ) ) ;
#14014=CARTESIAN_POINT ( 'NONE',  ( 0.03641803280491349298, -0.9675207775044110114, 0.6564218488141688734 ) ) ;
#14015=CARTESIAN_POINT ( 'NONE',  ( 0.1040734670749448865, -0.6192425880305225672, 0.3761511251374745068 ) ) ;
#14016=CARTESIAN_POINT ( 'NONE',  ( 0.5527105129315168508, -1.511112255258006076, 0.5682628627402200872 ) ) ;
#14017=CARTESIAN_POINT ( 'NONE',  ( 0.1867173357226489527, -0.5319602528017867149, 0.2749521773151894499 ) ) ;
#14019=CARTESIAN_POINT ( 'NONE',  ( 0.6350649561464823956, -1.569019770697453353, 0.4218989278589421743 ) ) ;
#14021=CARTESIAN_POINT ( 'NONE',  ( 0.3344130170398624813, -1.762663979654706781, 0.5617402743204308324 ) ) ;
#14023=CARTESIAN_POINT ( 'NONE',  ( 0.07014435923142074703, -1.325199841737238593, 0.5075297796643147841 ) ) ;
#14028=CARTESIAN_POINT ( 'NONE',  ( 8.553562515601560484E-05, -0.6062534121257077135, -0.09029379233708857699 ) ) ;
#14029=CARTESIAN_POINT ( 'NONE',  ( 0.5701105534977165545, -1.454650725906061481, 0.7252577283312120482 ) ) ;
#14031=EDGE_CURVE ( 'NONE', #40356, #38394, #35118, .T. ) ;
#14032=CARTESIAN_POINT ( 'NONE',  ( 0.008070443708631632601, -0.7078080424802363213, -0.01128278948062920277 ) ) ;
#14034=CARTESIAN_POINT ( 'NONE',  ( 0.04376425988958544677, -0.9339557565548041174, 0.7112009851976159869 ) ) ;
#14036=CARTESIAN_POINT ( 'NONE',  ( 0.3793958449840821867, -1.004087596663555848, 0.6383754926613092184 ) ) ;
#14038=CARTESIAN_POINT ( 'NONE',  ( 0.5117021325268811260, -1.128961434293810129, 0.8718124831259003171 ) ) ;
#14041=CARTESIAN_POINT ( 'NONE',  ( 0.3047912954742191260, -1.756872613064056399, 0.5682345314727886842 ) ) ;
#14043=ORIENTED_EDGE ( 'NONE', *, *, #24114, .F. ) ;
#14045=CARTESIAN_POINT ( 'NONE',  ( 0.002296835029420976181, -0.5198933010532034160, 0.1394354128953856353 ) ) ;
#14049=CARTESIAN_POINT ( 'NONE',  ( 0.2196843594954665801, -1.228680355308193084, 0.4993826538774071566 ) ) ;
#14050=ORIENTED_EDGE ( 'NONE', *, *, #30892, .T. ) ;
#14053=CARTESIAN_POINT ( 'NONE',  ( 0.3628146410451159598, -0.9034970372909253422, 0.7254628211502860413 ) ) ;
#14058=ORIENTED_EDGE ( 'NONE', *, *, #7465, .T. ) ;
#14062=CARTESIAN_POINT ( 'NONE',  ( 0.4422962341139744513, -1.227940648741109531, 0.5902935990525034482 ) ) ;
#14065=CARTESIAN_POINT ( 'NONE',  ( 0.1766140053765036799, -0.4884607529735562892, 0.1457336358543773192 ) ) ;
#14066=CARTESIAN_POINT ( 'NONE',  ( 0.09293816641532150202, -0.6949693946930408650, 0.2718681940744577252 ) ) ;
#14068=CARTESIAN_POINT ( 'NONE',  ( 0.1805964634074843922, -1.181094138890736334, 1.011330471386135743 ) ) ;
#14069=CARTESIAN_POINT ( 'NONE',  ( 0.4706205245075478771, -1.558028661862049136, 0.5883446331395899564 ) ) ;
#14071=CARTESIAN_POINT ( 'NONE',  ( 0.2705891343394069004, -1.683541877783801377, 0.6654023006082908642 ) ) ;
#14072=CARTESIAN_POINT ( 'NONE',  ( 0.3182330667144250280, -1.645712786916206927, 0.6043827481625060338 ) ) ;
#14073=CARTESIAN_POINT ( 'NONE',  ( 0.04894342265781252005, -0.9443920355984648518, 0.2726795326779477557 ) ) ;
#14074=ORIENTED_EDGE ( 'NONE', *, *, #9504, .F. ) ;
#14076=CARTESIAN_POINT ( 'NONE',  ( 0.1220876931611632188, -0.4987358795490002272, 0.3421387242878536905 ) ) ;
#14080=EDGE_CURVE ( 'NONE', #24800, #13526, #20806, .T. ) ;
#14083=CARTESIAN_POINT ( 'NONE',  ( 0.3991878447057942703, -0.9797369418029474586, 0.7176166460480870590 ) ) ;
#14084=AXIS2_PLACEMENT_3D ( 'NONE', #15617, #21179, #24470 ) ;
#14096=CARTESIAN_POINT ( 'NONE',  ( 0.5209244318938980323, -1.136454935809554589, 0.6601900591555691644 ) ) ;
#14098=B_SPLINE_CURVE_WITH_KNOTS ( 'NONE', 3,
 ( #25743, #16680, #3916, #29231, #38680, #10497, #35801, #19759, #10319, #16890 ),
 .UNSPECIFIED., .F., .F.,
 ( 4, 2, 2, 2, 4 ),
 ( 0.005469996267440097384, 0.006262957826661069011, 0.007055919385882040637, 0.007848880945103012263, 0.008641842504323983890 ),
 .UNSPECIFIED. ) ;
#14100=CARTESIAN_POINT ( 'NONE',  ( 0.2111199334379703363, -1.188696133188541282, 0.7441100336498001067 ) ) ;
#14107=CARTESIAN_POINT ( 'NONE',  ( 0.4674780132050370685, -1.240604882716528357, 0.6861010688927965395 ) ) ;
#14110=DIRECTION ( 'NONE',  ( 0.8660512985181133550, 0.4999551463232373982, 0.000000000000000000 ) ) ;
#14117=CARTESIAN_POINT ( 'NONE',  ( 0.1888324354095312907, -0.6407273034312881421, -0.03797464539687132185 ) ) ;
#14119=CARTESIAN_POINT ( 'NONE',  ( 0.1449436508646830823, -0.9125365724582368276, 0.7473170813620255704 ) ) ;
#14120=CARTESIAN_POINT ( 'NONE',  ( 0.08986786782462405365, -0.5434483850344659084, 0.1394973511444336789 ) ) ;
#14126=CARTESIAN_POINT ( 'NONE',  ( 0.5618860505435292474, -1.504674554817216903, 0.5302722728681629194 ) ) ;
#14127=CARTESIAN_POINT ( 'NONE',  ( 0.5739910737716292788, -1.499268627441381563, 0.5745547377076620776 ) ) ;
#14132=CARTESIAN_POINT ( 'NONE',  ( 0.6474224700345215799, -1.554264730535300343, 0.4226295179704261384 ) ) ;
#14133=CARTESIAN_POINT ( 'NONE',  ( 0.1619861451291866039, -1.262021649189480010, 0.4327121414366898455 ) ) ;
#14136=CARTESIAN_POINT ( 'NONE',  ( 0.1983812210006687116, -0.5262237738225362671, 0.3723155052761787376 ) ) ;
#14146=CARTESIAN_POINT ( 'NONE',  ( 0.02434420200121316033, -0.6484821100597173427, 0.5849520929678148073 ) ) ;
#14150=CARTESIAN_POINT ( 'NONE',  ( 0.7022701326239239039, -1.539209993927390219, 0.4224083929475443977 ) ) ;
#14153=ORIENTED_EDGE ( 'NONE', *, *, #7231, .T. ) ;
#14154=FACE_OUTER_BOUND ( 'NONE', #3278, .T. ) ;
#14155=CARTESIAN_POINT ( 'NONE',  ( 0.2320755761173002307, -1.232873731908348480, 0.4177417262808779674 ) ) ;
#14156=ORIENTED_EDGE ( 'NONE', *, *, #26089, .F. ) ;
#14159=CARTESIAN_POINT ( 'NONE',  ( 0.5380345666174809471, -1.356870216577685140, 0.6895596520374281946 ) ) ;
#14161=ORIENTED_EDGE ( 'NONE', *, *, #37142, .F. ) ;
#14162=CARTESIAN_POINT ( 'NONE',  ( 0.5135987199389938640, -1.118799288056715691, 0.5631670202300380623 ) ) ;
#14168=CARTESIAN_POINT ( 'NONE',  ( 0.3268949200113892006, -1.639137555909581323, 0.5723008474438366910 ) ) ;
#14169=CARTESIAN_POINT ( 'NONE',  ( 0.7064611863037917328, -1.500587082211219503, 0.5320914120227480115 ) ) ;
#14171=FACE_OUTER_BOUND ( 'NONE', #34245, .T. ) ;
#14181=CARTESIAN_POINT ( 'NONE',  ( 0.2434700144512876308, -1.137288946556442637, 0.7468722051079026425 ) ) ;
#14184=FACE_OUTER_BOUND ( 'NONE', #27515, .T. ) ;
#14189=CARTESIAN_POINT ( 'NONE',  ( 0.3967966609207765338, -1.138601119762225222, 0.4806637341673061226 ) ) ;
#14193=CARTESIAN_POINT ( 'NONE',  ( 0.4023555552517616429, -1.144080005235271980, 0.4308225822695866958 ) ) ;
#14195=DIRECTION ( 'NONE',  ( -0.8660512985181119117, -0.4999551463232398962, 0.000000000000000000 ) ) ;
#14197=CARTESIAN_POINT ( 'NONE',  ( 0.4366310749037827232, -1.106409655742623732, 0.5865638872146798910 ) ) ;
#14198=CARTESIAN_POINT ( 'NONE',  ( 0.1460529063005417405, -1.108260578017826958, 0.9816109277214414286 ) ) ;
#14202=ORIENTED_EDGE ( 'NONE', *, *, #27413, .T. ) ;
#14203=CARTESIAN_POINT ( 'NONE',  ( 0.1846896762568759620, -0.5250301188136093922, 0.2658526725181787898 ) ) ;
#14204=ORIENTED_EDGE ( 'NONE', *, *, #25766, .F. ) ;
#14207=CARTESIAN_POINT ( 'NONE',  ( 0.1346587401131250639, -0.5534557573801949237, 0.1697811908328959729 ) ) ;
#14208=CARTESIAN_POINT ( 'NONE',  ( 0.007458128862430835580, -0.7676047858832847348, 0.009162072377978345075 ) ) ;
#14213=CARTESIAN_POINT ( 'NONE',  ( 0.3331429932986941789, -1.175170333239869080, 0.4490264977604416230 ) ) ;
#14214=ADVANCED_FACE ( 'NONE', ( #35701 ), #25450, .T. ) ;
#14215=CARTESIAN_POINT ( 'NONE',  ( -0.01398755374478911906, -0.5253281656772126329, 0.1551995070683278577 ) ) ;
#14217=CARTESIAN_POINT ( 'NONE',  ( 0.1497796767655423800, -1.269200906667645068, 0.6056742027281973861 ) ) ;
#14222=ORIENTED_EDGE ( 'NONE', *, *, #28342, .T. ) ;
#14225=CARTESIAN_POINT ( 'NONE',  ( 0.08940417447797945061, -0.7934870992831885017, 0.2534929935647216026 ) ) ;
#14227=CARTESIAN_POINT ( 'NONE',  ( 0.1561519734742241317, -0.7461896296692774877, 0.5632227496451408522 ) ) ;
#14228=CARTESIAN_POINT ( 'NONE',  ( 0.5229475576413166182, -1.460849917182648117, 0.7558602880573046523 ) ) ;
#14229=CARTESIAN_POINT ( 'NONE',  ( 0.04419567591603339174, -1.150503204610852759, 0.6622665436056601740 ) ) ;
#14231=CARTESIAN_POINT ( 'NONE',  ( 0.6214871112804610798, -1.581993459657260459, 0.4227591190029512114 ) ) ;
#14238=CARTESIAN_POINT ( 'NONE',  ( 0.01137246303666041881, -0.9338259276304594625, 0.06621170400641679388 ) ) ;
#14242=CARTESIAN_POINT ( 'NONE',  ( 0.006548395810636918092, -0.8294761337169994642, 0.07557146525729462050 ) ) ;
#14244=CARTESIAN_POINT ( 'NONE',  ( 0.01517484414490882783, -0.7999702980829028753, 0.5364596547344525623 ) ) ;
#14245=CARTESIAN_POINT ( 'NONE',  ( 0.3394669778924194747, -0.9758008820872865474, 0.6115353432225060226 ) ) ;
#14247=CARTESIAN_POINT ( 'NONE',  ( 0.6952872927582756102, -1.427253715223001374, 0.8000406204621429707 ) ) ;
#14250=CARTESIAN_POINT ( 'NONE',  ( 0.3084692838263019543, -1.760909596431265323, 0.5689466516523863371 ) ) ;
#14253=CARTESIAN_POINT ( 'NONE',  ( 0.004762859065977665535, -0.5845126036323667895, 0.3389153922995538082 ) ) ;
#14259=CARTESIAN_POINT ( 'NONE',  ( 0.6159793682513172719, -1.299209393623256492, 0.5257027981018284057 ) ) ;
#14269=ORIENTED_EDGE ( 'NONE', *, *, #37185, .T. ) ;
#14270=CARTESIAN_POINT ( 'NONE',  ( 0.2014751060404549599, -1.236718649590243357, 0.5759633585842109937 ) ) ;
#14271=CARTESIAN_POINT ( 'NONE',  ( 0.09052338057520342707, -0.6901709929874992877, 0.2401866993428223851 ) ) ;
#14272=CARTESIAN_POINT ( 'NONE',  ( 0.2422216273152858479, -1.437769439691266360, 1.028655097037083799 ) ) ;
#14273=CARTESIAN_POINT ( 'NONE',  ( 0.09832713360691919258, -0.5593462231477130953, 0.2221295432580932538 ) ) ;
#14274=CARTESIAN_POINT ( 'NONE',  ( 0.2546023288931325013, -1.584778239651395859, 0.8703522911872779710 ) ) ;
#14276=CARTESIAN_POINT ( 'NONE',  ( 0.1143170209530945808, -0.9583121728649094395, 0.4320137086143686633 ) ) ;
#14277=EDGE_LOOP ( 'NONE', ( #6919, #22576, #5759, #38904, #13560 ) ) ;
#14281=CARTESIAN_POINT ( 'NONE',  ( 0.2124872757274005319, -0.6329494883420956342, 0.4106774159388293377 ) ) ;
#14283=EDGE_CURVE ( 'NONE', #13526, #799, #31222, .T. ) ;
#14285=EDGE_CURVE ( 'NONE', #1740, #15439, #7897, .T. ) ;
#14286=CARTESIAN_POINT ( 'NONE',  ( 0.07244838799016078967, -1.323543130859661465, 0.4946272753632746655 ) ) ;
#14290=CARTESIAN_POINT ( 'NONE',  ( 0.5591717342432651616, -1.201875270489466407, 0.7301083282254506868 ) ) ;
#14291=B_SPLINE_SURFACE_WITH_KNOTS ( 'NONE', 3, 3, ( 
 ( #27477, #21522, #2777, #24385, #36920, #27882, #8734, #5653, #30756, #12247, #24807, #37327, #9137, #1320, #17127, #4976, #29677, #14247, #1519, #5365, #30089, #39744, #11578, #26612, #29476, #39148, #1731, #8272, #38929, #7668, #14432, #36460, #29891, #13827, #39527, #14038, #5173, #8468, #26810, #36243, #35854, #2103, #26397, #24140, #1917, #26999, #14640, #7850, #10759, #23331, #21032, #39338, #33555, #11360, #20234, #36051, #11159, #32754, #20636, #8058, #33171, #4558, #23716, #10975, #23533, #20422, #32956, #4761, #17333, #27211, #17543, #23929, #20845, #33365, #17725, #30274, #36662, #31099 ),
 ( #15663, #10048, #18544, #34173, #39946, #31313, #27814, #34380, #24323, #40138, #24532, #11967, #18345, #22620, #33776, #30699, #40555, #24740, #12572, #35153, #38220, #24931, #17930, #28212, #30491, #2919, #5981, #11766, #40349, #5585, #18144, #5788, #15471, #2520, #25689, #2319, #14860, #15059, #21458, #37061, #28023, #2711, #8882, #33983, #30890, #12375, #27609, #37459, #78, #9276, #15255, #21649, #27423, #21852, #36851, #6196, #18764, #8664, #3122, #21239, #12178, #37267, #9083, #13456, #4567, #13645, #26022, #38332, #26411, #3973, #7862, #38542, #4180, #20041, #32970, #35447, #10557, #20433 ),
 ( #26632, #16944, #16339, #10369, #38733, #13243, #16749, #28878, #16536, #736, #10989, #25810, #7248, #22733, #29296, #10164, #35262, #19823, #1144, #7461, #22931, #32356, #29077, #26210, #19629, #38944, #23133, #39160, #17139, #7061, #23546, #23346, #35868, #35659, #13837, #32571, #4388, #29486, #7681, #32164, #36063, #944, #1330, #20246, #10773, #32765, #29691, #1533, #14053, #15070, #11591, #4991, #27623, #11780, #24336, #8289, #2335, #17740, #39761, #21044, #36865, #17348, #24548, #29907, #36256, #8680, #23942, #39351, #20861, #2122, #39959, #40152, #24153, #17558, #18156, #14656, #21255, #11172 ),
 ( #2532, #14259, #36677, #1748, #33382, #30290, #37077, #33792, #17946, #8483, #11982, #5599, #23729, #5185, #20648, #30710, #27225, #8074, #8897, #21469, #30100, #33571, #1931, #14445, #26824, #33187, #4774, #27013, #39540, #11374, #5384, #36476, #30504, #14874, #27435, #28981, #28040, #21869, #27827, #13353, #13566, #18564, #9506, #6974, #31118, #22085, #30903, #10285, #5997, #26133, #15677, #16437, #2932, #22851, #31332, #15489, #15273, #3884, #21659, #38647, #40568, #34397, #37685, #10466, #12387, #28223, #33993, #1057, #6211, #90, #7160, #32259, #5798, #34186, #35172, #24943, #18779, #37470 ),
 ( #4079, #9290, #18356, #3136, #12584, #25928, #2726, #12195, #19546, #845, #25146, #40366, #38451, #32078, #35370, #24754, #19727, #16646, #37276, #9093, #29195, #26314, #29403, #35768, #20762, #32469, #29801, #35559, #39056, #35975, #2028, #11278, #36165, #1643, #5091, #26921, #1247, #10887, #38840, #39451, #26520, #16860, #1841, #14557, #7579, #26732, #20153, #23241, #7356, #19934, #23845, #13748, #27125, #36367, #23457, #10669, #32681, #4487, #39261, #17459, #17050, #7781, #29593, #14357, #39655, #1437, #11084, #7975, #13951, #23645, #4294, #8188, #20350, #23033, #4678, #4892, #32870, #33284 ),
 ( #20549, #17250, #14162, #33082, #30008, #17651, #30197, #39868, #31231, #5896, #27339, #11689, #8386, #21761, #12094, #28139, #8578, #33911, #20954, #40052, #11492, #24243, #24057, #6100, #36583, #2439, #17847, #24444, #33476, #5282, #14976, #36976, #2631, #21155, #5496, #36766, #11875, #14777, #21570, #33684, #34295, #12301, #2237, #18668, #18457, #31010, #27530, #9008, #8796, #5708, #27726, #2831, #30406, #3048, #18063, #30614, #15382, #21374, #18266, #30810, #15167, #27938, #15592, #40261, #24660, #24859, #37191, #40478, #34093, #37379, #9192, #25251, #198, #25041, #37576, #3831, #6315, #4028 ),
 ( #6507, #413, #13098, #12690, #25657, #22796, #604, #12908, #3645, #35319, #16207, #9399, #38188, #28742, #16595, #13302, #7109, #16386, #19285, #25463, #4, #18888, #34702, #34504, #9612, #10014, #19078, #22377, #21975, #31425, #3228, #15777, #28324, #19676, #35112, #37793, #22187, #31617, #10227, #22586, #12484, #3433, #34900, #15991, #28537, #37995, #9805, #6711, #32212, #31826, #6918, #19492, #32023, #28927, #794, #25874, #38389, #20298, #38784, #23191, #1196, #29542, #32420, #39218, #10614, #11224, #29964, #19883, #23791, #36113, #7919, #32632, #26684, #1382, #23410, #4623, #20494, #1001 ) ),
 .UNSPECIFIED., .F., .F., .F.,
 ( 4, 1, 1, 1, 4 ),
 ( 4, 3, 1, 1, 1, 1, 1, 1, 1, 1, 1, 1, 1, 1, 1, 1, 1, 1, 1, 1, 1, 1, 1, 1, 1, 1, 1, 1, 1, 1, 1, 1, 1, 1, 1, 1, 1, 1, 1, 1, 1, 1, 1, 1, 1, 1, 1, 1, 1, 1, 1, 1, 1, 1, 1, 1, 1, 1, 1, 1, 1, 1, 1, 1, 1, 1, 1, 1, 1, 1, 1, 1, 1, 4 ),
 ( 0.000000000000000000, 0.2500000000000000000, 0.5000000000000000000, 0.7500000000000000000, 1.000000000000000000 ),
 ( -0.01000000000000000021, 0.000000000000000000, 0.002255859375000000052, 0.004511718750000000104, 0.006767578124999999722, 0.009023437500000000208, 0.01127929687499999896, 0.01353515624999999944, 0.01579101562499999820, 0.01804687500000000042, 0.02255859374999999792, 0.02707031249999999889, 0.03158203124999999639, 0.03609375000000000083, 0.04060546874999999833, 0.04511718749999999584, 0.04962890625000000028, 0.05414062499999999778, 0.05865234375000000222, 0.06316406249999999278, 0.06767578124999999722, 0.07218750000000000167, 0.07669921874999999223, 0.08121093749999999667, 0.09023437499999999167, 0.09925781250000000056, 0.1082812499999999956, 0.1173046875000000044, 0.1263281249999999856, 0.1353515624999999944, 0.1443750000000000033, 0.1533984374999999845, 0.1624218749999999933, 0.1714453125000000022, 0.1804687499999999833, 0.1894921874999999922, 0.1985156250000000011, 0.2075390624999999822, 0.2165624999999999911, 0.2346093750000000089, 0.2526562499999999711, 0.2707031249999999889, 0.2887500000000000067, 0.3067968749999999689, 0.3248437499999999867, 0.3428906250000000044, 0.3609374999999999667, 0.3789843749999999845, 0.3970312500000000022, 0.4150781249999999645, 0.4331249999999999822, 0.4511718750000000000, 0.4692187500000000178, 0.4872656250000000355, 0.5053124999999999423, 0.5414062499999999778, 0.5775000000000000133, 0.6303124999999999423, 0.6567187500000000178, 0.6831249999999999822, 0.7095312499999999467, 0.7359375000000000222, 0.7623437499999999867, 0.7887500000000000622, 0.8151562500000000266, 0.8415624999999999911, 0.8679687499999999556, 0.8943750000000001421, 0.9207812499999998845, 0.9471875000000000711, 0.9603906250000000533, 0.9735937500000000355, 0.9867968750000000178, 1.000000000000000000 ),
 .UNSPECIFIED. ) ;
#14292=( BOUNDED_SURFACE ( )  B_SPLINE_SURFACE ( 3, 2, ( 
 ( #31742, #28666, #6835 ),
 ( #6019, #19415, #31950 ),
 ( #18587, #110, #31144 ),
 ( #17689, #29639, #1480 ),
 ( #39913, #7627, #39706 ),
 ( #32916, #10934, #36209 ),
 ( #4726, #30054, #17296 ),
 ( #39107, #8021, #13998 ),
 ( #23290, #5326, #36421 ),
 ( #8433, #1690, #32719 ),
 ( #2285, #23683, #27389 ),
 ( #14208, #17091, #39303 ),
 ( #30235, #17888, #20194 ),
 ( #29850, #20598, #4526 ),
 ( #1884, #26776, #36013 ),
 ( #11124, #26570, #23497 ),
 ( #7818, #20389, #14823 ),
 ( #14395, #33130, #4939 ),
 ( #35813, #17505, #26960 ),
 ( #39493, #11322, #23892 ),
 ( #8232, #27173, #20810 ),
 ( #33328, #30455, #5135 ),
 ( #2066, #14601, #11539 ),
 ( #24104, #36629, #20997 ),
 ( #33518, #36811, #15434 ),
 ( #6158, #5755, #40313 ),
 ( #31278, #31469, #37022 ),
 ( #8625, #30854, #33734 ),
 ( #2881, #6365, #30664 ),
 ( #34344, #8845, #47 ),
 ( #15831, #15217, #24704 ),
 ( #15635, #40097, #15023 ),
 ( #18722, #27574, #11926 ),
 ( #24490, #21196, #22032 ) ),
 .UNSPECIFIED., .F., .F., .T. ) 
 B_SPLINE_SURFACE_WITH_KNOTS ( ( 4, 2, 2, 2, 2, 2, 2, 2, 2, 2, 2, 2, 2, 2, 2, 2, 4 ),
 ( 3, 3 ),
 ( 0.001355756759087015529, 0.002198797089660819298, 0.003041837420234622634, 0.003884877750808425970, 0.004727918081382229305, 0.005570958411956032641, 0.006413998742529836844, 0.007257039073103640180, 0.008100079403677443515, 0.008943119734251245984, 0.009786160064825050187, 0.01062920039539885439, 0.01147224072597265859, 0.01231528105654646280, 0.01315832138712026526, 0.01400136171769406773, 0.01484440204826787194 ),
 ( 0.000000000000000000, 1.000000000000000000 ),
 .UNSPECIFIED. ) 
 GEOMETRIC_REPRESENTATION_ITEM ( )  RATIONAL_B_SPLINE_SURFACE ( (
 ( 1.000000000000000000, 0.7632905047465364801, 1.000000000000000000),
 ( 1.000000000000000000, 0.7632367077656201371, 1.000000000000000000),
 ( 1.000000000000000000, 0.7632388388605254592, 1.000000000000000000),
 ( 1.000000000000000000, 0.7632991344096814457, 1.000000000000000000),
 ( 1.000000000000000000, 0.7633576247790648805, 1.000000000000000000),
 ( 1.000000000000000000, 0.7635011905928678067, 1.000000000000000000),
 ( 1.000000000000000000, 0.7635855781863163383, 1.000000000000000000),
 ( 1.000000000000000000, 0.7637789697554389079, 1.000000000000000000),
 ( 1.000000000000000000, 0.7638898926440848003, 1.000000000000000000),
 ( 1.000000000000000000, 0.7641372409602232851, 1.000000000000000000),
 ( 1.000000000000000000, 0.7642744383510835515, 1.000000000000000000),
 ( 1.000000000000000000, 0.7645793446138899885, 1.000000000000000000),
 ( 1.000000000000000000, 0.7647454238010300553, 1.000000000000000000),
 ( 1.000000000000000000, 0.7650925878231267241, 1.000000000000000000),
 ( 1.000000000000000000, 0.7652762098147284364, 1.000000000000000000),
 ( 1.000000000000000000, 0.7656549625587164565, 1.000000000000000000),
 ( 1.000000000000000000, 0.7658461486473470137, 1.000000000000000000),
 ( 1.000000000000000000, 0.7662298608678012046, 1.000000000000000000),
 ( 1.000000000000000000, 0.7664244233119626992, 1.000000000000000000),
 ( 1.000000000000000000, 0.7667980329912454929, 1.000000000000000000),
 ( 1.000000000000000000, 0.7669780830225270130, 1.000000000000000000),
 ( 1.000000000000000000, 0.7673223890870666253, 1.000000000000000000),
 ( 1.000000000000000000, 0.7674857715588927487, 1.000000000000000000),
 ( 1.000000000000000000, 0.7677804493114095408, 1.000000000000000000),
 ( 1.000000000000000000, 0.7679136995718428560, 1.000000000000000000),
 ( 1.000000000000000000, 0.7681530618753115158, 1.000000000000000000),
 ( 1.000000000000000000, 0.7682555419669827579, 1.000000000000000000),
 ( 1.000000000000000000, 0.7684354526188612589, 1.000000000000000000),
 ( 1.000000000000000000, 0.7685141687395736776, 1.000000000000000000),
 ( 1.000000000000000000, 0.7686421839867699779, 1.000000000000000000),
 ( 1.000000000000000000, 0.7686922298276939181, 1.000000000000000000),
 ( 1.000000000000000000, 0.7687384693205387975, 1.000000000000000000),
 ( 1.000000000000000000, 0.7687334298366129692, 1.000000000000000000),
 ( 1.000000000000000000, 0.7686749430622512591, 1.000000000000000000) ) ) 
 REPRESENTATION_ITEM ( '' )  SURFACE ( )  );
#14301=CARTESIAN_POINT ( 'NONE',  ( 0.3668321548077844163, -0.9575135872197984011, 0.6682895851757253425 ) ) ;
#14303=CARTESIAN_POINT ( 'NONE',  ( 0.06047107820563558944, -0.8445096946280080674, 0.3194460826658605535 ) ) ;
#14304=ORIENTED_EDGE ( 'NONE', *, *, #9504, .T. ) ;
#14309=CARTESIAN_POINT ( 'NONE',  ( 0.4691550673861196730, -1.240601932822466003, 0.5838046598153082689 ) ) ;
#14319=CARTESIAN_POINT ( 'NONE',  ( 0.1872963375802847441, -0.4547550531002670371, 0.1015045423513593059 ) ) ;
#14320=CARTESIAN_POINT ( 'NONE',  ( 0.06072818908143945427, -0.5500858300393093314, 0.2145042832497142393 ) ) ;
#14321=CARTESIAN_POINT ( 'NONE',  ( 0.08992183057946913360, -0.5436920459133731676, 0.1491868301061692603 ) ) ;
#14324=ORIENTED_EDGE ( 'NONE', *, *, #26089, .T. ) ;
#14326=CARTESIAN_POINT ( 'NONE',  ( 0.1260890751152980438, -0.6040517541015768543, 0.3288134516145302944 ) ) ;
#14331=CARTESIAN_POINT ( 'NONE',  ( 0.6047424516501676006, -1.591284807845871896, 0.4182417262808776903 ) ) ;
#14332=CARTESIAN_POINT ( 'NONE',  ( 0.09761789444427076967, -1.310832906678207399, 0.4542993516864344272 ) ) ;
#14334=CARTESIAN_POINT ( 'NONE',  ( 0.08905620747404956183, -0.5633431237458920160, 0.06417412856409884792 ) ) ;
#14335=CARTESIAN_POINT ( 'NONE',  ( 0.7203159877618242612, -1.479638488134456420, 0.5307775041526673343 ) ) ;
#14340=CARTESIAN_POINT ( 'NONE',  ( 0.6611009558453398993, -1.574486732712688353, 0.6100612929419876318 ) ) ;
#14342=FACE_OUTER_BOUND ( 'NONE', #8072, .T. ) ;
#14343=CARTESIAN_POINT ( 'NONE',  ( 0.003338613830247910610, -0.5117837562375455729, 0.3073580953312808339 ) ) ;
#14346=CARTESIAN_POINT ( 'NONE',  ( 0.4578876639573271623, -1.691832011784833334, 0.5885088351307257160 ) ) ;
#14354=CARTESIAN_POINT ( 'NONE',  ( 0.4603505868040601023, -1.234063264705831831, 0.7371433527421650256 ) ) ;
#14357=CARTESIAN_POINT ( 'NONE',  ( 0.2316395767834320274, -0.8375294501127626967, 0.4569101180231894821 ) ) ;
#14361=CARTESIAN_POINT ( 'NONE',  ( 0.3271890457909016336, -1.639240316579513301, 0.5762784469172572699 ) ) ;
#14362=CARTESIAN_POINT ( 'NONE',  ( 0.7083658949752495992, -1.503526964170632363, 0.5307393902334478497 ) ) ;
#14363=CARTESIAN_POINT ( 'NONE',  ( 0.1153056239832157825, -0.4463068649386734421, 0.1349004977409720973 ) ) ;
#14364=CARTESIAN_POINT ( 'NONE',  ( 0.4972671625857253974, -1.080199071502573771, 0.5707417262808780478 ) ) ;
#14370=CARTESIAN_POINT ( 'NONE',  ( 0.08122039712038266190, -0.8352997518968716673, 0.2480260592104332473 ) ) ;
#14373=CARTESIAN_POINT ( 'NONE',  ( 0.1458957113803953376, -0.9479994470368805493, 0.4102629441475512673 ) ) ;
#14376=CARTESIAN_POINT ( 'NONE',  ( 0.6584301050327935334, -1.489287037768582511, 0.4182417262808776903 ) ) ;
#14379=CARTESIAN_POINT ( 'NONE',  ( 0.01941756462488182511, -1.054556591395360732, 0.6186745803816108280 ) ) ;
#14384=CARTESIAN_POINT ( 'NONE',  ( 1.413395339180376537E-05, -0.4273865596755438423, 0.1159049528290725523 ) ) ;
#14386=CARTESIAN_POINT ( 'NONE',  ( 0.3182145041783619455, -1.756683996043875817, 0.4922019062452683835 ) ) ;
#14390=CARTESIAN_POINT ( 'NONE',  ( 0.1869361049589261248, -0.5056481182092611437, 0.1703966547429595357 ) ) ;
#14395=CARTESIAN_POINT ( 'NONE',  ( 0.008358225017219852657, -0.6771875044183260917, -0.01225903253533247063 ) ) ;
#14399=CARTESIAN_POINT ( 'NONE',  ( 0.3191007316647460068, -1.183265676571765068, 0.4690969661098124965 ) ) ;
#14402=CARTESIAN_POINT ( 'NONE',  ( 0.2421644059368991964, -1.556966573662585729, 0.8831382204369367939 ) ) ;
#14404=CARTESIAN_POINT ( 'NONE',  ( 0.2066987746313611596, -1.235937867595670925, 0.5698435078237830131 ) ) ;
#14406=FACE_OUTER_BOUND ( 'NONE', #27349, .T. ) ;
#14411=CARTESIAN_POINT ( 'NONE',  ( 0.01153542426051554215, -0.8583083583799452354, -0.04937503800822783118 ) ) ;
#14413=CARTESIAN_POINT ( 'NONE',  ( 0.08281856743603543958, -0.6169226312293338843, 0.3801866279162453566 ) ) ;
#14414=CARTESIAN_POINT ( 'NONE',  ( 0.1873051443137325467, -0.7000652135061801173, 0.03156626986716101063 ) ) ;
#14416=CARTESIAN_POINT ( 'NONE',  ( 0.06844213494250783736, -1.327645458249330002, 0.5609147710633128892 ) ) ;
#14418=CARTESIAN_POINT ( 'NONE',  ( 0.3968489921746024551, -1.715760314589834135, 0.4219785499399157924 ) ) ;
#14427=CARTESIAN_POINT ( 'NONE',  ( 0.2949815950263163233, -1.721662039081772733, 0.6893651101351793153 ) ) ;
#14429=CARTESIAN_POINT ( 'NONE',  ( 0.4515156439561487933, -1.057718100141998407, 0.6525781907329395448 ) ) ;
#14432=CARTESIAN_POINT ( 'NONE',  ( 0.5698123312952257935, -1.224001199585974087, 0.8774075775261976906 ) ) ;
#14433=EDGE_CURVE ( 'NONE', #3591, #849, #28551, .T. ) ;
#14440=CARTESIAN_POINT ( 'NONE',  ( 0.1464017060796926617, -1.195235124438886354, 0.9160713362441239571 ) ) ;
#14445=CARTESIAN_POINT ( 'NONE',  ( 0.5675876754196318430, -1.214623637701154335, 0.7236292717493534310 ) ) ;
#14451=EDGE_CURVE ( 'NONE', #9282, #10169, #15525, .T. ) ;
#14452=CARTESIAN_POINT ( 'NONE',  ( 0.4627101603843286615, -1.231251100330559067, 0.6049053019777383966 ) ) ;
#14458=CARTESIAN_POINT ( 'NONE',  ( 0.1000922401158252234, -0.7453142721180914254, 0.3380235344004010600 ) ) ;
#14459=CARTESIAN_POINT ( 'NONE',  ( 0.3063131332306592847, -1.685742840915233964, 0.8776895394429725661 ) ) ;
#14461=CARTESIAN_POINT ( 'NONE',  ( 0.1615841970432282948, -0.7812715960922147485, 0.6051956874001962472 ) ) ;
#14462=CARTESIAN_POINT ( 'NONE',  ( 0.2008187405414252891, -1.396362803482375181, 0.9475840340812614615 ) ) ;
#14463=CARTESIAN_POINT ( 'NONE',  ( 0.2871104898329135402, -1.663473480287219308, 0.5826563087959247822 ) ) ;
#14464=CARTESIAN_POINT ( 'NONE',  ( 0.08010764652114535367, -1.230296665588101801, 0.6540593777872614201 ) ) ;
#14468=CARTESIAN_POINT ( 'NONE',  ( 0.3820242417005274560, -0.9048593497249316497, 0.7921066019177993578 ) ) ;
#14470=CARTESIAN_POINT ( 'NONE',  ( 0.4685868260997171353, -1.116540410224083901, 0.5688321002147588290 ) ) ;
#14475=CARTESIAN_POINT ( 'NONE',  ( 0.6089993539687283963, -1.280207732015472333, 0.6563525730433853456 ) ) ;
#14479=AXIS2_PLACEMENT_3D ( 'NONE', #13649, #26215, #38738 ) ;
#14486=CARTESIAN_POINT ( 'NONE',  ( 0.6069176374591634948, -1.480164522464830990, 0.5706138896049881559 ) ) ;
#14488=ORIENTED_EDGE ( 'NONE', *, *, #16453, .F. ) ;
#14489=CARTESIAN_POINT ( 'NONE',  ( 0.1952262678655195816, -0.8446586641751220315, 0.3137089587960322778 ) ) ;
#14492=CARTESIAN_POINT ( 'NONE',  ( 0.1060741297991164983, -1.041550032235545764, 0.7252733955407512090 ) ) ;
#14501=CARTESIAN_POINT ( 'NONE',  ( 0.4280344223824243954, -1.180185467868497540, 0.6702189010033869909 ) ) ;
#14503=CARTESIAN_POINT ( 'NONE',  ( 0.5029219481274004311, -1.126576722786344797, 0.5684425849584162638 ) ) ;
#14506=EDGE_CURVE ( 'NONE', #2486, #33860, #38794, .T. ) ;
#14508=ORIENTED_EDGE ( 'NONE', *, *, #12809, .F. ) ;
#14510=EDGE_CURVE ( 'NONE', #40111, #1740, #13814, .T. ) ;
#14511=CARTESIAN_POINT ( 'NONE',  ( 0.2372522076649659917, -1.104445432429510543, 0.8445417033709822219 ) ) ;
#14512=CARTESIAN_POINT ( 'NONE',  ( 0.6987147365403517663, -1.542558173564892776, 0.5853929165781885935 ) ) ;
#14518=CARTESIAN_POINT ( 'NONE',  ( 0.5737671756752078522, -1.499224592217952123, 0.5704870461232408596 ) ) ;
#14521=CARTESIAN_POINT ( 'NONE',  ( 0.3225409073800189486, -1.758071532568285633, 0.5684393614938241246 ) ) ;
#14525=CARTESIAN_POINT ( 'NONE',  ( 0.6208236476055652986, -1.581963837082470903, 0.4231406649541298859 ) ) ;
#14526=AXIS2_PLACEMENT_3D ( 'NONE', #7964, #34891, #3040 ) ;
#14527=CARTESIAN_POINT ( 'NONE',  ( 0.1178701413495470002, -1.287575236778115473, 0.4358679387939850547 ) ) ;
#14529=CARTESIAN_POINT ( 'NONE',  ( 0.002304987189221298447, -0.5222059228616647841, 0.1457140420755211052 ) ) ;
#14532=CARTESIAN_POINT ( 'NONE',  ( 0.1875000000000003608, -0.4593131964907914422, 0.1498534765393862711 ) ) ;
#14535=EDGE_CURVE ( 'NONE', #23886, #14931, #34494, .T. ) ;
#14538=CARTESIAN_POINT ( 'NONE',  ( 0.6088579185943825411, -1.605814602209477249, 0.5994446572727915035 ) ) ;
#14540=PLANE ( 'NONE',  #8704 ) ;
#14542=CARTESIAN_POINT ( 'NONE',  ( 0.03474859143381433396, -0.6982915424597320175, 0.6540940360414806420 ) ) ;
#14546=CARTESIAN_POINT ( 'NONE',  ( 0.4521978803666491520, -1.695070482658580735, 0.5936670903620218098 ) ) ;
#14547=VERTEX_POINT ( 'NONE', #8720 ) ;
#14548=CARTESIAN_POINT ( 'NONE',  ( 0.4493096126656548339, -1.113522177362729959, 0.5923215117436996247 ) ) ;
#14550=CARTESIAN_POINT ( 'NONE',  ( 0.3878029384188880213, -1.139735408412443141, 0.6057421502664560586 ) ) ;
#14551=DIRECTION ( 'NONE',  ( 0.4999551463232372317, -0.8660512985181135770, 0.000000000000000000 ) ) ;
#14554=CARTESIAN_POINT ( 'NONE',  ( 0.5331776585576782912, -1.350023506793375461, 0.6065130868984314194 ) ) ;
#14557=CARTESIAN_POINT ( 'NONE',  ( 0.4199047739250627576, -1.021165802582503890, 0.6853183793762346321 ) ) ;
#14564=CARTESIAN_POINT ( 'NONE',  ( 0.3567070568950239662, -1.622554001505994270, 0.5819357718811433156 ) ) ;
#14565=CARTESIAN_POINT ( 'NONE',  ( 0.7091947434576362230, -1.510530529667985178, 0.5453121661639291906 ) ) ;
#14566=CARTESIAN_POINT ( 'NONE',  ( 0.1152431668949159965, -0.4475630518674869607, 0.1186598434184487072 ) ) ;
#14573=CARTESIAN_POINT ( 'NONE',  ( 0.1779430133141695625, -1.002639472607745219, 0.7064557712546435386 ) ) ;
#14577=CARTESIAN_POINT ( 'NONE',  ( 0.5860257985473278364, -1.592810714289450758, 0.4282417262808776437 ) ) ;
#14579=CARTESIAN_POINT ( 'NONE',  ( 0.3914506609052950670, -1.712970798409825690, 0.5197417262808792238 ) ) ;
#14587=CARTESIAN_POINT ( 'NONE',  ( 0.4767939168565226704, -1.131656391368646597, 0.4766437606999714416 ) ) ;
#14588=CARTESIAN_POINT ( 'NONE',  ( 0.4609956292016122448, -1.239833488668546480, 0.6057417262809813296 ) ) ;
#14592=CARTESIAN_POINT ( 'NONE',  ( 0.02557412545052138719, -0.6296114640116060590, 0.6017223022440639779 ) ) ;
#14596=CARTESIAN_POINT ( 'NONE',  ( 0.1766202724171772875, -0.4927511983303360932, 0.1950252429630008055 ) ) ;
#14601=CARTESIAN_POINT ( 'NONE',  ( 0.0008398931413175443400, -0.6066849459851459958, 0.007899750923771155578 ) ) ;
#14603=ORIENTED_EDGE ( 'NONE', *, *, #19810, .T. ) ;
#14604=CARTESIAN_POINT ( 'NONE',  ( 0.1205771420324995152, -0.4915166019810813247, 0.3243857998619378846 ) ) ;
#14607=CIRCLE ( 'NONE', #27751, 0.009999999999999995004 ) ;
#14608=CARTESIAN_POINT ( 'NONE',  ( -0.001512435542830417026, -0.5371720154798181879, 0.2089148858682966237 ) ) ;
#14610=CARTESIAN_POINT ( 'NONE',  ( 0.1287248250748170286, -1.260341800920546484, 0.6227168118355963511 ) ) ;
#14615=CARTESIAN_POINT ( 'NONE',  ( 0.5304035836234874957, -1.638499236635372780, 0.5682417262808785452 ) ) ;
#14618=CARTESIAN_POINT ( 'NONE',  ( 0.3246167692519850156, -1.179669033920380805, 0.5775999012672733413 ) ) ;
#14619=CARTESIAN_POINT ( 'NONE',  ( 0.2200407913522031411, -1.228412753058486073, 0.5340532311266873444 ) ) ;
#14620=B_SPLINE_SURFACE_WITH_KNOTS ( 'NONE', 3, 3, ( 
 ( #28736, #25867, #3638, #31420 ),
 ( #598, #25032, #34497, #13092 ),
 ( #3221, #18881, #3426, #405 ),
 ( #12902, #38382, #28317, #3825 ),
 ( #19486, #191, #37785, #12684 ),
 ( #9606, #28132, #19280, #25457 ),
 ( #5009, #37989, #22181, #25650 ) ),
 .UNSPECIFIED., .F., .F., .F.,
 ( 4, 3, 4 ),
 ( 4, 4 ),
 ( -6.200793099907373929, -3.019996348331698499, 0.1608004032439768194 ),
 ( -2.017105796196418055, 1.822539631016510064 ),
 .UNSPECIFIED. ) ;
#14621=CARTESIAN_POINT ( 'NONE',  ( 0.08992993224852839640, -0.5649945132296568806, 0.1558695816954820679 ) ) ;
#14622=CARTESIAN_POINT ( 'NONE',  ( 0.1872312464940305565, -0.7051497005520173111, 0.03070732711193139425 ) ) ;
#14630=CARTESIAN_POINT ( 'NONE',  ( 0.1614670899430008522, -0.7569536277469717245, 0.1022936816274460647 ) ) ;
#14631=CARTESIAN_POINT ( 'NONE',  ( 0.4378920954596315362, -1.115947916920391636, 0.5895459110645610012 ) ) ;
#14636=CARTESIAN_POINT ( 'NONE',  ( 0.2474040834808491629, -1.657462368044302137, 0.5682417262808785452 ) ) ;
#14637=CARTESIAN_POINT ( 'NONE',  ( 0.4907992349987285730, -1.081537398447262266, 0.5876768462667140147 ) ) ;
#14638=CARTESIAN_POINT ( 'NONE',  ( 0.01863187058585013059, -0.9402654431934535095, 0.5981457854821163878 ) ) ;
#14640=CARTESIAN_POINT ( 'NONE',  ( 0.3762811493344272451, -0.8989788859175238400, 0.7888608478858359918 ) ) ;
#14650=CARTESIAN_POINT ( 'NONE',  ( 0.03972200282294607865, -0.8089223363086154306, 0.6796728585062656869 ) ) ;
#14651=CARTESIAN_POINT ( 'NONE',  ( 0.5883443998395444519, -1.491224512076320341, 0.5816035368030421093 ) ) ;
#14656=CARTESIAN_POINT ( 'NONE',  ( 0.1906860423535042259, -0.5845769100630294757, 0.1622375173579828633 ) ) ;
#14667=CARTESIAN_POINT ( 'NONE',  ( 0.1199147042866572366, -1.258787245233497387, 0.6044491403675849028 ) ) ;
#14668=EDGE_CURVE ( 'NONE', #33002, #30450, #19218, .T. ) ;
#14669=CARTESIAN_POINT ( 'NONE',  ( 0.09122731847452461573, -0.7321966631737302222, 0.2618906540905704405 ) ) ;
#14672=CARTESIAN_POINT ( 'NONE',  ( 0.1822742746219855603, -1.224115163224249736, 1.025352947117986080 ) ) ;
#14674=CARTESIAN_POINT ( 'NONE',  ( 0.4973887099434665116, -1.542487569279054505, 0.5723575042553348258 ) ) ;
#14677=CARTESIAN_POINT ( 'NONE',  ( 0.02088642212014098221, -0.9663541300412515911, 0.3981965082845343451 ) ) ;
#14678=EDGE_LOOP ( 'NONE', ( #31632, #10715, #2954 ) ) ;
#14682=CARTESIAN_POINT ( 'NONE',  ( 0.4796154630067505087, -1.077685692966938502, 0.8624841813652754929 ) ) ;
#14689=CARTESIAN_POINT ( 'NONE',  ( 0.3668746095265688067, -1.158496670723085931, 0.4182417262808776903 ) ) ;
#14690=B_SPLINE_CURVE_WITH_KNOTS ( 'NONE', 3,
 ( #10672, #38651, #7582, #29805, #1844, #30201 ),
 .UNSPECIFIED., .F., .F.,
 ( 4, 2, 4 ),
 ( 0.000000000000000000, 0.5000000000000000000, 1.000000000000000000 ),
 .UNSPECIFIED. ) ;
#14692=CARTESIAN_POINT ( 'NONE',  ( 0.3097005752544714774, -1.188690221295249039, 0.5001884091346039396 ) ) ;
#14693=CARTESIAN_POINT ( 'NONE',  ( 0.1906860423535042259, -0.5845769100630294757, 0.1622375173579828633 ) ) ;
#14695=CARTESIAN_POINT ( 'NONE',  ( 0.4419048264408250715, -1.686280600454902245, 0.4284299735159858291 ) ) ;
#14702=CARTESIAN_POINT ( 'NONE',  ( 0.4665196626547312708, -1.234810002811577379, 0.6252536019874470608 ) ) ;
#14706=AXIS2_PLACEMENT_3D ( 'NONE', #28381, #37237, #34139 ) ;
#14712=CARTESIAN_POINT ( 'NONE',  ( 0.2256051981446139942, -1.349927307554772415, 0.5923384359580952108 ) ) ;
#14719=CARTESIAN_POINT ( 'NONE',  ( 0.4122725859440758978, -1.161157803837102431, 0.6802704944461144265 ) ) ;
#14721=LINE ( 'NONE', #12044, #22741 ) ;
#14724=CARTESIAN_POINT ( 'NONE',  ( 0.4076976354719489271, -1.154888438488554270, 0.4182417262808778013 ) ) ;
#14729=CARTESIAN_POINT ( 'NONE',  ( 0.06252399284434355387, -0.5703086016868591512, 0.2738859570674773702 ) ) ;
#14732=DIRECTION ( 'NONE',  ( 0.000000000000000000, 0.000000000000000000, -1.000000000000000000 ) ) ;
#14733=ORIENTED_EDGE ( 'NONE', *, *, #6749, .F. ) ;
#14739=CARTESIAN_POINT ( 'NONE',  ( 0.5686245264436429192, -1.473229231349149293, 0.7026948991434345260 ) ) ;
#14740=CARTESIAN_POINT ( 'NONE',  ( 0.6611503302885902711, -1.574458991221895143, 0.6100450518719389148 ) ) ;
#14741=CARTESIAN_POINT ( 'NONE',  ( 0.3178512907186139547, -1.645949601790900774, 0.6057417262800831592 ) ) ;
#14746=CARTESIAN_POINT ( 'NONE',  ( 0.01054817777343857940, -0.5296544771352952319, 0.1457185332388703236 ) ) ;
#14749=CARTESIAN_POINT ( 'NONE',  ( 0.7218807932984940834, -1.475040712527332376, 0.6299232363116300526 ) ) ;
#14757=CARTESIAN_POINT ( 'NONE',  ( 0.6013626892431855886, -1.610388389587162239, 0.5938553534641382026 ) ) ;
#14760=CARTESIAN_POINT ( 'NONE',  ( 0.005216780649377962716, -0.5315740328921342295, 0.3610413699792206499 ) ) ;
#14764=CARTESIAN_POINT ( 'NONE',  ( 0.4124147183372396386, -1.717743792098087141, 0.6107278818000745346 ) ) ;
#14770=CARTESIAN_POINT ( 'NONE',  ( 0.3442074111778197776, -1.154923315903912284, 0.6085910790176920493 ) ) ;
#14772=CARTESIAN_POINT ( 'NONE',  ( 0.07496066467185190374, -0.5410121364700161140, 0.1458279059002116351 ) ) ;
#14774=CARTESIAN_POINT ( 'NONE',  ( 0.3335272892300009118, -1.054689036592173945, 0.7480762832650960092 ) ) ;
#14777=CARTESIAN_POINT ( 'NONE',  ( 0.4556897805969272741, -1.061013212638954206, 0.6517789979982376858 ) ) ;
#14783=EDGE_LOOP ( 'NONE', ( #31832, #18946 ) ) ;
#14784=CARTESIAN_POINT ( 'NONE',  ( 0.03572657310119726343, -0.5431789479654421937, 0.2057126367031107406 ) ) ;
#14785=CARTESIAN_POINT ( 'NONE',  ( 0.6849494496261877563, -1.512191847840882453, 0.4544522245954892292 ) ) ;
#14786=CARTESIAN_POINT ( 'NONE',  ( 0.1772721291538777444, -0.4572599737788377583, 0.1350242392045666873 ) ) ;
#14788=EDGE_CURVE ( 'NONE', #26649, #1394, #8423, .T. ) ;
#14790=CARTESIAN_POINT ( 'NONE',  ( 0.4826283266143189810, -1.073631714458713970, 0.6135120272222409632 ) ) ;
#14791=ORIENTED_EDGE ( 'NONE', *, *, #17013, .T. ) ;
#14794=CARTESIAN_POINT ( 'NONE',  ( 0.2812000348737145328, -1.206196182835379993, 0.7249378850271948060 ) ) ;
#14795=LINE ( 'NONE', #4907, #21826 ) ;
#14796=CYLINDRICAL_SURFACE ( 'NONE', #25269, 0.08749999999977554899 ) ;
#14799=CARTESIAN_POINT ( 'NONE',  ( 0.3917590551332735815, -1.108679468675640933, 0.6260960277489386883 ) ) ;
#14803=CARTESIAN_POINT ( 'NONE',  ( 0.0008242595369169036616, -0.9534780057342879811, 0.2825590231195395652 ) ) ;
#14808=CARTESIAN_POINT ( 'NONE',  ( 0.4795168759268733649, -1.133137350430038826, 0.4754588475104733480 ) ) ;
#14809=CARTESIAN_POINT ( 'NONE',  ( 0.5536755335287484314, -1.186494592434074402, 0.6057417262809811076 ) ) ;
#14812=CARTESIAN_POINT ( 'NONE',  ( 0.01198934593465751479, -0.4904157440881893870, -0.02331765030193806015 ) ) ;
#14823=CARTESIAN_POINT ( 'NONE',  ( -0.0001009439540302022357, -0.6986278422313487724, -0.02210014490066574203 ) ) ;
#14829=CARTESIAN_POINT ( 'NONE',  ( 0.2631915173570256172, -1.522375190849774684, 0.8868596689731271798 ) ) ;
#14831=CARTESIAN_POINT ( 'NONE',  ( 0.2015425829111033018, -1.236709817947498458, 0.5758929572549138509 ) ) ;
#14838=ORIENTED_EDGE ( 'NONE', *, *, #12982, .F. ) ;
#14840=CARTESIAN_POINT ( 'NONE',  ( 0.4191100986681001173, -1.701672718972385701, 0.4233639548768205474 ) ) ;
#14842=CARTESIAN_POINT ( 'NONE',  ( 0.08108118076421688691, -1.187912308584602616, 0.7629475175450785018 ) ) ;
#14843=CARTESIAN_POINT ( 'NONE',  ( 0.3061189101312851712, -1.032064364196468631, 0.7779705550342140841 ) ) ;
#14844=CARTESIAN_POINT ( 'NONE',  ( 0.1874366911980140937, -0.6909370189385394267, 0.04366226709255235927 ) ) ;
#14845=CYLINDRICAL_SURFACE ( 'NONE', #25135, 0.09249999999977555343 ) ;
#14851=CARTESIAN_POINT ( 'NONE',  ( 0.3943456310756559002, -1.717985633627846287, 0.3157417262808776548 ) ) ;
#14852=CARTESIAN_POINT ( 'NONE',  ( 0.07497864282572899719, -1.322056043867073427, 0.4862695133534066794 ) ) ;
#14855=VECTOR ( 'NONE', #31354, 39.37007874015748143 ) ;
#14857=CARTESIAN_POINT ( 'NONE',  ( 0.2890670123411187564, -1.729633309587475187, 0.5682417262808785452 ) ) ;
#14858=CARTESIAN_POINT ( 'NONE',  ( 0.004642268657786469133, -0.8873649503241693992, 0.4600736514407574029 ) ) ;
#14860=CARTESIAN_POINT ( 'NONE',  ( 0.4993356427094534644, -1.110845742389603430, 0.8468575151840780357 ) ) ;
#14863=CARTESIAN_POINT ( 'NONE',  ( 0.3740960844805631957, -1.108072201694596526, 0.5182417262812423209 ) ) ;
#14868=CARTESIAN_POINT ( 'NONE',  ( 0.6505987497515465234, -1.453420545349225712, 0.4198196556257698941 ) ) ;
#14869=CARTESIAN_POINT ( 'NONE',  ( 0.1737062342642059776, -1.287475063264992503, 0.9337216465431702472 ) ) ;
#14870=CARTESIAN_POINT ( 'NONE',  ( 0.5876579976468534472, -1.491161407508044157, 0.5680417111487973125 ) ) ;
#14874=CARTESIAN_POINT ( 'NONE',  ( 0.5008076730341156635, -1.117067070538257489, 0.7495569431474730093 ) ) ;
#14876=ORIENTED_EDGE ( 'NONE', *, *, #10472, .F. ) ;
#14877=CARTESIAN_POINT ( 'NONE',  ( 0.6867278559859741893, -1.412191411537361274, 0.7037197479575562076 ) ) ;
#14884=CARTESIAN_POINT ( 'NONE',  ( 0.2472658003028177509, -0.9389390588893103962, 0.6883636664316881149 ) ) ;
#14886=CARTESIAN_POINT ( 'NONE',  ( 0.4981291757010007371, -1.537019023564916820, 0.6523613731338329114 ) ) ;
#14887=CARTESIAN_POINT ( 'NONE',  ( 0.3305348052992108654, -1.762648515960067330, 0.4809830086422206552 ) ) ;
#14889=CARTESIAN_POINT ( 'NONE',  ( 0.09805242145838187484, -1.310054031134214814, 0.5767050436540001046 ) ) ;
#14894=CARTESIAN_POINT ( 'NONE',  ( 0.2142115587710679836, -0.7293689487072348987, 0.6843368706038465143 ) ) ;
#14898=CARTESIAN_POINT ( 'NONE',  ( 0.3994099251164126563, -1.146822512724485765, 0.4244458817396841166 ) ) ;
#14900=CARTESIAN_POINT ( 'NONE',  ( 0.3219460272232844700, -1.170076428657419454, 0.4747704893780865798 ) ) ;
#14901=CARTESIAN_POINT ( 'NONE',  ( 0.5537997781288683807, -1.186498928682228504, 0.6031466697272260813 ) ) ;
#14907=CARTESIAN_POINT ( 'NONE',  ( 0.4459262886234038326, -1.207765542572133421, 0.6882926990457565175 ) ) ;
#14912=CARTESIAN_POINT ( 'NONE',  ( 0.4434255849441152142, -1.139149627293542189, 0.4381544910599347586 ) ) ;
#14918=CARTESIAN_POINT ( 'NONE',  ( 0.02310847749635362366, -0.8913551796067988864, 0.5089986389165233049 ) ) ;
#14919=VERTEX_POINT ( 'NONE', #18151 ) ;
#14924=CARTESIAN_POINT ( 'NONE',  ( 0.4084052577889880076, -1.157625084686668693, 0.6947072065425384801 ) ) ;
#14931=VERTEX_POINT ( 'NONE', #24748 ) ;
#14933=CARTESIAN_POINT ( 'NONE',  ( 0.4421500455968371268, -1.573867983067024356, 0.5805441873791059582 ) ) ;
#14936=CARTESIAN_POINT ( 'NONE',  ( 0.5792545670597167851, -1.619325922623725988, 0.4680594544321094452 ) ) ;
#14943=CARTESIAN_POINT ( 'NONE',  ( 0.5738275230768540291, -1.499242471352824069, 0.5716642358389814049 ) ) ;
#14944=CARTESIAN_POINT ( 'NONE',  ( 0.4880938837017151366, -1.659832216460053189, 0.5158750058761750745 ) ) ;
#14951=CARTESIAN_POINT ( 'NONE',  ( 0.2433107440384445208, -0.6632537007949954599, 0.5455544552538778014 ) ) ;
#14953=CARTESIAN_POINT ( 'NONE',  ( 0.007094984414204748985, -0.9940037754512424106, 0.4883039338829347487 ) ) ;
#14959=EDGE_CURVE ( 'NONE', #4497, #7711, #27094, .T. ) ;
#14963=CARTESIAN_POINT ( 'NONE',  ( 0.1176586183174064548, -1.298913320427260265, 0.5281503409082900502 ) ) ;
#14969=CARTESIAN_POINT ( 'NONE',  ( 0.1826134026666640375, -1.261648033191452578, 0.4282186462236585722 ) ) ;
#14973=CARTESIAN_POINT ( 'NONE',  ( 0.5093083032388259213, -1.308138162599655541, 0.6666047094510684223 ) ) ;
#14976=CARTESIAN_POINT ( 'NONE',  ( 0.4829770732687932999, -1.083865320555347678, 0.6394302686688468906 ) ) ;
#14983=CARTESIAN_POINT ( 'NONE',  ( 0.3067833816315509443, -1.474156006046335676, 0.8783781600432545300 ) ) ;
#14985=CARTESIAN_POINT ( 'NONE',  ( 0.06603965020215776804, -0.7527310131072945110, 0.01289759490777755632 ) ) ;
#14986=CARTESIAN_POINT ( 'NONE',  ( 0.1142304224324458134, -0.5268503339532456531, -0.03412200579080372498 ) ) ;
#14990=CARTESIAN_POINT ( 'NONE',  ( 0.3256465291941874063, -0.9849688007361252495, 0.5834247550187220410 ) ) ;
#14991=CARTESIAN_POINT ( 'NONE',  ( 0.3411737120602144624, -1.136299044918231527, 0.8205066405080015945 ) ) ;
#14995=CARTESIAN_POINT ( 'NONE',  ( 0.3280405094088094109, -1.284529511138909230, 0.6184389781141244047 ) ) ;
#14999=CARTESIAN_POINT ( 'NONE',  ( 0.7472019744968698696, -1.513150647243692637, 0.5707417262808793801 ) ) ;
#15004=CARTESIAN_POINT ( 'NONE',  ( 0.4681739163933527070, -1.133581507510084796, 0.4638371986610853592 ) ) ;
#15008=EDGE_CURVE ( 'NONE', #33383, #32917, #22162, .T. ) ;
#15009=CARTESIAN_POINT ( 'NONE',  ( 8.003345398980878371E-06, -0.5705062560190085064, -0.08785543567291767553 ) ) ;
#15012=CARTESIAN_POINT ( 'NONE',  ( 0.3105533536971931685, -1.758467965264669752, 0.5220181958261356225 ) ) ;
#15018=CARTESIAN_POINT ( 'NONE',  ( 0.1614573949321077284, -0.7569534866611321577, 0.1932149833450299559 ) ) ;
#15023=CARTESIAN_POINT ( 'NONE',  ( 0.002170355132208537634, -0.5205946845004905121, 0.1266085954518501588 ) ) ;
#15028=EDGE_CURVE ( 'NONE', #13059, #36473, #22585, .T. ) ;
#15029=CARTESIAN_POINT ( 'NONE',  ( 0.2671426166548651615, -1.675561005867882258, 0.5833829581153555655 ) ) ;
#15030=CARTESIAN_POINT ( 'NONE',  ( 0.4055497041687889936, -1.192612325472327983, 0.6891132521580926040 ) ) ;
#15038=EDGE_CURVE ( 'NONE', #12111, #17741, #21123, .T. ) ;
#15042=CARTESIAN_POINT ( 'NONE',  ( 0.4229144610190289089, -1.180059474700835498, 0.8097779815502904599 ) ) ;
#15043=CARTESIAN_POINT ( 'NONE',  ( 0.1857669404175232297, -0.8054308633438567178, 0.07733745057108264154 ) ) ;
#15045=CARTESIAN_POINT ( 'NONE',  ( 0.1864168460039302422, -0.7346540591771211215, 0.08921340677137505615 ) ) ;
#15047=CARTESIAN_POINT ( 'NONE',  ( 0.4168791804701151293, -1.706510454905088237, 0.4274202794507407366 ) ) ;
#15050=CARTESIAN_POINT ( 'NONE',  ( 0.2801809802548146933, -0.9759768125023459140, 0.7245117847987158077 ) ) ;
#15051=CARTESIAN_POINT ( 'NONE',  ( 0.4142910187529088017, -1.110460457557075564, 0.6154625682581813528 ) ) ;
#15052=CARTESIAN_POINT ( 'NONE',  ( 0.4356476796531106310, -1.231215465721436697, 0.5833139271779056445 ) ) ;
#15054=B_SPLINE_CURVE_WITH_KNOTS ( 'NONE', 3,
 ( #20097, #32626, #32813, #29958, #4435, #39596, #36527, #4235, #29535, #7727, #26460, #1794, #29738, #20293 ),
 .UNSPECIFIED., .F., .F.,
 ( 4, 2, 2, 2, 2, 2, 4 ),
 ( 3.332294980281255979E-17, 0.0007771933352389642172, 0.001554386670477895258, 0.001942983338097360128, 0.002331580005716824781, 0.002720176673336289867, 0.003108773340955754520 ),
 .UNSPECIFIED. ) ;
#15056=CARTESIAN_POINT ( 'NONE',  ( 0.01179864804857342665, -0.6562760587974182380, 0.4561945812754703011 ) ) ;
#15057=CARTESIAN_POINT ( 'NONE',  ( 0.09497277601810472092, -1.273348885617128889, 0.7438579102249397446 ) ) ;
#15059=CARTESIAN_POINT ( 'NONE',  ( 0.4897931935426230177, -1.095389100717072850, 0.8439147301884563079 ) ) ;
#15061=CARTESIAN_POINT ( 'NONE',  ( 0.7009476147591743311, -1.525393810516090909, 0.5735417758099603525 ) ) ;
#15065=CARTESIAN_POINT ( 'NONE',  ( -0.0004431470427073231017, -0.9367128829938298207, 0.1457185332388704069 ) ) ;
#15066=CARTESIAN_POINT ( 'NONE',  ( 0.2599175140567103193, -1.619495788301735351, 0.8180271650695088992 ) ) ;
#15067=CARTESIAN_POINT ( 'NONE',  ( 0.1289590727735309694, -0.5712154984990630568, 0.2405744295037446634 ) ) ;
#15068=CARTESIAN_POINT ( 'NONE',  ( 0.3839222738949826241, -1.728173381748683957, 0.4282780629211213053 ) ) ;
#15070=CARTESIAN_POINT ( 'NONE',  ( 0.3520862261316686226, -0.8866190960188533587, 0.7137788081797863393 ) ) ;
#15073=CARTESIAN_POINT ( 'NONE',  ( 0.2132597674873976390, -0.6354326468627278235, 0.4153990741051870605 ) ) ;
#15077=CARTESIAN_POINT ( 'NONE',  ( 0.4841487358689927634, -1.673745430023940717, 0.5182417262823179049 ) ) ;
#15078=ORIENTED_EDGE ( 'NONE', *, *, #13427, .T. ) ;
#15079=CARTESIAN_POINT ( 'NONE',  ( 0.1070314971879695043, -0.7548214689483502271, 0.3798963362569547364 ) ) ;
#15080=CARTESIAN_POINT ( 'NONE',  ( 0.3134922297020871773, -1.766968131109182050, 0.6133363199024374213 ) ) ;
#15081=CARTESIAN_POINT ( 'NONE',  ( 0.4974254930090974969, -1.542500022935912485, 0.5729870860315193770 ) ) ;
#15082=CARTESIAN_POINT ( 'NONE',  ( 0.07666882145575558416, -1.311286108063837164, 0.5563055692900464866 ) ) ;
#15083=CARTESIAN_POINT ( 'NONE',  ( 0.1712463865401376573, -1.267487284506117584, 0.5765326934465192510 ) ) ;
#15086=LINE ( 'NONE', #107, #12133 ) ;
#15087=CARTESIAN_POINT ( 'NONE',  ( 0.4904781775425864909, -1.197665561882578888, 0.9014511766705987084 ) ) ;
#15092=CARTESIAN_POINT ( 'NONE',  ( 0.3269603303531253835, -1.178766071222939527, 0.4747738120598547495 ) ) ;
#15093=CARTESIAN_POINT ( 'NONE',  ( 0.5544140612800516621, -1.190962001057203956, 0.5445415982692776158 ) ) ;
#15100=CARTESIAN_POINT ( 'NONE',  ( 0.4841277252458648928, -1.120042291950998248, 0.5405469610105025913 ) ) ;
#15105=CARTESIAN_POINT ( 'NONE',  ( 0.03743165412374005463, -0.9419925036766105819, 0.6214317009962998517 ) ) ;
#15107=EDGE_LOOP ( 'NONE', ( #17682, #795, #12101, #15221, #33475 ) ) ;
#15118=VERTEX_POINT ( 'NONE', #31502 ) ;
#15119=CARTESIAN_POINT ( 'NONE',  ( 0.08531374436275271367, -1.317707820694483445, 0.5634626972692623470 ) ) ;
#15121=( BOUNDED_SURFACE ( )  B_SPLINE_SURFACE ( 3, 2, ( 
 ( #9553, #4178, #28264 ),
 ( #37938, #34835, #19220 ),
 ( #31759, #20038, #23132 ),
 ( #8288, #35658, #23545 ),
 ( #17138, #7861, #36474 ),
 ( #1532, #29689, #20432 ) ),
 .UNSPECIFIED., .F., .F., .F. ) 
 B_SPLINE_SURFACE_WITH_KNOTS ( ( 4, 2, 4 ),
 ( 3, 3 ),
 ( 0.000000000000000000, 0.0004914683366409194638, 0.0009829366732818389275 ),
 ( 0.000000000000000000, 1.000000000000000000 ),
 .UNSPECIFIED. ) 
 GEOMETRIC_REPRESENTATION_ITEM ( )  RATIONAL_B_SPLINE_SURFACE ( (
 ( 1.000000000000000000, 0.9411999499705835381, 1.000000000000000000),
 ( 1.000000000000000000, 0.9445899725874141728, 1.000000000000000000),
 ( 1.000000000000000000, 0.9471079876882634307, 1.000000000000000000),
 ( 1.000000000000000000, 0.9513946071237538993, 1.000000000000000000),
 ( 1.000000000000000000, 0.9531191815715883697, 1.000000000000000000),
 ( 1.000000000000000000, 0.9544113358811291414, 1.000000000000000000) ) ) 
 REPRESENTATION_ITEM ( '' )  SURFACE ( )  );
#15123=CARTESIAN_POINT ( 'NONE',  ( 0.06506191882387997449, -0.5885835149343405792, 0.3205912525364184584 ) ) ;
#15125=CARTESIAN_POINT ( 'NONE',  ( 0.5643309268556270242, -1.618135655174819609, 0.5416644041066450699 ) ) ;
#15131=CARTESIAN_POINT ( 'NONE',  ( 0.5738848579949621387, -1.499255142838190169, 0.5726899272605390223 ) ) ;
#15133=DIRECTION ( 'NONE',  ( 0.7951751656451613304, 0.5387332766908925485, -0.2783215991027008784 ) ) ;
#15136=CARTESIAN_POINT ( 'NONE',  ( 0.2207932373118511316, -1.227997198505421217, 0.5267332555179391473 ) ) ;
#15138=DIRECTION ( 'NONE',  ( 0.8660512985181133550, 0.4999551463232372317, 0.000000000000000000 ) ) ;
#15139=CARTESIAN_POINT ( 'NONE',  ( 0.2322584854342325811, -1.232969341141011865, 0.4942330146944146629 ) ) ;
#15140=CARTESIAN_POINT ( 'NONE',  ( 0.6761021464639213052, -1.407442781842621171, 0.4761751337611269674 ) ) ;
#15141=VECTOR ( 'NONE', #36809, 39.37007874015748854 ) ;
#15143=CARTESIAN_POINT ( 'NONE',  ( 0.02191839362513907027, -1.011983551195656972, 0.5361064874689737136 ) ) ;
#15147=CARTESIAN_POINT ( 'NONE',  ( 0.5801239525038842659, -1.611124500691150541, 0.5902727294267513525 ) ) ;
#15156=CARTESIAN_POINT ( 'NONE',  ( 0.1543608876718505218, -1.277530715710694098, 0.5557375578266802174 ) ) ;
#15157=CARTESIAN_POINT ( 'NONE',  ( 0.3351195522891313172, -1.762354232558481337, 0.5631496603913015431 ) ) ;
#15160=CARTESIAN_POINT ( 'NONE',  ( 0.3270026267580349311, -1.166750842916578712, 0.5707716670974642970 ) ) ;
#15161=FACE_OUTER_BOUND ( 'NONE', #16162, .T. ) ;
#15163=CARTESIAN_POINT ( 'NONE',  ( 0.5135225295332491724, -1.315059133140256353, 0.6560163138962351592 ) ) ;
#15165=CARTESIAN_POINT ( 'NONE',  ( 0.1864644430607921566, -0.7573173996488720139, 0.1022963476796171639 ) ) ;
#15167=CARTESIAN_POINT ( 'NONE',  ( 0.2669631944262408907, -0.9256872934665847374, 0.5220607882127416000 ) ) ;
#15168=VERTEX_POINT ( 'NONE', #20341 ) ;
#15172=CARTESIAN_POINT ( 'NONE',  ( 0.01016927536616487118, -0.5376657146052628011, 0.09484175047482117094 ) ) ;
#15175=CARTESIAN_POINT ( 'NONE',  ( 0.06622580637515929070, -0.7619978381091805364, 0.6157077979737474172 ) ) ;
#15176=CARTESIAN_POINT ( 'NONE',  ( 0.1855093845756445592, -0.7772764304750825470, 0.005262776399236719464 ) ) ;
#15179=VECTOR ( 'NONE', #21467, 39.37007874015748143 ) ;
#15182=CARTESIAN_POINT ( 'NONE',  ( 0.2697801010412542722, -1.019695529454659688, 0.6051538852367689403 ) ) ;
#15183=CARTESIAN_POINT ( 'NONE',  ( 0.4007831926871883721, -1.251710563967610712, 0.8405983782434964802 ) ) ;
#15186=EDGE_CURVE ( 'NONE', #17370, #9161, #15875, .T. ) ;
#15187=DIRECTION ( 'NONE',  ( 0.4999551463232372317, -0.8660512985181135770, 0.000000000000000000 ) ) ;
#15191=EDGE_CURVE ( 'NONE', #6763, #3822, #36325, .T. ) ;
#15193=DIRECTION ( 'NONE',  ( -0.4999551463232372317, 0.8660512985181134660, 6.869252350113302335E-17 ) ) ;
#15194=CARTESIAN_POINT ( 'NONE',  ( 0.5705082898449433948, -1.615108203520839947, 0.3157417262808777658 ) ) ;
#15197=CARTESIAN_POINT ( 'NONE',  ( 0.08075236803977006717, -1.368778601871594836, 0.5682417262808778791 ) ) ;
#15199=CARTESIAN_POINT ( 'NONE',  ( 0.4807229719322908545, -1.126383887635181047, 0.4906570977974250569 ) ) ;
#15201=CARTESIAN_POINT ( 'NONE',  ( 0.5246395073518916874, -1.203093073328722840, 0.6057417262809805525 ) ) ;
#15206=CARTESIAN_POINT ( 'NONE',  ( 0.07670545266435074838, -1.210239791498856521, 0.7644951083879507614 ) ) ;
#15215=DIRECTION ( 'NONE',  ( 0.4999551463232372317, -0.8660512985181134660, 0.000000000000000000 ) ) ;
#15217=CARTESIAN_POINT ( 'NONE',  ( 0.002081379308398287331, -0.5326384292413223198, 0.1067899420028262103 ) ) ;
#15221=ORIENTED_EDGE ( 'NONE', *, *, #40072, .F. ) ;
#15223=ORIENTED_EDGE ( 'NONE', *, *, #22119, .T. ) ;
#15224=CARTESIAN_POINT ( 'NONE',  ( 0.2664752076017231075, -1.675363658809308820, 0.5749620007053757309 ) ) ;
#15226=CARTESIAN_POINT ( 'NONE',  ( 0.09592468290264696829, -1.296997100857483209, 0.6045289538570212118 ) ) ;
#15227=CARTESIAN_POINT ( 'NONE',  ( 0.3882495962481228857, -1.143537762327198948, 0.4808272649735114701 ) ) ;
#15231=ORIENTED_EDGE ( 'NONE', *, *, #27044, .F. ) ;
#15233=CARTESIAN_POINT ( 'NONE',  ( 0.3691166938341062242, -1.174453341100101689, 0.5182417262812423209 ) ) ;
#15237=CARTESIAN_POINT ( 'NONE',  ( 0.4406491928701437022, -1.207141337522043667, 0.7963399545800788903 ) ) ;
#15241=CARTESIAN_POINT ( 'NONE',  ( 0.2718953302849530518, -1.636696295107877841, 0.7785526595467455735 ) ) ;
#15245=CARTESIAN_POINT ( 'NONE',  ( 0.4226000438817401061, -1.709616762427843550, 0.4282184315516496809 ) ) ;
#15247=CARTESIAN_POINT ( 'NONE',  ( 0.4112031682589459836, -1.245393622654190846, 0.5280675622111803413 ) ) ;
#15249=CARTESIAN_POINT ( 'NONE',  ( 0.4256878781885970464, -1.117437563897770936, 0.5966076842664922442 ) ) ;
#15252=CARTESIAN_POINT ( 'NONE',  ( 0.002391669266185704034, -0.4944279760261894308, 0.2539263035736906149 ) ) ;
#15253=CARTESIAN_POINT ( 'NONE',  ( 0.08035207416351047849, -1.251254375864937707, 0.7454261770637490292 ) ) ;
#15255=CARTESIAN_POINT ( 'NONE',  ( 0.3337757566908341467, -0.8338946305499669309, 0.7209303476996544724 ) ) ;
#15259=CARTESIAN_POINT ( 'NONE',  ( 0.6672263256166638401, -1.559577713309558744, 0.6159734170043972279 ) ) ;
#15266=CARTESIAN_POINT ( 'NONE',  ( 0.1905612331079999666, -1.343658964144449408, 0.9374431420955621208 ) ) ;
#15268=CARTESIAN_POINT ( 'NONE',  ( 0.1284636661404361391, -0.5523917827180000462, 0.1701582641825293007 ) ) ;
#15271=VERTEX_POINT ( 'NONE', #14969 ) ;
#15272=ADVANCED_FACE ( 'NONE', ( #14154 ), #27661, .T. ) ;
#15273=CARTESIAN_POINT ( 'NONE',  ( 0.2980752164830456907, -0.8471807121723260448, 0.6106271213134966125 ) ) ;
#15274=ORIENTED_EDGE ( 'NONE', *, *, #32447, .T. ) ;
#15275=VERTEX_POINT ( 'NONE', #39253 ) ;
#15276=CARTESIAN_POINT ( 'NONE',  ( 0.6830109224318547945, -1.405801553408178917, 0.7155230334201035935 ) ) ;
#15282=CARTESIAN_POINT ( 'NONE',  ( 0.08866166269403266686, -0.7282185591720891082, 0.2282637218580873539 ) ) ;
#15284=CARTESIAN_POINT ( 'NONE',  ( 0.1059692563321519704, -0.5739410805619210576, 0.2614456175893158929 ) ) ;
#15285=CARTESIAN_POINT ( 'NONE',  ( 0.3219725102672574280, -1.761030903391374913, 0.4946895397007664008 ) ) ;
#15286=CARTESIAN_POINT ( 'NONE',  ( 0.0003868712903910354398, -0.6441692727094081583, -0.01675880997169623687 ) ) ;
#15287=CARTESIAN_POINT ( 'NONE',  ( 0.05376019824564439581, -1.293160722896381953, 0.6314177507418043955 ) ) ;
#15289=B_SPLINE_CURVE_WITH_KNOTS ( 'NONE', 3,
 ( #22254, #15045, #34365, #24919 ),
 .UNSPECIFIED., .F., .F.,
 ( 4, 4 ),
 ( 3.832980274770707779E-05, 0.002032193406424597382 ),
 .UNSPECIFIED. ) ;
#15292=EDGE_CURVE ( 'NONE', #23093, #11923, #34225, .T. ) ;
#15293=CARTESIAN_POINT ( 'NONE',  ( 0.4518247747909678869, -1.695278170436179233, 0.5936431579880691034 ) ) ;
#15294=CARTESIAN_POINT ( 'NONE',  ( 0.3798098266300030112, -0.9371975009833265480, 0.7311052114496043863 ) ) ;
#15298=( NAMED_UNIT ( * ) SI_UNIT ( $, .STERADIAN. ) SOLID_ANGLE_UNIT ( ) );
#15303=CARTESIAN_POINT ( 'NONE',  ( 0.3296273898434592398, -1.177227151265824556, 0.4697822230349337769 ) ) ;
#15304=CARTESIAN_POINT ( 'NONE',  ( 0.5549519752308349485, -1.188726111083455939, 0.5935319974400015131 ) ) ;
#15306=CARTESIAN_POINT ( 'NONE',  ( 0.5680013577321684215, -1.617641779642786215, 0.5731888350583983494 ) ) ;
#15307=AXIS2_PLACEMENT_3D ( 'NONE', #39516, #33759, #36835 ) ;
#15311=CARTESIAN_POINT ( 'NONE',  ( 0.5376480657271666130, -1.519209816999901985, 0.5607234942562306923 ) ) ;
#15314=DIRECTION ( 'NONE',  ( 0.4999551463232372317, -0.8660512985181134660, 0.000000000000000000 ) ) ;
#15316=AXIS2_PLACEMENT_3D ( 'NONE', #26152, #13163, #25729 ) ;
#15318=ORIENTED_EDGE ( 'NONE', *, *, #3181, .F. ) ;
#15320=CARTESIAN_POINT ( 'NONE',  ( 0.1576789310610952621, -1.193613890868073790, 0.7517759638675417522 ) ) ;
#15329=CARTESIAN_POINT ( 'NONE',  ( 3.466477128667603047, -1.051097370103299733, 0.4182417262808778013 ) ) ;
#15334=CARTESIAN_POINT ( 'NONE',  ( 0.1882806112850526625, -0.7844922771024498420, 0.6463987001619690975 ) ) ;
#15338=CARTESIAN_POINT ( 'NONE',  ( 0.07485732638563033503, -0.5697853684528622065, 0.2660001439021964509 ) ) ;
#15340=CARTESIAN_POINT ( 'NONE',  ( 0.5953197980378827081, -1.599064723402610300, 0.4311035055375515013 ) ) ;
#15341=CARTESIAN_POINT ( 'NONE',  ( 0.4980091573394558324, -1.195248457127482400, 0.4182417262808778013 ) ) ;
#15346=CARTESIAN_POINT ( 'NONE',  ( 0.5410910530678962882, -1.436320634972935828, 0.7616694271696782259 ) ) ;
#15347=CARTESIAN_POINT ( 'NONE',  ( 0.4693410224259870200, -1.672534098797133328, 0.5641912338472405697 ) ) ;
#15350=CARTESIAN_POINT ( 'NONE',  ( 0.5360537876065293306, -1.620675796450378181, 0.4182417262808775793 ) ) ;
#15352=CARTESIAN_POINT ( 'NONE',  ( 0.3509329672325016136, -1.164895094812919973, 0.4278180645112279468 ) ) ;
#15353=CARTESIAN_POINT ( 'NONE',  ( 0.5753152089321617035, -1.233008725051026655, 0.8518361925389578149 ) ) ;
#15357=CARTESIAN_POINT ( 'NONE',  ( -0.0004424791517057791407, -0.9367167128783578933, 0.1808097727947970967 ) ) ;
#15359=CARTESIAN_POINT ( 'NONE',  ( 0.6465835049539127022, -1.539613817736325441, 0.4282417262808769221 ) ) ;
#15360=CARTESIAN_POINT ( 'NONE',  ( 0.06676919707949596772, -0.8365002846677066506, 0.2371296666657259078 ) ) ;
#15366=DIRECTION ( 'NONE',  ( -0.8374990061932787722, -0.4718101308923743353, 0.2756639530526091564 ) ) ;
#15367=CARTESIAN_POINT ( 'NONE',  ( 0.3121344959780879558, -1.175754444927441300, 0.5182417262812437642 ) ) ;
#15368=CARTESIAN_POINT ( 'NONE',  ( 0.6636790156337686319, -1.488637877925755637, 0.4182417262808777458 ) ) ;
#15371=ORIENTED_EDGE ( 'NONE', *, *, #34575, .F. ) ;
#15373=( BOUNDED_SURFACE ( )  B_SPLINE_SURFACE ( 3, 2, ( 
 ( #27485, #15119, #40428 ),
 ( #30358, #8347, #15546 ),
 ( #36535, #6054, #2186 ),
 ( #2582, #24204, #34049 ),
 ( #40010, #18622, #31180 ),
 ( #17798, #2998, #39605 ) ),
 .UNSPECIFIED., .F., .F., .T. ) 
 B_SPLINE_SURFACE_WITH_KNOTS ( ( 4, 2, 4 ),
 ( 3, 3 ),
 ( -1.028582925126330799E-05, 0.0008016497212322824285, 0.001613585271715828069 ),
 ( 0.000000000000000000, 1.000000000000000000 ),
 .UNSPECIFIED. ) 
 GEOMETRIC_REPRESENTATION_ITEM ( )  RATIONAL_B_SPLINE_SURFACE ( (
 ( 1.000000000000000000, 0.7092489947169868802, 1.000000000000000000),
 ( 1.000000000000000000, 0.7095858694734782368, 1.000000000000000000),
 ( 1.000000000000000000, 0.7098079294007280104, 1.000000000000000000),
 ( 1.000000000000000000, 0.7100340289643065628, 1.000000000000000000),
 ( 1.000000000000000000, 0.7100334978315825385, 1.000000000000000000),
 ( 1.000000000000000000, 0.7099595931732594067, 1.000000000000000000) ) ) 
 REPRESENTATION_ITEM ( '' )  SURFACE ( )  );
#15377=B_SPLINE_CURVE_WITH_KNOTS ( 'NONE', 3,
 ( #13089, #10001, #22573, #6698, #16195, #7097, #6905, #16377, #13290, #10215 ),
 .UNSPECIFIED., .F., .F.,
 ( 4, 2, 2, 2, 4 ),
 ( 4.336808689942017736E-19, 0.0006631238949667744636, 0.001326247789933548494, 0.001989371684900322415, 0.002652495579867096553 ),
 .UNSPECIFIED. ) ;
#15379=CARTESIAN_POINT ( 'NONE',  ( 0.4227732138525802652, -1.178737739220398595, 0.7256702507413027581 ) ) ;
#15382=CARTESIAN_POINT ( 'NONE',  ( 0.3170172301852910435, -0.9601440561661597206, 0.5902234374070133294 ) ) ;
#15383=ORIENTED_EDGE ( 'NONE', *, *, #36623, .F. ) ;
#15389=CARTESIAN_POINT ( 'NONE',  ( 0.3286955653016211953, -1.530979031070108354, 0.8411537230885318683 ) ) ;
#15390=CARTESIAN_POINT ( 'NONE',  ( 0.1637585665034339832, -0.5994899851647166322, 0.1022936816274461203 ) ) ;
#15391=CARTESIAN_POINT ( 'NONE',  ( 0.1123234024242402845, -0.8095807605550189301, -0.06225138739832922902 ) ) ;
#15392=FACE_OUTER_BOUND ( 'NONE', #1750, .T. ) ;
#15394=CARTESIAN_POINT ( 'NONE',  ( 0.3859036440852527394, -1.104769981098987275, 0.6297154657313602799 ) ) ;
#15395=CARTESIAN_POINT ( 'NONE',  ( 0.5367984847559414963, -1.480828653130701555, 0.7264103812508763136 ) ) ;
#15404=CARTESIAN_POINT ( 'NONE',  ( 0.4814184380812144282, -1.664799897621735303, 0.3157417262808778213 ) ) ;
#15405=CARTESIAN_POINT ( 'NONE',  ( 0.5908959048872449715, -1.601544548465861473, 0.4282886817583849703 ) ) ;
#15406=DIRECTION ( 'NONE',  ( -0.4999551463232359549, 0.8660512985181140211, 0.000000000000000000 ) ) ;
#15407=CARTESIAN_POINT ( 'NONE',  ( 0.07959189571600921997, -1.355556588927695927, 0.6171934786799392336 ) ) ;
#15410=CARTESIAN_POINT ( 'NONE',  ( 0.3026114960654325836, -0.9782852559307895213, 0.5634791713200563157 ) ) ;
#15412=CARTESIAN_POINT ( 'NONE',  ( 0.4873759665769543115, -1.128466840950351768, 0.5006193672520922178 ) ) ;
#15413=CARTESIAN_POINT ( 'NONE',  ( 0.4509040138740343928, -1.222352207351879105, 0.6057417262810296243 ) ) ;
#15418=CARTESIAN_POINT ( 'NONE',  ( 0.01373823669757498131, -0.9963338274435274977, 0.5786879937691099540 ) ) ;
#15429=ORIENTED_EDGE ( 'NONE', *, *, #38178, .F. ) ;
#15430=CARTESIAN_POINT ( 'NONE',  ( 0.2709623010280027278, -1.672610760848568967, 0.4891849873696615392 ) ) ;
#15433=CARTESIAN_POINT ( 'NONE',  ( 0.5704759322846583158, -1.412223342220865652, 0.6612748060004949302 ) ) ;
#15434=CARTESIAN_POINT ( 'NONE',  ( 0.001117283261919534186, -0.5756253649193824318, 0.02022279314256347771 ) ) ;
#15439=VERTEX_POINT ( 'NONE', #35708 ) ;
#15440=CARTESIAN_POINT ( 'NONE',  ( 0.06122518135456767735, -0.8600918236809148576, 0.7294040382890789598 ) ) ;
#15441=CARTESIAN_POINT ( 'NONE',  ( 0.3229932430035513113, -1.082493911471395620, 0.7408616947465277436 ) ) ;
#15442=CARTESIAN_POINT ( 'NONE',  ( 0.3224586748600002384, -1.296590453040780799, 0.4182417262808783009 ) ) ;
#15443=CARTESIAN_POINT ( 'NONE',  ( 0.3763421349350077327, -1.150419605846286331, 0.4856841184440788273 ) ) ;
#15450=CARTESIAN_POINT ( 'NONE',  ( 0.1109049718728797040, -0.9286333055842316275, 0.1397141703224096809 ) ) ;
#15453=CARTESIAN_POINT ( 'NONE',  ( 0.5435548342818103951, -1.369150181482250872, 0.7844560790062110600 ) ) ;
#15459=CARTESIAN_POINT ( 'NONE',  ( 0.2297839753664799867, -1.355407543777841228, 1.031615039705529480 ) ) ;
#15461=CARTESIAN_POINT ( 'NONE',  ( 0.4103531506980909738, -1.245885523118785532, 0.5231355499499931172 ) ) ;
#15462=CARTESIAN_POINT ( 'NONE',  ( 0.6596209037232241279, -1.565455939274822184, 0.3157417262808776548 ) ) ;
#15463=CARTESIAN_POINT ( 'NONE',  ( 0.3406212661944226228, -1.061315175790578547, 0.7613082687028679407 ) ) ;
#15469=CARTESIAN_POINT ( 'NONE',  ( 0.05825259049622175112, -1.116031997329672620, 0.7479867058011834269 ) ) ;
#15471=CARTESIAN_POINT ( 'NONE',  ( 0.5405998635167484911, -1.177347015163466182, 0.8538091603066587654 ) ) ;
#15482=CARTESIAN_POINT ( 'NONE',  ( 0.1961652843398811463, -1.362277586928017037, 0.9373159428213221345 ) ) ;
#15483=EDGE_CURVE ( 'NONE', #34692, #32978, #39396, .T. ) ;
#15484=CARTESIAN_POINT ( 'NONE',  ( 0.5887134414239101332, -1.491024950170938945, 0.5921876951808361378 ) ) ;
#15489=CARTESIAN_POINT ( 'NONE',  ( 0.3057296174425681579, -0.8572510462883253801, 0.6221769111833096444 ) ) ;
#15492=CARTESIAN_POINT ( 'NONE',  ( 0.6989129671518158338, -1.435640316137777983, 0.6243391198283677612 ) ) ;
#15498=CARTESIAN_POINT ( 'NONE',  ( 0.1524884462945051700, -0.8417431550776262039, 0.5307603544456596101 ) ) ;
#15500=CARTESIAN_POINT ( 'NONE',  ( 0.4053429200396714283, -1.311055352502511484, 0.8450935282451459418 ) ) ;
#15502=CARTESIAN_POINT ( 'NONE',  ( -0.0007964796033632633252, -0.7717706572747778937, 0.0001241267463302354434 ) ) ;
#15506=CARTESIAN_POINT ( 'NONE',  ( 0.4751225739783559998, -1.681097010791106516, 0.5628964895538534075 ) ) ;
#15508=CARTESIAN_POINT ( 'NONE',  ( 0.7179022346679152511, -1.464906623875073644, 0.7581280492328499321 ) ) ;
#15513=CARTESIAN_POINT ( 'NONE',  ( 0.1678804100208123595, -0.8181538232278317002, 0.2820814646259393044 ) ) ;
#15516=CARTESIAN_POINT ( 'NONE',  ( 0.3137245967586478335, -1.174875666623787840, 0.5369163431172392364 ) ) ;
#15517=CARTESIAN_POINT ( 'NONE',  ( 0.4199047739250627576, -1.021165802582503890, 0.6853183793762346321 ) ) ;
#15520=CARTESIAN_POINT ( 'NONE',  ( 0.4042633028793005678, -1.711240744073932563, 0.4220515681607865388 ) ) ;
#15522=B_SPLINE_CURVE_WITH_KNOTS ( 'NONE', 3,
 ( #12522, #634, #22215, #38219, #18918, #9647, #16028, #34733, #37610, #31454 ),
 .UNSPECIFIED., .F., .F.,
 ( 4, 2, 2, 2, 4 ),
 ( 0.000000000000000000, 0.0005856409713472994797, 0.001171281942694598959, 0.001756922914041898331, 0.002342563885389197919 ),
 .UNSPECIFIED. ) ;
#15525=LINE ( 'NONE', #12423, #12160 ) ;
#15528=CARTESIAN_POINT ( 'NONE',  ( 0.2687203115727492264, -1.674044157977605529, 0.5754666865148680976 ) ) ;
#15532=CARTESIAN_POINT ( 'NONE',  ( 0.1730569967621003735, -1.381888235275370080, 0.5682417262808804326 ) ) ;
#15542=CARTESIAN_POINT ( 'NONE',  ( 0.001045174848116913347, -0.9423331098586125165, 0.1457102695410935345 ) ) ;
#15546=CARTESIAN_POINT ( 'NONE',  ( 0.07601207264773035543, -1.311676598773741764, 0.5551002690229728254 ) ) ;
#15548=CARTESIAN_POINT ( 'NONE',  ( 0.6864989062074844384, -1.545408043237719964, 0.6047936410314285194 ) ) ;
#15549=CARTESIAN_POINT ( 'NONE',  ( 0.07292080638518497193, -0.5442452056136308780, 0.1818665249886239066 ) ) ;
#15552=CARTESIAN_POINT ( 'NONE',  ( 0.6252338399778394340, -1.468100857423625838, 0.5182417262812428760 ) ) ;
#15554=EDGE_CURVE ( 'NONE', #5749, #12702, #21115, .T. ) ;
#15558=CARTESIAN_POINT ( 'NONE',  ( 0.1252279186956127277, -0.5551208408591088439, 0.1884588093939131292 ) ) ;
#15559=CARTESIAN_POINT ( 'NONE',  ( 0.4608582512679273435, -1.674906425203495530, 0.4445187640073551827 ) ) ;
#15566=CARTESIAN_POINT ( 'NONE',  ( 0.1895831464430141888, -0.5047047246472139426, 0.1503823323309240734 ) ) ;
#15568=CARTESIAN_POINT ( 'NONE',  ( 0.04836495276552613132, -1.258574261489486812, 0.6520114206213487584 ) ) ;
#15571=CARTESIAN_POINT ( 'NONE',  ( 0.1614573949321077284, -0.7569534866611321577, 0.1932149833450299559 ) ) ;
#15572=CARTESIAN_POINT ( 'NONE',  ( 0.1645591421022416789, -0.8833852852294274971, 0.5507895711055610377 ) ) ;
#15584=ORIENTED_EDGE ( 'NONE', *, *, #3635, .T. ) ;
#15586=CARTESIAN_POINT ( 'NONE',  ( 0.1802237425427333228, -0.5041004908202411094, 0.1773551390588752052 ) ) ;
#15587=DIRECTION ( 'NONE',  ( 0.1565050148243877226, -0.9876771640241653882, 0.000000000000000000 ) ) ;
#15589=CARTESIAN_POINT ( 'NONE',  ( 0.5012889143793337610, -1.295578934310636976, 0.5940465434816246670 ) ) ;
#15591=VERTEX_POINT ( 'NONE', #15926 ) ;
#15592=CARTESIAN_POINT ( 'NONE',  ( 0.2471460726071840197, -0.9121693139129607442, 0.4829066783201274027 ) ) ;
#15598=ORIENTED_EDGE ( 'NONE', *, *, #10901, .T. ) ;
#15599=CARTESIAN_POINT ( 'NONE',  ( 0.3549369896887015763, -1.516628842544784472, 0.8323203099904163960 ) ) ;
#15601=CARTESIAN_POINT ( 'NONE',  ( 0.1115015552682263461, -0.8978746070190919415, 0.02774221936830248078 ) ) ;
#15606=CARTESIAN_POINT ( 'NONE',  ( 0.3621525574119358049, -1.086908716195545743, 0.6383390412752412146 ) ) ;
#15607=CARTESIAN_POINT ( 'NONE',  ( 0.1617007434535638888, -0.7254083217123186156, 0.5341668825669240173 ) ) ;
#15613=CARTESIAN_POINT ( 'NONE',  ( 0.4343863265072839264, -1.688740028300337981, 0.4182417262807859859 ) ) ;
#15614=CARTESIAN_POINT ( 'NONE',  ( 0.07014435923142441076, -1.325199841737237261, 0.5075297796642793680 ) ) ;
#15617=CARTESIAN_POINT ( 'NONE',  ( 0.4115766028365042128, -1.733048369835246794, 0.5182417262812423209 ) ) ;
#15619=CARTESIAN_POINT ( 'NONE',  ( 0.3310978894898223834, -0.9939147606493616838, 0.5922533870212514095 ) ) ;
#15621=CARTESIAN_POINT ( 'NONE',  ( 0.5434173516999434295, -1.168945995238640068, 0.6057417262810176339 ) ) ;
#15623=( BOUNDED_SURFACE ( )  B_SPLINE_SURFACE ( 3, 2, ( 
 ( #21671, #24350, #24955 ),
 ( #21485, #27636, #2740 ),
 ( #40166, #24167, #34006 ),
 ( #5810, #5398, #30309 ),
 ( #30521, #30916, #15285 ),
 ( #14887, #27844, #24768 ),
 ( #27446, #28055, #8304 ),
 ( #20875, #33396, #39971 ),
 ( #37291, #34200, #11792 ),
 ( #6011, #18576, #31134 ) ),
 .UNSPECIFIED., .F., .F., .T. ) 
 B_SPLINE_SURFACE_WITH_KNOTS ( ( 4, 2, 2, 2, 4 ),
 ( 3, 3 ),
 ( 0.0007871759377455164221, 0.001415437681796649161, 0.002043699425847781900, 0.002671961169898914856, 0.003300222913950047812 ),
 ( 0.000000000000000000, 0.6905130149310136911 ),
 .UNSPECIFIED. ) 
 GEOMETRIC_REPRESENTATION_ITEM ( )  RATIONAL_B_SPLINE_SURFACE ( (
 ( 1.000000000000000000, 0.7888811462077213177, 0.8693229248972149659),
 ( 1.000000000000000000, 0.8426938665563540320, 0.9026315980553327734),
 ( 1.000000000000000000, 0.8781792394491754195, 0.9245961201966287346),
 ( 1.000000000000000000, 0.9251411795240688241, 0.9536643386901670905),
 ( 1.000000000000000000, 0.9360575408707458855, 0.9604212822123805449),
 ( 1.000000000000000000, 0.9355106661221218589, 0.9600827809780565492),
 ( 1.000000000000000000, 0.9241077274843783051, 0.9530246587782127410),
 ( 1.000000000000000000, 0.8766085888055522579, 0.9236239283320455407),
 ( 1.000000000000000000, 0.8402078199309059858, 0.9010927999056310700),
 ( 1.000000000000000000, 0.7857264936582148973, 0.8673702770842413035) ) ) 
 REPRESENTATION_ITEM ( '' )  SURFACE ( )  );
#15624=CARTESIAN_POINT ( 'NONE',  ( 0.1872829031602858685, -1.532932250049839906, 0.6789365607098191147 ) ) ;
#15625=CARTESIAN_POINT ( 'NONE',  ( 0.2713753197625269342, -1.672371506024731724, 0.4877530470170145516 ) ) ;
#15626=CARTESIAN_POINT ( 'NONE',  ( 0.6646178349955912390, -1.445333687840241410, 0.4440966220229920491 ) ) ;
#15628=ORIENTED_EDGE ( 'NONE', *, *, #8372, .F. ) ;
#15634=CARTESIAN_POINT ( 'NONE',  ( 0.5767692940198798635, -1.426262227725163090, 0.5925100300099771511 ) ) ;
#15635=CARTESIAN_POINT ( 'NONE',  ( 0.01043330323478177529, -0.5303232461374860485, 0.1276616220108156841 ) ) ;
#15640=CARTESIAN_POINT ( 'NONE',  ( 0.01139561368625759304, -0.5503006985288143582, 0.2442491123753702531 ) ) ;
#15643=CARTESIAN_POINT ( 'NONE',  ( 0.01208307744763006952, -0.4513789697288763669, 0.03872339057219081199 ) ) ;
#15650=CARTESIAN_POINT ( 'NONE',  ( 0.2475591123417469619, -0.9465702229060155570, 0.7371952982553420242 ) ) ;
#15651=CARTESIAN_POINT ( 'NONE',  ( 0.2702137124954268610, -0.9931619662810967641, 0.7111678352231335376 ) ) ;
#15652=CARTESIAN_POINT ( 'NONE',  ( 0.2702327675951550767, -1.674551853183180894, 0.5944435164687253970 ) ) ;
#15655=CARTESIAN_POINT ( 'NONE',  ( 0.07779920321647403048, -1.322114474344633583, 0.5682417262808776570 ) ) ;
#15656=DIRECTION ( 'NONE',  ( 0.4108529743908185816, -0.9117016142544761559, 0.000000000000000000 ) ) ;
#15661=CARTESIAN_POINT ( 'NONE',  ( 0.08861282632252902303, -1.303734040091387714, 0.7233710302893093802 ) ) ;
#15663=CARTESIAN_POINT ( 'NONE',  ( 0.7167626400851214719, -1.479603991551655895, 0.4558490598962456342 ) ) ;
#15672=CARTESIAN_POINT ( 'NONE',  ( 0.2544140537756520715, -1.595280948316114999, 0.8480660740215214544 ) ) ;
#15673=CARTESIAN_POINT ( 'NONE',  ( 0.5766093525687170374, -1.458620651149859171, 0.7164759587684025322 ) ) ;
#15677=CARTESIAN_POINT ( 'NONE',  ( 0.3484275328463246058, -0.9131724924592886650, 0.6749714385622568313 ) ) ;
#15680=CARTESIAN_POINT ( 'NONE',  ( 0.6762931815487975840, -1.394502623830513155, 0.7319977833246720245 ) ) ;
#15685=CARTESIAN_POINT ( 'NONE',  ( 0.2245517771038092192, -0.9157708072603734095, 0.6589336320736243202 ) ) ;
#15687=CARTESIAN_POINT ( 'NONE',  ( 0.5264717665343396913, -1.526446698549486891, 0.6019642009783892078 ) ) ;
#15688=EDGE_CURVE ( 'NONE', #13751, #4342, #28457, .T. ) ;
#15692=CARTESIAN_POINT ( 'NONE',  ( 0.4697787318353889852, -1.672242315053772854, 0.5632612846970690423 ) ) ;
#15693=CARTESIAN_POINT ( 'NONE',  ( 0.7441773965511153666, -1.515035653583309827, 0.6063620325133788347 ) ) ;
#15697=FACE_OUTER_BOUND ( 'NONE', #11135, .T. ) ;
#15700=CARTESIAN_POINT ( 'NONE',  ( 0.5779297624755960205, -1.623152544610868109, 0.5629341535590222101 ) ) ;
#15701=CARTESIAN_POINT ( 'NONE',  ( 0.2710216717077167936, -1.672577861558078416, 0.4888899872315822237 ) ) ;
#15703=CARTESIAN_POINT ( 'NONE',  ( 0.04206944528682795420, -1.152159445897246393, 0.6964886360393780507 ) ) ;
#15704=CARTESIAN_POINT ( 'NONE',  ( 0.5130887424854349010, -1.117175276521638505, 0.5842416974757255188 ) ) ;
#15708=CARTESIAN_POINT ( 'NONE',  ( 0.5612712793085452567, -1.506471590370649372, 0.5726843098148547417 ) ) ;
#15715=ORIENTED_EDGE ( 'NONE', *, *, #19465, .F. ) ;
#15717=CARTESIAN_POINT ( 'NONE',  ( 0.02680226611402111714, -1.057819507791903257, 0.7331982514440371634 ) ) ;
#15720=DIRECTION ( 'NONE',  ( 0.000000000000000000, 0.000000000000000000, -1.000000000000000000 ) ) ;
#15725=CARTESIAN_POINT ( 'NONE',  ( 0.1676694287369189240, -1.385544946528693089, 0.5182417262812420988 ) ) ;
#15727=VERTEX_POINT ( 'NONE', #21917 ) ;
#15728=CARTESIAN_POINT ( 'NONE',  ( 0.1032975704182374083, -0.6446288055514268756, 0.3563257787039654234 ) ) ;
#15731=CARTESIAN_POINT ( 'NONE',  ( 0.07376662319119976774, -0.5594476950009685812, 0.2363562539228321879 ) ) ;
#15733=CARTESIAN_POINT ( 'NONE',  ( 0.5631207333134724546, -1.617530675893939174, 0.5006452510992012161 ) ) ;
#15735=CARTESIAN_POINT ( 'NONE',  ( 0.3754938372491893328, -1.052735747919861797, 0.6361273785642954648 ) ) ;
#15736=VERTEX_POINT ( 'NONE', #34444 ) ;
#15737=UNCERTAINTY_MEASURE_WITH_UNIT (LENGTH_MEASURE( 1.000000000000000082E-05 ), #1126, 'distance_accuracy_value', 'NONE');
#15738=CARTESIAN_POINT ( 'NONE',  ( 0.3827394763927673971, -1.608088298394132254, 0.5182417262812428760 ) ) ;
#15739=CARTESIAN_POINT ( 'NONE',  ( 0.1887415726803808591, -0.4595355292632672395, 0.1470298804553386296 ) ) ;
#15740=CARTESIAN_POINT ( 'NONE',  ( 0.5808744538588486162, -1.495254402632689050, 0.5726140762454942079 ) ) ;
#15743=DIRECTION ( 'NONE',  ( -0.2929646265539834760, -0.1592115978499541173, 0.9427743074024396153 ) ) ;
#15745=EDGE_CURVE ( 'NONE', #10169, #36413, #36251, .T. ) ;
#15747=CARTESIAN_POINT ( 'NONE',  ( 0.4315909263077353786, -1.207668101024179430, 0.5182417262812423209 ) ) ;
#15749=CARTESIAN_POINT ( 'NONE',  ( 0.3234650319091952331, -0.8156164872106268504, 0.7066254915499745604 ) ) ;
#15751=CARTESIAN_POINT ( 'NONE',  ( 0.03483016372457843624, -1.090556708997785229, 0.6345047942266013319 ) ) ;
#15753=ADVANCED_FACE ( 'NONE', ( #9557 ), #22134, .F. ) ;
#15754=CARTESIAN_POINT ( 'NONE',  ( 0.1963401049631460227, -0.6876817530555039415, 0.3329214951892821017 ) ) ;
#15755=CARTESIAN_POINT ( 'NONE',  ( 0.08509807014988972351, -0.8316410974579127036, 0.1457185332388699350 ) ) ;
#15756=CARTESIAN_POINT ( 'NONE',  ( 0.4062230848227149638, -1.145582794160931117, 0.4248905050063955802 ) ) ;
#15759=ADVANCED_FACE ( 'NONE', ( #22737 ), #3976, .F. ) ;
#15764=CARTESIAN_POINT ( 'NONE',  ( 0.6632759560342388339, -1.473865492997792570, 0.4224349526775863506 ) ) ;
#15765=CARTESIAN_POINT ( 'NONE',  ( 0.07016588152529044942, -0.8342740451934566037, 0.1457185332388703236 ) ) ;
#15772=CARTESIAN_POINT ( 'NONE',  ( 0.4749432869989659856, -1.666646186687757547, 0.4653120090430740707 ) ) ;
#15774=CARTESIAN_POINT ( 'NONE',  ( 0.4662960040860855138, -1.240302083570733016, 0.7040906853573337676 ) ) ;
#15777=CARTESIAN_POINT ( 'NONE',  ( 0.4737957855049246270, -1.072208190283344909, 0.6181471139717461538 ) ) ;
#15780=CARTESIAN_POINT ( 'NONE',  ( 0.01749918469671574162, -0.9360414646517258852, 0.5901500853657657419 ) ) ;
#15783=CARTESIAN_POINT ( 'NONE',  ( 0.3878444664605486536, -1.599983213115868441, 0.6642460123331223043 ) ) ;
#15785=CARTESIAN_POINT ( 'NONE',  ( 0.1848348008737195070, -0.8303121680794297577, 0.06024004532681473401 ) ) ;
#15786=CARTESIAN_POINT ( 'NONE',  ( 0.06840157109000070956, -0.5700798809208006412, 0.05578865808313797359 ) ) ;
#15789=EDGE_LOOP ( 'NONE', ( #10015, #40613, #7977, #4203 ) ) ;
#15793=CARTESIAN_POINT ( 'NONE',  ( 0.5643467867757225864, -1.493973552341269162, 0.6681583330584175417 ) ) ;
#15794=EDGE_LOOP ( 'NONE', ( #40624, #7935, #9658, #39549, #31470, #6324, #16121, #20144, #465 ) ) ;
#15795=CARTESIAN_POINT ( 'NONE',  ( 0.1854530118307023689, -0.8267686003446883536, 0.1092990128771291342 ) ) ;
#15807=CARTESIAN_POINT ( 'NONE',  ( 0.2186326339716475331, -1.240032810101609373, 0.5763875373488478449 ) ) ;
#15811=CARTESIAN_POINT ( 'NONE',  ( 0.2042269006659602204, -0.9243050108670398668, 0.3357924985444922794 ) ) ;
#15812=CARTESIAN_POINT ( 'NONE',  ( 0.1802068938276927546, -1.378362688417822834, 0.4882610536917470490 ) ) ;
#15816=CARTESIAN_POINT ( 'NONE',  ( -0.002083146443013338383, -0.8967360763018588088, 0.1457185332388704624 ) ) ;
#15817=CARTESIAN_POINT ( 'NONE',  ( 0.0001225610919479534636, -0.5774639562824842587, -0.07786294252879151501 ) ) ;
#15823=VERTEX_POINT ( 'NONE', #3584 ) ;
#15830=CARTESIAN_POINT ( 'NONE',  ( 0.5400860642111662280, -1.363031247223201126, 0.7740706644004844428 ) ) ;
#15831=CARTESIAN_POINT ( 'NONE',  ( 0.01027559747412087367, -0.5340578617728122257, 0.1070821439362245192 ) ) ;
#15832=ORIENTED_EDGE ( 'NONE', *, *, #34609, .F. ) ;
#15834=CARTESIAN_POINT ( 'NONE',  ( 0.2031772314465054019, -0.6986852483529358837, 0.3457875108286008192 ) ) ;
#15836=CARTESIAN_POINT ( 'NONE',  ( 0.2061925047406416300, -1.267151160079532435, 0.9188585589093583028 ) ) ;
#15837=CARTESIAN_POINT ( 'NONE',  ( 0.1378772255622009446, -0.8829796579180423377, 0.5385982703296793295 ) ) ;
#15840=CARTESIAN_POINT ( 'NONE',  ( 0.01220508677664999299, -0.4284039737085656996, 0.1457185332388702959 ) ) ;
#15852=CARTESIAN_POINT ( 'NONE',  ( 0.03043063305005027849, -0.5845788966253381291, 0.5517386709610753170 ) ) ;
#15855=CARTESIAN_POINT ( 'NONE',  ( 0.3817504269947160078, -1.726033828776056378, 0.4251703030630522018 ) ) ;
#15859=CARTESIAN_POINT ( 'NONE',  ( 0.1626176757286639796, -0.6782218769987641283, 0.05683303076865411224 ) ) ;
#15865=CARTESIAN_POINT ( 'NONE',  ( 0.002083146443013488870, -0.4777046557262296100, 0.1283381445693447254 ) ) ;
#15866=CARTESIAN_POINT ( 'NONE',  ( 0.1002285206263032746, -1.304924405955540934, 0.7288703187181188037 ) ) ;
#15869=B_SPLINE_CURVE_WITH_KNOTS ( 'NONE', 3,
 ( #37198, #11, #31432, #18894, #21769, #2639, #9018, #12697, #21161, #21579, #30622, #34101, #14985, #34302, #33691, #12493, #5505, #5718 ),
 .UNSPECIFIED., .F., .F.,
 ( 4, 2, 2, 2, 2, 2, 2, 2, 4 ),
 ( 0.000000000000000000, 0.0007429904698459527390, 0.001485980939691905478, 0.002228971409537858217, 0.002971961879383810956, 0.003714952349229763695, 0.004457942819075716434, 0.005200933288921669173, 0.005943923758767621912 ),
 .UNSPECIFIED. ) ;
#15870=AXIS2_PLACEMENT_3D ( 'NONE', #11651, #14732, #18013 ) ;
#15871=CARTESIAN_POINT ( 'NONE',  ( 0.7025991982850786632, -1.521397541714836210, 0.5686247791543105334 ) ) ;
#15872=VERTEX_POINT ( 'NONE', #10372 ) ;
#15873=CARTESIAN_POINT ( 'NONE',  ( 0.1850410792631035362, -0.8547936666690981733, 0.1477569985384108442 ) ) ;
#15875=LINE ( 'NONE', #32861, #36196 ) ;
#15876=CARTESIAN_POINT ( 'NONE',  ( 0.2746276767615154490, -1.658875007953147573, 0.7201787504598219369 ) ) ;
#15878=CARTESIAN_POINT ( 'NONE',  ( 0.1317540737835983244, -0.5510263468228310257, 0.1532934214773048198 ) ) ;
#15880=CARTESIAN_POINT ( 'NONE',  ( 0.5446207946416926626, -1.171030664636589114, 0.5955391433021992587 ) ) ;
#15883=ORIENTED_EDGE ( 'NONE', *, *, #34374, .T. ) ;
#15884=CARTESIAN_POINT ( 'NONE',  ( 0.6672263256168233791, -1.559577713309469038, 0.6159734170043378310 ) ) ;
#15885=EDGE_LOOP ( 'NONE', ( #11682, #531, #13261, #40019, #360, #39171 ) ) ;
#15892=ORIENTED_EDGE ( 'NONE', *, *, #20852, .F. ) ;
#15893=CARTESIAN_POINT ( 'NONE',  ( 0.1135430571860531063, -0.7812966806583707680, 0.4098588298052969758 ) ) ;
#15895=CARTESIAN_POINT ( 'NONE',  ( 0.5249336263842677708, -1.526781716017400647, 0.5684230341163545308 ) ) ;
#15900=CARTESIAN_POINT ( 'NONE',  ( 0.6520986873597004463, -1.511863584991765208, 0.7630484353180611024 ) ) ;
#15902=CARTESIAN_POINT ( 'NONE',  ( 0.6098080674161761028, -1.478513402567430912, 0.5979631250306651769 ) ) ;
#15908=CARTESIAN_POINT ( 'NONE',  ( 0.5132401252193277141, -1.118795806750195077, 0.5530176081283582068 ) ) ;
#15919=CARTESIAN_POINT ( 'NONE',  ( 0.1850825143922525950, -0.8517056288164835953, 0.1806043688250910384 ) ) ;
#15921=CARTESIAN_POINT ( 'NONE',  ( 0.3206535937437295369, -1.182295409031864697, 0.3157417262808777658 ) ) ;
#15922=CARTESIAN_POINT ( 'NONE',  ( 0.01814112910464814668, -1.016494997226478070, 0.7024430388243299017 ) ) ;
#15926=CARTESIAN_POINT ( 'NONE',  ( 0.6929208297549553919, -1.429122597532291650, 0.5682417262808779901 ) ) ;
#15938=CARTESIAN_POINT ( 'NONE',  ( 0.08990515874724799850, -0.5631160408504091164, 0.1543070364275382633 ) ) ;
#15939=EDGE_LOOP ( 'NONE', ( #35964, #37422, #11788, #9765, #5423, #7931, #32114 ) ) ;
#15943=AXIS2_PLACEMENT_3D ( 'NONE', #32852, #4655, #635 ) ;
#15944=CARTESIAN_POINT ( 'NONE',  ( 0.2282559409138358864, -1.032523682450960267, 0.8073022102877677186 ) ) ;
#15948=CARTESIAN_POINT ( 'NONE',  ( 0.2487277522598718149, -0.9673568096827294127, 0.5239956023218622638 ) ) ;
#15951=CARTESIAN_POINT ( 'NONE',  ( 0.1897189402164200511, -0.5341521847524689504, 0.1523768035615612193 ) ) ;
#15952=CARTESIAN_POINT ( 'NONE',  ( 0.1298170261405827419, -0.5953669216844625911, 0.3065043694650786965 ) ) ;
#15956=FACE_OUTER_BOUND ( 'NONE', #35545, .T. ) ;
#15959=CARTESIAN_POINT ( 'NONE',  ( 0.3005352500653590830, -1.024020065930653756, 0.7747702324826710729 ) ) ;
#15961=CARTESIAN_POINT ( 'NONE',  ( 0.2413003582545148740, -0.7023676887333554220, 0.5126316699731913173 ) ) ;
#15962=CARTESIAN_POINT ( 'NONE',  ( 0.4824008369422878584, -1.130704479788579464, 0.4427808555068210583 ) ) ;
#15963=CARTESIAN_POINT ( 'NONE',  ( 0.02842665824954763304, -1.107459934983165972, 0.6590139982913070238 ) ) ;
#15964=VECTOR ( 'NONE', #35342, 39.37007874015748854 ) ;
#15969=EDGE_CURVE ( 'NONE', #16305, #23498, #1958, .T. ) ;
#15970=CARTESIAN_POINT ( 'NONE',  ( 0.6111956757316053812, -1.601608420676993827, 0.4350745821225746046 ) ) ;
#15975=CARTESIAN_POINT ( 'NONE',  ( 0.3470843243164753456, -1.069660623632250784, 0.7669445845107666360 ) ) ;
#15977=CARTESIAN_POINT ( 'NONE',  ( 0.6555154469717897614, -1.476457112295515905, 0.4182417262808776903 ) ) ;
#15979=CARTESIAN_POINT ( 'NONE',  ( 0.3607791945725288829, -1.125243654965698337, 0.6038723418466845905 ) ) ;
#15986=CARTESIAN_POINT ( 'NONE',  ( 0.4880443886438106116, -1.659886120534822096, 0.5165855446388504246 ) ) ;
#15988=EDGE_CURVE ( 'NONE', #32917, #23555, #24757, .T. ) ;
#15989=CARTESIAN_POINT ( 'NONE',  ( 0.4978345755714322918, -1.288570401096832407, 0.6247038493719151431 ) ) ;
#15990=CARTESIAN_POINT ( 'NONE',  ( 0.3183458363839229421, -1.763251125072305969, 0.5158787115206079354 ) ) ;
#15991=CARTESIAN_POINT ( 'NONE',  ( 0.4241296934850513067, -1.044958113096912777, 0.6349482895397999815 ) ) ;
#15992=EDGE_LOOP ( 'NONE', ( #30727, #18473, #142, #23857, #1590, #17049 ) ) ;
#15995=CARTESIAN_POINT ( 'NONE',  ( -0.002130502458654864786, -0.8570779732651497840, 0.2369880927919252311 ) ) ;
#15997=CARTESIAN_POINT ( 'NONE',  ( 0.3871526695961494124, -1.595276482059940548, 0.6939178973677117002 ) ) ;
#15998=CARTESIAN_POINT ( 'NONE',  ( 0.08661364503105330181, -0.7606219696568068400, 0.02128811888083972578 ) ) ;
#15999=CARTESIAN_POINT ( 'NONE',  ( 0.1744619341259203982, -0.9164761487563395370, 0.1198935801002234819 ) ) ;
#16000=CARTESIAN_POINT ( 'NONE',  ( 0.06923712653936904549, -0.5400029222721455247, 0.1457185332388703236 ) ) ;
#16004=B_SPLINE_CURVE_WITH_KNOTS ( 'NONE', 3,
 ( #3211, #21957, #22171, #5876 ),
 .UNSPECIFIED., .F., .F.,
 ( 4, 4 ),
 ( 0.007879993664335074866, 0.008137213426454060344 ),
 .UNSPECIFIED. ) ;
#16006=CARTESIAN_POINT ( 'NONE',  ( 0.3244236418308351078, -1.295451955201979866, 0.5689238818033025558 ) ) ;
#16007=CARTESIAN_POINT ( 'NONE',  ( 0.3203573007257789484, -1.073668807559134519, 0.7999796645404516626 ) ) ;
#16021=CARTESIAN_POINT ( 'NONE',  ( 0.5264113014007820723, -1.640729993778254014, 0.5682417262808777680 ) ) ;
#16022=CARTESIAN_POINT ( 'NONE',  ( 0.1698555401406868226, -1.244443917810318823, 0.6163427178748981383 ) ) ;
#16027=CARTESIAN_POINT ( 'NONE',  ( 0.1875000000000002498, -0.9151275355372966436, 0.1457185332388701016 ) ) ;
#16028=CARTESIAN_POINT ( 'NONE',  ( 0.3164589185008098160, -1.173239401124993364, 0.4880957576780184937 ) ) ;
#16029=CARTESIAN_POINT ( 'NONE',  ( 0.4509257687968690753, -1.222389892490845620, 0.5856983068965044836 ) ) ;
#16031=CARTESIAN_POINT ( 'NONE',  ( 0.1849096901904442591, -1.549205955729530793, 0.5682417262808778791 ) ) ;
#16032=CARTESIAN_POINT ( 'NONE',  ( -0.0003565257878083244957, -0.9235813610340595226, 0.06569692014612905917 ) ) ;
#16037=AXIS2_PLACEMENT_3D ( 'NONE', #39588, #16989, #35914 ) ;
#16046=CARTESIAN_POINT ( 'NONE',  ( 0.4914727279001435689, -1.286330727027781728, 0.8049515525046259112 ) ) ;
#16048=EDGE_LOOP ( 'NONE', ( #23844, #21915 ) ) ;
#16054=CARTESIAN_POINT ( 'NONE',  ( 0.2979046102063983015, -1.656890573677640921, 0.5828864586326335528 ) ) ;
#16055=CARTESIAN_POINT ( 'NONE',  ( 0.6396152150128876501, -1.561615300510546200, 0.4193375745894342144 ) ) ;
#16058=CARTESIAN_POINT ( 'NONE',  ( 0.1877036592482687616, -0.9196856789278203825, 0.1015045423513593059 ) ) ;
#16059=CARTESIAN_POINT ( 'NONE',  ( 0.4191100986680896257, -1.701672718972387477, 0.4233639548768124428 ) ) ;
#16063=CARTESIAN_POINT ( 'NONE',  ( 0.1862143093560912621, -0.9153542374866666664, 0.1462684119608146649 ) ) ;
#16066=CARTESIAN_POINT ( 'NONE',  ( 0.1773078868329161784, -0.8723994076705423595, 0.5291939128694373995 ) ) ;
#16071=CARTESIAN_POINT ( 'NONE',  ( 0.4870128057575630054, -1.169653738304198054, 0.4224702079871185401 ) ) ;
#16073=AXIS2_PLACEMENT_3D ( 'NONE', #2848, #8595, #36992 ) ;
#16078=CARTESIAN_POINT ( 'NONE',  ( 0.1854100492481942641, -0.7689184785536463673, 0.1457185332388699350 ) ) ;
#16085=CARTESIAN_POINT ( 'NONE',  ( 0.1155264449205179456, -1.390086609329345801, 0.6489119185965581682 ) ) ;
#16090=B_SPLINE_CURVE_WITH_KNOTS ( 'NONE', 3,
 ( #37260, #15463, #40548, #12368, #19158, #6187, #9268, #3113, #9480, #490, #34980, #21845, #34370, #12989, #22062, #25536, #18755, #31305 ),
 .UNSPECIFIED., .F., .F.,
 ( 4, 2, 2, 2, 2, 2, 2, 2, 4 ),
 ( 0.01935643071104403007, 0.02032766186723907603, 0.02129889302343412200, 0.02227012417962916796, 0.02324135533582421392, 0.02421258649201925989, 0.02518381764821430238, 0.02615504880440934835, 0.02712627996060439431 ),
 .UNSPECIFIED. ) ;
#16091=CARTESIAN_POINT ( 'NONE',  ( 0.6544078563150221850, -1.544269123161552626, 0.4241055859090109292 ) ) ;
#16092=CARTESIAN_POINT ( 'NONE',  ( 0.1969360143439681521, -0.5736523733507086220, 0.3127385286629807970 ) ) ;
#16095=CARTESIAN_POINT ( 'NONE',  ( 0.2665534027467502676, -1.663858438167157283, 0.7214166325115675127 ) ) ;
#16098=CARTESIAN_POINT ( 'NONE',  ( 0.4326761725401005454, -1.237000291097626770, 0.8252275854053723325 ) ) ;
#16112=CARTESIAN_POINT ( 'NONE',  ( 0.2614565024141662919, -0.7584087153545726601, 0.1023043458361303226 ) ) ;
#16114=CARTESIAN_POINT ( 'NONE',  ( 0.1896256107075826869, -0.8716025430740738100, 0.6086388917311702507 ) ) ;
#16116=CARTESIAN_POINT ( 'NONE',  ( 0.08990936761269915922, -0.5436479961250830772, 0.1370866209488758314 ) ) ;
#16118=CARTESIAN_POINT ( 'NONE',  ( 0.1184657642459996246, -0.6327582549063645034, 0.3942365859262391692 ) ) ;
#16121=ORIENTED_EDGE ( 'NONE', *, *, #24094, .T. ) ;
#16122=CARTESIAN_POINT ( 'NONE',  ( 0.4034423500592668188, -1.711423766529257762, 0.6205252146552449055 ) ) ;
#16123=CARTESIAN_POINT ( 'NONE',  ( 0.6671799058731299192, -1.556892339446394269, 0.6418398848070931972 ) ) ;
#16126=CARTESIAN_POINT ( 'NONE',  ( 0.1356025888936704948, -0.5758974039257369615, 0.2504448515252820084 ) ) ;
#16131=AXIS2_PLACEMENT_3D ( 'NONE', #36234, #30259, #17916 ) ;
#16133=CARTESIAN_POINT ( 'NONE',  ( 0.02591418161326580066, -1.064383994110095877, 0.6545759956939124491 ) ) ;
#16134=CARTESIAN_POINT ( 'NONE',  ( 0.5003933895997771941, -1.101010879683239629, 0.6202731239902519178 ) ) ;
#16136=DIRECTION ( 'NONE',  ( 0.4999551463232372317, -0.8660512985181135770, 0.000000000000000000 ) ) ;
#16144=CARTESIAN_POINT ( 'NONE',  ( 0.08794433374487309329, -0.6550045186490311977, 0.02677513513356245822 ) ) ;
#16147=CARTESIAN_POINT ( 'NONE',  ( 0.06554679988413804337, -1.239417238573976787, 0.7589085834725802782 ) ) ;
#16153=CARTESIAN_POINT ( 'NONE',  ( 0.3540817610093318635, -1.633452470505663667, 0.5182417262812423209 ) ) ;
#16155=CARTESIAN_POINT ( 'NONE',  ( 0.1837188672183508453, -1.376100911138345761, 0.5510147385948768184 ) ) ;
#16158=ORIENTED_EDGE ( 'NONE', *, *, #34775, .F. ) ;
#16159=CARTESIAN_POINT ( 'NONE',  ( 0.2237400956572660471, -0.6730011667035054046, 0.6888067665799237904 ) ) ;
#16162=EDGE_LOOP ( 'NONE', ( #29651, #30620, #1497, #35410, #14791, #20849, #18005 ) ) ;
#16163=CARTESIAN_POINT ( 'NONE',  ( 0.2241624023114427433, -0.8762251062628222398, 0.6812710069543531644 ) ) ;
#16166=CARTESIAN_POINT ( 'NONE',  ( 0.001988497880919273385, -0.4774668436778984892, 0.3122510010075223441 ) ) ;
#16167=CARTESIAN_POINT ( 'NONE',  ( 0.07778086292406850843, -0.5899326820504365854, 0.3178732319592481037 ) ) ;
#16168=CARTESIAN_POINT ( 'NONE',  ( 0.03036294788238842746, -0.7483465999182054018, 0.6255648834759816035 ) ) ;
#16170=CARTESIAN_POINT ( 'NONE',  ( 0.6127029595038788745, -1.475330056106460175, 0.4882469897972008255 ) ) ;
#16171=CARTESIAN_POINT ( 'NONE',  ( 0.1410436376702208783, -0.9237311270473411717, 0.1925856316968101722 ) ) ;
#16173=DIRECTION ( 'NONE',  ( 0.01265474379914247223, 0.8659329421511292590, -0.4999999971568669932 ) ) ;
#16175=CARTESIAN_POINT ( 'NONE',  ( 0.2439137596789311413, -0.8887190363322325926, 0.6933903873120049743 ) ) ;
#16180=CARTESIAN_POINT ( 'NONE',  ( 0.2143793204313029777, -0.6499299462495844448, 0.4116214953459712556 ) ) ;
#16182=CARTESIAN_POINT ( 'NONE',  ( 0.02461225487835269621, -1.084833808655251364, 0.6449087556199543103 ) ) ;
#16185=CARTESIAN_POINT ( 'NONE',  ( 0.1923911736828807784, -0.6113561202327233435, 0.3150503200843174922 ) ) ;
#16186=CARTESIAN_POINT ( 'NONE',  ( 0.1876172797476865217, -0.9222972260603201633, 0.6278714507645634102 ) ) ;
#16189=PLANE ( 'NONE',  #25192 ) ;
#16191=ORIENTED_EDGE ( 'NONE', *, *, #28286, .T. ) ;
#16195=CARTESIAN_POINT ( 'NONE',  ( 0.1077839203105155352, -1.313547715378476477, 0.4360033019131892562 ) ) ;
#16199=EDGE_CURVE ( 'NONE', #40356, #11170, #22080, .T. ) ;
#16204=CARTESIAN_POINT ( 'NONE',  ( 0.5114492881455343642, -1.312534973236980207, 0.6060176179980171218 ) ) ;
#16206=CARTESIAN_POINT ( 'NONE',  ( 0.3177034180418226716, -1.763592183760435139, 0.5237719207440205693 ) ) ;
#16207=CARTESIAN_POINT ( 'NONE',  ( 0.4927680500253098783, -1.082617619565096723, 0.5740975660237009892 ) ) ;
#16209=CARTESIAN_POINT ( 'NONE',  ( 0.03244452491656055204, -0.9937768954163109791, 0.6733904430455559531 ) ) ;
#16210=VERTEX_POINT ( 'NONE', #35819 ) ;
#16212=CARTESIAN_POINT ( 'NONE',  ( 0.2241274359060463905, -1.183323756640323188, 0.8809317799930992399 ) ) ;
#16213=CARTESIAN_POINT ( 'NONE',  ( 0.08638846605571078030, -0.7763520792700653317, 0.03197444058538126410 ) ) ;
#16214=CARTESIAN_POINT ( 'NONE',  ( 0.1745799861983162171, -0.9110852329601157873, 0.09004006346363319091 ) ) ;
#16218=CARTESIAN_POINT ( 'NONE',  ( 0.5382321766149011921, -1.161161941655080465, 0.5682417262808779901 ) ) ;
#16219=CARTESIAN_POINT ( 'NONE',  ( 0.5679525285178691485, -1.502762679576377547, 0.6000120267691632092 ) ) ;
#16229=CARTESIAN_POINT ( 'NONE',  ( 0.5225354986670117663, -1.146792065252953297, 0.8742509268737332917 ) ) ;
#16230=EDGE_CURVE ( 'NONE', #8849, #10513, #23009, .T. ) ;
#16233=DIRECTION ( 'NONE',  ( 0.8660512985181133550, 0.4999551463232372317, 0.000000000000000000 ) ) ;
#16241=CARTESIAN_POINT ( 'NONE',  ( 0.003124719664520334353, -0.5686731593868922241, 0.1635439462316863046 ) ) ;
#16242=CARTESIAN_POINT ( 'NONE',  ( -0.0001024326674552539332, -0.7830864717413182907, -0.08467859722999726557 ) ) ;
#16244=AXIS2_PLACEMENT_3D ( 'NONE', #20847, #17336, #11363 ) ;
#16245=CARTESIAN_POINT ( 'NONE',  ( 0.3668746095265680296, -1.158496670723083710, 0.4182417262808777458 ) ) ;
#16251=CARTESIAN_POINT ( 'NONE',  ( 0.3794340307020034886, -1.736095262011157825, 0.4301452658221664449 ) ) ;
#16253=CARTESIAN_POINT ( 'NONE',  ( 0.5048440467754061745, -1.307303468802018864, 0.7988581323005864432 ) ) ;
#16255=ORIENTED_EDGE ( 'NONE', *, *, #27792, .F. ) ;
#16256=ORIENTED_EDGE ( 'NONE', *, *, #8448, .F. ) ;
#16257=CARTESIAN_POINT ( 'NONE',  ( 0.1927077495703349852, -0.8180328145591141409, 0.2791508387892263077 ) ) ;
#16259=CARTESIAN_POINT ( 'NONE',  ( 0.3001998578127315076, -1.656212505849981698, 0.6213433347872623358 ) ) ;
#16261=CARTESIAN_POINT ( 'NONE',  ( 0.1115696861367231063, -0.8921960531934336469, 0.01816369405970581427 ) ) ;
#16263=FACE_OUTER_BOUND ( 'NONE', #1695, .T. ) ;
#16267=CARTESIAN_POINT ( 'NONE',  ( 0.1942853770376357925, -0.8441127787454487663, 0.2952251170591385088 ) ) ;
#16269=CARTESIAN_POINT ( 'NONE',  ( 0.6018439701642503969, -1.465521054425967362, 0.6780457446538449284 ) ) ;
#16272=CARTESIAN_POINT ( 'NONE',  ( 0.4227463786284310632, -1.145941386794042671, 0.4182417262808777458 ) ) ;
#16287=CARTESIAN_POINT ( 'NONE',  ( 0.3561222603844115264, -1.742508409003949987, 0.4387334599642109811 ) ) ;
#16292=CARTESIAN_POINT ( 'NONE',  ( 0.3564258580595303649, -1.150190177429248672, 0.4382532076974842705 ) ) ;
#16294=CARTESIAN_POINT ( 'NONE',  ( 0.1058947752955989308, -1.412241959666070912, 0.5633263997903267262 ) ) ;
#16295=CARTESIAN_POINT ( 'NONE',  ( 0.2711279843670483802, -1.680576011916085521, 0.6848605795586665268 ) ) ;
#16296=ADVANCED_FACE ( 'NONE', ( #27989 ), #12542, .F. ) ;
#16297=CARTESIAN_POINT ( 'NONE',  ( 0.1317540737835982967, -0.5510263468228310257, 0.1457185332388695742 ) ) ;
#16305=VERTEX_POINT ( 'NONE', #33738 ) ;
#16310=EDGE_LOOP ( 'NONE', ( #37097, #23026 ) ) ;
#16311=CARTESIAN_POINT ( 'NONE',  ( 0.1340034493811799732, -0.8053594121975541364, 0.4832924993268126190 ) ) ;
#16313=CARTESIAN_POINT ( 'NONE',  ( 0.06924669681850037506, -0.5400070402892428456, 0.1467347635635346537 ) ) ;
#16314=CARTESIAN_POINT ( 'NONE',  ( 0.5390309913773138062, -1.513666831327822537, 0.6478081614881986416 ) ) ;
#16318=CARTESIAN_POINT ( 'NONE',  ( 0.3715339819472113225, -1.730447381542274066, 0.6049165315556401801 ) ) ;
#16319=CARTESIAN_POINT ( 'NONE',  ( 0.6898418300915178936, -1.417705155587995369, 0.6911030477506114877 ) ) ;
#16320=CARTESIAN_POINT ( 'NONE',  ( 0.1048591973540500683, -1.410537849644770025, 0.5682417262808777680 ) ) ;
#16321=CARTESIAN_POINT ( 'NONE',  ( 0.6011624602559976216, -1.464707089772093740, 0.6803405452985709090 ) ) ;
#16324=CARTESIAN_POINT ( 'NONE',  ( 0.2320755761173002307, -1.232873731908348480, 0.4177417262808779674 ) ) ;
#16327=CARTESIAN_POINT ( 'NONE',  ( 0.0008242595369169036616, -0.9534780057342879811, 0.2825590231195395652 ) ) ;
#16328=CARTESIAN_POINT ( 'NONE',  ( 0.4004013247085298488, -1.001184149470538909, 0.6774742858917212063 ) ) ;
#16330=DIRECTION ( 'NONE',  ( 0.000000000000000000, 0.8660489055767764954, 0.4999592914920847897 ) ) ;
#16331=CARTESIAN_POINT ( 'NONE',  ( 0.3806791355520856568, -1.717835243773888854, 0.4208876441603489615 ) ) ;
#16335=CARTESIAN_POINT ( 'NONE',  ( 0.01055999354155550199, -0.5296565605740121141, 0.1467999231854481279 ) ) ;
#16336=CARTESIAN_POINT ( 'NONE',  ( 0.1857430203655689449, -0.8056635886342103925, 0.2698372336795830662 ) ) ;
#16337=ORIENTED_EDGE ( 'NONE', *, *, #35891, .T. ) ;
#16338=CARTESIAN_POINT ( 'NONE',  ( 0.1438681892407857876, -1.284094082863941111, 0.3157417262808777658 ) ) ;
#16339=CARTESIAN_POINT ( 'NONE',  ( 0.6789872039812443472, -1.407470790535994221, 0.5375528621076278712 ) ) ;
#16341=ORIENTED_EDGE ( 'NONE', *, *, #15554, .F. ) ;
#16344=ORIENTED_EDGE ( 'NONE', *, *, #39380, .T. ) ;
#16350=CARTESIAN_POINT ( 'NONE',  ( 0.04687500000000013878, -0.4345172148286635116, 0.1457185332388691301 ) ) ;
#16351=CARTESIAN_POINT ( 'NONE',  ( 0.1770748127338239997, -0.8007700866384124261, 0.6050427707434069546 ) ) ;
#16352=EDGE_LOOP ( 'NONE', ( #2078, #29707, #23906, #16337, #26790, #38646, #20904 ) ) ;
#16353=CARTESIAN_POINT ( 'NONE',  ( 0.01610093497955936842, -0.4922387448986250136, 0.3764339700947045286 ) ) ;
#16354=CARTESIAN_POINT ( 'NONE',  ( 0.4697542972204731826, -1.557995369357642934, 0.5737367010564736747 ) ) ;
#16358=CARTESIAN_POINT ( 'NONE',  ( 0.4442549097070609410, -1.097829417026605858, 0.6115672446538368279 ) ) ;
#16365=CARTESIAN_POINT ( 'NONE',  ( 0.5195754528810989648, -1.145330933930835959, 0.8096739517683957388 ) ) ;
#16366=CARTESIAN_POINT ( 'NONE',  ( 0.4571661123351543066, -1.116215641761870936, 0.5698312831065212025 ) ) ;
#16367=CARTESIAN_POINT ( 'NONE',  ( 0.06792916418419493729, -1.318672173847188711, 0.5972585457936512299 ) ) ;
#16369=CARTESIAN_POINT ( 'NONE',  ( 0.1949081798141291400, -0.7265219913688031328, 0.3259659631419143944 ) ) ;
#16370=CARTESIAN_POINT ( 'NONE',  ( 0.3363202282376455132, -1.061977972960397976, 0.7384839447874953500 ) ) ;
#16371=CARTESIAN_POINT ( 'NONE',  ( 0.5164663794816727327, -1.539710880569944207, 0.5182417262812423209 ) ) ;
#16372=CARTESIAN_POINT ( 'NONE',  ( 0.6174474092321283747, -1.596955002812002089, 0.4316719645203795364 ) ) ;
#16377=CARTESIAN_POINT ( 'NONE',  ( 0.1429230018409890501, -1.294172685953591362, 0.4193902154642965563 ) ) ;
#16378=B_SPLINE_CURVE_WITH_KNOTS ( 'NONE', 3,
 ( #35629, #9923, #19609, #32541, #918, #13422 ),
 .UNSPECIFIED., .F., .F.,
 ( 4, 2, 4 ),
 ( 0.000000000000000000, 0.5000000000000000000, 1.000000000000000000 ),
 .UNSPECIFIED. ) ;
#16381=CARTESIAN_POINT ( 'NONE',  ( 0.1863410289239364470, -0.5450895766423083932, 0.2630702390344190622 ) ) ;
#16383=CARTESIAN_POINT ( 'NONE',  ( 0.3917195419103990384, -1.137763892611062699, 0.7222388353537541050 ) ) ;
#16386=CARTESIAN_POINT ( 'NONE',  ( 0.4912263342062789806, -1.081771733098906729, 0.5857582446664630904 ) ) ;
#16387=ORIENTED_EDGE ( 'NONE', *, *, #10680, .T. ) ;
#16390=EDGE_LOOP ( 'NONE', ( #32671, #28792, #3489, #32013 ) ) ;
#16392=CARTESIAN_POINT ( 'NONE',  ( 0.3157976591183140336, -1.353229759395969678, 0.8845812709865115142 ) ) ;
#16394=CARTESIAN_POINT ( 'NONE',  ( 0.1747443221411794922, -0.8985867114839785064, 0.05431702021998949942 ) ) ;
#16396=EDGE_LOOP ( 'NONE', ( #23305, #14603, #22595, #34057 ) ) ;
#16397=B_SPLINE_CURVE_WITH_KNOTS ( 'NONE', 3,
 ( #35037, #19428, #31961, #3778, #728, #13229, #38322, #13443, #35858, #936, #29478, #35440 ),
 .UNSPECIFIED., .F., .F.,
 ( 4, 2, 2, 2, 2, 4 ),
 ( 0.001615335599980241782, 0.002213674370351530803, 0.002812013140722820041, 0.003410351911094108845, 0.003709521296279748477, 0.004008690681465387241 ),
 .UNSPECIFIED. ) ;
#16400=CARTESIAN_POINT ( 'NONE',  ( 0.4113960816100760698, -1.246834456972530703, 0.8355117767174224941 ) ) ;
#16402=CARTESIAN_POINT ( 'NONE',  ( 0.1874578000378240850, -0.6893444085712847613, 0.06304793604024336307 ) ) ;
#16409=DIRECTION ( 'NONE',  ( 0.8660512985181134660, 0.4999551463232372872, 0.000000000000000000 ) ) ;
#16410=LINE ( 'NONE', #28769, #25934 ) ;
#16411=CARTESIAN_POINT ( 'NONE',  ( 0.3200662685693974052, -1.759564150209586897, 0.5682417262808787672 ) ) ;
#16412=CARTESIAN_POINT ( 'NONE',  ( 0.09095675709397832431, -1.344211122730877506, 0.7083116771559543334 ) ) ;
#16418=CARTESIAN_POINT ( 'NONE',  ( 0.1840090184099318349, -0.5566218984093596056, 0.02008366405345159145 ) ) ;
#16419=CARTESIAN_POINT ( 'NONE',  ( 0.4264813724157178187, -1.236570049007190919, 0.4854677512712051723 ) ) ;
#16421=CARTESIAN_POINT ( 'NONE',  ( 0.2518326032030922534, -1.639413698222365046, 0.7148483533190357342 ) ) ;
#16427=EDGE_LOOP ( 'NONE', ( #39071, #6105, #5386, #5659, #8190, #7063, #20495, #32716 ) ) ;
#16429=CARTESIAN_POINT ( 'NONE',  ( 0.1727391575749071539, -1.224311773214861176, 0.5182417262812423209 ) ) ;
#16433=CARTESIAN_POINT ( 'NONE',  ( 0.4994410488334536380, -1.297393737506421951, 0.7727712239381648862 ) ) ;
#16437=CARTESIAN_POINT ( 'NONE',  ( 0.3392765801623501276, -0.9012043381553855870, 0.6651284465457234507 ) ) ;
#16443=CARTESIAN_POINT ( 'NONE',  ( 0.07674151747445530358, -0.8568903145152425571, 0.7207360041014601038 ) ) ;
#16445=CARTESIAN_POINT ( 'NONE',  ( 0.1110248181161190423, -0.9270180154169346265, 0.1138591024880182823 ) ) ;
#16451=VERTEX_POINT ( 'NONE', #34751 ) ;
#16453=EDGE_CURVE ( 'NONE', #3787, #16305, #10263, .T. ) ;
#16455=CARTESIAN_POINT ( 'NONE',  ( 0.1868366425318004342, -0.9712607208092176592, 0.5097868630048105754 ) ) ;
#16457=CARTESIAN_POINT ( 'NONE',  ( 0.5762190745332915753, -1.421659016055986990, 0.7172490134945124218 ) ) ;
#16458=CARTESIAN_POINT ( 'NONE',  ( 0.3788791674705027090, -1.253375940808735489, 0.6247566768318951747 ) ) ;
#16460=CARTESIAN_POINT ( 'NONE',  ( 0.3405242896115074913, -1.744906522954273731, 0.4484829386636806081 ) ) ;
#16461=B_SPLINE_CURVE_WITH_KNOTS ( 'NONE', 3,
 ( #9804, #22376, #26265, #13891, #11037, #26465 ),
 .UNSPECIFIED., .F., .F.,
 ( 4, 2, 4 ),
 ( 0.000000000000000000, 0.0005950409463462349047, 0.001190081892692469809 ),
 .UNSPECIFIED. ) ;
#16463=CARTESIAN_POINT ( 'NONE',  ( 0.4000099798367660608, -1.704638381955401183, 0.4182417262808776903 ) ) ;
#16465=EDGE_CURVE ( 'NONE', #34098, #34794, #7304, .T. ) ;
#16466=LINE ( 'NONE', #25733, #23380 ) ;
#16471=CARTESIAN_POINT ( 'NONE',  ( 0.1807325509464224600, -0.4982638852683227704, 0.1182772881561286321 ) ) ;
#16477=DIRECTION ( 'NONE',  ( 0.4987694591008374201, -0.8667346922030165768, 0.000000000000000000 ) ) ;
#16482=CARTESIAN_POINT ( 'NONE',  ( 0.1318168234680600626, -0.5697357792748470873, 0.2343947008844321500 ) ) ;
#16491=PLANE ( 'NONE',  #1425 ) ;
#16496=CARTESIAN_POINT ( 'NONE',  ( 0.002000609201561052118, -0.6339827964191878662, -0.01138449076159552854 ) ) ;
#16499=CARTESIAN_POINT ( 'NONE',  ( 0.09914491568847688674, -0.8039099662830504478, 0.3344751936899787448 ) ) ;
#16502=CARTESIAN_POINT ( 'NONE',  ( 0.1151237624173331725, -0.5938742608929095113, 0.3101306348406044910 ) ) ;
#16504=DIRECTION ( 'NONE',  ( 0.01455087615875041117, 0.9998941303973198913, 0.000000000000000000 ) ) ;
#16509=CARTESIAN_POINT ( 'NONE',  ( 0.3498557339129456656, -1.754787963452209887, 0.5848441301335288722 ) ) ;
#16511=B_SPLINE_CURVE_WITH_KNOTS ( 'NONE', 3,
 ( #28133, #40047, #21969, #3042 ),
 .UNSPECIFIED., .F., .F.,
 ( 4, 4 ),
 ( 0.000000000000000000, 0.0006205162911372014709 ),
 .UNSPECIFIED. ) ;
#16513=CARTESIAN_POINT ( 'NONE',  ( 0.1927291533531542422, -0.7490955637697421787, 0.5554573830606346352 ) ) ;
#16514=CARTESIAN_POINT ( 'NONE',  ( 3.250805436079486516E-05, -0.6542315385261258109, -0.1016538680321513732 ) ) ;
#16517=CARTESIAN_POINT ( 'NONE',  ( 0.1436225252650951412, -1.283668529478381393, 0.4687417262808780127 ) ) ;
#16519=CARTESIAN_POINT ( 'NONE',  ( 0.08097120591835743619, -1.368856899881548683, 0.5761801428003342496 ) ) ;
#16520=CARTESIAN_POINT ( 'NONE',  ( 0.5123549971852071616, -1.116020584419624928, 0.5891410297636010540 ) ) ;
#16526=CARTESIAN_POINT ( 'NONE',  ( 0.07882260269869785507, -1.330132293077975314, 0.5081289575126681779 ) ) ;
#16528=ORIENTED_EDGE ( 'NONE', *, *, #3117, .F. ) ;
#16529=CARTESIAN_POINT ( 'NONE',  ( 0.4625308732612979923, -1.562160397472748707, 0.5754140938433903729 ) ) ;
#16532=CARTESIAN_POINT ( 'NONE',  ( 0.1865761819245507769, -0.8562558704779227314, 0.1990025499142320520 ) ) ;
#16534=DIRECTION ( 'NONE',  ( -1.000000000000000000, -0.000000000000000000, -0.000000000000000000 ) ) ;
#16536=CARTESIAN_POINT ( 'NONE',  ( 0.6791962457086077043, -1.401251971513146621, 0.6322342638419099492 ) ) ;
#16542=CARTESIAN_POINT ( 'NONE',  ( 0.6022976011930347706, -1.482297354951358503, 0.5545281621470995459 ) ) ;
#16543=EDGE_CURVE ( 'NONE', #243, #8849, #14690, .T. ) ;
#16548=CARTESIAN_POINT ( 'NONE',  ( 0.1955653942118278366, -0.8581851384218914802, 0.6256584387592237784 ) ) ;
#16549=CARTESIAN_POINT ( 'NONE',  ( 0.01941772917732825440, -0.5190691814311400032, 0.4360231708482461555 ) ) ;
#16550=CARTESIAN_POINT ( 'NONE',  ( 0.4698255749495779399, -1.558011031807577496, 0.5747976326119568213 ) ) ;
#16554=ORIENTED_EDGE ( 'NONE', *, *, #26344, .F. ) ;
#16566=CARTESIAN_POINT ( 'NONE',  ( 0.2019795930595086331, -0.6216091269244319317, 0.3384082674912240463 ) ) ;
#16567=B_SPLINE_SURFACE_WITH_KNOTS ( 'NONE', 5, 5, ( 
 ( #22698, #32530, #1298, #26370, #704, #10521 ),
 ( #7030, #19598, #3935, #32132, #13409, #39121 ),
 ( #7419, #13199, #16707, #13615, #20399, #1495 ),
 ( #38903, #23509, #4536, #16496, #23091, #25985 ),
 ( #35618, #38510, #10338, #10730, #23303, #22901 ),
 ( #17307, #7828, #7214, #4139, #32321, #35828 ) ),
 .UNSPECIFIED., .F., .F., .F.,
 ( 6, 6 ),
 ( 6, 6 ),
 ( -6.761171338546692944, 6.761171338546684950 ),
 ( -2.171890115185114656, 4.589281223359888529 ),
 .UNSPECIFIED. ) ;
#16570=CARTESIAN_POINT ( 'NONE',  ( 0.6069176374591634948, -1.480164522464830990, 0.5706138896049881559 ) ) ;
#16573=CARTESIAN_POINT ( 'NONE',  ( 0.3527420388993543487, -1.124787755445947113, 0.7358831224922630643 ) ) ;
#16578=CARTESIAN_POINT ( 'NONE',  ( 0.09723417313752830138, -0.6135477923982464166, 0.3092590504431999565 ) ) ;
#16582=CARTESIAN_POINT ( 'NONE',  ( 0.1002847947475375562, -0.9216047912797521446, 0.6044655177918580868 ) ) ;
#16588=CARTESIAN_POINT ( 'NONE',  ( 0.4645646215180628258, -1.672710978628429102, 0.4491217904219667045 ) ) ;
#16590=CARTESIAN_POINT ( 'NONE',  ( 0.4534472899590196726, -1.218434779631715204, 0.6820681023121225595 ) ) ;
#16594=CARTESIAN_POINT ( 'NONE',  ( 0.3177287329960665208, -1.760453033344018703, 0.4998481136542969883 ) ) ;
#16595=CARTESIAN_POINT ( 'NONE',  ( 0.4922096163030106331, -1.082311226180449504, 0.5799505941865350511 ) ) ;
#16597=CARTESIAN_POINT ( 'NONE',  ( 0.06448306067890459403, -1.151813066880623015, 0.7546316310809547678 ) ) ;
#16599=CARTESIAN_POINT ( 'NONE',  ( 0.4137764936004748595, -1.589585228628171532, 0.5759508131641624118 ) ) ;
#16601=CARTESIAN_POINT ( 'NONE',  ( 0.1987655437495040311, -0.5941059772690211460, 0.3236942554273257722 ) ) ;
#16605=CARTESIAN_POINT ( 'NONE',  ( 0.5258573571825243542, -1.427028965149156114, 0.7758776250953042242 ) ) ;
#16607=CARTESIAN_POINT ( 'NONE',  ( 0.07497864282573103722, -1.322056043867067876, 0.4862695133534068459 ) ) ;
#16612=CARTESIAN_POINT ( 'NONE',  ( 0.1614670899430008522, -0.7569536277469717245, 0.1022936816274460647 ) ) ;
#16615=CARTESIAN_POINT ( 'NONE',  ( 0.5640992009001688512, -1.512213347522166185, 0.5182417262812423209 ) ) ;
#16616=AXIS2_PLACEMENT_3D ( 'NONE', #10259, #22825, #35345 ) ;
#16619=CARTESIAN_POINT ( 'NONE',  ( 0.7002079545642244662, -1.577973572399679725, 0.5182417262812423209 ) ) ;
#16630=CARTESIAN_POINT ( 'NONE',  ( 0.07582666994630285484, -1.068917391567854036, 0.8049195030047635591 ) ) ;
#16631=CARTESIAN_POINT ( 'NONE',  ( -0.0003059967544939336411, -0.9037512443581188215, 0.02100609841003503453 ) ) ;
#16638=DIRECTION ( 'NONE',  ( 0.9998941247116546194, -0.01455087607601020412, 0.0001066420868422379362 ) ) ;
#16643=CARTESIAN_POINT ( 'NONE',  ( 0.4981282648377903244, -1.293502761169403881, 0.7428242663174567939 ) ) ;
#16646=CARTESIAN_POINT ( 'NONE',  ( 0.5416676161616581497, -1.167047932790743037, 0.6420073683128293407 ) ) ;
#16649=CARTESIAN_POINT ( 'NONE',  ( 0.2031820619477883449, -0.6660346396928469304, 0.3462152820027419864 ) ) ;
#16653=CARTESIAN_POINT ( 'NONE',  ( 0.2817677660706678910, -1.487235381464147910, 0.8882017575617421334 ) ) ;
#16656=CARTESIAN_POINT ( 'NONE',  ( 0.3088664963667261398, -1.757905065063135597, 0.5295467280985148850 ) ) ;
#16660=CARTESIAN_POINT ( 'NONE',  ( 0.2362093653773955082, -0.9997838659200906086, 0.5753361218662520482 ) ) ;
#16663=CARTESIAN_POINT ( 'NONE',  ( 0.6076235955870944450, -1.477448194379718194, 0.6267975502367186813 ) ) ;
#16665=CARTESIAN_POINT ( 'NONE',  ( 0.1627620917790547350, -0.9015321819263497627, 0.5877156909771449333 ) ) ;
#16667=CARTESIAN_POINT ( 'NONE',  ( 0.4410077156479240146, -1.144291324537809462, 0.4235185031147128409 ) ) ;
#16670=CARTESIAN_POINT ( 'NONE',  ( 0.6335034399251443515, -1.559158136585290233, 0.4182417262808776903 ) ) ;
#16678=CIRCLE ( 'NONE', #25891, 0.009999999999999930819 ) ;
#16679=PRODUCT_DEFINITION_SHAPE ( 'NONE', 'NONE',  #38779 ) ;
#16680=CARTESIAN_POINT ( 'NONE',  ( 0.4311296713360665001, -1.704400165977600468, 0.4305790789625640880 ) ) ;
#16683=CARTESIAN_POINT ( 'NONE',  ( 0.3026265312661224893, -1.684849445872222296, 0.8620389816118222415 ) ) ;
#16684=CARTESIAN_POINT ( 'NONE',  ( 0.7072999403808241103, -1.506214808821535023, 0.5537687555486060509 ) ) ;
#16691=CARTESIAN_POINT ( 'NONE',  ( 0.2626259013267802644, -1.679529066113947700, 0.6053279492784264804 ) ) ;
#16692=CARTESIAN_POINT ( 'NONE',  ( 0.2816542641881043529, -0.9456696404293912783, 0.7252052400065256421 ) ) ;
#16696=ORIENTED_EDGE ( 'NONE', *, *, #23188, .F. ) ;
#16698=CARTESIAN_POINT ( 'NONE',  ( 0.6641929375487872766, -1.545761309749121848, 0.6885940231374464426 ) ) ;
#16702=CARTESIAN_POINT ( 'NONE',  ( -0.01061162201870326748, -0.5808848742743736304, 0.3378471357688186960 ) ) ;
#16707=CARTESIAN_POINT ( 'NONE',  ( -0.002842236103788325745, -0.7404579356088996089, 0.04185307883324737577 ) ) ;
#16709=CARTESIAN_POINT ( 'NONE',  ( 0.2612906772968546787, -0.9851395584723477983, 0.6798953947484819293 ) ) ;
#16711=CARTESIAN_POINT ( 'NONE',  ( 0.06927010083464776868, -0.5404361519564938598, 0.1579025348389868078 ) ) ;
#16713=CARTESIAN_POINT ( 'NONE',  ( 0.5335437526992924395, -1.503445527284964500, 0.6930812907888218577 ) ) ;
#16718=CARTESIAN_POINT ( 'NONE',  ( 0.6786717105919251036, -1.448527022901674233, 0.4644334021538232826 ) ) ;
#16723=CARTESIAN_POINT ( 'NONE',  ( 0.3480859549341126513, -1.062997586067646827, 0.7846658571238425139 ) ) ;
#16725=CARTESIAN_POINT ( 'NONE',  ( -0.0003596754992817568900, -0.9247255903860709392, 0.06913601831629608008 ) ) ;
#16726=CARTESIAN_POINT ( 'NONE',  ( 0.06928988850528894350, -0.5407624024163444343, 0.1615399141407840300 ) ) ;
#16727=CARTESIAN_POINT ( 'NONE',  ( 0.006645421451714178529, -0.8246033869726616672, 0.06648983423800172710 ) ) ;
#16729=EDGE_CURVE ( 'NONE', #40221, #23093, #30327, .T. ) ;
#16730=CARTESIAN_POINT ( 'NONE',  ( 0.004566372195762857279, -0.8656213538948328567, 0.4622093217984943880 ) ) ;
#16731=CARTESIAN_POINT ( 'NONE',  ( 0.4929465528686921560, -1.082715557938388029, 0.5685663778595840823 ) ) ;
#16735=CIRCLE ( 'NONE', #39720, 0.01000000000000002970 ) ;
#16739=CIRCLE ( 'NONE', #28576, 0.01000000000000003143 ) ;
#16740=AXIS2_PLACEMENT_3D ( 'NONE', #23249, #9861, #7166 ) ;
#16744=CARTESIAN_POINT ( 'NONE',  ( 0.002392601678638947398, -0.5315622534075540306, 0.1816553975050167746 ) ) ;
#16749=CARTESIAN_POINT ( 'NONE',  ( 0.6809224168725948045, -1.405736369044236378, 0.6042223006942389896 ) ) ;
#16750=VERTEX_POINT ( 'NONE', #27344 ) ;
#16760=CARTESIAN_POINT ( 'NONE',  ( 0.09446234534901919166, -0.6589171955595342078, 0.2802060902332455528 ) ) ;
#16761=CARTESIAN_POINT ( 'NONE',  ( 0.1037934690335643728, -0.9534350347034203921, 0.9068416015443596656 ) ) ;
#16762=CARTESIAN_POINT ( 'NONE',  ( 0.09694864982818704457, -0.6210372448765658637, 0.3796554584802787624 ) ) ;
#16763=CARTESIAN_POINT ( 'NONE',  ( 0.2665433607519571702, -1.687828102416362830, 0.5925423054000314993 ) ) ;
#16765=CARTESIAN_POINT ( 'NONE',  ( 0.2764337282391635120, -1.207704344519197504, 0.5682417262808777680 ) ) ;
#16769=CARTESIAN_POINT ( 'NONE',  ( 0.3186278594696675404, -1.645101200862095325, 0.5280450199627192420 ) ) ;
#16770=CARTESIAN_POINT ( 'NONE',  ( 0.2627070462085436264, -0.7490940406976871468, 0.5657688020081199642 ) ) ;
#16775=CARTESIAN_POINT ( 'NONE',  ( 0.08058916068514938857, -1.309220013881621680, 0.4727703015479236548 ) ) ;
#16777=CARTESIAN_POINT ( 'NONE',  ( 0.1037539007929738771, -1.411184382869408616, 0.5260835464586457455 ) ) ;
#16778=CARTESIAN_POINT ( 'NONE',  ( 0.3979743647030599130, -0.9582897341353557863, 0.7577590062044536889 ) ) ;
#16781=CARTESIAN_POINT ( 'NONE',  ( 0.004845387396406415983, -0.8792891026250457820, 0.4619221541178868962 ) ) ;
#16787=CARTESIAN_POINT ( 'NONE',  ( 0.2631241314290992395, -0.9694475436486175157, 0.6931444287947289284 ) ) ;
#16790=CARTESIAN_POINT ( 'NONE',  ( 0.4679778500672936992, -1.237826332153874942, 0.6057417262809768888 ) ) ;
#16792=EDGE_CURVE ( 'NONE', #13556, #33386, #4832, .T. ) ;
#16793=CARTESIAN_POINT ( 'NONE',  ( 0.4685502202651029569, -1.116536938686066183, 0.5688043585934901003 ) ) ;
#16794=CARTESIAN_POINT ( 'NONE',  ( 0.5382177704477151270, -1.161136986456818176, 0.5551899235458804815 ) ) ;
#16797=CARTESIAN_POINT ( 'NONE',  ( 0.06954336310279328470, -0.8599038886713844532, 0.4255655716258943122 ) ) ;
#16798=ORIENTED_EDGE ( 'NONE', *, *, #28134, .F. ) ;
#16804=ADVANCED_FACE ( 'NONE', ( #23142 ), #40251, .F. ) ;
#16806=CARTESIAN_POINT ( 'NONE',  ( 0.4561128394006527254, -1.223906212898765222, 0.6959908130051005726 ) ) ;
#16811=ADVANCED_FACE ( 'NONE', ( #3592 ), #13058, .T. ) ;
#16815=CARTESIAN_POINT ( 'NONE',  ( 0.4131346768878386144, -1.589365865636619191, 0.5663133035555527606 ) ) ;
#16816=CARTESIAN_POINT ( 'NONE',  ( 0.08593876023563185029, -0.8031142711107595034, 0.05926891841886761103 ) ) ;
#16817=CARTESIAN_POINT ( 'NONE',  ( 0.2011461926870026229, -0.7184356070491879631, 0.3342384739243060010 ) ) ;
#16822=CARTESIAN_POINT ( 'NONE',  ( 0.5748457419294008552, -1.497445084182354114, 0.6198248605900839037 ) ) ;
#16823=ORIENTED_EDGE ( 'NONE', *, *, #10258, .F. ) ;
#16826=CARTESIAN_POINT ( 'NONE',  ( 0.1856725227377205856, -0.8111418809926428386, 0.1833442776911899941 ) ) ;
#16828=B_SPLINE_CURVE_WITH_KNOTS ( 'NONE', 3,
 ( #27299, #39828, #21112, #5668, #20923, #18223, #2793, #21328, #36541, #36734, #11839, #5056 ),
 .UNSPECIFIED., .F., .F.,
 ( 4, 2, 2, 2, 2, 4 ),
 ( 3.088587339835645537E-17, 0.0003359336526506150403, 0.0006718673053011991808, 0.001343734610602367353, 0.002015601915903535418, 0.002687469221204703915 ),
 .UNSPECIFIED. ) ;
#16832=B_SPLINE_CURVE_WITH_KNOTS ( 'NONE', 3,
 ( #21178, #26754, #30216, #14376, #36188, #24082, #36792, #30643, #39283, #8602 ),
 .UNSPECIFIED., .F., .F.,
 ( 4, 2, 2, 2, 4 ),
 ( 0.000000000000000000, 0.0004973432167690093435, 0.0009946864335380186870, 0.001492029650307028030, 0.001989372867076037374 ),
 .UNSPECIFIED. ) ;
#16833=CARTESIAN_POINT ( 'NONE',  ( 0.6221473432577675489, -1.308691071842436493, 0.8644659521288400317 ) ) ;
#16843=CARTESIAN_POINT ( 'NONE',  ( 0.2590277710115678755, -1.679485505736613149, 0.4634944759858370955 ) ) ;
#16845=CARTESIAN_POINT ( 'NONE',  ( 0.1252549559024136727, -1.296835781121829845, 0.4238276788641243131 ) ) ;
#16846=CARTESIAN_POINT ( 'NONE',  ( 0.003124719664520433666, -0.5686731593868930013, 0.1115160683991335139 ) ) ;
#16851=ORIENTED_EDGE ( 'NONE', *, *, #21749, .F. ) ;
#16854=ORIENTED_EDGE ( 'NONE', *, *, #1920, .F. ) ;
#16857=CARTESIAN_POINT ( 'NONE',  ( 0.4638821911974275181, -1.242580118564127645, 0.7881282199712437153 ) ) ;
#16860=CARTESIAN_POINT ( 'NONE',  ( 0.4384178598954188155, -1.040563892421024983, 0.6900182345289431751 ) ) ;
#16862=CARTESIAN_POINT ( 'NONE',  ( 0.1399722631084863167, -0.4537238383118586404, 0.1457373701026924706 ) ) ;
#16865=CARTESIAN_POINT ( 'NONE',  ( 0.3276507143392576316, -1.639361389215603371, 0.5824061036618035647 ) ) ;
#16866=CARTESIAN_POINT ( 'NONE',  ( 0.6280878869109404183, -1.573568221354046281, 0.4189938828952650685 ) ) ;
#16867=CARTESIAN_POINT ( 'NONE',  ( 0.1131241454731939100, -0.6872203660140440151, -0.09530310615070609892 ) ) ;
#16871=ORIENTED_EDGE ( 'NONE', *, *, #32041, .T. ) ;
#16872=CARTESIAN_POINT ( 'NONE',  ( 0.3211449588372387587, -1.297375842027792325, 0.4762509439642684250 ) ) ;
#16874=CARTESIAN_POINT ( 'NONE',  ( 0.1574420996541403550, -0.9545193198765702380, 0.4442515449357353763 ) ) ;
#16877=CARTESIAN_POINT ( 'NONE',  ( 0.3838258328925114871, -1.260744394557325121, 0.5882158180126604297 ) ) ;
#16878=CARTESIAN_POINT ( 'NONE',  ( 0.4642954988900184210, -1.156858560228702260, 0.4182417262808743597 ) ) ;
#16886=CARTESIAN_POINT ( 'NONE',  ( 0.04152565108029027119, -1.188198874194366761, 0.6784721777313348356 ) ) ;
#16888=CARTESIAN_POINT ( 'NONE',  ( 0.1046051313612698097, -1.402039145303610734, 0.6143806765046105900 ) ) ;
#16890=CARTESIAN_POINT ( 'NONE',  ( 0.4841487358689927634, -1.673745430023940717, 0.5182417262823179049 ) ) ;
#16892=CARTESIAN_POINT ( 'NONE',  ( 0.3066092890089989198, -1.757470180272292959, 0.5913806063715120187 ) ) ;
#16893=CARTESIAN_POINT ( 'NONE',  ( 0.7075884434940304946, -1.499667991049689952, 0.5400310817953950515 ) ) ;
#16895=CARTESIAN_POINT ( 'NONE',  ( 0.1826337464091716545, -0.5596885952557434374, 0.2690888922271704176 ) ) ;
#16896=ORIENTED_EDGE ( 'NONE', *, *, #820, .T. ) ;
#16897=CARTESIAN_POINT ( 'NONE',  ( 0.2657064854856445724, -1.675227424430884238, 0.6641665367988364155 ) ) ;
#16898=CARTESIAN_POINT ( 'NONE',  ( 0.6019823243568848126, -1.483134150572406940, 0.5732773657679698376 ) ) ;
#16900=B_SPLINE_CURVE_WITH_KNOTS ( 'NONE', 3,
 ( #20305, #32825, #4631, #33038, #17207, #26693 ),
 .UNSPECIFIED., .F., .F.,
 ( 4, 2, 4 ),
 ( 2.660867628118834816, 5.798205611760163691, 8.935543595401492567 ),
 .UNSPECIFIED. ) ;
#16905=CARTESIAN_POINT ( 'NONE',  ( 0.3114253368378466225, -1.187765832548442813, 0.5446703740600618016 ) ) ;
#16907=CARTESIAN_POINT ( 'NONE',  ( 0.06342771192242831202, -0.9335166984577768501, 0.7937027791328541415 ) ) ;
#16913=CARTESIAN_POINT ( 'NONE',  ( 0.2482514041270085792, -0.9705348356143717048, 0.6681873673986314932 ) ) ;
#16914=CARTESIAN_POINT ( 'NONE',  ( 0.09015534308186123891, -0.5467265198224540157, 0.1782017856848721049 ) ) ;
#16915=CARTESIAN_POINT ( 'NONE',  ( 0.5390489187139376748, -1.519039902820679133, 0.5725961793155519564 ) ) ;
#16916=VERTEX_POINT ( 'NONE', #14065 ) ;
#16917=CARTESIAN_POINT ( 'NONE',  ( 0.03360078502195575773, -1.082923033457784401, 0.6287642814980498596 ) ) ;
#16920=CARTESIAN_POINT ( 'NONE',  ( 0.3610463218409277197, -1.748328711707529459, 0.5952565890379123426 ) ) ;
#16925=CARTESIAN_POINT ( 'NONE',  ( 0.01170413314921280555, -0.7214729979845280194, -0.1114895720740121249 ) ) ;
#16926=CARTESIAN_POINT ( 'NONE',  ( 0.5575849190334257743, -1.430655059094382731, 0.7536012745007747426 ) ) ;
#16929=CARTESIAN_POINT ( 'NONE',  ( 0.1799043607419438529, -1.488798643046104875, 0.7589116457392215409 ) ) ;
#16930=B_SPLINE_CURVE_WITH_KNOTS ( 'NONE', 3,
 ( #30799, #20751, #11476, #5080, #18048, #30603, #17832, #8173, #15156, #8376, #2226, #33899, #20533, #33067, #14963, #27518 ),
 .UNSPECIFIED., .F., .F.,
 ( 4, 2, 2, 2, 2, 2, 2, 4 ),
 ( 0.002977954013962045166, 0.003350115589110935245, 0.003722277164259825757, 0.004094438739408716270, 0.004466600314557606782, 0.004838761889706495560, 0.005210923464855384338, 0.005955246615153174036 ),
 .UNSPECIFIED. ) ;
#16931=CARTESIAN_POINT ( 'NONE',  ( 0.2246580631734754474, -0.8968525156641222740, 0.4249663362035034364 ) ) ;
#16933=EDGE_CURVE ( 'NONE', #3626, #3536, #26938, .T. ) ;
#16938=EDGE_LOOP ( 'NONE', ( #24951, #14156, #9858, #14838 ) ) ;
#16940=CARTESIAN_POINT ( 'NONE',  ( 0.01056076242565423713, -0.5297871112653679271, 0.1536645982759194395 ) ) ;
#16941=CARTESIAN_POINT ( 'NONE',  ( 0.2209956536232957902, -1.227897296991992793, 0.5182417262820130377 ) ) ;
#16942=ORIENTED_EDGE ( 'NONE', *, *, #33135, .F. ) ;
#16944=CARTESIAN_POINT ( 'NONE',  ( 0.6775446752225827707, -1.407456786189307696, 0.5068639979343774193 ) ) ;
#16949=VERTEX_POINT ( 'NONE', #36073 ) ;
#16954=CARTESIAN_POINT ( 'NONE',  ( 0.1875000000000003331, -0.4943738020624263707, 0.3123409581947972358 ) ) ;
#16956=CARTESIAN_POINT ( 'NONE',  ( 0.08753440268785939171, -0.6845692626716118889, 0.1457185332388692967 ) ) ;
#16958=CARTESIAN_POINT ( 'NONE',  ( 0.01220488679410611232, -0.4284039384462490774, 0.1900330486215427162 ) ) ;
#16959=CARTESIAN_POINT ( 'NONE',  ( 0.4698606666588109326, -1.558018086733606200, 0.5753270877166933861 ) ) ;
#16960=CARTESIAN_POINT ( 'NONE',  ( 0.1148172011972283663, -0.4713019633547693155, 0.03899715547817009936 ) ) ;
#16962=CARTESIAN_POINT ( 'NONE',  ( 0.1230772935360478215, -0.9703466098372804938, 0.4773990857995715764 ) ) ;
#16967=CARTESIAN_POINT ( 'NONE',  ( 0.2702030311564788123, -0.6895941179718233505, 0.6181208260419542855 ) ) ;
#16971=CARTESIAN_POINT ( 'NONE',  ( 0.0004750592482352814579, -0.4386115460793976739, 0.1457185332388683252 ) ) ;
#16974=CARTESIAN_POINT ( 'NONE',  ( 0.4340563226180833012, -1.025953197730038458, 0.7364845616659437821 ) ) ;
#16976=EDGE_CURVE ( 'NONE', #12586, #24566, #10172, .T. ) ;
#16977=CARTESIAN_POINT ( 'NONE',  ( 0.01522254512315708574, -0.9178457916527728022, 0.5707280127493563615 ) ) ;
#16981=CARTESIAN_POINT ( 'NONE',  ( 0.2764424605908987753, -0.9705060276339172454, 0.7215845397199748268 ) ) ;
#16987=CARTESIAN_POINT ( 'NONE',  ( 0.09587083108297865530, -0.6074767732719537072, 0.2950264738744098891 ) ) ;
#16988=CARTESIAN_POINT ( 'NONE',  ( 0.3088664963667261398, -1.757905065063135597, 0.5295467280985148850 ) ) ;
#16989=DIRECTION ( 'NONE',  ( -0.9998941247116546194, 0.01455087607601020239, -0.0001066420868422379362 ) ) ;
#16990=CARTESIAN_POINT ( 'NONE',  ( 0.1420085715566430373, -1.022094752421645492, 0.7158645833976974293 ) ) ;
#16996=CARTESIAN_POINT ( 'NONE',  ( 0.3506455678375485219, -1.087518136233734278, 0.7199871270596691630 ) ) ;
#17005=CARTESIAN_POINT ( 'NONE',  ( 0.3994775562665067725, -1.543474704417578502, 0.7765694768245218205 ) ) ;
#17006=CARTESIAN_POINT ( 'NONE',  ( 0.08840096076972359107, -0.6251151962830620024, 0.03934731828055227504 ) ) ;
#17008=CARTESIAN_POINT ( 'NONE',  ( 0.1825980849618502877, -1.261391773294454399, 0.5182417262812422099 ) ) ;
#17009=ORIENTED_EDGE ( 'NONE', *, *, #1442, .T. ) ;
#17013=EDGE_CURVE ( 'NONE', #19731, #9282, #14098, .T. ) ;
#17014=CARTESIAN_POINT ( 'NONE',  ( 0.5500705290592691199, -1.461052471298058375, 0.7365222812456531098 ) ) ;
#17020=CARTESIAN_POINT ( 'NONE',  ( 0.1811801731470885635, -1.262447345873583426, 0.4381703640825295731 ) ) ;
#17021=CARTESIAN_POINT ( 'NONE',  ( 0.3842063748693837488, -1.733091723360132841, 0.4185254220199500774 ) ) ;
#17022=B_SPLINE_CURVE_WITH_KNOTS ( 'NONE', 3,
 ( #37363, #9174, #25022, #37172, #18650, #37553, #31408, #8987, #21555, #25230, #34074, #24640, #13681, #26244 ),
 .UNSPECIFIED., .F., .F.,
 ( 4, 2, 2, 2, 2, 2, 4 ),
 ( 5.637184056103667372E-17, 0.0004877684492138178052, 0.0007316526738207009039, 0.0008535947861241437000, 0.0009145658422758637428, 0.0009450513703517257700, 0.0009755368984275879056 ),
 .UNSPECIFIED. ) ;
#17024=CARTESIAN_POINT ( 'NONE',  ( 0.1893427799090355301, -0.4853919354581605061, 0.2707563002020392240 ) ) ;
#17027=CARTESIAN_POINT ( 'NONE',  ( 0.08110577511515054683, -1.318921603477608118, 0.5655786468447775439 ) ) ;
#17029=B_SPLINE_CURVE_WITH_KNOTS ( 'NONE', 3,
 ( #4997, #33388, #14452, #36069, #17746, #7468, #1540, #32578, #14062, #26639, #39168, #5604 ),
 .UNSPECIFIED., .F., .F.,
 ( 4, 2, 2, 2, 2, 4 ),
 ( 0.000000000000000000, 0.0002481559604999103051, 0.0004963119209998206102, 0.0007444678814997309152, 0.0008685458617496860136, 0.0009926238419996412203 ),
 .UNSPECIFIED. ) ;
#17030=CARTESIAN_POINT ( 'NONE',  ( 0.3174141940625345160, -1.772900390203313137, 0.5327102575848723376 ) ) ;
#17034=FACE_OUTER_BOUND ( 'NONE', #4684, .T. ) ;
#17035=CARTESIAN_POINT ( 'NONE',  ( 0.1001698831744081003, -1.307806316238550703, 0.4450799649317093709 ) ) ;
#17037=CARTESIAN_POINT ( 'NONE',  ( 0.1576987512544144876, -1.257723164589890308, 0.9396174402501648038 ) ) ;
#17044=CARTESIAN_POINT ( 'NONE',  ( 0.4971324743577882899, -1.079965756743124006, 0.4177417262808780229 ) ) ;
#17046=FACE_OUTER_BOUND ( 'NONE', #32692, .T. ) ;
#17047=DIRECTION ( 'NONE',  ( -0.4999551463232372317, 0.8660512985181135770, -0.000000000000000000 ) ) ;
#17048=CARTESIAN_POINT ( 'NONE',  ( 0.5153315922689613027, -1.320405065595526839, 0.7260202612431515545 ) ) ;
#17049=ORIENTED_EDGE ( 'NONE', *, *, #201, .T. ) ;
#17050=CARTESIAN_POINT ( 'NONE',  ( 0.2577558225373174916, -0.8624250852862554995, 0.5195666343558283939 ) ) ;
#17054=CARTESIAN_POINT ( 'NONE',  ( 0.3183059118147241184, -1.589430717261796744, 0.7981046197357909433 ) ) ;
#17055=CARTESIAN_POINT ( 'NONE',  ( 0.6732088238915016065, -1.530595336554058550, 0.4388990213126219841 ) ) ;
#17057=CARTESIAN_POINT ( 'NONE',  ( 0.2320755761173002307, -1.232873731908348480, 0.4177417262808779674 ) ) ;
#17064=CARTESIAN_POINT ( 'NONE',  ( 0.2857211932547981115, -1.109133886523115731, 0.7441438648489260288 ) ) ;
#17065=DIRECTION ( 'NONE',  ( 0.01265474379914258672, 0.8659329421511292590, -0.4999999971568669932 ) ) ;
#17068=CARTESIAN_POINT ( 'NONE',  ( 0.6652959480876716736, -1.517233971325829600, 0.4231557572046961146 ) ) ;
#17075=CARTESIAN_POINT ( 'NONE',  ( 0.3881929885797955615, -1.150008520685900315, 0.4234575807221065968 ) ) ;
#17086=CARTESIAN_POINT ( 'NONE',  ( 0.3921921748761933446, -1.728262305561636181, 0.4265845344340060685 ) ) ;
#17089=CARTESIAN_POINT ( 'NONE',  ( 0.1459722773112856753, -0.6340201870151221941, 0.3850682184254722862 ) ) ;
#17090=B_SPLINE_CURVE_WITH_KNOTS ( 'NONE', 3,
 ( #38262, #4319, #7182, #16670, #39084, #675, #10696, #29222 ),
 .UNSPECIFIED., .F., .F.,
 ( 4, 2, 2, 4 ),
 ( 0.000000000000000000, 0.0004476527168006422686, 0.0008953054336012845373, 0.001790610867202582519 ),
 .UNSPECIFIED. ) ;
#17091=CARTESIAN_POINT ( 'NONE',  ( -0.0008433103373208181977, -0.7682816629019912913, 0.007858431574465824659 ) ) ;
#17092=ORIENTED_EDGE ( 'NONE', *, *, #904, .T. ) ;
#17097=CARTESIAN_POINT ( 'NONE',  ( 0.2154282780885227178, -1.466805515833779383, 0.9278870098542323364 ) ) ;
#17106=CARTESIAN_POINT ( 'NONE',  ( 0.09278199725800895248, -0.7971562777438269132, 0.2877230682800478445 ) ) ;
#17107=CARTESIAN_POINT ( 'NONE',  ( 0.1188169051961329437, -1.413502985213658247, 0.5800534899519873555 ) ) ;
#17108=CARTESIAN_POINT ( 'NONE',  ( 0.06935100149987896700, -0.5417505261625371604, 0.1708526567523814543 ) ) ;
#17109=CARTESIAN_POINT ( 'NONE',  ( 0.5540999761718204963, -1.510283947878215516, 0.6075923333766917178 ) ) ;
#17112=CARTESIAN_POINT ( 'NONE',  ( 0.7007246779392307667, -1.487338553264568208, 0.4637699275333992954 ) ) ;
#17114=CARTESIAN_POINT ( 'NONE',  ( 0.4880253864272864894, -1.700462583248872894, 0.5182417262812423209 ) ) ;
#17115=CARTESIAN_POINT ( 'NONE',  ( 0.6654360144368460794, -1.561514405424819119, 0.5611086426770289792 ) ) ;
#17116=CARTESIAN_POINT ( 'NONE',  ( 0.06463019578131175280, -1.332095939219700487, 0.5196073683862424408 ) ) ;
#17117=CARTESIAN_POINT ( 'NONE',  ( 0.07885325192267222949, -1.319783927197341944, 0.4754891053729509154 ) ) ;
#17119=CARTESIAN_POINT ( 'NONE',  ( 0.3336325236675090067, -1.050835064020409160, 0.7593003920438236021 ) ) ;
#17120=CARTESIAN_POINT ( 'NONE',  ( 0.01166930780816748982, -0.7552342480465903396, -0.1042461971847544744 ) ) ;
#17121=FACE_OUTER_BOUND ( 'NONE', #40169, .T. ) ;
#17124=CARTESIAN_POINT ( 'NONE',  ( 0.1861033513463754285, -1.549633035783825497, 0.5860151309145639198 ) ) ;
#17125=CARTESIAN_POINT ( 'NONE',  ( 0.4929465528686921005, -1.082715557938388029, 0.5682417262808779901 ) ) ;
#17127=CARTESIAN_POINT ( 'NONE',  ( 0.7185399166019250661, -1.465950542831855330, 0.7545741816404391011 ) ) ;
#17131=ORIENTED_EDGE ( 'NONE', *, *, #2937, .T. ) ;
#17133=CARTESIAN_POINT ( 'NONE',  ( 0.01055999354154114368, -0.5296565605740094496, 0.1394354128953858296 ) ) ;
#17135=CARTESIAN_POINT ( 'NONE',  ( 0.1947076744186670427, -1.243108242024598242, 0.4512817965407442955 ) ) ;
#17138=CARTESIAN_POINT ( 'NONE',  ( 0.3267680042207918301, -1.758262944587549503, 0.4789874961554916322 ) ) ;
#17139=CARTESIAN_POINT ( 'NONE',  ( 0.5691520580847880817, -1.222151117369431939, 0.8040585553043922973 ) ) ;
#17145=CARTESIAN_POINT ( 'NONE',  ( 0.1637488714925408873, -0.5994898440788770655, 0.1932149833450298726 ) ) ;
#17152=CARTESIAN_POINT ( 'NONE',  ( 0.1058028591704159582, -0.7174348744888263685, 0.3722218170207774457 ) ) ;
#17153=CARTESIAN_POINT ( 'NONE',  ( 0.2539806336202973247, -1.480393849963148600, 1.018971347781354231 ) ) ;
#17154=CARTESIAN_POINT ( 'NONE',  ( 0.2457936252450182157, -1.026797302826530034, 0.7978041782991802666 ) ) ;
#17155=CARTESIAN_POINT ( 'NONE',  ( 0.2681791922883234869, -1.687400927718340826, 0.6168360553784030254 ) ) ;
#17157=CARTESIAN_POINT ( 'NONE',  ( 0.1811302593339075007, -1.059783243163161970, 0.6264505142422892581 ) ) ;
#17160=CARTESIAN_POINT ( 'NONE',  ( 0.1932692805625377541, -0.5636194602968859213, 0.2661166255916873058 ) ) ;
#17167=FACE_OUTER_BOUND ( 'NONE', #39108, .T. ) ;
#17168=CARTESIAN_POINT ( 'NONE',  ( 0.5387674647098039671, -1.171534441891039169, 0.7413454372389880476 ) ) ;
#17170=( BOUNDED_SURFACE ( )  B_SPLINE_SURFACE ( 3, 2, ( 
 ( #2009, #11468, #24031 ),
 ( #20935, #2213, #15357 ),
 ( #24421, #39633, #33657 ),
 ( #37359, #5871, #30786 ),
 ( #24836, #21551, #33457 ),
 ( #17822, #34070, #30592 ),
 ( #37166, #21734, #39844 ),
 ( #36747, #8558, #2415 ),
 ( #18431, #14953, #8771 ),
 ( #33884, #5687, #2606 ),
 ( #15143, #27704, #12073 ),
 ( #8980, #24636, #30985 ),
 ( #2808, #25224, #28115 ),
 ( #22558, #18864, #38365 ),
 ( #28723, #3206, #35089 ),
 ( #15751, #40646, #16182 ),
 ( #28905, #31404, #9587 ),
 ( #585, #13078, #15963 ),
 ( #13277, #6485, #386 ),
 ( #3811, #18646, #34480 ),
 ( #6291, #31591, #28301 ),
 ( #771, #31206, #37768 ),
 ( #169, #19054, #25633 ),
 ( #25017, #31804, #38164 ),
 ( #3023, #9988, #12659 ),
 ( #3408, #22166, #3618 ),
 ( #28510, #15568, #34680 ),
 ( #12884, #22770, #25845 ),
 ( #25443, #12463, #37974 ),
 ( #37549, #9784, #22354 ),
 ( #34875, #6686, #19261 ),
 ( #6893, #19467, #32000 ),
 ( #16367, #9371, #10203 ),
 ( #6076, #21953, #33363 ),
 ( #13676, #4004, #29112 ),
 ( #35693, #39944, #8270 ) ),
 .UNSPECIFIED., .F., .F., .F. ) 
 B_SPLINE_SURFACE_WITH_KNOTS ( ( 4, 2, 2, 2, 2, 2, 2, 2, 2, 2, 2, 2, 2, 2, 2, 2, 2, 4 ),
 ( 3, 3 ),
 ( 0.006158837752303239141, 0.008831284596174333867, 0.01150373144004543033, 0.01417617828391652506, 0.01551240170585207329, 0.01684862512778761978, 0.01818484854972316628, 0.01952107197165871277, 0.02018918368262648602, 0.02085729539359425927, 0.02152540710456203599, 0.02219351881552980923, 0.02352974223746535920, 0.02486596565940090570, 0.02553407737036867894, 0.02620218908133645219, 0.02687030079230422544, 0.02753841250327199869 ),
 ( 0.000000000000000000, 1.000000000000000000 ),
 .UNSPECIFIED. ) 
 GEOMETRIC_REPRESENTATION_ITEM ( )  RATIONAL_B_SPLINE_SURFACE ( (
 ( 1.000000000000000000, 0.6567084680803600971, 1.000000000000000000),
 ( 1.000000000000000000, 0.6566839907465437109, 1.000000000000000000),
 ( 1.000000000000000000, 0.6572021228041137197, 1.000000000000000000),
 ( 1.000000000000000000, 0.6579559531357345170, 1.000000000000000000),
 ( 1.000000000000000000, 0.6581132063349907080, 1.000000000000000000),
 ( 1.000000000000000000, 0.6570134697022161907, 1.000000000000000000),
 ( 1.000000000000000000, 0.6557949822498931880, 1.000000000000000000),
 ( 1.000000000000000000, 0.6519304267099326200, 1.000000000000000000),
 ( 1.000000000000000000, 0.6503122123076459093, 1.000000000000000000),
 ( 1.000000000000000000, 0.6462645446810073580, 1.000000000000000000),
 ( 1.000000000000000000, 0.6438349337072757361, 1.000000000000000000),
 ( 1.000000000000000000, 0.6382227172733763165, 1.000000000000000000),
 ( 1.000000000000000000, 0.6351102327385169666, 1.000000000000000000),
 ( 1.000000000000000000, 0.6287744411780002984, 1.000000000000000000),
 ( 1.000000000000000000, 0.6257180153651936694, 1.000000000000000000),
 ( 1.000000000000000000, 0.6223102534591248292, 1.000000000000000000),
 ( 1.000000000000000000, 0.6213451726380976314, 1.000000000000000000),
 ( 1.000000000000000000, 0.6201746544136139683, 1.000000000000000000),
 ( 1.000000000000000000, 0.6200976022680225741, 1.000000000000000000),
 ( 1.000000000000000000, 0.6203287173039150337, 1.000000000000000000),
 ( 1.000000000000000000, 0.6206481638358333219, 1.000000000000000000),
 ( 1.000000000000000000, 0.6220779520615170588, 1.000000000000000000),
 ( 1.000000000000000000, 0.6233032503211219932, 1.000000000000000000),
 ( 1.000000000000000000, 0.6274491077548256523, 1.000000000000000000),
 ( 1.000000000000000000, 0.6306542643529917669, 1.000000000000000000),
 ( 1.000000000000000000, 0.6389337287488969785, 1.000000000000000000),
 ( 1.000000000000000000, 0.6434217649977074238, 1.000000000000000000),
 ( 1.000000000000000000, 0.6522238611423898380, 1.000000000000000000),
 ( 1.000000000000000000, 0.6557613510651914002, 1.000000000000000000),
 ( 1.000000000000000000, 0.6639824573846913047, 1.000000000000000000),
 ( 1.000000000000000000, 0.6683217727600526681, 1.000000000000000000),
 ( 1.000000000000000000, 0.6790624151853396073, 1.000000000000000000),
 ( 1.000000000000000000, 0.6862971593358724309, 1.000000000000000000),
 ( 1.000000000000000000, 0.7000895111908658208, 1.000000000000000000),
 ( 1.000000000000000000, 0.7087223284753119135, 1.000000000000000000),
 ( 1.000000000000000000, 0.7109670133747438836, 1.000000000000000000) ) ) 
 REPRESENTATION_ITEM ( '' )  SURFACE ( )  );
#17171=CARTESIAN_POINT ( 'NONE',  ( 0.08973038502581247300, -1.323151139955826450, 0.4733271373649473035 ) ) ;
#17174=CARTESIAN_POINT ( 'NONE',  ( 0.3224586748600002384, -1.296590453040780799, 0.4182417262808783009 ) ) ;
#17177=CARTESIAN_POINT ( 'NONE',  ( 0.3121678834194830943, -1.028870205852967512, 0.7302106030273709525 ) ) ;
#17185=CARTESIAN_POINT ( 'NONE',  ( 0.4292533899499677563, -1.122974568708051013, 0.5176300287282207258 ) ) ;
#17186=ADVANCED_FACE ( 'NONE', ( #39900 ), #30044, .T. ) ;
#17187=CARTESIAN_POINT ( 'NONE',  ( 0.04712643034123224772, -0.8746274208907861558, 0.4664299315230325815 ) ) ;
#17193=CARTESIAN_POINT ( 'NONE',  ( 0.4773696427185842861, -1.254357306845002684, 0.6502240367204457083 ) ) ;
#17195=CARTESIAN_POINT ( 'NONE',  ( 0.3924513946351673721, -1.141110873382124913, 0.4807468720547258823 ) ) ;
#17196=CARTESIAN_POINT ( 'NONE',  ( 0.1640786445897259860, -1.229311324678093786, 0.5182417262812423209 ) ) ;
#17198=ORIENTED_EDGE ( 'NONE', *, *, #35147, .T. ) ;
#17202=CARTESIAN_POINT ( 'NONE',  ( 0.1873046210896235908, -0.4547550531002670371, 0.1479976049341028554 ) ) ;
#17204=CARTESIAN_POINT ( 'NONE',  ( 0.04867247092399697161, -0.5557472067246875813, 0.2394143140500440414 ) ) ;
#17206=CARTESIAN_POINT ( 'NONE',  ( 0.06920015087246249308, -0.5397947987972752104, 0.1394826760052076675 ) ) ;
#17207=CARTESIAN_POINT ( 'NONE',  ( 0.08986174638071832421, -0.6039319072276565503, 0.1463024350879380542 ) ) ;
#17212=CARTESIAN_POINT ( 'NONE',  ( 0.5628430809287441328, -1.504124224925729170, 0.5331533104258753264 ) ) ;
#17213=CARTESIAN_POINT ( 'NONE',  ( 0.5741976824997229167, -1.499288812830245954, 0.5782747764390164802 ) ) ;
#17214=VERTEX_POINT ( 'NONE', #14852 ) ;
#17218=CARTESIAN_POINT ( 'NONE',  ( 0.2336506187151118352, -1.232159623642217872, 0.5021138023866104083 ) ) ;
#17221=CARTESIAN_POINT ( 'NONE',  ( 0.6786648513340227673, -1.399193080605451334, 0.7803980693475389696 ) ) ;
#17226=CARTESIAN_POINT ( 'NONE',  ( 0.1838283605672264565, -0.5363226265955328698, 0.04314883391416569208 ) ) ;
#17227=CARTESIAN_POINT ( 'NONE',  ( 0.4343450670606688879, -1.232029114211916854, 0.4817113837480122007 ) ) ;
#17229=ADVANCED_FACE ( 'NONE', ( #8050 ), #34222, .F. ) ;
#17237=DIRECTION ( 'NONE',  ( 0.01455087615875041117, 0.9998941303973198913, 0.000000000000000000 ) ) ;
#17240=VERTEX_POINT ( 'NONE', #31697 ) ;
#17243=CARTESIAN_POINT ( 'NONE',  ( 0.1434010736994648927, -1.283284918233685623, 0.5707417262808780478 ) ) ;
#17244=ORIENTED_EDGE ( 'NONE', *, *, #28025, .F. ) ;
#17247=CARTESIAN_POINT ( 'NONE',  ( 0.5552441641573474529, -1.389167795574909547, 0.5900859616208992131 ) ) ;
#17250=CARTESIAN_POINT ( 'NONE',  ( 0.5134194225791607336, -1.118797547403455273, 0.5580923141791981346 ) ) ;
#17254=CARTESIAN_POINT ( 'NONE',  ( 0.3224727725618313778, -1.601339809662290614, 0.7774851842373180499 ) ) ;
#17256=CARTESIAN_POINT ( 'NONE',  ( 0.6910102488910387919, -1.503481276490886254, 0.4663957319702505822 ) ) ;
#17257=CARTESIAN_POINT ( 'NONE',  ( 0.1875666489605907761, -0.5533060011614776563, 0.04426231146092830110 ) ) ;
#17261=ORIENTED_EDGE ( 'NONE', *, *, #488, .F. ) ;
#17267=CARTESIAN_POINT ( 'NONE',  ( 0.4388835414683293634, -1.230108148053269179, 0.5682417262808738823 ) ) ;
#17273=CARTESIAN_POINT ( 'NONE',  ( 0.3558973088851713484, -1.163486677007739667, 0.4185315289370134528 ) ) ;
#17277=CARTESIAN_POINT ( 'NONE',  ( 0.3974763075531499990, -1.145280806970993659, 0.4306062601161479431 ) ) ;
#17281=CARTESIAN_POINT ( 'NONE',  ( 0.01182178933247767828, -0.6030406541726748282, -0.09969815838237815198 ) ) ;
#17284=EDGE_CURVE ( 'NONE', #4940, #25265, #30787, .T. ) ;
#17287=ORIENTED_EDGE ( 'NONE', *, *, #7884, .T. ) ;
#17288=ORIENTED_EDGE ( 'NONE', *, *, #34609, .T. ) ;
#17294=CARTESIAN_POINT ( 'NONE',  ( 0.2008624261879642658, -0.7759890251660743754, 0.5855711181173813840 ) ) ;
#17295=ORIENTED_EDGE ( 'NONE', *, *, #1420, .F. ) ;
#17296=CARTESIAN_POINT ( 'NONE',  ( -0.001637768206801153191, -0.8343066215553702758, 0.06341441842760701941 ) ) ;
#17297=ORIENTED_EDGE ( 'NONE', *, *, #36503, .F. ) ;
#17299=CARTESIAN_POINT ( 'NONE',  ( 0.5253935478925986224, -1.258261529843748727, 0.9008978830525721238 ) ) ;
#17302=CARTESIAN_POINT ( 'NONE',  ( 0.2479547223653777166, -1.576436051040469355, 0.8688751265680482172 ) ) ;
#17307=CARTESIAN_POINT ( 'NONE',  ( -0.0001922331839921582748, -0.4210325180397646583, 0.1483282180229311964 ) ) ;
#17311=CARTESIAN_POINT ( 'NONE',  ( 0.2187263053623307030, -0.9276774108102062710, 0.6425196885543180692 ) ) ;
#17313=CARTESIAN_POINT ( 'NONE',  ( 0.1125434483652356515, -0.6674345388938710544, 0.4183932267472516564 ) ) ;
#17314=CARTESIAN_POINT ( 'NONE',  ( 0.5507456769299096111, -1.501809185380300393, 0.6702287185426054616 ) ) ;
#17315=EDGE_CURVE ( 'NONE', #31663, #2486, #16090, .T. ) ;
#17316=CARTESIAN_POINT ( 'NONE',  ( 0.1972041951826758455, -0.5769445034669802297, 0.3142228439387118599 ) ) ;
#17318=CARTESIAN_POINT ( 'NONE',  ( 0.3211332658540719254, -1.297355586764235236, 0.4182417297899396202 ) ) ;
#17322=FACE_OUTER_BOUND ( 'NONE', #18621, .T. ) ;
#17326=CARTESIAN_POINT ( 'NONE',  ( 0.01138001396866243804, -0.9310208032443704207, 0.05798820300846099784 ) ) ;
#17327=CARTESIAN_POINT ( 'NONE',  ( 0.4351293263873937667, -1.231514889939106849, 0.5832342842089121016 ) ) ;
#17330=CARTESIAN_POINT ( 'NONE',  ( 0.1209218709639075517, -1.413449759333152755, 0.6688053819537839173 ) ) ;
#17331=CARTESIAN_POINT ( 'NONE',  ( 0.4679067357895266843, -1.070896998011005019, 0.6479521087143890190 ) ) ;
#17333=CARTESIAN_POINT ( 'NONE',  ( 0.1907823988372855106, -0.4944553380418882926, 0.2959634315342150046 ) ) ;
#17335=EDGE_CURVE ( 'NONE', #30976, #12637, #9321, .T. ) ;
#17336=DIRECTION ( 'NONE',  ( -0.4999551463232372317, 0.8660512985181135770, -0.000000000000000000 ) ) ;
#17341=CARTESIAN_POINT ( 'NONE',  ( 0.04683743026951789346, -0.8297330588939687557, 0.7132132020604889933 ) ) ;
#17344=CARTESIAN_POINT ( 'NONE',  ( 0.08271545042603034581, -1.307985630826135059, 0.4687282396759575587 ) ) ;
#17345=CARTESIAN_POINT ( 'NONE',  ( 0.2421510470436483708, -1.227192766047864758, 0.5682417262808779901 ) ) ;
#17348=CARTESIAN_POINT ( 'NONE',  ( 0.2318926187578342901, -0.6847811903715324000, 0.4821206442548801596 ) ) ;
#17350=VERTEX_POINT ( 'NONE', #31491 ) ;
#17360=CARTESIAN_POINT ( 'NONE',  ( 0.08670746357302318297, -1.302632728992202837, 0.5759743761708646659 ) ) ;
#17361=CARTESIAN_POINT ( 'NONE',  ( 0.1293136892229509449, -0.7528337723472907639, 0.4737154814036002026 ) ) ;
#17363=CARTESIAN_POINT ( 'NONE',  ( 0.2758292747667600575, -1.561373478687104743, 0.9870382891917031110 ) ) ;
#17364=CARTESIAN_POINT ( 'NONE',  ( 0.09869151381832386161, -0.5631343475376648922, 0.2335645800241998582 ) ) ;
#17366=CARTESIAN_POINT ( 'NONE',  ( 0.1132205867452878156, -0.6714125266378772050, -0.09528610095238206068 ) ) ;
#17367=CARTESIAN_POINT ( 'NONE',  ( 0.3181856309082868317, -1.645723040471628762, 0.6029037648573117858 ) ) ;
#17368=CARTESIAN_POINT ( 'NONE',  ( 0.09699292618303559377, -0.9356975710665345058, 0.2689778393378690069 ) ) ;
#17370=VERTEX_POINT ( 'NONE', #15859 ) ;
#17371=DIRECTION ( 'NONE',  ( 0.5741533254374902029, 0.3983735212876081122, -0.7152946920158034239 ) ) ;
#17372=CARTESIAN_POINT ( 'NONE',  ( 0.1177181460812074948, -0.4737793742729833890, 0.2761546688069523858 ) ) ;
#17376=CARTESIAN_POINT ( 'NONE',  ( 0.07069647374262323647, -1.314947515254170307, 0.5019162079743227922 ) ) ;
#17377=VECTOR ( 'NONE', #1072, 39.37007874015748143 ) ;
#17380=CARTESIAN_POINT ( 'NONE',  ( 0.6183701179687098870, -1.298963174629117479, 0.5817474467243960445 ) ) ;
#17390=CARTESIAN_POINT ( 'NONE',  ( 0.4040203406124813212, -0.9939942186036138105, 0.7028486825154387496 ) ) ;
#17391=CARTESIAN_POINT ( 'NONE',  ( 0.5207218691171461300, -1.171053392212251021, 0.4666017006239680520 ) ) ;
#17393=CARTESIAN_POINT ( 'NONE',  ( 0.05122501923433656068, -0.8846498927777804999, 0.5029692314556662991 ) ) ;
#17397=DIRECTION ( 'NONE',  ( -1.000000000000000000, 0.000000000000000000, 0.000000000000000000 ) ) ;
#17400=CARTESIAN_POINT ( 'NONE',  ( 0.4023727053442279766, -1.150481506616649607, 0.6972092212261085109 ) ) ;
#17402=CARTESIAN_POINT ( 'NONE',  ( 0.4828795985232906540, -1.118743695481591915, 0.5686671663553843903 ) ) ;
#17410=CARTESIAN_POINT ( 'NONE',  ( 0.06359643539015311098, -0.5791250426409843000, 0.2975846012595457779 ) ) ;
#17411=CARTESIAN_POINT ( 'NONE',  ( 0.06671632896744131291, -0.6969372051195925621, -0.001946471286827283678 ) ) ;
#17412=CARTESIAN_POINT ( 'NONE',  ( 0.1937362933224030803, -0.7983156727584820311, 0.2891542942581120657 ) ) ;
#17413=CARTESIAN_POINT ( 'NONE',  ( 0.1637585665034339832, -0.5994899851647166322, 0.1022936816274461203 ) ) ;
#17415=EDGE_LOOP ( 'NONE', ( #10058, #17680, #132, #9289 ) ) ;
#17418=CARTESIAN_POINT ( 'NONE',  ( 0.5739118490517725046, -1.499259023535516988, 0.5731568487034417458 ) ) ;
#17422=CARTESIAN_POINT ( 'NONE',  ( 0.6017231405399463551, -1.610171036770066122, 0.5941483199617545452 ) ) ;
#17425=CARTESIAN_POINT ( 'NONE',  ( 0.6335034394193310714, -1.559158136216843404, 0.4182417262808776903 ) ) ;
#17426=CARTESIAN_POINT ( 'NONE',  ( 0.1524794451307193710, -1.279078254004480053, 0.4205905341015664378 ) ) ;
#17429=CARTESIAN_POINT ( 'NONE',  ( 0.08845320025402096664, -0.5635964745544715937, 0.02268293738053128727 ) ) ;
#17431=CARTESIAN_POINT ( 'NONE',  ( 0.1875104876115774588, -0.4605130342159906021, 0.1706505080850997946 ) ) ;
#17436=CARTESIAN_POINT ( 'NONE',  ( 0.6475056143351221039, -1.571742384113670621, 0.6112107622448768041 ) ) ;
#17442=CARTESIAN_POINT ( 'NONE',  ( 0.3137727395043992673, -1.722325404801505089, 0.8203598276066251804 ) ) ;
#17444=CARTESIAN_POINT ( 'NONE',  ( 0.1131241454731939100, -0.6872203660140440151, -0.09530310615070609892 ) ) ;
#17445=CARTESIAN_POINT ( 'NONE',  ( 0.4718448929443245232, -1.683416021769955861, 0.5701492720201403186 ) ) ;
#17456=CARTESIAN_POINT ( 'NONE',  ( 0.5337193422410454469, -1.352074988199290617, 0.5876441216552129587 ) ) ;
#17459=CARTESIAN_POINT ( 'NONE',  ( 0.2706875035899702353, -0.8747201880513900685, 0.5443116846754595395 ) ) ;
#17461=ORIENTED_EDGE ( 'NONE', *, *, #13715, .F. ) ;
#17463=CARTESIAN_POINT ( 'NONE',  ( 0.02497539211394332256, -0.5654553311636884017, 0.2802127003532230431 ) ) ;
#17464=CARTESIAN_POINT ( 'NONE',  ( 0.6781574892493564821, -1.522851489271323189, 0.4444256985947928063 ) ) ;
#17465=CARTESIAN_POINT ( 'NONE',  ( 0.1770450918743750601, -0.4681907750250927647, 0.07469303172640867627 ) ) ;
#17466=CARTESIAN_POINT ( 'NONE',  ( 0.4093611158985690501, -1.131941421409890403, 0.5197417262808780025 ) ) ;
#17470=CIRCLE ( 'NONE', #31281, 0.08249999999977555842 ) ;
#17471=FACE_OUTER_BOUND ( 'NONE', #29356, .T. ) ;
#17474=CARTESIAN_POINT ( 'NONE',  ( 0.08825382088300037786, -0.8443243380302292156, 0.3515346555839444220 ) ) ;
#17476=CARTESIAN_POINT ( 'NONE',  ( 0.3323178337258445580, -1.749637176862759880, 0.4593294054832028350 ) ) ;
#17488=CARTESIAN_POINT ( 'NONE',  ( 0.4168500870363872068, -1.141030447601083742, 0.4330279073753918739 ) ) ;
#17490=CARTESIAN_POINT ( 'NONE',  ( 0.7083987901907250473, -1.516814183290504214, 0.5551003832434545648 ) ) ;
#17493=CARTESIAN_POINT ( 'NONE',  ( 0.01221484228109331709, -0.4284514069139452874, 0.1505827212209437382 ) ) ;
#17494=CARTESIAN_POINT ( 'NONE',  ( 0.4246513848252074785, -1.105208224189071942, 0.5933906341394227235 ) ) ;
#17500=CARTESIAN_POINT ( 'NONE',  ( 0.4226000438817392180, -1.709616762427842218, 0.4282184315516496809 ) ) ;
#17504=CARTESIAN_POINT ( 'NONE',  ( 0.5512873130268265420, -1.413716574473140142, 0.7672181155003892083 ) ) ;
#17505=CARTESIAN_POINT ( 'NONE',  ( 0.0002045689356396978231, -0.6663330284319074481, -0.01264868658114923390 ) ) ;
#17507=AXIS2_PLACEMENT_3D ( 'NONE', #932, #10147, #28456 ) ;
#17511=CARTESIAN_POINT ( 'NONE',  ( 0.2700346912201526672, -1.656539685250784766, 0.7399851559723034100 ) ) ;
#17513=CARTESIAN_POINT ( 'NONE',  ( 0.1995953702521893469, -1.242370031073753323, 0.5988181646041325079 ) ) ;
#17519=CARTESIAN_POINT ( 'NONE',  ( 0.01137586991659313325, -0.9325856198352224791, 0.06247312220023811674 ) ) ;
#17520=CARTESIAN_POINT ( 'NONE',  ( 0.1182319155106198311, -1.406289766173004052, 0.6146117128210031311 ) ) ;
#17522=CARTESIAN_POINT ( 'NONE',  ( 0.1708199212777183340, -0.7760174123164113036, 0.5959575580650713356 ) ) ;
#17523=CARTESIAN_POINT ( 'NONE',  ( 0.06843411546424661707, -1.327640554429453168, 0.5682417262808774350 ) ) ;
#17524=PLANE ( 'NONE',  #11326 ) ;
#17539=CARTESIAN_POINT ( 'NONE',  ( 0.03132541776874769868, -0.7585458590990268313, 0.6287131927338691639 ) ) ;
#17540=CARTESIAN_POINT ( 'NONE',  ( 0.4756538103953397711, -1.077424610118791648, 0.6442006390088441670 ) ) ;
#17543=CARTESIAN_POINT ( 'NONE',  ( 0.1883801994403443147, -0.4771412664261568959, 0.2456734866192890887 ) ) ;
#17544=EDGE_CURVE ( 'NONE', #2251, #8719, #17090, .T. ) ;
#17545=EDGE_LOOP ( 'NONE', ( #26877, #38201, #1994, #35809, #35876 ) ) ;
#17552=CARTESIAN_POINT ( 'NONE',  ( 0.06682382353313973122, -0.8940662392066401898, 0.7548868145630993620 ) ) ;
#17558=CARTESIAN_POINT ( 'NONE',  ( 0.1912376716460947867, -0.5867422834582064484, 0.1926850933134615362 ) ) ;
#17564=FACE_OUTER_BOUND ( 'NONE', #5129, .T. ) ;
#17568=CARTESIAN_POINT ( 'NONE',  ( 0.09322317613841625550, -1.292681667036668536, 0.5862519905939423959 ) ) ;
#17569=CARTESIAN_POINT ( 'NONE',  ( 0.08630836114928054636, -0.7249243428820488777, 0.1580372468105708250 ) ) ;
#17570=B_SPLINE_CURVE_WITH_KNOTS ( 'NONE', 3,
 ( #19958, #29221, #19750, #17068, #4104, #26940, #32492, #23264, #32700, #1458 ),
 .UNSPECIFIED., .F., .F.,
 ( 4, 2, 2, 2, 4 ),
 ( 0.002191118811101763590, 0.002741761465162498475, 0.003292404119223232926, 0.003843046773283967377, 0.004393689427344702261 ),
 .UNSPECIFIED. ) ;
#17571=CARTESIAN_POINT ( 'NONE',  ( 0.2459797859955291377, -1.413075159975130557, 1.027285411072242027 ) ) ;
#17572=CARTESIAN_POINT ( 'NONE',  ( 0.1330595972864711818, -0.7019348493605459538, 0.5085182576753194406 ) ) ;
#17573=CARTESIAN_POINT ( 'NONE',  ( 0.1148637460941117766, -0.4678991626007031890, 0.04620028533150236788 ) ) ;
#17575=CARTESIAN_POINT ( 'NONE',  ( 0.3724417182818310357, -1.137927301686664894, 0.6120655133956764971 ) ) ;
#17580=CARTESIAN_POINT ( 'NONE',  ( 0.1960084681062461975, -0.5083467667687623370, 0.3310205429436359204 ) ) ;
#17581=ADVANCED_FACE ( 'NONE', ( #8821 ), #39765, .T. ) ;
#17588=CARTESIAN_POINT ( 'NONE',  ( 0.5081268369560435483, -1.127385812641128693, 0.7490048996577514107 ) ) ;
#17589=B_SPLINE_SURFACE_WITH_KNOTS ( 'NONE', 5, 5, ( 
 ( #5920, #30640, #34118, #2046, #2261, #2653 ),
 ( #8820, #14579, #40286, #21398, #24684, #33494 ),
 ( #37214, #40501, #11901, #17667, #33937, #15404 ),
 ( #24466, #27150, #9034, #21593, #40077, #15194 ),
 ( #18088, #37000, #18482, #11516, #36393, #5112 ),
 ( #14999, #30832, #31038, #2464, #21175, #2856 ) ),
 .UNSPECIFIED., .F., .F., .F.,
 ( 6, 6 ),
 ( 6, 6 ),
 ( -6.477000000001651436, 6.477000000001640778 ),
 ( -2.080605796196440593, 4.396394203803596135 ),
 .UNSPECIFIED. ) ;
#17593=ORIENTED_EDGE ( 'NONE', *, *, #26350, .F. ) ;
#17595=CARTESIAN_POINT ( 'NONE',  ( 0.4352891435086604921, -1.230633402764584217, 0.5979772237276071989 ) ) ;
#17600=CARTESIAN_POINT ( 'NONE',  ( 0.05369492612522367564, -0.8909568881529167372, 0.5212784798856601176 ) ) ;
#17606=CARTESIAN_POINT ( 'NONE',  ( 0.4658302039846137221, -1.234123384229465437, 0.6126497851603042166 ) ) ;
#17608=CARTESIAN_POINT ( 'NONE',  ( 0.5205119442373250527, -1.138897204853200229, 0.5683089796893805445 ) ) ;
#17614=CARTESIAN_POINT ( 'NONE',  ( 0.1000474123420599382, -0.7296998566091608129, 0.5617000639417457641 ) ) ;
#17615=CARTESIAN_POINT ( 'NONE',  ( 0.08936724799475873060, -0.5571496410808217670, 0.08395718622765509231 ) ) ;
#17620=CARTESIAN_POINT ( 'NONE',  ( 0.2615233978049238406, -1.678084768816710648, 0.5373352594323992371 ) ) ;
#17621=CARTESIAN_POINT ( 'NONE',  ( 0.4497016209966545053, -1.290036543533680913, 0.8253355315714806517 ) ) ;
#17624=CARTESIAN_POINT ( 'NONE',  ( 0.6522658206810004744, -1.579593865398426722, 0.6111888698553425980 ) ) ;
#17626=CARTESIAN_POINT ( 'NONE',  ( 0.6486139156353442070, -1.547557828783085121, 0.4182417262808776903 ) ) ;
#17627=CARTESIAN_POINT ( 'NONE',  ( 0.1136150038498828785, -1.301558380274246751, 0.4408081706944013689 ) ) ;
#17630=CARTESIAN_POINT ( 'NONE',  ( 0.3508337187165347926, -0.8535322721259723799, 0.7608596062780633718 ) ) ;
#17634=LINE ( 'NONE', #33459, #290 ) ;
#17637=CARTESIAN_POINT ( 'NONE',  ( 0.1282168942194763239, -1.302307715041175928, 0.4238844456335508215 ) ) ;
#17638=CARTESIAN_POINT ( 'NONE',  ( 0.03506116283237684095, -0.6633195576212149724, 0.6677130251333698308 ) ) ;
#17648=CARTESIAN_POINT ( 'NONE',  ( 0.5200485381878245938, -1.326553309810435399, 0.6274662840736040526 ) ) ;
#17651=CARTESIAN_POINT ( 'NONE',  ( 0.5138550893713603740, -1.118750960246259307, 0.5715134594416469982 ) ) ;
#17656=CARTESIAN_POINT ( 'NONE',  ( 0.3570248845998820197, -1.622585014455490304, 0.5866312166437432918 ) ) ;
#17657=CARTESIAN_POINT ( 'NONE',  ( 0.7071432900848956260, -1.497117398935195354, 0.5333719091693975844 ) ) ;
#17658=CARTESIAN_POINT ( 'NONE',  ( 0.1437340355044557927, -1.283861693981850349, 0.4177417262808780229 ) ) ;
#17663=CARTESIAN_POINT ( 'NONE',  ( 0.3183040104215587029, -1.268443597496760056, 0.6598424690337639786 ) ) ;
#17667=CARTESIAN_POINT ( 'NONE',  ( 0.4793488899164102257, -1.661214906270700453, 0.4177417262808786336 ) ) ;
#17668=CARTESIAN_POINT ( 'NONE',  ( 0.3613793631777935111, -1.160337313064966347, 0.4225651295761964632 ) ) ;
#17672=CARTESIAN_POINT ( 'NONE',  ( 0.3579638268247242183, -1.149302532586722103, 0.4372416223683186498 ) ) ;
#17679=ADVANCED_FACE ( 'NONE', ( #23663, #23870 ), #7999, .T. ) ;
#17680=ORIENTED_EDGE ( 'NONE', *, *, #25847, .F. ) ;
#17682=ORIENTED_EDGE ( 'NONE', *, *, #16543, .F. ) ;
#17683=CARTESIAN_POINT ( 'NONE',  ( 0.1788859795914834461, -0.5039164411451052539, 0.2269575196228969527 ) ) ;
#17689=CARTESIAN_POINT ( 'NONE',  ( 0.006255712965108143654, -0.8411565454896892113, 0.1072706165909301929 ) ) ;
#17695=CARTESIAN_POINT ( 'NONE',  ( 0.2666826698441861487, -1.675428791908667892, 0.5775416952914532720 ) ) ;
#17697=CARTESIAN_POINT ( 'NONE',  ( 0.1475177807054492418, -1.270527447976652180, 0.6057499628053283347 ) ) ;
#17698=DIRECTION ( 'NONE',  ( 0.4999551463232372317, -0.8660512985181135770, 0.000000000000000000 ) ) ;
#17703=CARTESIAN_POINT ( 'NONE',  ( 0.3866205031219385191, -1.115072307344278535, 0.6234536249022221144 ) ) ;
#17705=CARTESIAN_POINT ( 'NONE',  ( 0.2101951102887192890, -1.233953443661628846, 0.5631135429232324574 ) ) ;
#17706=CARTESIAN_POINT ( 'NONE',  ( 0.1724982287072397702, -0.8035217669752177105, 0.5910157953457164659 ) ) ;
#17707=CARTESIAN_POINT ( 'NONE',  ( 0.1852881512505511474, -0.8378655682486129130, 0.1409330132775444278 ) ) ;
#17709=DIRECTION ( 'NONE',  ( 0.9848077530122080203, -0.1736481776669303589, -3.189865274363657256E-17 ) ) ;
#17716=CARTESIAN_POINT ( 'NONE',  ( -1.133455804397020025E-05, -0.9470593448225452793, 0.1159768874212486062 ) ) ;
#17720=EDGE_CURVE ( 'NONE', #5090, #40153, #31316, .T. ) ;
#17721=CARTESIAN_POINT ( 'NONE',  ( 0.2322327485446251394, -1.539891620887370749, 0.8667544471685157959 ) ) ;
#17722=CARTESIAN_POINT ( 'NONE',  ( 0.2530466182501821537, -0.9510907114987208200, 0.4863111693326979679 ) ) ;
#17723=CARTESIAN_POINT ( 'NONE',  ( 0.02653710545434064677, -0.9701798883197163548, 0.6461398643848382806 ) ) ;
#17725=CARTESIAN_POINT ( 'NONE',  ( 0.1875104876115774588, -0.4605130342159906021, 0.1706505080850997946 ) ) ;
#17730=ORIENTED_EDGE ( 'NONE', *, *, #33508, .F. ) ;
#17732=CARTESIAN_POINT ( 'NONE',  ( 0.02323507894693532111, -0.7204624892072191145, 0.5750910600171844633 ) ) ;
#17734=CARTESIAN_POINT ( 'NONE',  ( 0.5879123204753100573, -1.491226093260655583, 0.5729944458046030142 ) ) ;
#17739=ADVANCED_FACE ( 'NONE', ( #12325 ), #3425, .T. ) ;
#17740=CARTESIAN_POINT ( 'NONE',  ( 0.2790103250938448243, -0.7681568326658522183, 0.6036499921438334137 ) ) ;
#17741=VERTEX_POINT ( 'NONE', #27752 ) ;
#17746=CARTESIAN_POINT ( 'NONE',  ( 0.4549080897931743750, -1.227294277471189465, 0.6004711738143356792 ) ) ;
#17753=CARTESIAN_POINT ( 'NONE',  ( 0.1550089719294916735, -0.8025920081343739243, 0.5453556522365147208 ) ) ;
#17754=CARTESIAN_POINT ( 'NONE',  ( 0.2518910028716056515, -1.434241493328622941, 1.024070326526868469 ) ) ;
#17756=CARTESIAN_POINT ( 'NONE',  ( 0.2083161643468393331, -0.8974363671813946342, 0.7129651506473948519 ) ) ;
#17760=CARTESIAN_POINT ( 'NONE',  ( 0.01684860433265163854, -0.9502109314606926871, 0.2753421542032672975 ) ) ;
#17764=CARTESIAN_POINT ( 'NONE',  ( 0.4470003202926319807, -1.034455986214164902, 0.7862651520392351934 ) ) ;
#17767=DIRECTION ( 'NONE',  ( 0.08797602414327373999, 0.6303231869445276025, 0.7713318994933610062 ) ) ;
#17769=CARTESIAN_POINT ( 'NONE',  ( 0.3206377073886440554, -1.170977842177069350, 0.5588165336952308770 ) ) ;
#17770=CARTESIAN_POINT ( 'NONE',  ( 0.5761226916817485666, -1.227707429964641328, 0.7155794456320599961 ) ) ;
#17780=VERTEX_POINT ( 'NONE', #15405 ) ;
#17785=CARTESIAN_POINT ( 'NONE',  ( 0.2203738904872941939, -1.339329718032100880, 0.6315676663001210667 ) ) ;
#17792=CARTESIAN_POINT ( 'NONE',  ( 0.4069238378739554185, -1.154943970571837175, 0.6833052645732561325 ) ) ;
#17798=CARTESIAN_POINT ( 'NONE',  ( 0.06653396568654543208, -1.328888091817681749, 0.5069507058184855586 ) ) ;
#17801=CARTESIAN_POINT ( 'NONE',  ( 0.4426374324197126509, -1.573834870353632898, 0.5890683219565086004 ) ) ;
#17802=CARTESIAN_POINT ( 'NONE',  ( 0.08771197480159868831, -0.6713012847033815733, 0.02348685380516160603 ) ) ;
#17811=CARTESIAN_POINT ( 'NONE',  ( 0.5779626767790062569, -1.486117140961969563, 0.6660763835963422475 ) ) ;
#17813=AXIS2_PLACEMENT_3D ( 'NONE', #10828, #4616, #17397 ) ;
#17816=CARTESIAN_POINT ( 'NONE',  ( 0.1743562189534910989, -1.266421578639647327, 0.4246093132792315150 ) ) ;
#17820=CARTESIAN_POINT ( 'NONE',  ( 0.7220926616001757115, -1.479655736425856682, 0.5682417262808782121 ) ) ;
#17821=CARTESIAN_POINT ( 'NONE',  ( 0.07497864282572903882, -1.322056043867073427, 0.4862695133534064018 ) ) ;
#17822=CARTESIAN_POINT ( 'NONE',  ( 0.01423347799720674905, -0.9652063955883527502, 0.3874744253929337523 ) ) ;
#17827=CARTESIAN_POINT ( 'NONE',  ( 0.5881428029937501023, -1.617990245335324984, 0.5794342689744652608 ) ) ;
#17828=CARTESIAN_POINT ( 'NONE',  ( 0.6973771390368941336, -1.438889517336061408, 0.5421659396764333394 ) ) ;
#17830=CARTESIAN_POINT ( 'NONE',  ( 0.1835961851041346959, -0.5126270562563732813, 0.08826789480522242992 ) ) ;
#17832=CARTESIAN_POINT ( 'NONE',  ( 0.1664437047740607023, -1.270578109106206277, 0.5509909136888835324 ) ) ;
#17833=VECTOR ( 'NONE', #8256, 39.37007874015748854 ) ;
#17834=ADVANCED_FACE ( 'NONE', ( #32389 ), #38443, .T. ) ;
#17836=ORIENTED_EDGE ( 'NONE', *, *, #35512, .F. ) ;
#17840=CARTESIAN_POINT ( 'NONE',  ( 0.3870156086493387604, -1.114928226039928028, 0.6233982234651463950 ) ) ;
#17844=CARTESIAN_POINT ( 'NONE',  ( 0.5323400999026242086, -1.348064161999662280, 0.6174472662931688172 ) ) ;
#17846=ORIENTED_EDGE ( 'NONE', *, *, #21883, .F. ) ;
#17847=CARTESIAN_POINT ( 'NONE',  ( 0.4955945803445692133, -1.095919195860131534, 0.6270439991606266972 ) ) ;
#17850=ORIENTED_EDGE ( 'NONE', *, *, #37441, .T. ) ;
#17851=CARTESIAN_POINT ( 'NONE',  ( 0.3690965330173307524, -1.099411688709415413, 0.5182417262812423209 ) ) ;
#17852=CARTESIAN_POINT ( 'NONE',  ( 0.1349261257125279889, -0.9884281589464994910, 0.8058857660061659045 ) ) ;
#17853=CARTESIAN_POINT ( 'NONE',  ( 0.7014158978116333820, -1.493052833726295381, 0.5008243877641355146 ) ) ;
#17855=CARTESIAN_POINT ( 'NONE',  ( 0.1637488714925408873, -0.5994898440788770655, 0.1932149833450298726 ) ) ;
#17858=CARTESIAN_POINT ( 'NONE',  ( 0.3743249978302641279, -1.006520688755567106, 0.6168196747304992567 ) ) ;
#17862=CARTESIAN_POINT ( 'NONE',  ( 0.08497705572000407992, -0.8399793145007137252, 0.3168515346811236477 ) ) ;
#17864=ADVANCED_FACE ( 'NONE', ( #17167 ), #29327, .F. ) ;
#17865=CARTESIAN_POINT ( 'NONE',  ( 0.000000000000000000, -0.6872203660140440151, 0.1457185332388702681 ) ) ;
#17871=FACE_OUTER_BOUND ( 'NONE', #30948, .T. ) ;
#17874=CARTESIAN_POINT ( 'NONE',  ( 0.4471907055705798273, -1.138637937364841646, 0.4406841123770021684 ) ) ;
#17875=CARTESIAN_POINT ( 'NONE',  ( 0.4033617574584467680, -1.135069255774922015, 0.5545239497365388459 ) ) ;
#17877=CARTESIAN_POINT ( 'NONE',  ( 4.197799705714884069E-05, -0.4263059253886176680, 0.1506519890000039552 ) ) ;
#17888=CARTESIAN_POINT ( 'NONE',  ( -0.0007351284806403281420, -0.7588986013227282390, 0.002782588056763008258 ) ) ;
#17890=ORIENTED_EDGE ( 'NONE', *, *, #12267, .T. ) ;
#17895=CARTESIAN_POINT ( 'NONE',  ( 0.2052211579314608680, -1.341797434425455515, 0.9341812257356882920 ) ) ;
#17904=B_SPLINE_CURVE_WITH_KNOTS ( 'NONE', 3,
 ( #40620, #34044, #31380, #8532, #21102, #18003 ),
 .UNSPECIFIED., .F., .F.,
 ( 4, 2, 4 ),
 ( 0.000000000000000000, 0.5000000000000000000, 1.000000000000000000 ),
 .UNSPECIFIED. ) ;
#17905=CARTESIAN_POINT ( 'NONE',  ( 0.08509544147734073027, -0.8123111742434827587, 0.1597949892228995861 ) ) ;
#17906=CARTESIAN_POINT ( 'NONE',  ( 0.1146236400730676064, -1.385147693593549389, 0.6565552975533486268 ) ) ;
#17907=B_SPLINE_SURFACE_WITH_KNOTS ( 'NONE', 3, 3, ( 
 ( #35028, #9537, #28863, #37924, #3957, #3348, #12832, #723, #22717, #25173, #28452, #22114, #19421, #31955, #22304, #113, #7047, #25395, #34819, #13222, #12414, #24964, #3772, #16327, #34635, #25791, #6240, #3159, #539, #10144, #35249 ),
 ( #6628, #16519, #37495, #38316, #13034, #6432, #28249, #19204, #18813, #19004, #31746, #31536, #15703, #3564, #16133, #28670, #19616, #32151, #9317, #25586, #38113, #21898, #23328, #4555, #36048, #928, #8054, #13436, #19804, #20419, #7447 ),
 ( #38527, #20231, #7664, #35641, #1130, #17330, #10543, #22920, #35435, #32342, #7235, #26005, #20632, #4163, #35851, #10972, #26609, #13632, #38925, #16730, #13824, #29473, #32751, #26198, #29281, #20021, #38722, #32953, #32554, #23118, #7847 ),
 ( #1317, #17124, #33168, #4374, #4757, #29674, #16929, #4973, #29888, #26394, #29059, #10357, #1516, #10755, #23529, #14034, #39145, #1728, #14244, #26807, #39334, #11156, #23713, #36240, #39524, #8661, #5169, #34170, #12173, #30086, #8464 ),
 ( #14636, #30487, #37057, #30269, #30696, #21234, #21455, #17721, #2099, #9080, #11356, #36848, #27206, #33361, #2316, #23925, #30887, #17539, #40344, #2517, #15056, #2708, #36658, #26996, #36456, #37264, #17926, #21646, #27606, #8268, #24136 ),
 ( #14857, #11963, #24737, #14427, #39740, #33980, #27420, #5785, #20841, #11574, #21028, #40135, #33552, #1914, #5361, #33772, #18342, #39943, #11763, #24320, #24528, #5582, #18141, #8879, #15252, #27810, #22263, #28019, #15865, #21849, #9696 ),
 ( #6394, #37881, #10097, #22065, #9884, #34776, #12372, #22671, #6792, #34590, #38266, #31095, #6581, #28413, #496, #75, #18960, #40552, #25541, #25739, #31309, #19163, #2915, #25128, #24928, #31701, #34376, #37456, #28821, #5978, #28625 ) ),
 .UNSPECIFIED., .F., .F., .F.,
 ( 4, 1, 1, 1, 4 ),
 ( 4, 1, 1, 1, 1, 1, 1, 1, 1, 1, 1, 1, 1, 1, 1, 1, 1, 1, 1, 1, 1, 1, 1, 1, 1, 3, 4 ),
 ( 0.000000000000000000, 0.2500000000000000000, 0.5000000000000000000, 0.7500000000000000000, 1.000000000000000000 ),
 ( 0.000000000000000000, 0.03051875000000000074, 0.04577812500000000978, 0.06103750000000000148, 0.09155625000000001956, 0.1220750000000000030, 0.1525937500000000002, 0.1831125000000000391, 0.2136312499999999948, 0.2441500000000000059, 0.2993062499999999959, 0.3544624999999999027, 0.4096187500000000314, 0.4647750000000000492, 0.5199312500000002890, 0.5750875000000000847, 0.6302437499999999915, 0.6854000000000000092, 0.7247249999999998415, 0.7640500000000001180, 0.8033749999999999503, 0.8427000000000000046, 0.8820249999999999480, 0.9213500000000000023, 0.9606749999999998346, 1.000000000000000000, 1.037727370758942724 ),
 .UNSPECIFIED. ) ;
#17908=CARTESIAN_POINT ( 'NONE',  ( 0.2242084987759379311, -0.9108783394681766454, 0.7161520956205715827 ) ) ;
#17909=CARTESIAN_POINT ( 'NONE',  ( 0.1874345095996926280, -0.6910927985529788931, 0.04286511273904547448 ) ) ;
#17913=CARTESIAN_POINT ( 'NONE',  ( 0.01221471773871474209, -0.4297850025901314708, 0.1735288129617342245 ) ) ;
#17916=DIRECTION ( 'NONE',  ( 0.8660512985181135770, 0.4999551463232371762, 0.000000000000000000 ) ) ;
#17918=CARTESIAN_POINT ( 'NONE',  ( 0.3060205578877235877, -1.769002121529782423, 0.4687417262808789009 ) ) ;
#17919=CARTESIAN_POINT ( 'NONE',  ( 0.4548090296651450259, -1.115736959625045932, 0.5760494755837164416 ) ) ;
#17922=EDGE_CURVE ( 'NONE', #13839, #12748, #1460, .T. ) ;
#17923=CIRCLE ( 'NONE', #30418, 0.08749999999977552123 ) ;
#17926=CARTESIAN_POINT ( 'NONE',  ( 0.003124719664520334353, -0.5686731593868922241, 0.1635439462316863046 ) ) ;
#17930=CARTESIAN_POINT ( 'NONE',  ( 0.6419406851146725046, -1.339736372716090917, 0.8215813590131169075 ) ) ;
#17938=VERTEX_POINT ( 'NONE', #7491 ) ;
#17941=CARTESIAN_POINT ( 'NONE',  ( 0.1793448322649782434, -1.306301048382400465, 0.9356552813208593999 ) ) ;
#17942=CARTESIAN_POINT ( 'NONE',  ( 0.1287628997187199309, -0.5693032371059245644, 0.2349318639996405556 ) ) ;
#17946=CARTESIAN_POINT ( 'NONE',  ( 0.6170741104697204937, -1.294989041298300947, 0.6128831306409553425 ) ) ;
#17947=EDGE_LOOP ( 'NONE', ( #29033, #37625, #2289, #15371 ) ) ;
#17951=CYLINDRICAL_SURFACE ( 'NONE', #38385, 0.2500000000000000000 ) ;
#17954=DIRECTION ( 'NONE',  ( -0.8660512985181133550, -0.4999551463232372317, 0.000000000000000000 ) ) ;
#17955=VERTEX_POINT ( 'NONE', #32600 ) ;
#17956=CARTESIAN_POINT ( 'NONE',  ( 0.2374407952065339944, -0.9329004813706425203, 0.6724982063807530830 ) ) ;
#17958=CARTESIAN_POINT ( 'NONE',  ( 0.2243373955775073425, -1.373658029840927997, 1.035783466587031132 ) ) ;
#17960=CARTESIAN_POINT ( 'NONE',  ( 0.1177320669826718569, -0.6536998228781175646, 0.4362173610713035443 ) ) ;
#17962=CARTESIAN_POINT ( 'NONE',  ( -0.001619896210524758443, -0.8333112946399738874, 0.06168507148062359058 ) ) ;
#17963=CARTESIAN_POINT ( 'NONE',  ( 0.01081354071025426335, -1.017577864057874315, 0.5450223083628769061 ) ) ;
#17967=CARTESIAN_POINT ( 'NONE',  ( 0.6157026484039241909, -1.296264186265224438, 0.8027992624428816892 ) ) ;
#17978=CARTESIAN_POINT ( 'NONE',  ( 0.3172427931101068910, -1.184417370245142376, 0.5253393887875316137 ) ) ;
#17979=CARTESIAN_POINT ( 'NONE',  ( 0.1937691639527174270, -0.6993326081247003279, 0.2764035553309984738 ) ) ;
#17988=ADVANCED_FACE ( 'NONE', ( #33601 ), #7427, .F. ) ;
#17991=CARTESIAN_POINT ( 'NONE',  ( 0.2012009467146754493, -0.8934095266790128553, 0.6235197419108591266 ) ) ;
#17994=CARTESIAN_POINT ( 'NONE',  ( 0.01696032325262748774, -0.8707704970672307532, 0.4345434047485409179 ) ) ;
#18001=CARTESIAN_POINT ( 'NONE',  ( 0.4262369507677812308, -1.179622181167630179, 0.6860357087046927704 ) ) ;
#18003=CARTESIAN_POINT ( 'NONE',  ( 0.0004750592482352814579, -0.4386115460793976739, 0.1457185332388683252 ) ) ;
#18005=ORIENTED_EDGE ( 'NONE', *, *, #24480, .T. ) ;
#18006=FACE_OUTER_BOUND ( 'NONE', #33965, .T. ) ;
#18008=( BOUNDED_SURFACE ( )  B_SPLINE_SURFACE ( 3, 2, ( 
 ( #28763, #10034, #13116 ),
 ( #19513, #2002, #13911 ),
 ( #36550, #14332, #29561 ),
 ( #29981, #17627, #36130 ),
 ( #26284, #5066, #14527 ),
 ( #30174, #26483, #1608 ),
 ( #27090, #23209, #20930 ),
 ( #17426, #33452, #5257 ),
 ( #4456, #7752, #39236 ),
 ( #38805, #24026, #14133 ),
 ( #17816, #30376, #7546 ),
 ( #4854, #17020, #29763 ),
 ( #26703, #10855, #11058 ),
 ( #13718, #23816, #36337 ),
 ( #8155, #39624, #1816 ),
 ( #11461, #8361, #26895 ),
 ( #20317, #10635, #23616 ),
 ( #20729, #35735, #32837 ),
 ( #23428, #35946, #33048 ),
 ( #20121, #32651, #33256 ),
 ( #1403, #39021, #4645 ),
 ( #17218, #7940, #20516 ),
 ( #11245, #39423, #34259 ),
 ( #12065, #18639, #8551 ),
 ( #34474, #37543, #15136 ),
 ( #40639, #31200, #6071 ),
 ( #8763, #11660, #40025 ),
 ( #3017, #24630, #21124 ) ),
 .UNSPECIFIED., .F., .F., .F. ) 
 B_SPLINE_SURFACE_WITH_KNOTS ( ( 4, 2, 2, 2, 2, 2, 2, 2, 2, 2, 2, 2, 2, 4 ),
 ( 3, 3 ),
 ( 0.002672765802653568300, 0.003643729169957819151, 0.004614692537262070002, 0.005100174220914195644, 0.005585655904566321286, 0.006071137588218446929, 0.006556619271870572571, 0.007042100955522698214, 0.007527582639174823856, 0.008013064322826949498, 0.008498546006479075141, 0.008984027690131200783, 0.009469509373783326425, 0.01044047274108757771 ),
 ( 0.000000000000000000, 1.000000000000000000 ),
 .UNSPECIFIED. ) 
 GEOMETRIC_REPRESENTATION_ITEM ( )  RATIONAL_B_SPLINE_SURFACE ( (
 ( 1.000000000000000000, 0.7094119666599625340, 1.000000000000000000),
 ( 1.000000000000000000, 0.7091975995508440489, 1.000000000000000000),
 ( 1.000000000000000000, 0.7089641823995880276, 1.000000000000000000),
 ( 1.000000000000000000, 0.7085568111716973316, 1.000000000000000000),
 ( 1.000000000000000000, 0.7083776127384138199, 1.000000000000000000),
 ( 1.000000000000000000, 0.7081748109123476853, 1.000000000000000000),
 ( 1.000000000000000000, 0.7081166372635343542, 1.000000000000000000),
 ( 1.000000000000000000, 0.7080222590712177411, 1.000000000000000000),
 ( 1.000000000000000000, 0.7079861540317865520, 1.000000000000000000),
 ( 1.000000000000000000, 0.7079344075164385464, 1.000000000000000000),
 ( 1.000000000000000000, 0.7079189101953833330, 1.000000000000000000),
 ( 1.000000000000000000, 0.7079093227531754184, 1.000000000000000000),
 ( 1.000000000000000000, 0.7079148671191604070, 1.000000000000000000),
 ( 1.000000000000000000, 0.7079463893497752736, 1.000000000000000000),
 ( 1.000000000000000000, 0.7079724427870122128, 1.000000000000000000),
 ( 1.000000000000000000, 0.7080416038675461099, 1.000000000000000000),
 ( 1.000000000000000000, 0.7080851831062294766, 1.000000000000000000),
 ( 1.000000000000000000, 0.7081858060029823099, 1.000000000000000000),
 ( 1.000000000000000000, 0.7082416808879808956, 1.000000000000000000),
 ( 1.000000000000000000, 0.7083570905282395858, 1.000000000000000000),
 ( 1.000000000000000000, 0.7084173298865795720, 1.000000000000000000),
 ( 1.000000000000000000, 0.7085256194978258870, 1.000000000000000000),
 ( 1.000000000000000000, 0.7085739217061582940, 1.000000000000000000),
 ( 1.000000000000000000, 0.7086427899149944087, 1.000000000000000000),
 ( 1.000000000000000000, 0.7086627554150931596, 1.000000000000000000),
 ( 1.000000000000000000, 0.7086506118568940416, 1.000000000000000000),
 ( 1.000000000000000000, 0.7085441098889576628, 1.000000000000000000),
 ( 1.000000000000000000, 0.7082931127450711184, 1.000000000000000000) ) ) 
 REPRESENTATION_ITEM ( '' )  SURFACE ( )  );
#18010=CARTESIAN_POINT ( 'NONE',  ( 0.4311562402287792972, -1.539438156933338631, 0.7516812456913292140 ) ) ;
#18013=DIRECTION ( 'NONE',  ( -1.000000000000000000, 0.000000000000000000, 0.000000000000000000 ) ) ;
#18014=ORIENTED_EDGE ( 'NONE', *, *, #2858, .F. ) ;
#18019=CARTESIAN_POINT ( 'NONE',  ( 0.1222542343297059741, -0.5526425588814477541, 0.1793279953326599452 ) ) ;
#18020=CARTESIAN_POINT ( 'NONE',  ( 0.4865950407719751292, -1.661532037359216840, 0.5397203252285756037 ) ) ;
#18031=ADVANCED_FACE ( 'NONE', ( #9117 ), #21682, .F. ) ;
#18032=AXIS2_PLACEMENT_3D ( 'NONE', #13475, #23152, #25833 ) ;
#18033=CARTESIAN_POINT ( 'NONE',  ( 0.1914513227106267590, -0.5214848928147161056, 0.2513073325497693911 ) ) ;
#18038=CARTESIAN_POINT ( 'NONE',  ( 0.2626070881998294193, -0.6796769646063650638, 0.05684369497733833543 ) ) ;
#18044=CARTESIAN_POINT ( 'NONE',  ( 0.003300039066125767893, -0.4845961630426517952, 0.3648084845760091732 ) ) ;
#18048=CARTESIAN_POINT ( 'NONE',  ( 0.1760551381089313916, -1.265079013133070474, 0.5412798231591671172 ) ) ;
#18049=CARTESIAN_POINT ( 'NONE',  ( 0.3740960844805631957, -1.108072201694596526, 0.5182417262812423209 ) ) ;
#18052=CIRCLE ( 'NONE', #39081, 0.01000000000000007827 ) ;
#18055=ADVANCED_FACE ( 'NONE', ( #12610 ), #17907, .T. ) ;
#18058=CARTESIAN_POINT ( 'NONE',  ( 0.3422943015738595385, -1.758122929102525989, 0.4605087972123807494 ) ) ;
#18060=CARTESIAN_POINT ( 'NONE',  ( 0.4290884103726456122, -1.188868616449923366, 0.7477856797621026397 ) ) ;
#18063=CARTESIAN_POINT ( 'NONE',  ( 0.3318484986314376162, -0.9704704429389122700, 0.6048456486855374736 ) ) ;
#18068=EDGE_LOOP ( 'NONE', ( #39822, #25161, #15429 ) ) ;
#18069=CARTESIAN_POINT ( 'NONE',  ( 0.2040651102238323633, -1.191688104741121856, 0.8916119944643040585 ) ) ;
#18071=CARTESIAN_POINT ( 'NONE',  ( 0.1771057343352051561, -0.4639829428808278089, 0.08932164138973593126 ) ) ;
#18075=CARTESIAN_POINT ( 'NONE',  ( 0.4041790769229076097, -0.9940227595139969896, 0.7031909273260571469 ) ) ;
#18076=CARTESIAN_POINT ( 'NONE',  ( 0.1162211104444988985, -0.5562432141033685218, 0.1993352053206045305 ) ) ;
#18080=CARTESIAN_POINT ( 'NONE',  ( 0.1224489045975470647, -0.8957878257233655717, 0.5611759970749146120 ) ) ;
#18087=CARTESIAN_POINT ( 'NONE',  ( 0.1822807072488307478, -0.9686607882321045526, 0.5003333243558089061 ) ) ;
#18088=CARTESIAN_POINT ( 'NONE',  ( 0.6601361389616772213, -1.566348459635070522, 0.5707417262808793801 ) ) ;
#18091=CARTESIAN_POINT ( 'NONE',  ( 0.04965997019300262549, -1.266850117287420696, 0.6475152895583352608 ) ) ;
#18094=CARTESIAN_POINT ( 'NONE',  ( 0.4842989215684344595, -1.127184663968222589, 0.5007281051682350714 ) ) ;
#18098=CARTESIAN_POINT ( 'NONE',  ( 1.621299365906332885E-05, -0.4335896441111527500, 0.08190102398457659028 ) ) ;
#18100=CARTESIAN_POINT ( 'NONE',  ( 0.3204139389452037023, -1.755336229099433654, 0.4849083929475442867 ) ) ;
#18109=FACE_BOUND ( 'NONE', #16310, .T. ) ;
#18113=EDGE_LOOP ( 'NONE', ( #6821, #14304 ) ) ;
#18115=EDGE_LOOP ( 'NONE', ( #9846, #34345, #4846, #7316 ) ) ;
#18116=CARTESIAN_POINT ( 'NONE',  ( 0.2685697523530611308, -1.675616378658084438, 0.6036540740780101943 ) ) ;
#18118=CARTESIAN_POINT ( 'NONE',  ( 0.2112634585974465518, -1.245876612383048032, 0.5715387936656939338 ) ) ;
#18121=CARTESIAN_POINT ( 'NONE',  ( 0.4953328006973022335, -1.658154532889615895, 0.5682417262808785452 ) ) ;
#18124=CARTESIAN_POINT ( 'NONE',  ( 0.01138352277355129775, -0.9296896336311132325, 0.05438588250771710098 ) ) ;
#18126=CARTESIAN_POINT ( 'NONE',  ( 0.3405242896115940887, -1.744906522954217110, 0.4484829386635745263 ) ) ;
#18128=CARTESIAN_POINT ( 'NONE',  ( 0.4280571948436235341, -1.214389859197892108, 0.8188955122002271603 ) ) ;
#18129=CARTESIAN_POINT ( 'NONE',  ( 0.1868462052469743451, -0.7315845167432759588, 0.03397798300244578296 ) ) ;
#18133=CARTESIAN_POINT ( 'NONE',  ( 0.4034340626290945364, -1.711742532993089982, 0.4219718062392947555 ) ) ;
#18137=CARTESIAN_POINT ( 'NONE',  ( 0.4370114410068630106, -1.106456163932805881, 0.5863244257242559154 ) ) ;
#18141=CARTESIAN_POINT ( 'NONE',  ( 0.005216780649377962716, -0.5315740328921342295, 0.3610413699792206499 ) ) ;
#18142=CARTESIAN_POINT ( 'NONE',  ( 0.08354342017514641838, -1.252940714712708958, 0.7526680972150427973 ) ) ;
#18144=CARTESIAN_POINT ( 'NONE',  ( 0.5633425123490871655, -1.213831759034801561, 0.8533915188341715252 ) ) ;
#18151=CARTESIAN_POINT ( 'NONE',  ( 0.6568730927750874304, -1.460570608776338597, 0.4224083929475443977 ) ) ;
#18152=CARTESIAN_POINT ( 'NONE',  ( 0.05418309106442487783, -0.8367704788373211411, 0.7042074783075930045 ) ) ;
#18153=CARTESIAN_POINT ( 'NONE',  ( 0.5875422609861711276, -1.491128227361789182, 0.5657178549513129928 ) ) ;
#18154=CARTESIAN_POINT ( 'NONE',  ( 0.3702892772755569384, -1.736523176964394732, 0.4320996613930846442 ) ) ;
#18156=CARTESIAN_POINT ( 'NONE',  ( 0.1909052096321314784, -0.5854118129141068216, 0.1777712087850742972 ) ) ;
#18166=CARTESIAN_POINT ( 'NONE',  ( 0.08829421125485691080, -0.7067105924166853237, 0.2075677057826203209 ) ) ;
#18167=CARTESIAN_POINT ( 'NONE',  ( 0.3227739583020200476, -1.719409737019245155, 0.8075189798695981969 ) ) ;
#18168=CARTESIAN_POINT ( 'NONE',  ( 0.4974589431443675047, -1.542506574375496209, 0.5734728255214222026 ) ) ;
#18170=CARTESIAN_POINT ( 'NONE',  ( -0.0003951118247478632847, -0.7312479731468258803, -0.01669275631305656288 ) ) ;
#18171=CARTESIAN_POINT ( 'NONE',  ( 0.05992090360963508999, -1.332693131100006756, 0.5682417262808777680 ) ) ;
#18174=ORIENTED_EDGE ( 'NONE', *, *, #2225, .T. ) ;
#18176=CARTESIAN_POINT ( 'NONE',  ( 0.3001519255637661865, -0.8839599682347554221, 0.8021632040787142204 ) ) ;
#18183=CARTESIAN_POINT ( 'NONE',  ( 0.4062230848227143531, -1.145582794160930895, 0.4248905050063966349 ) ) ;
#18184=CARTESIAN_POINT ( 'NONE',  ( 0.2606473226204091831, -1.679216544086299612, 0.4886760040442115205 ) ) ;
#18185=CARTESIAN_POINT ( 'NONE',  ( 0.3207953251618635981, -1.182327106099470448, 0.4907902897447509183 ) ) ;
#18186=CARTESIAN_POINT ( 'NONE',  ( 0.5317104447742054818, -1.152447470094080328, 0.6575248185080280194 ) ) ;
#18188=CARTESIAN_POINT ( 'NONE',  ( 0.1901359855603551308, -0.5909830539303996266, 0.3021763630842474457 ) ) ;
#18192=CARTESIAN_POINT ( 'NONE',  ( 0.6059691746655119227, -1.480133143157562170, 0.5526975506195443977 ) ) ;
#18194=ORIENTED_EDGE ( 'NONE', *, *, #9731, .F. ) ;
#18195=CARTESIAN_POINT ( 'NONE',  ( 0.4841659176569872991, -1.131373688278120238, 0.4858252441513852826 ) ) ;
#18197=CARTESIAN_POINT ( 'NONE',  ( 0.2209338557910215939, -0.9109865339892553315, 0.6537527485991542209 ) ) ;
#18201=CARTESIAN_POINT ( 'NONE',  ( 0.01310383523850323917, -0.8587138684673197853, 0.3611815158424811489 ) ) ;
#18202=VERTEX_POINT ( 'NONE', #37666 ) ;
#18209=EDGE_CURVE ( 'NONE', #16210, #12748, #14607, .T. ) ;
#18210=CARTESIAN_POINT ( 'NONE',  ( 0.4306335752601955780, -1.183459269765066102, 0.6683203921661764468 ) ) ;
#18212=CARTESIAN_POINT ( 'NONE',  ( 0.1633160071118299750, -1.272099323608264276, 0.4248106349649071189 ) ) ;
#18220=CARTESIAN_POINT ( 'NONE',  ( 0.4417812153713224221, -1.573793491951804402, 0.5750929000743407737 ) ) ;
#18222=CARTESIAN_POINT ( 'NONE',  ( 0.5623656178733204003, -1.618086598301832435, 0.5064396494810395888 ) ) ;
#18223=CARTESIAN_POINT ( 'NONE',  ( 0.4737925448037723086, -1.158599824872910800, 0.4226906129777907029 ) ) ;
#18229=CARTESIAN_POINT ( 'NONE',  ( 0.1226644528301022302, -0.5666400526987965813, 0.2303931865571023363 ) ) ;
#18230=CARTESIAN_POINT ( 'NONE',  ( 0.4722973099718666412, -1.670488640416608606, 0.5579311128194459624 ) ) ;
#18240=CARTESIAN_POINT ( 'NONE',  ( 0.2033263846434442690, -0.5675993867538808857, 0.3776288918835234987 ) ) ;
#18254=B_SPLINE_SURFACE_WITH_KNOTS ( 'NONE', 3, 3, ( 
 ( #27648, #2556, #21499, #18184 ),
 ( #24361, #18811, #6431, #19002 ),
 ( #31355, #12609, #3158, #2966 ),
 ( #40178, #8708, #21284, #15701 ) ),
 .UNSPECIFIED., .F., .F., .F.,
 ( 4, 4 ),
 ( 4, 4 ),
 ( -6.214954718652347943, -5.911709546377296398 ),
 ( -1.271269362639431799, -0.03735764515002289871 ),
 .UNSPECIFIED. ) ;
#18259=CARTESIAN_POINT ( 'NONE',  ( 0.3672888026336380562, -1.149235926965803012, 0.6020051486042412581 ) ) ;
#18263=CARTESIAN_POINT ( 'NONE',  ( 0.4508755845972571286, -1.219119228265584276, 0.7279328556006846584 ) ) ;
#18266=CARTESIAN_POINT ( 'NONE',  ( 0.2957689212018802527, -0.9454471935599602084, 0.5654756054326123271 ) ) ;
#18274=ORIENTED_EDGE ( 'NONE', *, *, #35292, .T. ) ;
#18275=CARTESIAN_POINT ( 'NONE',  ( 0.03561864634767011872, -0.5348410626444256577, 0.1638778232741606444 ) ) ;
#18277=CARTESIAN_POINT ( 'NONE',  ( 0.1760631799394591079, -0.6276024324974762703, -0.07686131200774137806 ) ) ;
#18280=CARTESIAN_POINT ( 'NONE',  ( 0.3979951050334158968, -1.018748020539158805, 0.6285197686894602453 ) ) ;
#18281=CARTESIAN_POINT ( 'NONE',  ( 0.5529634792074666905, -1.511186030616493259, 0.5729129695539203482 ) ) ;
#18282=B_SPLINE_CURVE_WITH_KNOTS ( 'NONE', 3,
 ( #14746, #23211, #11462, #20931, #14529, #26896 ),
 .UNSPECIFIED., .F., .F.,
 ( 4, 2, 4 ),
 ( 0.000000000000000000, 0.5000000000000000000, 1.000000000000000000 ),
 .UNSPECIFIED. ) ;
#18286=EDGE_CURVE ( 'NONE', #16916, #6325, #38575, .T. ) ;
#18294=CARTESIAN_POINT ( 'NONE',  ( 0.6540709664215760277, -1.593060928864740156, 0.5182417262812423209 ) ) ;
#18296=CARTESIAN_POINT ( 'NONE',  ( 1.365923996832131609E-16, -0.9481888444201347355, 0.09803024984676507458 ) ) ;
#18298=CARTESIAN_POINT ( 'NONE',  ( 0.4829265164743086758, -1.123232261319281333, 0.5052793004277540412 ) ) ;
#18300=VECTOR ( 'NONE', #33202, 39.37007874015748854 ) ;
#18302=CARTESIAN_POINT ( 'NONE',  ( 0.001991602493628476505, -0.9268535620581923595, 0.4078208622452191290 ) ) ;
#18304=CARTESIAN_POINT ( 'NONE',  ( 0.01645090811047977483, -0.5819932753755481247, 0.5292683286643183882 ) ) ;
#18311=EDGE_CURVE ( 'NONE', #24913, #27710, #1084, .T. ) ;
#18313=CARTESIAN_POINT ( 'NONE',  ( 0.2637382839637063547, -0.6009449316864781121, 0.1932256475537140750 ) ) ;
#18318=CARTESIAN_POINT ( 'NONE',  ( 0.2667337750453726564, -1.675443482348580648, 0.5781907244941091317 ) ) ;
#18319=CARTESIAN_POINT ( 'NONE',  ( 0.06443582815874832059, -0.8352844082028780814, 0.1887074755868990705 ) ) ;
#18320=CARTESIAN_POINT ( 'NONE',  ( 0.08995075563790964901, -1.315447267446937074, 0.5712668678535780531 ) ) ;
#18325=CARTESIAN_POINT ( 'NONE',  ( 0.3516693977051734143, -1.145166927642649046, 0.6147136096956975493 ) ) ;
#18326=DIRECTION ( 'NONE',  ( 0.9998941247116546194, -0.01455087607601020239, 0.0001066420868422379362 ) ) ;
#18328=CARTESIAN_POINT ( 'NONE',  ( 0.3234613948553985430, -1.057064862004813088, 0.7871205450755927036 ) ) ;
#18333=CARTESIAN_POINT ( 'NONE',  ( 0.2117376410295460365, -1.291494683274178268, 1.029451941043375562 ) ) ;
#18334=CARTESIAN_POINT ( 'NONE',  ( 0.3804897312162703882, -1.724958420852153118, 0.4230015755326726468 ) ) ;
#18335=EDGE_CURVE ( 'NONE', #24709, #14547, #9662, .T. ) ;
#18336=CARTESIAN_POINT ( 'NONE',  ( 0.2616322387702281205, -1.678013124025769187, 0.5382687897764735219 ) ) ;
#18337=CARTESIAN_POINT ( 'NONE',  ( 0.3922353094782703997, -1.714330012172307294, 0.4177417262808784115 ) ) ;
#18338=CARTESIAN_POINT ( 'NONE',  ( 0.3998620935691268308, -1.132090473766685035, 0.6053150776564958369 ) ) ;
#18342=CARTESIAN_POINT ( 'NONE',  ( 0.04961935711675592720, -0.7636540146707464505, 0.7296111229395446651 ) ) ;
#18343=CARTESIAN_POINT ( 'NONE',  ( 0.06061003669112926401, -1.113841305498648904, 0.7547552038151051912 ) ) ;
#18345=CARTESIAN_POINT ( 'NONE',  ( 0.7110913793137424443, -1.453804679565707803, 0.7028629728786995878 ) ) ;
#18346=CARTESIAN_POINT ( 'NONE',  ( 0.6863592619258633842, -1.545543250144949310, 0.6049187728663865116 ) ) ;
#18349=ORIENTED_EDGE ( 'NONE', *, *, #2155, .T. ) ;
#18351=CARTESIAN_POINT ( 'NONE',  ( 0.2568884488902449248, -1.570716599475997510, 0.8655622903500216347 ) ) ;
#18353=CARTESIAN_POINT ( 'NONE',  ( 0.1311038971828588640, -0.5870549638996708230, 0.2845027658977437590 ) ) ;
#18354=PLANE ( 'NONE',  #9948 ) ;
#18355=ORIENTED_EDGE ( 'NONE', *, *, #36419, .F. ) ;
#18356=CARTESIAN_POINT ( 'NONE',  ( 0.5549275037195743332, -1.190966985655177890, 0.5563916622750778584 ) ) ;
#18359=CARTESIAN_POINT ( 'NONE',  ( 0.6513739094900949933, -1.353581159747916374, 0.7728549212624699072 ) ) ;
#18361=CARTESIAN_POINT ( 'NONE',  ( 0.3401273707089542131, -1.774294669406801583, 0.5182417262812423209 ) ) ;
#18363=B_SPLINE_CURVE_WITH_KNOTS ( 'NONE', 3,
 ( #18192, #11629, #24186, #27055, #39584, #14486 ),
 .UNSPECIFIED., .F., .F.,
 ( 4, 2, 4 ),
 ( 0.0008740713857989025094, 0.001092763134855501183, 0.001311454883912099856 ),
 .UNSPECIFIED. ) ;
#18366=CARTESIAN_POINT ( 'NONE',  ( 0.2343816454659662929, -0.9209986304437879356, 0.6741416622544036397 ) ) ;
#18367=CARTESIAN_POINT ( 'NONE',  ( 0.3086358606916266845, -1.716562723882868680, 0.8052685041170501989 ) ) ;
#18368=CARTESIAN_POINT ( 'NONE',  ( 0.5251400411238811294, -1.526848766764422827, 0.5721117033549915076 ) ) ;
#18370=CARTESIAN_POINT ( 'NONE',  ( 0.0004851977134181738034, -0.6337081043291690197, -0.01359677011322422274 ) ) ;
#18373=CARTESIAN_POINT ( 'NONE',  ( 0.4676456642793518359, -1.686044861640426884, 0.5768288019549496770 ) ) ;
#18374=CARTESIAN_POINT ( 'NONE',  ( 0.5093620481516674126, -1.230189073184877468, 0.9022058255351600442 ) ) ;
#18375=CARTESIAN_POINT ( 'NONE',  ( 0.2698036132048247104, -0.9625005881386677897, 0.7146062034794288254 ) ) ;
#18378=CARTESIAN_POINT ( 'NONE',  ( 0.6407227470148669779, -1.336152316681919805, 0.6057417262806679137 ) ) ;
#18381=CARTESIAN_POINT ( 'NONE',  ( 0.2393369856776542404, -0.7683812882957752333, 0.4887749849253086309 ) ) ;
#18394=CARTESIAN_POINT ( 'NONE',  ( 0.03183846471128804617, -0.9219432159619347367, 0.5839824611533311893 ) ) ;
#18408=CARTESIAN_POINT ( 'NONE',  ( 0.1396468697112676072, -0.6922978612330201731, 0.5287085477509265719 ) ) ;
#18410=CARTESIAN_POINT ( 'NONE',  ( 0.7029356573940241937, -1.521348978687367515, 0.5776904582050019776 ) ) ;
#18411=CARTESIAN_POINT ( 'NONE',  ( 0.4521839067189716843, -1.514453368521524235, 0.7626995238331509830 ) ) ;
#18413=CARTESIAN_POINT ( 'NONE',  ( 0.5643649638864810525, -1.503238486482124658, 0.4993898684233098462 ) ) ;
#18417=CARTESIAN_POINT ( 'NONE',  ( 0.5321775012407692351, -1.423729542427319972, 0.7737387429086715063 ) ) ;
#18418=CARTESIAN_POINT ( 'NONE',  ( 0.4290948641688455689, -1.693752172740113693, 0.4322454032524135070 ) ) ;
#18422=CARTESIAN_POINT ( 'NONE',  ( 0.5409081234724703036, -1.629499156560143325, 0.4182417262803311830 ) ) ;
#18427=CARTESIAN_POINT ( 'NONE',  ( 0.2690787404081327883, -0.7149439305734058836, 0.6099944544563858928 ) ) ;
#18428=ADVANCED_FACE ( 'NONE', ( #8828 ), #1935, .T. ) ;
#18431=CARTESIAN_POINT ( 'NONE',  ( 0.01861955870168061425, -0.9920946170940110331, 0.4882401372334904677 ) ) ;
#18433=EDGE_CURVE ( 'NONE', #25042, #1588, #22426, .T. ) ;
#18437=CARTESIAN_POINT ( 'NONE',  ( 0.08509462337972205359, -0.8106601073492546439, 0.1910513156228427489 ) ) ;
#18438=EDGE_CURVE ( 'NONE', #18789, #20299, #22216, .T. ) ;
#18442=CARTESIAN_POINT ( 'NONE',  ( 0.6723167204675445374, -1.568148218941692429, 0.6167698549942565167 ) ) ;
#18444=CARTESIAN_POINT ( 'NONE',  ( 0.6605962927874261537, -1.467029229620433917, 0.4224020735106358559 ) ) ;
#18446=ORIENTED_EDGE ( 'NONE', *, *, #18335, .F. ) ;
#18448=ADVANCED_FACE ( 'NONE', ( #38028 ), #232, .T. ) ;
#18449=CARTESIAN_POINT ( 'NONE',  ( 0.3204450882031337211, -1.182672964233338675, 0.5682417262808777680 ) ) ;
#18453=CARTESIAN_POINT ( 'NONE',  ( 0.4997376312364609774, -1.291901472916908045, 0.6589433602268506274 ) ) ;
#18457=CARTESIAN_POINT ( 'NONE',  ( 0.4130926557567901058, -1.028576094973266963, 0.6508837067575374835 ) ) ;
#18464=CARTESIAN_POINT ( 'NONE',  ( 0.3455691795635327801, -1.573870377985774338, 0.7908454336058577949 ) ) ;
#18465=CARTESIAN_POINT ( 'NONE',  ( 0.3663975874019590462, -1.157438136726378408, 0.4269148889825721827 ) ) ;
#18466=CARTESIAN_POINT ( 'NONE',  ( 0.1752893795992640225, -0.8297571003230018727, -0.03550332207696408476 ) ) ;
#18471=CARTESIAN_POINT ( 'NONE',  ( 0.4408732154518923418, -1.039102903811854883, 0.7181090867236722408 ) ) ;
#18472=CARTESIAN_POINT ( 'NONE',  ( 0.1217566883381065168, -0.6226032096887995637, 0.3725731591225738271 ) ) ;
#18473=ORIENTED_EDGE ( 'NONE', *, *, #26840, .T. ) ;
#18480=DIRECTION ( 'NONE',  ( 0.4999551463232372317, -0.8660512985181135770, 0.000000000000000000 ) ) ;
#18482=CARTESIAN_POINT ( 'NONE',  ( 0.6586301574024518990, -1.563739711041315816, 0.4687417262808791230 ) ) ;
#18485=CARTESIAN_POINT ( 'NONE',  ( 0.02115399423329476433, -1.083931147575175613, 0.6303919839426973537 ) ) ;
#18489=CARTESIAN_POINT ( 'NONE',  ( 0.3142644354089449421, -0.9846788231241262457, 0.5762604841115940291 ) ) ;
#18490=CARTESIAN_POINT ( 'NONE',  ( 0.4557391318645251932, -1.137478852754574055, 0.4468712729341908219 ) ) ;
#18491=ADVANCED_FACE ( 'NONE', ( #4274, #32663 ), #27461, .T. ) ;
#18492=CARTESIAN_POINT ( 'NONE',  ( 0.4668197292635641871, -1.236307873514313149, 0.6057417262809816627 ) ) ;
#18496=CARTESIAN_POINT ( 'NONE',  ( 0.1057086693319095883, -1.337907155632660716, 0.7376750060448485913 ) ) ;
#18497=CARTESIAN_POINT ( 'NONE',  ( 0.4778170654558047126, -1.668016138613298560, 0.5682417262808788783 ) ) ;
#18499=CARTESIAN_POINT ( 'NONE',  ( 0.0005053628357002480209, -0.4419962224268538242, 0.1895056222691282322 ) ) ;
#18500=CARTESIAN_POINT ( 'NONE',  ( 0.3177853311222696431, -1.645584418359625545, 0.5133479035088005515 ) ) ;
#18505=ORIENTED_EDGE ( 'NONE', *, *, #1524, .T. ) ;
#18510=ORIENTED_EDGE ( 'NONE', *, *, #8372, .T. ) ;
#18514=CARTESIAN_POINT ( 'NONE',  ( 0.03048937143879262845, -0.7350047429437137625, 0.5937430055735584133 ) ) ;
#18515=CARTESIAN_POINT ( 'NONE',  ( 0.3599329779412693275, -1.134708076405642307, 0.7326428524546826360 ) ) ;
#18516=CARTESIAN_POINT ( 'NONE',  ( 0.2672982121950731038, -1.328276981695355907, 0.4182417262808770797 ) ) ;
#18517=CARTESIAN_POINT ( 'NONE',  ( 0.6054889487767985967, -1.479703267939684874, 0.5856070495615782745 ) ) ;
#18520=ORIENTED_EDGE ( 'NONE', *, *, #1995, .F. ) ;
#18525=CARTESIAN_POINT ( 'NONE',  ( 0.4402953823516241316, -1.206777924729731444, 0.8122253986942317150 ) ) ;
#18528=CARTESIAN_POINT ( 'NONE',  ( 0.2310769326552300218, -0.9374521120563168441, 0.6578705068509248521 ) ) ;
#18540=DIRECTION ( 'NONE',  ( 1.000000000000000000, 0.000000000000000000, 0.000000000000000000 ) ) ;
#18541=EDGE_CURVE ( 'NONE', #27338, #38731, #39098, .T. ) ;
#18542=CARTESIAN_POINT ( 'NONE',  ( 0.04583756681245852727, -1.039559191613112832, 0.7214566118523848548 ) ) ;
#18544=CARTESIAN_POINT ( 'NONE',  ( 0.7203159877618242612, -1.479638488134456420, 0.5307775041526673343 ) ) ;
#18550=AXIS2_PLACEMENT_3D ( 'NONE', #4147, #7650, #16504 ) ;
#18551=ADVANCED_FACE ( 'NONE', ( #17034 ), #7763, .T. ) ;
#18552=ORIENTED_EDGE ( 'NONE', *, *, #6447, .T. ) ;
#18554=VERTEX_POINT ( 'NONE', #10050 ) ;
#18556=CARTESIAN_POINT ( 'NONE',  ( 0.2643552029519708468, -1.643455541575042700, 0.7762602543266098332 ) ) ;
#18559=CARTESIAN_POINT ( 'NONE',  ( 0.1428196694608256101, -0.6338724602092423721, 0.3861684053016066764 ) ) ;
#18564=CARTESIAN_POINT ( 'NONE',  ( 0.4444209036527600465, -1.039833579653637319, 0.7404771872114588316 ) ) ;
#18567=CARTESIAN_POINT ( 'NONE',  ( 0.6660153594396612808, -1.377480952862383923, 0.7519195793979284170 ) ) ;
#18569=CARTESIAN_POINT ( 'NONE',  ( 0.3186320389496528627, -1.760431904683431359, 0.5682417262808792113 ) ) ;
#18573=CARTESIAN_POINT ( 'NONE',  ( 0.1924078334994414607, -0.8864580494542387834, 0.6093570016390645883 ) ) ;
#18574=FACE_OUTER_BOUND ( 'NONE', #2124, .T. ) ;
#18575=CARTESIAN_POINT ( 'NONE',  ( 0.1038860818051843410, -0.5481585384591742827, 0.1713426774629287497 ) ) ;
#18576=CARTESIAN_POINT ( 'NONE',  ( 0.3466922049894854974, -1.748660810794147258, 0.4514553480157271204 ) ) ;
#18577=CARTESIAN_POINT ( 'NONE',  ( -0.001987662015349134573, -0.8501386850767141956, 0.1022911480739698287 ) ) ;
#18578=CARTESIAN_POINT ( 'NONE',  ( 0.03559495875357140959, -1.028803249407966858, 0.5691659535643065482 ) ) ;
#18579=ORIENTED_EDGE ( 'NONE', *, *, #15038, .F. ) ;
#18581=CARTESIAN_POINT ( 'NONE',  ( 0.4468553387825724421, -1.686585475485919972, 0.5936113863420847681 ) ) ;
#18582=CARTESIAN_POINT ( 'NONE',  ( 0.7431273937626133863, -1.516426637506990360, 0.5641520672112426693 ) ) ;
#18583=MANIFOLD_SOLID_BREP ( 'Fillet15', #7616 ) ;
#18584=CYLINDRICAL_SURFACE ( 'NONE', #23333, 0.03749999999977545601 ) ;
#18585=AXIS2_PLACEMENT_3D ( 'NONE', #11525, #32901, #14195 ) ;
#18587=CARTESIAN_POINT ( 'NONE',  ( 0.006100135935846554350, -0.8448938542399410112, 0.1277644845294366172 ) ) ;
#18591=CARTESIAN_POINT ( 'NONE',  ( 0.3925326341959034515, -1.148401673189667571, 0.4243628868813368316 ) ) ;
#18594=CARTESIAN_POINT ( 'NONE',  ( 0.3337689465763037377, -1.163262234248904736, 0.4559311481246714481 ) ) ;
#18595=CARTESIAN_POINT ( 'NONE',  ( 0.2043709925794569282, -0.7174950807506157435, 0.3538749514786183048 ) ) ;
#18597=CARTESIAN_POINT ( 'NONE',  ( 0.6672263256168233791, -1.559577713309469038, 0.6159734170043378310 ) ) ;
#18603=CARTESIAN_POINT ( 'NONE',  ( 0.4882304408116465155, -1.126680077128302093, 0.5092034011547009742 ) ) ;
#18604=CARTESIAN_POINT ( 'NONE',  ( 0.4015936175283410514, -1.155705023113092533, 0.5182417262812423209 ) ) ;
#18609=CARTESIAN_POINT ( 'NONE',  ( 0.07659735200988204706, -1.288566765071073261, 0.7428858345647274541 ) ) ;
#18619=DIRECTION ( 'NONE',  ( 0.9998941247116546194, -0.01455087607601020412, 0.0001066420868422379362 ) ) ;
#18621=EDGE_LOOP ( 'NONE', ( #36941, #32517, #29448, #837 ) ) ;
#18622=CARTESIAN_POINT ( 'NONE',  ( 0.07405132550584739293, -1.324440054897002561, 0.5176829506697802064 ) ) ;
#18626=CARTESIAN_POINT ( 'NONE',  ( 0.3727629667123311119, -1.357639913737091808, 0.8616512673511037557 ) ) ;
#18629=CARTESIAN_POINT ( 'NONE',  ( 0.5726702689957759995, -1.625473326825089160, 0.5525775856678601938 ) ) ;
#18635=CARTESIAN_POINT ( 'NONE',  ( 0.5809530576852517392, -1.495264608998207789, 0.5740006802652367623 ) ) ;
#18636=CARTESIAN_POINT ( 'NONE',  ( 0.4746182331242696506, -1.678388708763134396, 0.4747050670221392710 ) ) ;
#18639=CARTESIAN_POINT ( 'NONE',  ( 0.2260995971937757310, -1.236443303375862390, 0.5209257643876351596 ) ) ;
#18640=AXIS2_PLACEMENT_3D ( 'NONE', #17030, #10645, #3863 ) ;
#18642=CARTESIAN_POINT ( 'NONE',  ( 0.1934691495297424235, -1.255374174182389391, 0.4342266066129076285 ) ) ;
#18643=CARTESIAN_POINT ( 'NONE',  ( 0.2073655362268157221, -0.5791461380176760043, 0.4026997059449013427 ) ) ;
#18646=CARTESIAN_POINT ( 'NONE',  ( 0.02926306740268063214, -1.136388740552946031, 0.6581294774663873914 ) ) ;
#18650=CARTESIAN_POINT ( 'NONE',  ( 0.2650653946250867143, -1.676094176783521128, 0.5635705756526244725 ) ) ;
#18657=CARTESIAN_POINT ( 'NONE',  ( 0.6652220256568632806, -1.517545837045118473, 0.4231643303188328820 ) ) ;
#18663=CARTESIAN_POINT ( 'NONE',  ( 0.3390201860129213318, -1.162303158162408812, 0.6024826139476634479 ) ) ;
#18666=CARTESIAN_POINT ( 'NONE',  ( 0.3350890287386661948, -1.062171315605431321, 0.7337690394249966053 ) ) ;
#18668=CARTESIAN_POINT ( 'NONE',  ( 0.4216623502531439693, -1.034931331451964143, 0.6525378447207771382 ) ) ;
#18671=ORIENTED_EDGE ( 'NONE', *, *, #33175, .T. ) ;
#18673=ORIENTED_EDGE ( 'NONE', *, *, #260, .T. ) ;
#18674=VECTOR ( 'NONE', #4620, 39.37007874015748143 ) ;
#18675=CARTESIAN_POINT ( 'NONE',  ( 0.2931371671966536696, -1.364037168738611250, 0.8947199202213534930 ) ) ;
#18677=CARTESIAN_POINT ( 'NONE',  ( 0.1748881817888952583, -0.8846221646991694332, 0.02718377953341061248 ) ) ;
#18683=CARTESIAN_POINT ( 'NONE',  ( 0.3669132811502856528, -0.9575263150705904946, 0.6684360246000486949 ) ) ;
#18684=CARTESIAN_POINT ( 'NONE',  ( 0.3813006723851273816, -1.191008781084291313, 0.8308973255029469263 ) ) ;
#18692=CARTESIAN_POINT ( 'NONE',  ( 0.4092750486073892247, -1.698390055749431138, 0.4182417262808776903 ) ) ;
#18695=ADVANCED_FACE ( 'NONE', ( #1825 ), #14540, .T. ) ;
#18700=CIRCLE ( 'NONE', #1661, 0.08749999999977552123 ) ;
#18701=CARTESIAN_POINT ( 'NONE',  ( 0.4892015816964360719, -1.080660821007120020, 0.5933591780025184725 ) ) ;
#18703=CARTESIAN_POINT ( 'NONE',  ( 0.4427163477200127262, -1.139245542564126357, 0.4379379976781114792 ) ) ;
#18704=CARTESIAN_POINT ( 'NONE',  ( 0.06518445159565730562, -1.341084469003575030, 0.5526808653810328931 ) ) ;
#18709=CARTESIAN_POINT ( 'NONE',  ( -0.002023118427450016753, -0.8974731051190899533, 0.1948784381876195460 ) ) ;
#18710=CARTESIAN_POINT ( 'NONE',  ( 0.2709623010280027278, -1.672610760848568967, 0.4891849873696615392 ) ) ;
#18718=CARTESIAN_POINT ( 'NONE',  ( 0.2667797934877766397, -1.675028870926974500, 0.5053016059147321659 ) ) ;
#18719=B_SPLINE_CURVE_WITH_KNOTS ( 'NONE', 3,
 ( #27793, #20613, #24120, #4954, #8446, #17519, #18124, #33749, #21439, #1898, #20823, #14411, #26973, #27188, #24303, #5770, #33147, #23908, #39721, #30871, #36436, #8250, #11944 ),
 .UNSPECIFIED., .F., .F.,
 ( 4, 2, 2, 2, 2, 2, 2, 2, 1, 2, 2, 4 ),
 ( 0.000000000000000000, 0.001303949395765936943, 0.001955924093648904981, 0.002607898791531872585, 0.003911848187297809962, 0.005215797583063746905, 0.006519746978829682980, 0.007171721676712655355, 0.007823696374595628597, 0.008475671072478601839, 0.009127645770361575081, 0.01043159516612753024 ),
 .UNSPECIFIED. ) ;
#18721=CARTESIAN_POINT ( 'NONE',  ( 0.4256811042841359138, -1.183992690650692348, 0.8157300287015782914 ) ) ;
#18722=CARTESIAN_POINT ( 'NONE',  ( 0.01050449021347792111, -0.5294792378225862128, 0.1383083324213474075 ) ) ;
#18728=CARTESIAN_POINT ( 'NONE',  ( 0.01091791702278631891, -0.5391733969928702574, 0.2078372220302295847 ) ) ;
#18729=CARTESIAN_POINT ( 'NONE',  ( 0.1606430264876529124, -0.9001996987827759478, 0.5837366715005726236 ) ) ;
#18730=CARTESIAN_POINT ( 'NONE',  ( 0.09670933914072363247, -1.286966393572076761, 0.5906442777704791203 ) ) ;
#18731=CARTESIAN_POINT ( 'NONE',  ( 0.01207335092558379890, -0.4550518931080567708, 0.03096792667458423548 ) ) ;
#18734=EDGE_CURVE ( 'NONE', #24067, #37440, #13966, .T. ) ;
#18740=EDGE_CURVE ( 'NONE', #17780, #8227, #25342, .T. ) ;
#18745=CARTESIAN_POINT ( 'NONE',  ( 0.5371247828146922254, -1.393663287660293237, 0.7819316079650096007 ) ) ;
#18746=CARTESIAN_POINT ( 'NONE',  ( 0.1270245264032780486, -0.8251090115851287266, 0.2117204377992136233 ) ) ;
#18749=CARTESIAN_POINT ( 'NONE',  ( 0.06481568609301656403, -0.7456345099580035107, 0.7576189738271701390 ) ) ;
#18753=LINE ( 'NONE', #10309, #27244 ) ;
#18754=( BOUNDED_SURFACE ( )  B_SPLINE_SURFACE ( 3, 2, ( 
 ( #12356, #24912, #37438 ),
 ( #22438, #34149, #31074 ),
 ( #25106, #12972, #34966 ),
 ( #22244, #9865, #16059 ) ),
 .UNSPECIFIED., .F., .F., .F. ) 
 B_SPLINE_SURFACE_WITH_KNOTS ( ( 4, 4 ),
 ( 3, 3 ),
 ( -3.123586458930738274E-16, 0.0004255989732716984912 ),
 ( 0.000000000000000000, 1.000000000000000000 ),
 .UNSPECIFIED. ) 
 GEOMETRIC_REPRESENTATION_ITEM ( )  RATIONAL_B_SPLINE_SURFACE ( (
 ( 1.000000000000000000, 0.8997265729122759792, 1.000000000000000000),
 ( 1.000000000000000000, 0.8954993961798249913, 1.000000000000000000),
 ( 1.000000000000000000, 0.8844303544522131855, 1.000000000000000000),
 ( 1.000000000000000000, 0.8624897507815776354, 1.000000000000000000) ) ) 
 REPRESENTATION_ITEM ( '' )  SURFACE ( )  );
#18755=CARTESIAN_POINT ( 'NONE',  ( 0.4667937283406220494, -1.235624442469605899, 0.6184277979272206904 ) ) ;
#18762=CARTESIAN_POINT ( 'NONE',  ( 0.07209178019044594488, -1.135423765654719919, 0.7590189199326136116 ) ) ;
#18764=CARTESIAN_POINT ( 'NONE',  ( 0.2791332027808016703, -0.7342173681784933681, 0.6310308052199803397 ) ) ;
#18767=CARTESIAN_POINT ( 'NONE',  ( 0.6889662060151644507, -1.555147259246191016, 0.5968497998442635621 ) ) ;
#18768=EDGE_CURVE ( 'NONE', #1496, #14919, #21910, .T. ) ;
#18774=CARTESIAN_POINT ( 'NONE',  ( 0.1882598819837821291, -1.364719520154515475, 0.9410996297614753203 ) ) ;
#18775=CARTESIAN_POINT ( 'NONE',  ( 0.4749671191778466750, -1.308524979286208367, 0.8177814803665567345 ) ) ;
#18779=CARTESIAN_POINT ( 'NONE',  ( 0.1874999999999996669, -0.6872203660140441261, 0.1527381444932270627 ) ) ;
#18782=CARTESIAN_POINT ( 'NONE',  ( 0.3956566811268355521, -0.9596954108736347466, 0.7461004073261953140 ) ) ;
#18785=CARTESIAN_POINT ( 'NONE',  ( 0.3186755585808466740, -1.760356642135124439, 0.5625658558758077632 ) ) ;
#18788=FACE_OUTER_BOUND ( 'NONE', #13042, .T. ) ;
#18789=VERTEX_POINT ( 'NONE', #3412 ) ;
#18790=EDGE_CURVE ( 'NONE', #14, #32680, #16004, .T. ) ;
#18791=CARTESIAN_POINT ( 'NONE',  ( 0.08837989099891704892, -0.7491984653599970123, 0.2305845840354824039 ) ) ;
#18792=CARTESIAN_POINT ( 'NONE',  ( 0.3150771742308554058, -1.733448878803460991, 0.7884676298878301459 ) ) ;
#18793=CARTESIAN_POINT ( 'NONE',  ( 0.5262589651392098888, -1.523534812712205477, 0.6368633379848268605 ) ) ;
#18796=ORIENTED_EDGE ( 'NONE', *, *, #1707, .T. ) ;
#18798=B_SPLINE_CURVE_WITH_KNOTS ( 'NONE', 3,
 ( #2194, #34055, #5854, #18413, #1991, #11448, #24015, #33443, #5251, #3801, #13259, #28892, #16170, #753, #6876, #25829 ),
 .UNSPECIFIED., .F., .F.,
 ( 4, 2, 2, 2, 2, 2, 2, 4 ),
 ( 0.002977951493358533663, 0.003350111319365782318, 0.003722271145373030974, 0.004094430971380279630, 0.004466590797387528719, 0.004838750623394776941, 0.005210910449402025163, 0.005955230101416519005 ),
 .UNSPECIFIED. ) ;
#18800=CARTESIAN_POINT ( 'NONE',  ( 0.6660103463786463118, -1.561565158697419742, 0.5710166038345764195 ) ) ;
#18811=CARTESIAN_POINT ( 'NONE',  ( 0.2644881156243384379, -1.676263310743548063, 0.5220153280337084256 ) ) ;
#18813=CARTESIAN_POINT ( 'NONE',  ( 0.06824055730039223222, -1.289945330482348496, 0.6789996349980699231 ) ) ;
#18814=CARTESIAN_POINT ( 'NONE',  ( 0.5549275037195743332, -1.190966985655177890, 0.5563916622750778584 ) ) ;
#18818=CARTESIAN_POINT ( 'NONE',  ( 0.6077657638426647857, -1.479710398481848266, 0.5717087807361217466 ) ) ;
#18820=ORIENTED_EDGE ( 'NONE', *, *, #6749, .T. ) ;
#18821=CARTESIAN_POINT ( 'NONE',  ( 0.1876053338355621880, -0.6785855078148245179, 0.1477569985384105666 ) ) ;
#18822=DIRECTION ( 'NONE',  ( 0.8849907732522489523, 0.000000000000000000, 0.4656085601214676739 ) ) ;
#18823=CARTESIAN_POINT ( 'NONE',  ( 0.08572064877627985635, -0.7939468086886716236, 0.08347532546618800786 ) ) ;
#18828=CARTESIAN_POINT ( 'NONE',  ( -0.006649224014923847334, -0.8922124784979929002, 0.4965188763020696450 ) ) ;
#18835=EDGE_CURVE ( 'NONE', #40111, #30976, #4264, .T. ) ;
#18837=CARTESIAN_POINT ( 'NONE',  ( 0.3088664963667261398, -1.757905065063135597, 0.5295467280985148850 ) ) ;
#18838=B_SPLINE_CURVE_WITH_KNOTS ( 'NONE', 3,
 ( #12409, #24960, #37490, #9311, #6234, #16320 ),
 .UNSPECIFIED., .F., .F.,
 ( 4, 2, 4 ),
 ( 0.000000000000000000, 0.5000000000000000000, 1.000000000000000000 ),
 .UNSPECIFIED. ) ;
#18840=ORIENTED_EDGE ( 'NONE', *, *, #2886, .T. ) ;
#18843=CARTESIAN_POINT ( 'NONE',  ( 0.09535664604372214026, -0.5879077161293799758, 0.2928325945560249499 ) ) ;
#18845=CARTESIAN_POINT ( 'NONE',  ( 0.7043850983579452718, -1.516419193711280311, 0.5648052198873427798 ) ) ;
#18846=CARTESIAN_POINT ( 'NONE',  ( 0.07323308598001919412, -0.5520613865617218785, 0.2133277464804944623 ) ) ;
#18850=CARTESIAN_POINT ( 'NONE',  ( 0.2049605114958119589, -0.9388532809880968388, 0.4165185827052858003 ) ) ;
#18852=CARTESIAN_POINT ( 'NONE',  ( 0.1887412855916273946, -0.4595320686313617564, 0.1458683203705864184 ) ) ;
#18853=CARTESIAN_POINT ( 'NONE',  ( 0.5808478773694798480, -1.495250919194240691, 0.5721815422400771123 ) ) ;
#18861=CARTESIAN_POINT ( 'NONE',  ( 0.6807551469422991053, -1.407487954066357183, 0.5751647024762112093 ) ) ;
#18862=EDGE_CURVE ( 'NONE', #27951, #13401, #17022, .T. ) ;
#18864=CARTESIAN_POINT ( 'NONE',  ( 0.01746090273258609979, -1.060756659779402034, 0.6072269701260313290 ) ) ;
#18870=CARTESIAN_POINT ( 'NONE',  ( 0.6358155198048017764, -1.579893599062534459, 0.4258446345833196700 ) ) ;
#18871=EDGE_LOOP ( 'NONE', ( #7783, #18349, #32165 ) ) ;
#18877=B_SPLINE_CURVE_WITH_KNOTS ( 'NONE', 3,
 ( #38346, #363, #34665, #6469, #12867, #9768, #22338, #19243, #31786, #38148, #16168, #28705, #9971, #569, #10181, #29095, #961, #26037, #4402, #7478, #38961, #36078, #1159, #29704, #35675, #32587, #7878, #11187, #14462, #36269, #1344, #1762, #1550, #23362, #13851, #20450, #4583, #14274, #23747, #32984, #8091, #26838, #26424, #7695, #13659, #14071, #20668, #17155, #26224, #16763, #10791, #38746, #11002, #39177 ),
 .UNSPECIFIED., .F., .F.,
 ( 4, 2, 2, 2, 2, 2, 2, 2, 2, 2, 2, 2, 2, 2, 2, 2, 2, 2, 2, 2, 2, 2, 2, 2, 2, 2, 4 ),
 ( 0.000000000000000000, 0.001467739507578043421, 0.002935479015156086842, 0.005870958030312173684, 0.01174191606062434216, 0.01467739507578042814, 0.01761287409093651238, 0.02054835310609260182, 0.02201609261367064654, 0.02348383212124869474, 0.02641931113640478071, 0.02935479015156086668, 0.03082252965913890794, 0.03229026916671694919, 0.03375800867429499391, 0.03522574818187304557, 0.03669348768945108336, 0.03742735744324009184, 0.03816122719702910726, 0.03962896670460712423, 0.04109670621218514119, 0.04256444571976315816, 0.04403218522734117513, 0.04549992473491919209, 0.04623379448870819364, 0.04660072936560270829, 0.04696766424249720906 ),
 .UNSPECIFIED. ) ;
#18881=CARTESIAN_POINT ( 'NONE',  ( 0.1871937864180454048, -1.374138184793721518, 0.5181962843648889594 ) ) ;
#18882=DIRECTION ( 'NONE',  ( -0.9876771640241659433, -0.1565050148243856687, -1.024672052421402957E-13 ) ) ;
#18884=CARTESIAN_POINT ( 'NONE',  ( 0.4704808408627720873, -1.246563891206539099, 0.7003883943243975896 ) ) ;
#18888=CARTESIAN_POINT ( 'NONE',  ( 0.4892015816964360719, -1.080660821007120020, 0.5933591780025184725 ) ) ;
#18889=ORIENTED_EDGE ( 'NONE', *, *, #40222, .T. ) ;
#18891=CARTESIAN_POINT ( 'NONE',  ( 0.02352711120663245753, -0.9586990007338236364, 0.6297157671916142618 ) ) ;
#18893=CARTESIAN_POINT ( 'NONE',  ( 0.3851754998513399753, -1.605598480965388708, 0.5732781203792557401 ) ) ;
#18894=CARTESIAN_POINT ( 'NONE',  ( 0.06469648274370130847, -0.8304785510687793249, 0.1072521381146411823 ) ) ;
#18895=CARTESIAN_POINT ( 'NONE',  ( 0.1755999888594793890, -0.7630904603782766582, -0.07194964429679771845 ) ) ;
#18896=CARTESIAN_POINT ( 'NONE',  ( 0.06694067462889406739, -0.6776034894424159960, -0.001903836934785778628 ) ) ;
#18902=CARTESIAN_POINT ( 'NONE',  ( 0.5195437916533927059, -1.430322578995237182, 0.7780002750953179946 ) ) ;
#18903=ORIENTED_EDGE ( 'NONE', *, *, #37637, .T. ) ;
#18904=CARTESIAN_POINT ( 'NONE',  ( 0.1873341288634420843, -0.6980686425579779586, 0.03222456286304159478 ) ) ;
#18912=CARTESIAN_POINT ( 'NONE',  ( 0.1782772739027001230, -1.243608455402465340, 0.6125714912171157378 ) ) ;
#18914=CARTESIAN_POINT ( 'NONE',  ( 0.5971614065082352374, -1.461417804984935342, 0.6057417262805111502 ) ) ;
#18917=CARTESIAN_POINT ( 'NONE',  ( 0.1877336102437491272, -0.9152557094465934018, 0.1737200839639440053 ) ) ;
#18918=CARTESIAN_POINT ( 'NONE',  ( 0.3257277097560854484, -1.167896984018933493, 0.4676436393436195216 ) ) ;
#18919=CARTESIAN_POINT ( 'NONE',  ( 0.4409357815299598804, -1.228106680636185111, 0.6057417262809895453 ) ) ;
#18921=ORIENTED_EDGE ( 'NONE', *, *, #8343, .T. ) ;
#18922=CARTESIAN_POINT ( 'NONE',  ( 0.1362517741244128056, -1.308408735431443093, 0.8505046261270597929 ) ) ;
#18925=CARTESIAN_POINT ( 'NONE',  ( 0.3302717389963351624, -1.638372317322708716, 0.4882842553274441277 ) ) ;
#18927=ORIENTED_EDGE ( 'NONE', *, *, #39615, .F. ) ;
#18933=CARTESIAN_POINT ( 'NONE',  ( 0.4150272135712330113, -1.167431181930913553, 0.8149900857543223021 ) ) ;
#18936=ORIENTED_EDGE ( 'NONE', *, *, #3117, .T. ) ;
#18938=ORIENTED_EDGE ( 'NONE', *, *, #5102, .T. ) ;
#18939=CARTESIAN_POINT ( 'NONE',  ( 0.2966820077695481173, -1.656469531661595163, 0.5666191999804250923 ) ) ;
#18940=CARTESIAN_POINT ( 'NONE',  ( 0.2437792440929114346, -0.9773701458837178446, 0.6962579099302033114 ) ) ;
#18941=CARTESIAN_POINT ( 'NONE',  ( 0.1245238869884406352, -1.284104819735092606, 0.6026496813689052878 ) ) ;
#18943=CARTESIAN_POINT ( 'NONE',  ( 0.01182080120375270972, -0.6039130564843261384, -0.09998022549266330494 ) ) ;
#18946=ORIENTED_EDGE ( 'NONE', *, *, #37295, .T. ) ;
#18950=CYLINDRICAL_SURFACE ( 'NONE', #31889, 0.09249999999977555343 ) ;
#18953=CARTESIAN_POINT ( 'NONE',  ( 0.01954262108197177966, -0.5199582741543401498, 0.4378456291139402046 ) ) ;
#18959=DIRECTION ( 'NONE',  ( 0.4999551463232372317, -0.8660512985181135770, 0.000000000000000000 ) ) ;
#18960=CARTESIAN_POINT ( 'NONE',  ( 0.05109603825399443300, -0.7331182637548316894, 0.7465514741729609716 ) ) ;
#18961=CARTESIAN_POINT ( 'NONE',  ( 0.07257591959104818524, -1.183556761366722387, 0.7640614581424595153 ) ) ;
#18966=CARTESIAN_POINT ( 'NONE',  ( 0.7050067303326591484, -1.529446169236064135, 0.5714306314579442603 ) ) ;
#18967=EDGE_CURVE ( 'NONE', #25362, #19095, #28728, .T. ) ;
#18968=FACE_OUTER_BOUND ( 'NONE', #29358, .T. ) ;
#18971=CARTESIAN_POINT ( 'NONE',  ( 0.2742629518370554575, -1.653361553673516227, 0.7386680983805660183 ) ) ;
#18972=CARTESIAN_POINT ( 'NONE',  ( 0.4015825763966658912, -1.182054300648716083, 0.8205428547305109177 ) ) ;
#18973=CARTESIAN_POINT ( 'NONE',  ( 0.3460651993684921712, -1.167700608961039332, 0.4299100439411554508 ) ) ;
#18985=CARTESIAN_POINT ( 'NONE',  ( 0.2010125963195148191, -0.8858709603250995990, 0.6259238706880295711 ) ) ;
#18987=CARTESIAN_POINT ( 'NONE',  ( 0.1039182570229498503, -0.5495296521639349008, 0.1804408898608185485 ) ) ;
#18993=CARTESIAN_POINT ( 'NONE',  ( 0.7430585616337137544, -1.516428101037593512, 0.5626827419390632024 ) ) ;
#18994=B_SPLINE_CURVE_WITH_KNOTS ( 'NONE', 3,
 ( #38383, #7103, #7299, #19671, #34695, #28737, #15986, #32207, #19281, #19072, #4022, #15772, #28531, #16588, #34893, #6706, #12685, #13093 ),
 .UNSPECIFIED., .F., .F.,
 ( 4, 2, 2, 2, 2, 2, 2, 2, 4 ),
 ( 0.000000000000000000, 0.0005104183120475769102, 0.001020836624095153820, 0.001531254936142730731, 0.002041673248190307641, 0.002552091560237884551, 0.003062509872285461461, 0.003572928184333038371, 0.004083346496380615281 ),
 .UNSPECIFIED. ) ;
#18997=CARTESIAN_POINT ( 'NONE',  ( 0.1460988943316244848, -0.6240739943263109435, 0.3647668637918258239 ) ) ;
#19002=CARTESIAN_POINT ( 'NONE',  ( 0.2640998637001502058, -1.676998255898582091, 0.4887480333912877506 ) ) ;
#19004=CARTESIAN_POINT ( 'NONE',  ( 0.06399702207960011879, -1.267566535398010563, 0.6886354586937382116 ) ) ;
#19005=CARTESIAN_POINT ( 'NONE',  ( 0.2706875035899702353, -0.8747201880513900685, 0.5443116846754595395 ) ) ;
#19016=CARTESIAN_POINT ( 'NONE',  ( 0.08862505653733224187, -0.6119536582126900992, 0.04826979502260971000 ) ) ;
#19018=CARTESIAN_POINT ( 'NONE',  ( 0.2320755761173002307, -1.232873731908348480, 0.4177417262808779674 ) ) ;
#19019=CARTESIAN_POINT ( 'NONE',  ( 0.03746391227491855519, -1.107308778534258131, 0.7549414212349836450 ) ) ;
#19033=CARTESIAN_POINT ( 'NONE',  ( 0.09184176262540320879, -0.6123617702671079188, 0.2291278788234172303 ) ) ;
#19037=CARTESIAN_POINT ( 'NONE',  ( 0.1528396677094553124, -0.8424192790127347230, 0.6801078269868232606 ) ) ;
#19041=CARTESIAN_POINT ( 'NONE',  ( 0.1723742836622136898, -0.9181944984900098916, 0.1915515737749588221 ) ) ;
#19042=UNCERTAINTY_MEASURE_WITH_UNIT (LENGTH_MEASURE( 1.000000000000000082E-05 ), #12411, 'distance_accuracy_value', 'NONE');
#19044=CARTESIAN_POINT ( 'NONE',  ( 0.1887412855915411858, -0.4595320686313046910, 0.1385946963835863743 ) ) ;
#19045=CARTESIAN_POINT ( 'NONE',  ( 0.1269878671055759134, -0.5786664369199111535, 0.2632502270387737653 ) ) ;
#19049=CARTESIAN_POINT ( 'NONE',  ( 0.06924657687967017416, -0.5400045886221176428, 0.1476626190087814705 ) ) ;
#19050=FACE_OUTER_BOUND ( 'NONE', #21989, .T. ) ;
#19051=CARTESIAN_POINT ( 'NONE',  ( 0.4107733320947055122, -0.9780847931859447675, 0.7674390821536307694 ) ) ;
#19053=CARTESIAN_POINT ( 'NONE',  ( 0.4570320186965683984, -1.145281013718252305, 0.4021993759966799864 ) ) ;
#19054=CARTESIAN_POINT ( 'NONE',  ( 0.03430157769017382757, -1.168583015135568504, 0.6655574557517952572 ) ) ;
#19059=CARTESIAN_POINT ( 'NONE',  ( 0.1887090023420391338, -0.9018070888474317703, 0.5958977073701414717 ) ) ;
#19061=DIRECTION ( 'NONE',  ( -9.042510699458645841E-13, 1.566396143878659165E-12, -1.000000000000000000 ) ) ;
#19062=VECTOR ( 'NONE', #26911, 39.37007874015748143 ) ;
#19067=CARTESIAN_POINT ( 'NONE',  ( 0.6578511400472081272, -1.468260077009814202, 0.4182417262808778013 ) ) ;
#19072=CARTESIAN_POINT ( 'NONE',  ( 0.4824891092964968542, -1.662412547341785896, 0.4835662331627371135 ) ) ;
#19075=CARTESIAN_POINT ( 'NONE',  ( 0.3489069294160111467, -1.081181803243002504, 0.7355034317277300282 ) ) ;
#19078=CARTESIAN_POINT ( 'NONE',  ( 0.4851165728318759252, -1.078419517084477697, 0.6030839855583299824 ) ) ;
#19082=CARTESIAN_POINT ( 'NONE',  ( 0.04035408590310328447, -1.027233222095623510, 0.7038666329257657894 ) ) ;
#19085=CARTESIAN_POINT ( 'NONE',  ( 0.3863278360478267781, -1.605740116755117075, 0.5905161093819162321 ) ) ;
#19087=CARTESIAN_POINT ( 'NONE',  ( 0.1859259531917270003, -0.7321509755579215240, -0.01543098434727066537 ) ) ;
#19088=CARTESIAN_POINT ( 'NONE',  ( 0.06795783451517332929, -0.5973041244007833983, 0.02846421222436375589 ) ) ;
#19094=CARTESIAN_POINT ( 'NONE',  ( 0.5670196490188851302, -1.503246592690220540, 0.5746465183166465929 ) ) ;
#19095=VERTEX_POINT ( 'NONE', #23985 ) ;
#19096=CARTESIAN_POINT ( 'NONE',  ( 0.1874000730451391150, -0.6935093423028750870, 0.03601873687098033211 ) ) ;
#19101=LINE ( 'NONE', #10249, #34363 ) ;
#19104=B_SPLINE_CURVE_WITH_KNOTS ( 'NONE', 3,
 ( #3112, #22451, #12987, #25731 ),
 .UNSPECIFIED., .F., .F.,
 ( 4, 4 ),
 ( 0.000000000000000000, 0.0003323657284514935093 ),
 .UNSPECIFIED. ) ;
#19105=CARTESIAN_POINT ( 'NONE',  ( 0.4191100986681119411, -1.701672718972377929, 0.4233639548768234895 ) ) ;
#19106=CYLINDRICAL_SURFACE ( 'NONE', #2920, 0.2500000000000000000 ) ;
#19107=CARTESIAN_POINT ( 'NONE',  ( 0.07945738019374083694, -1.321132034926529419, 0.5723852862170456524 ) ) ;
#19109=CARTESIAN_POINT ( 'NONE',  ( 0.08214737558356681457, -1.311413488239922431, 0.7308976325429462628 ) ) ;
#19112=CARTESIAN_POINT ( 'NONE',  ( 0.1885390680155161480, -0.9156976364345736918, 0.1977769869421455440 ) ) ;
#19115=CARTESIAN_POINT ( 'NONE',  ( 0.4857742178082134488, -1.202222293638773420, 0.6057417262810468328 ) ) ;
#19116=CARTESIAN_POINT ( 'NONE',  ( 0.2615177342056695942, -1.679396441256837846, 0.5426384715137531067 ) ) ;
#19117=CARTESIAN_POINT ( 'NONE',  ( 0.1230419690069037980, -1.441173760443279050, 0.5802947806848592904 ) ) ;
#19118=CARTESIAN_POINT ( 'NONE',  ( -0.0003704575336267049244, -0.9283305954846620134, 0.08133701872469059624 ) ) ;
#19121=CARTESIAN_POINT ( 'NONE',  ( 0.3629635372387383652, -1.169857193776045357, 0.4182417262808778013 ) ) ;
#19123=ORIENTED_EDGE ( 'NONE', *, *, #879, .F. ) ;
#19128=CARTESIAN_POINT ( 'NONE',  ( 0.7053410326410682885, -1.513865973459305625, 0.5669051209305092653 ) ) ;
#19130=CIRCLE ( 'NONE', #5945, 0.009999999999999991535 ) ;
#19131=CARTESIAN_POINT ( 'NONE',  ( 0.5256885457656272909, -1.340177190190134704, 0.7859048212681565282 ) ) ;
#19132=CARTESIAN_POINT ( 'NONE',  ( 0.5800224671949608668, -1.618884289167087376, 0.4664561499407959833 ) ) ;
#19135=CARTESIAN_POINT ( 'NONE',  ( 0.1987699546958638652, -0.5941503706980315602, 0.3237227049863830031 ) ) ;
#19137=CARTESIAN_POINT ( 'NONE',  ( 0.2964680571446819402, -1.656381576221859664, 0.5636775978236220341 ) ) ;
#19138=CARTESIAN_POINT ( 'NONE',  ( 0.6374551337379976701, -1.567405544265130013, 0.4255985356709496292 ) ) ;
#19139=CARTESIAN_POINT ( 'NONE',  ( 0.09204888577508196779, -1.303414576269683822, 0.5990285209990867665 ) ) ;
#19145=ORIENTED_EDGE ( 'NONE', *, *, #26840, .F. ) ;
#19147=CARTESIAN_POINT ( 'NONE',  ( 0.1852851918485090843, -0.8388979443186348472, 0.1523375349326095973 ) ) ;
#19149=CARTESIAN_POINT ( 'NONE',  ( 0.5787394239162922949, -1.425886802764863459, 0.7111292081977039770 ) ) ;
#19151=CARTESIAN_POINT ( 'NONE',  ( 0.1386179493822486397, -1.168326298757728754, 0.9079011523149604912 ) ) ;
#19152=CIRCLE ( 'NONE', #32927, 0.01000000000000001756 ) ;
#19153=CARTESIAN_POINT ( 'NONE',  ( 0.05112782467887915655, -0.6866549243560603477, 0.6943072588412673163 ) ) ;
#19158=CARTESIAN_POINT ( 'NONE',  ( 0.3690276056097920865, -1.103968407447001088, 0.7607293476182939163 ) ) ;
#19160=CIRCLE ( 'NONE', #32198, 0.03749999999977551152 ) ;
#19161=VECTOR ( 'NONE', #22687, 39.37007874015748143 ) ;
#19163=CARTESIAN_POINT ( 'NONE',  ( 0.006340579314978117206, -0.5092170189304694450, 0.4201425565785884553 ) ) ;
#19164=CARTESIAN_POINT ( 'NONE',  ( 0.1024573188296521581, -1.387117369751432516, 0.6458262573307184118 ) ) ;
#19172=CARTESIAN_POINT ( 'NONE',  ( 0.2620066386687194826, -1.629889363925806522, 0.8018636163776085013 ) ) ;
#19174=CARTESIAN_POINT ( 'NONE',  ( 0.5618993035917507761, -1.439841365341236301, 0.7442830156648372331 ) ) ;
#19188=CARTESIAN_POINT ( 'NONE',  ( 0.1421881664906101961, -0.8149641224533534789, 0.5057660219216387754 ) ) ;
#19190=CARTESIAN_POINT ( 'NONE',  ( 0.1111526859351814611, -0.6027224132271093993, 0.3326396559898295857 ) ) ;
#19195=CARTESIAN_POINT ( 'NONE',  ( 0.6208886523625545273, -1.439521707992974298, 0.8392336777283556648 ) ) ;
#19199=CARTESIAN_POINT ( 'NONE',  ( 0.1492234730455878899, -0.6341753046231629609, 0.3839420049399517310 ) ) ;
#19200=CARTESIAN_POINT ( 'NONE',  ( 0.1902649460295288697, -0.8349739946900058829, 0.2559003878554159117 ) ) ;
#19202=CARTESIAN_POINT ( 'NONE',  ( 0.05567535398968421340, -1.335339640988971288, 0.4687417262808780127 ) ) ;
#19204=CARTESIAN_POINT ( 'NONE',  ( 0.07208523036626358904, -1.310649742666034401, 0.6665797303350883274 ) ) ;
#19205=CARTESIAN_POINT ( 'NONE',  ( 0.5030539720840632167, -1.104010818905506675, 0.6157662270679344907 ) ) ;
#19209=EDGE_CURVE ( 'NONE', #1394, #24994, #26779, .T. ) ;
#19211=AXIS2_PLACEMENT_3D ( 'NONE', #28688, #555, #13051 ) ;
#19215=CARTESIAN_POINT ( 'NONE',  ( 0.4491434351882165887, -1.570148841160289299, 0.6050572309278747785 ) ) ;
#19217=CARTESIAN_POINT ( 'NONE',  ( 0.08726992027127385143, -0.7030455430075180923, 0.02343504253866055334 ) ) ;
#19218=B_SPLINE_CURVE_WITH_KNOTS ( 'NONE', 3,
 ( #730, #16529, #32158, #6640, #3780, #34830, #19430, #35039, #10157, #9744, #4172, #13043, #28873, #38534, #38121, #28463, #13448, #13638, #19215, #22727 ),
 .UNSPECIFIED., .F., .F.,
 ( 4, 2, 2, 2, 2, 2, 2, 2, 2, 4 ),
 ( 0.001303671507411563674, 0.001768902510528973845, 0.002234133513646384232, 0.002350441264425739106, 0.002466749015205093980, 0.002524902890594771850, 0.002583056765984450154, 0.002699364516763816738, 0.002931980018322547302, 0.003164595519881276998 ),
 .UNSPECIFIED. ) ;
#19220=CARTESIAN_POINT ( 'NONE',  ( 0.3363288196684174891, -1.747766409858011238, 0.4536835104966877585 ) ) ;
#19221=CARTESIAN_POINT ( 'NONE',  ( 0.04869497213076193903, -1.160534407236927246, 0.7642094061772998215 ) ) ;
#19228=CIRCLE ( 'NONE', #11354, 0.1762268159172233339 ) ;
#19229=CARTESIAN_POINT ( 'NONE',  ( 0.5982834170520250350, -1.597405224470788365, 0.4331267408012325903 ) ) ;
#19235=CARTESIAN_POINT ( 'NONE',  ( 0.09655467777909068627, -0.5920640895833686468, 0.3065293990379648892 ) ) ;
#19236=ORIENTED_EDGE ( 'NONE', *, *, #22119, .F. ) ;
#19240=LINE ( 'NONE', #38344, #21394 ) ;
#19242=CARTESIAN_POINT ( 'NONE',  ( 0.07967440850021659249, -0.5998154657116770982, 0.3398716057233205912 ) ) ;
#19243=CARTESIAN_POINT ( 'NONE',  ( 0.009002175164704872418, -0.6190142101949668296, 0.4357503115026744034 ) ) ;
#19246=FACE_OUTER_BOUND ( 'NONE', #29546, .T. ) ;
#19252=CARTESIAN_POINT ( 'NONE',  ( 0.2732903649954732117, -0.9481965803008104432, 0.7299041271556375721 ) ) ;
#19256=CARTESIAN_POINT ( 'NONE',  ( 0.1382093149295521017, -0.7546047068524435186, 0.5802775608379149297 ) ) ;
#19258=CARTESIAN_POINT ( 'NONE',  ( 0.3319931610750171957, -0.8547376211461308326, 0.6892644829257473793 ) ) ;
#19261=CARTESIAN_POINT ( 'NONE',  ( 0.06116565050235212714, -1.313871996917011398, 0.6258069960581069680 ) ) ;
#19263=B_SPLINE_CURVE_WITH_KNOTS ( 'NONE', 3,
 ( #30783, #27911, #30588, #40450 ),
 .UNSPECIFIED., .F., .F.,
 ( 4, 4 ),
 ( 0.000000000000000000, 5.151976560715283563E-05 ),
 .UNSPECIFIED. ) ;
#19267=CARTESIAN_POINT ( 'NONE',  ( 0.1767056452462499871, -0.9130954350749045378, 0.6111087866971379734 ) ) ;
#19269=CARTESIAN_POINT ( 'NONE',  ( 0.6910433967563797131, -1.503458314657174721, 0.4665392483146700298 ) ) ;
#19271=ORIENTED_EDGE ( 'NONE', *, *, #14668, .T. ) ;
#19272=DIRECTION ( 'NONE',  ( 0.8660512985181135770, 0.4999551463232368431, 0.000000000000000000 ) ) ;
#19275=CARTESIAN_POINT ( 'NONE',  ( 0.3484677573834994435, -1.177852168535778565, 0.4182417262808778013 ) ) ;
#19280=CARTESIAN_POINT ( 'NONE',  ( 0.2953996865216445000, -1.312084307709316278, 0.4675629788832125211 ) ) ;
#19281=CARTESIAN_POINT ( 'NONE',  ( 0.4857864678016971527, -1.660707689634011386, 0.4964627840106182188 ) ) ;
#19283=CARTESIAN_POINT ( 'NONE',  ( 0.4580930487831912923, -1.228282708841101689, 0.7098083865471490617 ) ) ;
#19285=CARTESIAN_POINT ( 'NONE',  ( 0.4907992349987285730, -1.081537398447262266, 0.5876768462667140147 ) ) ;
#19288=CARTESIAN_POINT ( 'NONE',  ( 0.08396792514988114797, -1.274408769650567708, 0.7373487296590384155 ) ) ;
#19291=CARTESIAN_POINT ( 'NONE',  ( 0.1520549073577694699, -0.9832709360364392248, 0.7962433701957113419 ) ) ;
#19292=CARTESIAN_POINT ( 'NONE',  ( 0.06524015413155181964, -0.8058748789547460767, 0.05685236492229539529 ) ) ;
#19295=ORIENTED_EDGE ( 'NONE', *, *, #34421, .T. ) ;
#19298=CARTESIAN_POINT ( 'NONE',  ( 0.3417327841951403045, -1.285448577080334998, 0.5750830755287759111 ) ) ;
#19300=CARTESIAN_POINT ( 'NONE',  ( 0.5552477155703334777, -1.480784202266746341, 0.7056114995199435080 ) ) ;
#19301=VERTEX_POINT ( 'NONE', #1278 ) ;
#19308=CARTESIAN_POINT ( 'NONE',  ( 0.1844690651293379724, -0.8537165418084496915, 0.1701664619867762351 ) ) ;
#19309=LINE ( 'NONE', #16612, #12817 ) ;
#19310=CARTESIAN_POINT ( 'NONE',  ( 0.08875358319671960983, -0.6432264665877226451, 0.1460232572880605928 ) ) ;
#19312=CARTESIAN_POINT ( 'NONE',  ( 0.5337404313129848754, -1.165174529015815530, 0.8761190665599410954 ) ) ;
#19317=DIRECTION ( 'NONE',  ( -0.4999551463232372317, 0.8660512985181135770, -0.000000000000000000 ) ) ;
#19321=EDGE_CURVE ( 'NONE', #30110, #7904, #3670, .T. ) ;
#19323=CARTESIAN_POINT ( 'NONE',  ( 0.5434391066227751699, -1.168983680377609691, 0.5856983068965047057 ) ) ;
#19324=CARTESIAN_POINT ( 'NONE',  ( 0.2643655332618012888, -1.686843913603420342, 0.5679419890486603339 ) ) ;
#19325=CARTESIAN_POINT ( 'NONE',  ( 0.005948235723147832048, -0.6142029534155015735, 0.3540208382306603840 ) ) ;
#19326=CARTESIAN_POINT ( 'NONE',  ( 0.0003922654375693484163, -0.4465883730080376646, 0.08090056108615809038 ) ) ;
#19331=ORIENTED_EDGE ( 'NONE', *, *, #2991, .F. ) ;
#19339=CARTESIAN_POINT ( 'NONE',  ( 0.5962429284462779089, -1.457299488734417281, 0.6386903328529611734 ) ) ;
#19346=CARTESIAN_POINT ( 'NONE',  ( 0.01081953179195815559, -0.5297023241700838936, 0.1457185332388694354 ) ) ;
#19347=CARTESIAN_POINT ( 'NONE',  ( 0.6358170330921433244, -1.565712325321040987, 0.4189323858537951639 ) ) ;
#19350=CARTESIAN_POINT ( 'NONE',  ( 0.01200886551622900103, -0.4814612145085635508, -0.01224044998698113965 ) ) ;
#19353=ORIENTED_EDGE ( 'NONE', *, *, #36279, .T. ) ;
#19355=B_SPLINE_CURVE_WITH_KNOTS ( 'NONE', 3,
 ( #34603, #6406, #3315, #15880, #29240, #10113, #29442, #38084, #35605, #3925 ),
 .UNSPECIFIED., .F., .F.,
 ( 4, 2, 2, 2, 4 ),
 ( 0.000000000000000000, 0.2500000000000000000, 0.5000000000000000000, 0.7500000000000000000, 1.000000000000000000 ),
 .UNSPECIFIED. ) ;
#19358=CARTESIAN_POINT ( 'NONE',  ( 0.1109049718728753187, -0.9286333055842326267, 0.1462684119608117506 ) ) ;
#19360=CARTESIAN_POINT ( 'NONE',  ( 0.5765078172467388296, -1.467567902266393887, 0.7032344926564899623 ) ) ;
#19362=CARTESIAN_POINT ( 'NONE',  ( 0.1678358338209908485, -0.8626253651800752653, 0.4958334663961649902 ) ) ;
#19368=DIRECTION ( 'NONE',  ( -0.4999551463232372317, 0.8660512985181134660, -0.000000000000000000 ) ) ;
#19370=CARTESIAN_POINT ( 'NONE',  ( 0.1852718761952666104, -0.8389489029336036907, 0.1457185345930598341 ) ) ;
#19383=CARTESIAN_POINT ( 'NONE',  ( 0.1942945430039405008, -0.5567045476596680365, 0.2821869111984989242 ) ) ;
#19388=CARTESIAN_POINT ( 'NONE',  ( 0.5916383604625806703, -1.478183414026097653, 0.6639549887419504692 ) ) ;
#19400=B_SPLINE_CURVE_WITH_KNOTS ( 'NONE', 3,
 ( #17523, #30073, #39130, #25992, #13620, #13810, #29872, #38516, #8042, #10954, #32538, #10347, #4356, #23516, #1711, #26185, #36228, #14229, #38709, #32939, #36031, #10529, #16917, #29461, #1305, #26380, #7835, #20406, #26794, #39321, #30474, #34717, #31636, #30684, #28345, #9629, #27591, #23911, #36441, #12505 ),
 .UNSPECIFIED., .F., .F.,
 ( 4, 2, 2, 2, 2, 2, 2, 2, 2, 2, 2, 2, 2, 2, 2, 2, 2, 2, 2, 4 ),
 ( -5.999999991662925479E-08, 0.0006628589721972678959, 0.001325777944394452386, 0.001988696916591636658, 0.002651615888788821148, 0.003314534860986005638, 0.003977453833183190561, 0.004640372805380374617, 0.005303291777577559540, 0.006629129721971918111, 0.007292048694169097831, 0.007954967666366280152, 0.008617886638563462473, 0.009280805610760644794, 0.01060664355515499729, 0.01193248149954934806, 0.01325831944394370229, 0.01590999533273240382, 0.01856167122152111229, 0.02121334711030981729 ),
 .UNSPECIFIED. ) ;
#19403=ORIENTED_EDGE ( 'NONE', *, *, #12490, .T. ) ;
#19404=CARTESIAN_POINT ( 'NONE',  ( 0.1009731816307408991, -0.7855298059080080275, 0.3453887576930584902 ) ) ;
#19406=CARTESIAN_POINT ( 'NONE',  ( 0.08990536851188023204, -0.5646295468556784547, 0.1437216542238681782 ) ) ;
#19407=CARTESIAN_POINT ( 'NONE',  ( 0.5100517597868143849, -1.467776873700488371, 0.7596160885929598150 ) ) ;
#19408=CARTESIAN_POINT ( 'NONE',  ( 0.1876095839365586326, -1.270310460104812966, 0.4182417262808778013 ) ) ;
#19410=CARTESIAN_POINT ( 'NONE',  ( 0.7036498145888742117, -1.518298014128231843, 0.5677572928519309947 ) ) ;
#19411=CARTESIAN_POINT ( 'NONE',  ( 0.3924667225388316916, -1.718121829093100406, 0.6106704844410693056 ) ) ;
#19412=CARTESIAN_POINT ( 'NONE',  ( 0.6620118083207074955, -1.538948419689354363, 0.7089722153523403403 ) ) ;
#19414=CARTESIAN_POINT ( 'NONE',  ( 0.2858528607535977262, -0.9443831972166216726, 0.7228252558026528884 ) ) ;
#19415=CARTESIAN_POINT ( 'NONE',  ( -0.002306167831732802449, -0.8472269691890851329, 0.1380695624520867359 ) ) ;
#19419=DIMENSIONAL_EXPONENTS ( 1.000000000000000000, 0.000000000000000000, 0.000000000000000000, 0.000000000000000000, 0.000000000000000000, 0.000000000000000000, 0.000000000000000000 ) ;
#19421=CARTESIAN_POINT ( 'NONE',  ( 0.03259135683726806926, -1.157323147438684030, 0.6652026314908382476 ) ) ;
#19422=CARTESIAN_POINT ( 'NONE',  ( 0.3146548270004942971, -0.9167534899940792403, 0.6079632372063322743 ) ) ;
#19428=CARTESIAN_POINT ( 'NONE',  ( 0.4155056390950594980, -1.153651200484786532, 0.4182417262808778569 ) ) ;
#19430=CARTESIAN_POINT ( 'NONE',  ( 0.4358234066720084177, -1.577671767360221411, 0.5885670104086981880 ) ) ;
#19431=CARTESIAN_POINT ( 'NONE',  ( 0.002296835029421147919, -0.5198933010532066357, 0.1431176680404081247 ) ) ;
#19432=CARTESIAN_POINT ( 'NONE',  ( 0.08515941055999551312, -0.8106121384747535519, 0.1370161859660417591 ) ) ;
#19435=CARTESIAN_POINT ( 'NONE',  ( 0.1637184504418466302, -1.361439334600449413, 0.6509539637277043100 ) ) ;
#19439=CARTESIAN_POINT ( 'NONE',  ( 0.1464009668243671236, -1.281690631858763085, 0.4243433165416301001 ) ) ;
#19440=DIRECTION ( 'NONE',  ( -0.8660512985181132439, -0.4999551463232376758, 0.000000000000000000 ) ) ;
#19441=CARTESIAN_POINT ( 'NONE',  ( 0.5933601670058918920, -1.600162351846436959, 0.4297890903611187308 ) ) ;
#19445=CARTESIAN_POINT ( 'NONE',  ( 0.04687499999999977102, -0.4772001287898267607, 0.3417740242638161452 ) ) ;
#19446=CARTESIAN_POINT ( 'NONE',  ( 0.1008052951643304829, -0.6052764826558847400, 0.3473834472754093738 ) ) ;
#19447=CARTESIAN_POINT ( 'NONE',  ( 0.05299811827002062770, -0.7416351888791600233, 0.7575765924777226878 ) ) ;
#19448=CARTESIAN_POINT ( 'NONE',  ( 0.4694448353715036659, -1.557891597669167849, 0.5687246758769614052 ) ) ;
#19452=CARTESIAN_POINT ( 'NONE',  ( 0.2113724693258398346, -0.9282255387282759562, 0.3698535518934624733 ) ) ;
#19457=CARTESIAN_POINT ( 'NONE',  ( 0.6865478901158108549, -1.574312610877731000, 0.5182417262812423209 ) ) ;
#19458=CARTESIAN_POINT ( 'NONE',  ( 0.1897112079047655053, -0.5340520988485696341, 0.1458683203705843090 ) ) ;
#19464=CARTESIAN_POINT ( 'NONE',  ( 0.1918124086860224231, -0.5891232155910660628, 0.2119633080407007653 ) ) ;
#19465=EDGE_CURVE ( 'NONE', #14547, #13190, #2274, .T. ) ;
#19467=CARTESIAN_POINT ( 'NONE',  ( 0.05768477182288792027, -1.318213558294332621, 0.6059538573116379778 ) ) ;
#19469=CARTESIAN_POINT ( 'NONE',  ( 0.1940226371263356897, -0.6293705748991054172, 0.3231715484426654350 ) ) ;
#19470=CARTESIAN_POINT ( 'NONE',  ( 0.2934445204131819196, -1.040484148307386780, 0.7330325571301972154 ) ) ;
#19472=CARTESIAN_POINT ( 'NONE',  ( 0.6753500143071270445, -1.527325197043427174, 0.4408735696681176930 ) ) ;
#19478=EDGE_CURVE ( 'NONE', #19301, #507, #11543, .T. ) ;
#19481=CARTESIAN_POINT ( 'NONE',  ( 0.3270275536375774617, -1.166728321694489034, 0.5708165179803514899 ) ) ;
#19486=CARTESIAN_POINT ( 'NONE',  ( 0.2589322829653118996, -1.332681345024160136, 0.5684962963264375002 ) ) ;
#19489=CARTESIAN_POINT ( 'NONE',  ( 0.4486771734934781319, -1.213265135394009597, 0.7011102436740401789 ) ) ;
#19492=CARTESIAN_POINT ( 'NONE',  ( 0.3611884512188844321, -1.010424417365897831, 0.6143157383772529512 ) ) ;
#19495=CARTESIAN_POINT ( 'NONE',  ( 0.04445114182618741666, -1.045807839346486023, 0.7169660596555416099 ) ) ;
#19498=CARTESIAN_POINT ( 'NONE',  ( 0.04805158389062868379, -0.5422655091108523617, 0.1936128867396182673 ) ) ;
#19500=CARTESIAN_POINT ( 'NONE',  ( 0.06443734679387699837, -0.8352580946475701706, 0.1484956170147023191 ) ) ;
#19501=CARTESIAN_POINT ( 'NONE',  ( 0.1957912801600528441, -0.6579173162935690877, 0.3309778881921752736 ) ) ;
#19502=DIRECTION ( 'NONE',  ( 0.5784884052584775560, 0.000000000000000000, 0.8156906061623510062 ) ) ;
#19505=CARTESIAN_POINT ( 'NONE',  ( 0.3249184713931745350, -1.295165278265719699, 0.5695263721355144915 ) ) ;
#19506=CARTESIAN_POINT ( 'NONE',  ( 0.5666678245060221553, -1.503163312012688602, 0.5681760653518421744 ) ) ;
#19508=CARTESIAN_POINT ( 'NONE',  ( 0.1874447297040617022, -0.6903549970268514357, 0.04771061563518469439 ) ) ;
#19511=CARTESIAN_POINT ( 'NONE',  ( 0.5931354683067489031, -1.451137063721512854, 0.6550951170253309641 ) ) ;
#19513=CARTESIAN_POINT ( 'NONE',  ( 0.08393556449649998419, -1.318818014269400818, 0.4567686614275936474 ) ) ;
#19517=CARTESIAN_POINT ( 'NONE',  ( 0.7390121836339409445, -1.515703229308124955, 0.4860421661703527851 ) ) ;
#19524=CARTESIAN_POINT ( 'NONE',  ( 0.1835961851041346959, -0.5126270562563732813, 0.08826789480522242992 ) ) ;
#19527=EDGE_CURVE ( 'NONE', #15591, #33383, #21396, .T. ) ;
#19528=CARTESIAN_POINT ( 'NONE',  ( -8.537024980200822558E-17, -0.6872203660140394632, 0.1631394164078588394 ) ) ;
#19532=CARTESIAN_POINT ( 'NONE',  ( -19685.04193433331602, 285.7890798983738136, -1.951739244310253252 ) ) ;
#19540=EDGE_LOOP ( 'NONE', ( #31682, #38503 ) ) ;
#19543=CARTESIAN_POINT ( 'NONE',  ( 0.5474171421754882028, -1.374785517832714854, 0.7657286113707925113 ) ) ;
#19545=ORIENTED_EDGE ( 'NONE', *, *, #26009, .T. ) ;
#19546=CARTESIAN_POINT ( 'NONE',  ( 0.5549519752308349485, -1.188726111083455939, 0.5935319974400015131 ) ) ;
#19550=CARTESIAN_POINT ( 'NONE',  ( 0.2975162600608768360, -1.656784140337124844, 0.5778434474647357044 ) ) ;
#19552=CARTESIAN_POINT ( 'NONE',  ( 0.6514719573431750899, -1.551752319599670971, 0.4274254745435299152 ) ) ;
#19553=CARTESIAN_POINT ( 'NONE',  ( 0.1109615456377447129, -0.9286233301030853982, 0.1297943113072267118 ) ) ;
#19554=CARTESIAN_POINT ( 'NONE',  ( 0.3173964913805102928, -1.761064994645753723, 0.5509206800346062582 ) ) ;
#19561=CARTESIAN_POINT ( 'NONE',  ( 0.1853397838168331091, -0.8389294303635135286, 0.1596565228427437311 ) ) ;
#19564=CARTESIAN_POINT ( 'NONE',  ( 0.3065843538909625021, -1.143276311498060194, 0.7392926086299859145 ) ) ;
#19565=CARTESIAN_POINT ( 'NONE',  ( 0.01054817777343857940, -0.5296544771352952319, 0.1457185332388703236 ) ) ;
#19574=CARTESIAN_POINT ( 'NONE',  ( 0.1058691297379534685, -1.387140299098825746, 0.6606319638582223153 ) ) ;
#19577=ADVANCED_FACE ( 'NONE', ( #25084 ), #34381, .T. ) ;
#19580=CARTESIAN_POINT ( 'NONE',  ( 0.4638079127942061897, -1.130673443964558267, 0.4607559890518187484 ) ) ;
#19584=CARTESIAN_POINT ( 'NONE',  ( 0.5944485256643038396, -1.487068444243248022, 0.5633783733039713360 ) ) ;
#19590=CARTESIAN_POINT ( 'NONE',  ( 0.6130353677484411401, -1.423293888972499976, 0.8492375987371474366 ) ) ;
#19591=( BOUNDED_SURFACE ( )  B_SPLINE_SURFACE ( 3, 2, ( 
 ( #2900, #31484, #15450 ),
 ( #3291, #25326, #8641 ),
 ( #21214, #33750, #35190 ),
 ( #6990, #6569, #28996 ),
 ( #3506, #29209, #13581 ),
 ( #26146, #16063, #19358 ),
 ( #32482, #10081, #860 ),
 ( #38660, #1071, #25528 ),
 ( #19147, #34970, #6777 ),
 ( #19561, #28611, #22442 ),
 ( #481, #22655, #31895 ),
 ( #9683, #10480, #7373 ),
 ( #13368, #7173, #3715 ),
 ( #1261, #23046, #13155 ),
 ( #22248, #25943, #32091 ),
 ( #16267, #25720, #31684 ),
 ( #35572, #13762, #35383 ),
 ( #28805, #12976, #38467 ),
 ( #19947, #38055, #38251 ),
 ( #4308, #9869, #16874 ),
 ( #10302, #29414, #37866 ),
 ( #668, #3898, #16455 ),
 ( #34762, #22865, #19740 ),
 ( #32277, #4092, #16660 ),
 ( #9023, #8593, #33925 ),
 ( #5725, #14990, #15182 ),
 ( #21990, #27738, #37203 ),
 ( #27543, #3062, #34106 ),
 ( #18683, #34307, #21584 ),
 ( #24456, #17858, #40275 ),
 ( #30421, #9206, #31244 ),
 ( #18075, #18280, #5911 ),
 ( #27352, #25058, #34517 ),
 ( #37592, #9413, #39883 ),
 ( #18471, #12317, #15606 ),
 ( #2644, #28152, #12109 ),
 ( #24255, #16, #24675 ),
 ( #31023, #21166, #30824 ),
 ( #2844, #40064, #15394 ),
 ( #2250, #27952, #40491 ),
 ( #11892, #12501, #24872 ),
 ( #36989, #37394, #8809 ),
 ( #33697, #21778, #6116 ),
 ( #5510, #14790, #11701 ),
 ( #30628, #36778, #2453 ),
 ( #21388, #28940, #1017 ),
 ( #7121, #12920, #31841 ),
 ( #210, #22390, #3658 ),
 ( #3842, #12704, #38404 ),
 ( #16218, #22810, #25266 ) ),
 .UNSPECIFIED., .F., .F., .T. ) 
 B_SPLINE_SURFACE_WITH_KNOTS ( ( 4, 2, 2, 2, 2, 2, 2, 2, 2, 2, 2, 2, 2, 2, 2, 2, 2, 2, 2, 2, 2, 2, 2, 2, 4 ),
 ( 3, 3 ),
 ( 0.005623516400726650925, 0.005723388427146605673, 0.005773324440356582612, 0.005823260453566559552, 0.006023004506406469047, 0.006422492612086288036, 0.007221468823445924279, 0.008819421246165196765, 0.01201532609160374174, 0.01361327851432301422, 0.01521123093704228671, 0.01840713578248083168, 0.02000508820520010417, 0.02160304062791937665, 0.02240201683927901116, 0.02320099305063864914, 0.02479894547335792163, 0.02559792168471755613, 0.02639689789607719411, 0.02719587410743683209, 0.02799485031879646660, 0.02879382653015610111, 0.02959280274151573908, 0.03039177895287537706, 0.03119075516423501157 ),
 ( 0.000000000000000000, 1.000000000000000000 ),
 .UNSPECIFIED. ) 
 GEOMETRIC_REPRESENTATION_ITEM ( )  RATIONAL_B_SPLINE_SURFACE ( (
 ( 1.000000000000000000, 0.7620600366887108068, 1.000000000000000000),
 ( 1.000000000000000000, 0.7620600366887108068, 1.000000000000000000),
 ( 1.000000000000000000, 0.7620600366887158028, 1.000000000000000000),
 ( 1.000000000000000000, 0.7620600366887158028, 1.000000000000000000),
 ( 1.000000000000000000, 0.7620600366887131383, 1.000000000000000000),
 ( 1.000000000000000000, 0.7620600366887131383, 1.000000000000000000),
 ( 1.000000000000000000, 0.7620601373306783444, 1.000000000000000000),
 ( 1.000000000000000000, 0.7620613354069938339, 1.000000000000000000),
 ( 1.000000000000000000, 0.7620643364853295632, 1.000000000000000000),
 ( 1.000000000000000000, 0.7620789881756452333, 1.000000000000000000),
 ( 1.000000000000000000, 0.7620966974486877987, 1.000000000000000000),
 ( 1.000000000000000000, 0.7621581026411062831, 1.000000000000000000),
 ( 1.000000000000000000, 0.7622273003792526813, 1.000000000000000000),
 ( 1.000000000000000000, 0.7624999364063211882, 1.000000000000000000),
 ( 1.000000000000000000, 0.7627161346585163981, 1.000000000000000000),
 ( 1.000000000000000000, 0.7636758486171694171, 1.000000000000000000),
 ( 1.000000000000000000, 0.7646916490131634436, 1.000000000000000000),
 ( 1.000000000000000000, 0.7677082388477355357, 1.000000000000000000),
 ( 1.000000000000000000, 0.7689336181571234663, 1.000000000000000000),
 ( 1.000000000000000000, 0.7719590375727899412, 1.000000000000000000),
 ( 1.000000000000000000, 0.7737898733456646250, 1.000000000000000000),
 ( 1.000000000000000000, 0.7800033286103639218, 1.000000000000000000),
 ( 1.000000000000000000, 0.7857684595439522468, 1.000000000000000000),
 ( 1.000000000000000000, 0.7921457430830625146, 1.000000000000000000),
 ( 1.000000000000000000, 0.7937413855588997258, 1.000000000000000000),
 ( 1.000000000000000000, 0.7926007200054989710, 1.000000000000000000),
 ( 1.000000000000000000, 0.7894156645656090765, 1.000000000000000000),
 ( 1.000000000000000000, 0.7801802461530837896, 1.000000000000000000),
 ( 1.000000000000000000, 0.7764660701984593683, 1.000000000000000000),
 ( 1.000000000000000000, 0.7687415604991519880, 1.000000000000000000),
 ( 1.000000000000000000, 0.7647330715239430976, 1.000000000000000000),
 ( 1.000000000000000000, 0.7535529938687155482, 1.000000000000000000),
 ( 1.000000000000000000, 0.7471814462217952757, 1.000000000000000000),
 ( 1.000000000000000000, 0.7390326041316310768, 1.000000000000000000),
 ( 1.000000000000000000, 0.7365891473593165761, 1.000000000000000000),
 ( 1.000000000000000000, 0.7323603040016591903, 1.000000000000000000),
 ( 1.000000000000000000, 0.7305422876197090742, 1.000000000000000000),
 ( 1.000000000000000000, 0.7274945417416857074, 1.000000000000000000),
 ( 1.000000000000000000, 0.7263021831926989025, 1.000000000000000000),
 ( 1.000000000000000000, 0.7242655549562223571, 1.000000000000000000),
 ( 1.000000000000000000, 0.7233863612473971916, 1.000000000000000000),
 ( 1.000000000000000000, 0.7214440151235159693, 1.000000000000000000),
 ( 1.000000000000000000, 0.7204350154428263986, 1.000000000000000000),
 ( 1.000000000000000000, 0.7178948928364506932, 1.000000000000000000),
 ( 1.000000000000000000, 0.7163188285908211883, 1.000000000000000000),
 ( 1.000000000000000000, 0.7134120004149256955, 1.000000000000000000),
 ( 1.000000000000000000, 0.7119817938359319642, 1.000000000000000000),
 ( 1.000000000000000000, 0.7091286251562103349, 1.000000000000000000),
 ( 1.000000000000000000, 0.7077534102919452730, 1.000000000000000000),
 ( 1.000000000000000000, 0.7067354993702915644, 1.000000000000000000) ) ) 
 REPRESENTATION_ITEM ( '' )  SURFACE ( )  );
#19594=B_SPLINE_CURVE_WITH_KNOTS ( 'NONE', 3,
 ( #25898, #28952, #19700, #38417 ),
 .UNSPECIFIED., .F., .F.,
 ( 4, 4 ),
 ( 0.1593719612050745749, 0.5040661668275804308 ),
 .UNSPECIFIED. ) ;
#19598=CARTESIAN_POINT ( 'NONE',  ( -0.003741027592045935348, -0.8469330747986104635, 0.09509064842809024365 ) ) ;
#19601=CARTESIAN_POINT ( 'NONE',  ( 0.2749031748901358263, -1.001131492694471437, 0.6892845736347759100 ) ) ;
#19603=CARTESIAN_POINT ( 'NONE',  ( 0.06925372759623750485, -0.5401403334181544835, 0.1535009965860707482 ) ) ;
#19604=CARTESIAN_POINT ( 'NONE',  ( 0.1122763543019365540, -0.5767954232603237363, 0.2660804929407222796 ) ) ;
#19609=CARTESIAN_POINT ( 'NONE',  ( 0.3135891416034363721, -1.762206823249338639, 0.5687299299776570338 ) ) ;
#19612=CARTESIAN_POINT ( 'NONE',  ( 0.1554726304735147280, -0.6543779252168671068, 0.4222922872362036006 ) ) ;
#19613=CARTESIAN_POINT ( 'NONE',  ( -2.493673021531738797E-05, -0.9153651195070918734, 0.01783759308780035260 ) ) ;
#19614=CARTESIAN_POINT ( 'NONE',  ( 0.4094665197507286747, -1.132124008075320098, 0.5707417262808780478 ) ) ;
#19616=CARTESIAN_POINT ( 'NONE',  ( 0.01373823669757498131, -0.9963338274435274977, 0.5786879937691099540 ) ) ;
#19617=CARTESIAN_POINT ( 'NONE',  ( 0.5134194225791607336, -1.118797547403455273, 0.5580923141791981346 ) ) ;
#19621=CARTESIAN_POINT ( 'NONE',  ( 0.6935470237484337996, -1.428868995382490237, 0.5856070495622788252 ) ) ;
#19622=CARTESIAN_POINT ( 'NONE',  ( 0.3136119174726084147, -1.762228313981181849, 0.5679019586572930933 ) ) ;
#19625=FACE_OUTER_BOUND ( 'NONE', #20343, .T. ) ;
#19628=CARTESIAN_POINT ( 'NONE',  ( 0.05579155178881651383, -1.335540925555324332, 0.3667417262808778111 ) ) ;
#19629=CARTESIAN_POINT ( 'NONE',  ( 0.6027116599735458102, -1.274749097762014616, 0.7879118535713135474 ) ) ;
#19631=ORIENTED_EDGE ( 'NONE', *, *, #39716, .T. ) ;
#19636=FACE_OUTER_BOUND ( 'NONE', #2070, .T. ) ;
#19639=CARTESIAN_POINT ( 'NONE',  ( 0.1718750000000003608, -0.4565580874172214809, 0.1856949347217508317 ) ) ;
#19640=CARTESIAN_POINT ( 'NONE',  ( 0.2472017802686538868, -0.9017822974133011815, 0.7202505716065562558 ) ) ;
#19641=CARTESIAN_POINT ( 'NONE',  ( 0.007466387553240696855, -0.5173474752212334771, 0.4375680074810365250 ) ) ;
#19642=CARTESIAN_POINT ( 'NONE',  ( 0.4697186253659513255, -1.557987743023917071, 0.5732339134589082841 ) ) ;
#19645=CARTESIAN_POINT ( 'NONE',  ( 0.2188631975425677223, -0.9478063358918615844, 0.4590906284417705097 ) ) ;
#19647=ORIENTED_EDGE ( 'NONE', *, *, #15688, .T. ) ;
#19653=CYLINDRICAL_SURFACE ( 'NONE', #4330, 0.08749999999977552123 ) ;
#19654=CARTESIAN_POINT ( 'NONE',  ( 0.4381829047093346863, -1.020301330954181518, 0.7847444992166355826 ) ) ;
#19656=CARTESIAN_POINT ( 'NONE',  ( 0.008016308253612618520, -0.8914097450206520667, 0.5066122301535544992 ) ) ;
#19659=CARTESIAN_POINT ( 'NONE',  ( 0.3575911698065382116, -1.086899798299411302, 0.7623387881491152651 ) ) ;
#19666=CARTESIAN_POINT ( 'NONE',  ( 0.3549243309889831277, -1.132073402205351131, 0.6013745090441735552 ) ) ;
#19667=CARTESIAN_POINT ( 'NONE',  ( 0.05555397280955033656, -0.8368505189396917565, 0.1801077275890973495 ) ) ;
#19671=CARTESIAN_POINT ( 'NONE',  ( 0.4858726280787338259, -1.662107068784129504, 0.5433456355363511792 ) ) ;
#19673=CARTESIAN_POINT ( 'NONE',  ( 0.4568688193648175466, -1.223409423111213368, 0.6787920684031271135 ) ) ;
#19675=CARTESIAN_POINT ( 'NONE',  ( 0.3143066584002391917, -1.762151917645995880, 0.5150212063305845689 ) ) ;
#19676=CARTESIAN_POINT ( 'NONE',  ( 0.4678749147552476173, -1.068959612060700115, 0.6229948197350051453 ) ) ;
#19681=CARTESIAN_POINT ( 'NONE',  ( 0.2690476586069101561, -1.239345786690793316, 0.8867825711151151591 ) ) ;
#19682=CARTESIAN_POINT ( 'NONE',  ( 0.08702963661190515898, -0.7199049649723878730, 0.02678892191856024202 ) ) ;
#19683=CARTESIAN_POINT ( 'NONE',  ( 0.2031833423866013510, -0.6661378789744705209, 0.3462199175563250297 ) ) ;
#19686=CARTESIAN_POINT ( 'NONE',  ( 0.3696611067744549062, -1.269317993774967235, 0.5790240320825449372 ) ) ;
#19689=CARTESIAN_POINT ( 'NONE',  ( 0.3249529450033704081, -1.071926163521130793, 0.7974727990734679084 ) ) ;
#19694=FACE_OUTER_BOUND ( 'NONE', #28879, .T. ) ;
#19698=CARTESIAN_POINT ( 'NONE',  ( 0.1202810120457312587, -1.413329640664104714, 0.4915196355915492643 ) ) ;
#19700=CARTESIAN_POINT ( 'NONE',  ( 0.5140726076881749762, -1.533129850232453073, 0.5729469988205835307 ) ) ;
#19706=CARTESIAN_POINT ( 'NONE',  ( 0.1742110732111710192, -1.381820364732997630, 0.4951799650135631503 ) ) ;
#19709=CARTESIAN_POINT ( 'NONE',  ( 0.1676694287369189240, -1.385544946528693089, 0.5182417262812420988 ) ) ;
#19712=CARTESIAN_POINT ( 'NONE',  ( 0.2510700677566410910, -1.656657411791499168, 0.6264822711378978948 ) ) ;
#19713=CARTESIAN_POINT ( 'NONE',  ( 3.174100321265008938E-05, -0.6549929327938652790, -0.1017423426240838952 ) ) ;
#19719=DIRECTION ( 'NONE',  ( -1.000000000000000000, 0.000000000000000000, 0.000000000000000000 ) ) ;
#19723=CARTESIAN_POINT ( 'NONE',  ( 0.4754990182428835421, -1.260416879592009209, 0.7839229098787490191 ) ) ;
#19727=CARTESIAN_POINT ( 'NONE',  ( 0.5440395270977919084, -1.170651503450800268, 0.6371399293509031336 ) ) ;
#19731=VERTEX_POINT ( 'NONE', #11069 ) ;
#19733=CARTESIAN_POINT ( 'NONE',  ( 0.02321681876055776625, -0.5326713631696793350, 0.1642138666653286949 ) ) ;
#19735=CARTESIAN_POINT ( 'NONE',  ( 0.1114269046118611800, -0.9037280467778343596, 0.03884140610461449955 ) ) ;
#19739=CARTESIAN_POINT ( 'NONE',  ( 0.3211368908745024231, -1.297361866234852279, 0.5668322337678470824 ) ) ;
#19740=CARTESIAN_POINT ( 'NONE',  ( 0.2048707271511035211, -0.9816035136465564026, 0.5387368206152267636 ) ) ;
#19744=CARTESIAN_POINT ( 'NONE',  ( 0.4035173398106813303, -1.183714493217256525, 0.6980592135633917339 ) ) ;
#19745=CARTESIAN_POINT ( 'NONE',  ( 0.08149770795327589135, -0.9555731122693961188, 0.8005031696937210395 ) ) ;
#19747=CARTESIAN_POINT ( 'NONE',  ( 0.4621675984227249789, -1.110867290327286261, 0.5635151220948720896 ) ) ;
#19749=CARTESIAN_POINT ( 'NONE',  ( 0.4470762725457128051, -1.224665299296468168, 0.5557458780183651692 ) ) ;
#19750=CARTESIAN_POINT ( 'NONE',  ( 0.6610220512682888350, -1.531173313024449145, 0.4235823276999062248 ) ) ;
#19757=CARTESIAN_POINT ( 'NONE',  ( 0.1180724459482614536, -1.405395761025577173, 0.6161712495310950333 ) ) ;
#19759=CARTESIAN_POINT ( 'NONE',  ( 0.4823721729254818458, -1.674185189763958359, 0.4975600008975328281 ) ) ;
#19762=CARTESIAN_POINT ( 'NONE',  ( 0.3080579051995495088, -1.757131687391454644, 0.6134035025875401725 ) ) ;
#19763=CARTESIAN_POINT ( 'NONE',  ( 0.6635321361362904735, -1.532953086552128141, 0.4286296017635089495 ) ) ;
#19768=CARTESIAN_POINT ( 'NONE',  ( 0.1891999079356043167, -0.7494799771669461430, 0.5572005692116146491 ) ) ;
#19776=CARTESIAN_POINT ( 'NONE',  ( 0.06954796871655651025, -1.315582234632707515, 0.5182417262812430980 ) ) ;
#19781=ORIENTED_EDGE ( 'NONE', *, *, #35512, .T. ) ;
#19782=CARTESIAN_POINT ( 'NONE',  ( 0.1672826910485447904, -0.8876356709551983526, 0.5561758849923722492 ) ) ;
#19786=CARTESIAN_POINT ( 'NONE',  ( 0.3315238338797135698, -1.140207891145209596, 0.8255108127574939392 ) ) ;
#19788=CARTESIAN_POINT ( 'NONE',  ( 0.1768208203293339109, -0.4924928695182538840, 0.1890629170402937931 ) ) ;
#19794=CARTESIAN_POINT ( 'NONE',  ( 0.4042633028796379646, -1.711240744074478570, 0.4220515681607872605 ) ) ;
#19795=CARTESIAN_POINT ( 'NONE',  ( 0.6981352535869485010, -1.438782441872884732, 0.5605301977290049198 ) ) ;
#19798=CARTESIAN_POINT ( 'NONE',  ( 0.6089969234689213140, -1.479027626961725295, 0.5722973471840744342 ) ) ;
#19799=CARTESIAN_POINT ( 'NONE',  ( -1.458240315477721432E-08, -0.7217202255946222333, -0.1135441531130386150 ) ) ;
#19801=CARTESIAN_POINT ( 'NONE',  ( 0.4245907089628130904, -1.708467588870119513, 0.4184861834727511276 ) ) ;
#19804=CARTESIAN_POINT ( 'NONE',  ( -0.002083146443013340551, -0.8967360763018591419, 0.1296726476164832831 ) ) ;
#19805=CARTESIAN_POINT ( 'NONE',  ( 0.1845475678902450123, -0.7902170579836453879, 0.1696330687313138408 ) ) ;
#19809=AXIS2_PLACEMENT_3D ( 'NONE', #30763, #11645, #30961 ) ;
#19810=EDGE_CURVE ( 'NONE', #24607, #36909, #16930, .T. ) ;
#19818=CARTESIAN_POINT ( 'NONE',  ( 0.002296899787676456861, -0.5199047658870934452, 0.1480254331800099632 ) ) ;
#19822=CARTESIAN_POINT ( 'NONE',  ( 0.2322138788700108258, -1.233113307957229177, 0.3157417262808777658 ) ) ;
#19823=CARTESIAN_POINT ( 'NONE',  ( 0.6448460108028967186, -1.341977515531164844, 0.7437914968157772755 ) ) ;
#19833=CARTESIAN_POINT ( 'NONE',  ( 0.6470938791149390967, -1.584427830297316264, 0.8325270323136898520 ) ) ;
#19834=CARTESIAN_POINT ( 'NONE',  ( 0.08886448817286804469, -0.6447356382513865780, 0.1659436972385093245 ) ) ;
#19835=CARTESIAN_POINT ( 'NONE',  ( 0.08857948564287103366, -0.8409399715488701244, 0.8385396921228991385 ) ) ;
#19836=CARTESIAN_POINT ( 'NONE',  ( 0.1369971865350032569, -0.7548644416457152007, 0.5821855080690007123 ) ) ;
#19837=CARTESIAN_POINT ( 'NONE',  ( 0.1137578413796589971, -0.5878045126424163991, -0.07386395797409718578 ) ) ;
#19839=CARTESIAN_POINT ( 'NONE',  ( 0.2987922164586632179, -1.070374400135252646, 0.6380231227814501249 ) ) ;
#19847=CARTESIAN_POINT ( 'NONE',  ( 0.2146879954751789998, -0.5662268874561233734, 0.4488732130404408105 ) ) ;
#19854=CARTESIAN_POINT ( 'NONE',  ( 0.07340065495868035306, -1.319686002187802520, 0.5021441993942140636 ) ) ;
#19856=CARTESIAN_POINT ( 'NONE',  ( 0.2889710164712426255, -0.7847915145120791802, 0.6224945701162477585 ) ) ;
#19857=CARTESIAN_POINT ( 'NONE',  ( 0.5382276305428630447, -1.161165069882498013, 0.5699001961276483064 ) ) ;
#19858=CARTESIAN_POINT ( 'NONE',  ( -0.002288348195189989116, -0.8555288688122629770, 0.1457185332388701293 ) ) ;
#19860=CARTESIAN_POINT ( 'NONE',  ( 0.3282822130750457923, -1.293256442918319538, 0.5434200829396130805 ) ) ;
#19862=CARTESIAN_POINT ( 'NONE',  ( 0.2101702454653370800, -0.9424526697851294266, 0.6590696260816275576 ) ) ;
#19864=CARTESIAN_POINT ( 'NONE',  ( 0.5105486452057178548, -1.310984060847071975, 0.6057417262808281189 ) ) ;
#19867=CARTESIAN_POINT ( 'NONE',  ( 0.5311646237512303026, -1.165099885119055712, 0.5038258806297195580 ) ) ;
#19871=CARTESIAN_POINT ( 'NONE',  ( 0.2606834830056775076, -1.287120324457716736, 0.6747163837352363469 ) ) ;
#19880=CARTESIAN_POINT ( 'NONE',  ( 0.4706509655328846575, -1.243911349059814375, 0.6624884991776383014 ) ) ;
#19883=CARTESIAN_POINT ( 'NONE',  ( 0.2159838750730762591, -0.9307556585230835067, 0.3864363914520806964 ) ) ;
#19888=CARTESIAN_POINT ( 'NONE',  ( 0.4162243804113466839, -1.587913871921676989, 0.6315551494585328607 ) ) ;
#19891=CARTESIAN_POINT ( 'NONE',  ( 0.1113603080763501257, -0.9086058680110904451, 0.04931519565019508444 ) ) ;
#19892=CARTESIAN_POINT ( 'NONE',  ( 0.1416495210772664437, -1.285147657081797012, 0.4817276165705878244 ) ) ;
#19895=CARTESIAN_POINT ( 'NONE',  ( 0.1472892881247072627, -0.6767312212032746688, 0.4647785827719352891 ) ) ;
#19900=CARTESIAN_POINT ( 'NONE',  ( 0.3019775573823714199, -1.138158212549354120, 0.5182417262812423209 ) ) ;
#19901=AXIS2_PLACEMENT_3D ( 'NONE', #25, #3254, #40076 ) ;
#19904=CARTESIAN_POINT ( 'NONE',  ( 0.7110566119663160878, -1.453354452021889731, 0.7718588955819412067 ) ) ;
#19912=CARTESIAN_POINT ( 'NONE',  ( 0.2285146069045126682, -1.350404058286757136, 0.4993478297109967268 ) ) ;
#19916=CARTESIAN_POINT ( 'NONE',  ( 0.1472911887417822641, -1.284155632031082517, 0.4182314466967200772 ) ) ;
#19917=VERTEX_POINT ( 'NONE', #17444 ) ;
#19918=CARTESIAN_POINT ( 'NONE',  ( 0.05992416651567116642, -0.8828589634183678925, 0.7642515975180658172 ) ) ;
#19925=CARTESIAN_POINT ( 'NONE',  ( 0.2321526281619643584, -1.233007205928619232, 0.3667417262808778111 ) ) ;
#19930=CARTESIAN_POINT ( 'NONE',  ( 0.4074053067644164972, -1.158105270543656085, 0.7726839899096992204 ) ) ;
#19932=CARTESIAN_POINT ( 'NONE',  ( 0.5676041605235047083, -1.626300245317876980, 0.5026027723836924421 ) ) ;
#19934=CARTESIAN_POINT ( 'NONE',  ( 0.3637128952805344095, -0.9645059733743139851, 0.6550525653421633843 ) ) ;
#19940=CARTESIAN_POINT ( 'NONE',  ( 0.02322307456033168363, -0.5318894034165194684, 0.1457185332388691024 ) ) ;
#19941=CARTESIAN_POINT ( 'NONE',  ( 0.6300906668383386977, -1.574674102679878063, 0.4263063865966011945 ) ) ;
#19943=CARTESIAN_POINT ( 'NONE',  ( 0.1435064959217801916, -1.283467536720964697, 0.5197417262808780025 ) ) ;
#19947=CARTESIAN_POINT ( 'NONE',  ( 0.2172743585675568356, -0.8579260410846445417, 0.4051362072568608919 ) ) ;
#19953=CARTESIAN_POINT ( 'NONE',  ( 0.3583570516064159550, -1.223096128769133317, 0.6863269740785166162 ) ) ;
#19954=CARTESIAN_POINT ( 'NONE',  ( 0.01083811821583093374, -0.5479617008785322430, 0.2379223945615984992 ) ) ;
#19956=CARTESIAN_POINT ( 'NONE',  ( 0.4076976354719480944, -1.154888438488553826, 0.4182417262808778013 ) ) ;
#19958=CARTESIAN_POINT ( 'NONE',  ( 0.6544078563150221850, -1.544269123161552626, 0.4241055859090109292 ) ) ;
#19964=CARTESIAN_POINT ( 'NONE',  ( 0.02906710819876866247, -1.111300232264741172, 0.6609726249879336324 ) ) ;
#19965=CARTESIAN_POINT ( 'NONE',  ( 0.1786313307395676619, -0.4924000933286005743, 0.1338216977563466970 ) ) ;
#19966=CARTESIAN_POINT ( 'NONE',  ( 0.1099256020772691467, -1.419293905719575477, 0.5685549581676759834 ) ) ;
#19971=CARTESIAN_POINT ( 'NONE',  ( 0.2934918387085203584, -1.644164324632618301, 0.9129472502802961076 ) ) ;
#19979=CARTESIAN_POINT ( 'NONE',  ( 0.1828835028638483573, -0.5190310081367575101, 0.2566657934198534052 ) ) ;
#19980=ORIENTED_EDGE ( 'NONE', *, *, #32903, .T. ) ;
#19983=CARTESIAN_POINT ( 'NONE',  ( 0.4807263528268903019, -1.305708637018340834, 0.8152355762322205379 ) ) ;
#19984=ADVANCED_FACE ( 'NONE', ( #37778 ), #39991, .T. ) ;
#19990=CARTESIAN_POINT ( 'NONE',  ( 0.3088934897170949045, -1.189159158785630277, 0.5061700154489670034 ) ) ;
#19992=CARTESIAN_POINT ( 'NONE',  ( -0.004170050296584535375, -0.6270701198925358044, 0.4329761698911018253 ) ) ;
#19993=CARTESIAN_POINT ( 'NONE',  ( 0.1711601909574965164, -1.383443734294387939, 0.5378582171031165426 ) ) ;
#19996=AXIS2_PLACEMENT_3D ( 'NONE', #27020, #30300, #11379 ) ;
#20000=CARTESIAN_POINT ( 'NONE',  ( 0.09474359960899157718, -0.7992767504562960923, 0.3037933874108209031 ) ) ;
#20002=CARTESIAN_POINT ( 'NONE',  ( 0.07274636059270921107, -0.5712887667331841834, 0.2713463052083351368 ) ) ;
#20004=CARTESIAN_POINT ( 'NONE',  ( 0.1117061238851624477, -0.5727138467974830505, 0.2548588568801546383 ) ) ;
#20005=CARTESIAN_POINT ( 'NONE',  ( 0.1777497266415261346, -0.4987312181850360182, 0.2142283185154747749 ) ) ;
#20010=CARTESIAN_POINT ( 'NONE',  ( 0.3329225671462469061, -1.751883312225780420, 0.5693379886238489895 ) ) ;
#20014=CARTESIAN_POINT ( 'NONE',  ( 0.1890965627226634804, -1.347655541994686068, 0.5182417262812423209 ) ) ;
#20017=CARTESIAN_POINT ( 'NONE',  ( -9.774798136714478227E-06, -0.8191943866653442763, -0.07958805542202744554 ) ) ;
#20018=CARTESIAN_POINT ( 'NONE',  ( 0.4028317915878064648, -1.175318803141969681, 0.8151889077341930578 ) ) ;
#20019=CARTESIAN_POINT ( 'NONE',  ( 0.007470885619759358443, -0.7664851069221876312, 0.008519161373831274017 ) ) ;
#20021=CARTESIAN_POINT ( 'NONE',  ( -0.003075981321608621880, -0.8070878537792822716, 0.1960017582677906212 ) ) ;
#20022=CARTESIAN_POINT ( 'NONE',  ( 0.4929465528686912679, -1.082715557938388029, 0.5639242819095140469 ) ) ;
#20025=AXIS2_PLACEMENT_3D ( 'NONE', #16153, #28691, #25605 ) ;
#20034=CARTESIAN_POINT ( 'NONE',  ( 0.01149458178949343268, -0.5639228391815407360, 0.2834883079787945959 ) ) ;
#20036=CARTESIAN_POINT ( 'NONE',  ( 0.2106106046344508043, -1.233927216831852025, 0.4729821282189752840 ) ) ;
#20038=CARTESIAN_POINT ( 'NONE',  ( 0.3339246645468108010, -1.752618221267800536, 0.4594630238594379357 ) ) ;
#20039=EDGE_CURVE ( 'NONE', #1740, #6763, #25750, .T. ) ;
#20040=VECTOR ( 'NONE', #33358, 39.37007874015748143 ) ;
#20041=CARTESIAN_POINT ( 'NONE',  ( 0.1898244942508440503, -0.5073357646527311138, 0.1864979583367220028 ) ) ;
#20047=CARTESIAN_POINT ( 'NONE',  ( 0.3434800707738386305, -1.169184835483333185, 0.4282596159935695423 ) ) ;
#20050=CARTESIAN_POINT ( 'NONE',  ( 0.2209899243456227846, -1.361115721219026797, 1.190013540297138572 ) ) ;
#20051=CARTESIAN_POINT ( 'NONE',  ( 0.08767352474349697500, -0.6847778086286057109, 0.1675417422483599927 ) ) ;
#20052=CARTESIAN_POINT ( 'NONE',  ( 0.1058629817858797312, -0.9473122495338976989, 0.9158932442105627292 ) ) ;
#20053=CARTESIAN_POINT ( 'NONE',  ( 0.4695230613062974512, -1.557919065767196187, 0.5700130294922880481 ) ) ;
#20055=CARTESIAN_POINT ( 'NONE',  ( 0.1153471662232078698, -0.4465907064269051263, 0.1457432652200511269 ) ) ;
#20058=CARTESIAN_POINT ( 'NONE',  ( 0.3296550237143848205, -1.099205586124516909, 0.6409462830847290071 ) ) ;
#20062=CARTESIAN_POINT ( 'NONE',  ( 0.3177859269536487119, -1.645585450493298962, 0.5231366550910405699 ) ) ;
#20064=CARTESIAN_POINT ( 'NONE',  ( 0.1185549026673793083, -0.4796779786644438937, 0.2928297671798744672 ) ) ;
#20070=FACE_OUTER_BOUND ( 'NONE', #38879, .T. ) ;
#20073=CARTESIAN_POINT ( 'NONE',  ( 0.5974340449968663647, -1.261189741147681787, 0.6853727476855657752 ) ) ;
#20074=( BOUNDED_SURFACE ( )  B_SPLINE_SURFACE ( 3, 2, ( 
 ( #30143, #13688, #11028 ),
 ( #7721, #4609, #11421 ),
 ( #17185, #32807, #36103 ),
 ( #10602, #20288, #7512 ),
 ( #29730, #26254, #11214 ),
 ( #4429, #7907, #29529 ) ),
 .UNSPECIFIED., .F., .F., .F. ) 
 B_SPLINE_SURFACE_WITH_KNOTS ( ( 4, 2, 4 ),
 ( 3, 3 ),
 ( 0.01236296969923212849, 0.01327412252728663034, 0.01418527535534113218 ),
 ( 0.8365089563635481618, 1.000000000000000000 ),
 .UNSPECIFIED. ) 
 GEOMETRIC_REPRESENTATION_ITEM ( )  RATIONAL_B_SPLINE_SURFACE ( (
 ( 0.9196845010948848653, 0.9519936407768658793, 1.000000000000000000),
 ( 0.9196791632980176878, 0.9519904502570114557, 1.000000000000000000),
 ( 0.9196826974396685728, 0.9519925626920452411, 1.000000000000000000),
 ( 0.9196970493731875251, 0.9520011411617733676, 1.000000000000000000),
 ( 0.9197077343035476860, 0.9520075277821907767, 1.000000000000000000),
 ( 0.9197191540535247789, 0.9520143536206293611, 1.000000000000000000) ) ) 
 REPRESENTATION_ITEM ( '' )  SURFACE ( )  );
#20075=CARTESIAN_POINT ( 'NONE',  ( 0.5409940809552228336, -1.629370368867399055, 0.4283118504128637927 ) ) ;
#20076=CARTESIAN_POINT ( 'NONE',  ( 0.005974781723437884440, -0.8455926680098735382, 0.1913255637356532368 ) ) ;
#20080=CARTESIAN_POINT ( 'NONE',  ( 0.2399278993395743964, -0.9290780320567488815, 0.6800090796796801618 ) ) ;
#20089=DIRECTION ( 'NONE',  ( 0.4999551463232372317, -0.8660512985181135770, 0.000000000000000000 ) ) ;
#20092=CARTESIAN_POINT ( 'NONE',  ( 0.09229806196967101084, -0.9044670966804603252, 0.5687378640879924285 ) ) ;
#20093=VERTEX_POINT ( 'NONE', #30125 ) ;
#20097=CARTESIAN_POINT ( 'NONE',  ( 0.1223045647424210181, -1.412159682085746271, 0.4849083929475432320 ) ) ;
#20099=CARTESIAN_POINT ( 'NONE',  ( 0.3840497050944557955, -1.128614810062711360, 0.7138234942851187093 ) ) ;
#20106=ORIENTED_EDGE ( 'NONE', *, *, #28657, .T. ) ;
#20107=CARTESIAN_POINT ( 'NONE',  ( 0.4135726104504772183, -1.589529505291096489, 0.5730501051810202862 ) ) ;
#20108=CARTESIAN_POINT ( 'NONE',  ( 0.08792459278225348007, -0.6496347354946547803, 0.006458355081153737201 ) ) ;
#20116=CARTESIAN_POINT ( 'NONE',  ( 0.1192362759130453781, -0.5567294128173433387, 0.1990477325651368867 ) ) ;
#20117=EDGE_LOOP ( 'NONE', ( #18520, #9743, #26789, #9618 ) ) ;
#20120=CARTESIAN_POINT ( 'NONE',  ( 0.6521185033023279010, -1.542907011849267596, 0.4182417262808777458 ) ) ;
#20121=CARTESIAN_POINT ( 'NONE',  ( 0.2292879920235051938, -1.234689012067045066, 0.4835017060594773430 ) ) ;
#20126=CARTESIAN_POINT ( 'NONE',  ( 0.5536297569049346556, -1.186194075236972179, 0.6057417262809815517 ) ) ;
#20133=CARTESIAN_POINT ( 'NONE',  ( 0.1836761679754468357, -0.5203768919390597825, 0.06931577267137481457 ) ) ;
#20134=CARTESIAN_POINT ( 'NONE',  ( 0.2590195079428145863, -1.679471191969716060, 0.4398509372606123069 ) ) ;
#20136=CARTESIAN_POINT ( 'NONE',  ( 0.1209954484009972825, -1.306288436253663976, 0.4272974611868050610 ) ) ;
#20138=CARTESIAN_POINT ( 'NONE',  ( 0.04376425988958544677, -0.9339557565548041174, 0.7112009851976159869 ) ) ;
#20144=ORIENTED_EDGE ( 'NONE', *, *, #13025, .T. ) ;
#20150=CARTESIAN_POINT ( 'NONE',  ( 0.4016278364854861116, -1.148462343513625639, 0.7933350346235505945 ) ) ;
#20153=CARTESIAN_POINT ( 'NONE',  ( 0.3909368226714677319, -0.9916197579736178991, 0.6726537802841677793 ) ) ;
#20159=CARTESIAN_POINT ( 'NONE',  ( 0.02723342787037887069, -0.5846365886964711711, 0.3289579258136214879 ) ) ;
#20160=CARTESIAN_POINT ( 'NONE',  ( 0.7050266291804438978, -1.514791320213222159, 0.5680628335673595375 ) ) ;
#20166=AXIS2_PLACEMENT_3D ( 'NONE', #9626, #37808, #4041 ) ;
#20170=CARTESIAN_POINT ( 'NONE',  ( 0.2135156657176371930, -0.9834570136538726137, 0.6967854075931073643 ) ) ;
#20172=CARTESIAN_POINT ( 'NONE',  ( 0.4750664305519962105, -1.163578551645441550, 0.4182417262808777458 ) ) ;
#20180=CARTESIAN_POINT ( 'NONE',  ( 0.3812246895800440738, -1.141621232065750391, 0.4312472505867336325 ) ) ;
#20181=CARTESIAN_POINT ( 'NONE',  ( 0.1799323859991091290, -0.4957562479442227388, 0.1245508302704903536 ) ) ;
#20182=DIRECTION ( 'NONE',  ( -0.4999551463232371762, 0.8660512985181134660, -0.000000000000000000 ) ) ;
#20185=CARTESIAN_POINT ( 'NONE',  ( 0.2969171742742482412, -1.658742054446402658, 0.8971516434728256106 ) ) ;
#20191=ORIENTED_EDGE ( 'NONE', *, *, #8886, .F. ) ;
#20193=CARTESIAN_POINT ( 'NONE',  ( 0.6027832162698157914, -1.482621114427892461, 0.5983148804162514711 ) ) ;
#20194=CARTESIAN_POINT ( 'NONE',  ( -0.0007010309512375748758, -0.7626727799179832123, -0.004770403981119245192 ) ) ;
#20198=CARTESIAN_POINT ( 'NONE',  ( 0.5609749049919212638, -1.322492582006539852, 0.8902790116251644292 ) ) ;
#20200=CARTESIAN_POINT ( 'NONE',  ( -0.01396963725348175298, -0.5351778444009501756, 0.2100693574405696207 ) ) ;
#20208=CARTESIAN_POINT ( 'NONE',  ( 0.1095666333324003955, -0.8145518545241268171, 0.3913258102692879770 ) ) ;
#20209=B_SPLINE_CURVE_WITH_KNOTS ( 'NONE', 3,
 ( #6724, #16006, #19505, #10241, #13527, #38608, #25885, #10430, #28552, #19298, #32035, #13313, #19686, #26092, #22990, #6327 ),
 .UNSPECIFIED., .F., .F.,
 ( 4, 2, 2, 2, 2, 2, 2, 4 ),
 ( 0.000000000000000000, 5.224492126191339130E-05, 0.0001044898425238267826, 0.0002089796850476577665, 0.0004179593700953283266, 0.0008359187401906626163, 0.001671837480381325883, 0.003343674960762656970 ),
 .UNSPECIFIED. ) ;
#20210=CARTESIAN_POINT ( 'NONE',  ( 0.1075258522074294676, -1.346637391717543375, 0.6997241829952332015 ) ) ;
#20211=CARTESIAN_POINT ( 'NONE',  ( 0.09179313224142107708, -0.5838716517235741366, 0.2326204640114538647 ) ) ;
#20212=CARTESIAN_POINT ( 'NONE',  ( 0.5027379836985736983, -1.456623547386490136, 0.7738150853535875617 ) ) ;
#20213=CARTESIAN_POINT ( 'NONE',  ( 0.1959931128787035237, -0.5695994422963300829, 0.3097654547218591237 ) ) ;
#20215=CARTESIAN_POINT ( 'NONE',  ( 0.6859986618141611370, -1.527025669111474526, 0.4781287526575291325 ) ) ;
#20216=CARTESIAN_POINT ( 'NONE',  ( 0.3529334898677526922, -1.741231243591691014, 0.5928160496120983280 ) ) ;
#20217=CARTESIAN_POINT ( 'NONE',  ( 0.6655612380268166595, -1.561523951251945874, 0.5631882573506850065 ) ) ;
#20222=EDGE_CURVE ( 'NONE', #849, #3787, #34557, .T. ) ;
#20225=CARTESIAN_POINT ( 'NONE',  ( -0.0001519008987895401682, -0.8203875425039895974, -0.06507672622562246656 ) ) ;
#20226=CARTESIAN_POINT ( 'NONE',  ( 0.5836794880485997039, -1.483121240051231471, 0.6621808355073148800 ) ) ;
#20228=CARTESIAN_POINT ( 'NONE',  ( 0.4971920908461615607, -1.080069027881642052, 0.4687417262808780127 ) ) ;
#20231=CARTESIAN_POINT ( 'NONE',  ( 0.1230419690069037980, -1.441173760443279050, 0.5802947806848592904 ) ) ;
#20232=CARTESIAN_POINT ( 'NONE',  ( 0.4373890596466497582, -1.046786911024660593, 0.6537231983888873721 ) ) ;
#20234=CARTESIAN_POINT ( 'NONE',  ( 0.2888622377148890585, -0.7373900025806978675, 0.6684008680139050806 ) ) ;
#20235=DIRECTION ( 'NONE',  ( -0.4999551463232372317, 0.8660512985181135770, -0.000000000000000000 ) ) ;
#20241=CARTESIAN_POINT ( 'NONE',  ( 0.003262416371409640210, -0.5547458529584512466, 0.2870733929886844504 ) ) ;
#20246=CARTESIAN_POINT ( 'NONE',  ( 0.4241633753480167357, -0.9987333192354345135, 0.7764642562231158784 ) ) ;
#20252=CARTESIAN_POINT ( 'NONE',  ( 0.1876095839365584383, -1.270310460104812744, 0.4182417262808780234 ) ) ;
#20254=B_SPLINE_CURVE_WITH_KNOTS ( 'NONE', 3,
 ( #16941, #32353, #14049, #26818, #20036, #1925, #17135, #4770, #32568, #39347, #26627, #10366, #13834, #23542, #11168, #22928, #4384, #26408, #29482, #7858, #17344, #29901 ),
 .UNSPECIFIED., .F., .F.,
 ( 4, 2, 2, 2, 2, 2, 2, 2, 2, 2, 4 ),
 ( 0.001187924609274661029, 0.001905614920410501206, 0.002623305231546341383, 0.003340995542682181560, 0.004058685853818020869, 0.004776376164953861914, 0.005494066476089702090, 0.005852911631657626082, 0.006211756787225550074, 0.006570601942793475800, 0.006929447098361399791 ),
 .UNSPECIFIED. ) ;
#20256=CARTESIAN_POINT ( 'NONE',  ( 0.1045998439320173501, -1.275504460590098033, 0.5978142315846559640 ) ) ;
#20257=CARTESIAN_POINT ( 'NONE',  ( 0.1167100500347143938, -0.7341236526051606592, 0.4239359085789457526 ) ) ;
#20258=CARTESIAN_POINT ( 'NONE',  ( 0.2362853573231588344, -1.416426150276697937, 1.031910927484303020 ) ) ;
#20259=CARTESIAN_POINT ( 'NONE',  ( 0.08712330498557509240, -0.5673539409833764369, 0.2525723869550539069 ) ) ;
#20261=DIRECTION ( 'NONE',  ( 0.4999551463232372317, -0.8660512985181135770, 0.000000000000000000 ) ) ;
#20262=CARTESIAN_POINT ( 'NONE',  ( 0.2055788005570233501, -0.9799573814450284193, 0.5334445023266595198 ) ) ;
#20263=ORIENTED_EDGE ( 'NONE', *, *, #5244, .F. ) ;
#20266=CARTESIAN_POINT ( 'NONE',  ( 0.2013267960816771396, -0.5279965997290305690, 0.3764562652743823623 ) ) ;
#20272=ADVANCED_FACE ( 'NONE', ( #15697 ), #14292, .T. ) ;
#20274=CARTESIAN_POINT ( 'NONE',  ( 0.6182635900321699074, -1.298039841913932513, 0.5932631914600888789 ) ) ;
#20279=CARTESIAN_POINT ( 'NONE',  ( 0.2576571872773831262, -0.9936220594909095372, 0.7090459653281796504 ) ) ;
#20280=CARTESIAN_POINT ( 'NONE',  ( 0.3244517107433588787, -1.756899521929603081, 0.5670097850713597953 ) ) ;
#20284=CARTESIAN_POINT ( 'NONE',  ( 0.4956832342913312650, -1.106712120975469782, 0.6967973883462599272 ) ) ;
#20288=CARTESIAN_POINT ( 'NONE',  ( 0.4112729528620188146, -1.130284805869275599, 0.4964726040806888840 ) ) ;
#20289=CARTESIAN_POINT ( 'NONE',  ( 0.03345570897536777333, -0.8438603944194037476, 0.2510648449414971117 ) ) ;
#20293=CARTESIAN_POINT ( 'NONE',  ( 0.2038749045098602886, -1.364881829950852721, 0.4182417262808790226 ) ) ;
#20295=CARTESIAN_POINT ( 'NONE',  ( 0.4793885211484971709, -1.257667511030738927, 0.5965085062872911292 ) ) ;
#20298=CARTESIAN_POINT ( 'NONE',  ( 0.3142644354089449421, -0.9846788231241262457, 0.5762604841115940291 ) ) ;
#20299=VERTEX_POINT ( 'NONE', #18313 ) ;
#20302=CARTESIAN_POINT ( 'NONE',  ( 0.1882219672280248668, -0.6407273034312881421, -0.08446770797961487831 ) ) ;
#20303=CARTESIAN_POINT ( 'NONE',  ( 0.1929482915730646453, -1.044195424190118571, 0.8266095843266986209 ) ) ;
#20304=CARTESIAN_POINT ( 'NONE',  ( 0.08759942705067334801, -0.6779500844790127267, 0.001722161171260314571 ) ) ;
#20305=CARTESIAN_POINT ( 'NONE',  ( 0.08510361377861434817, -0.8106636051554854117, 0.1454306519311501233 ) ) ;
#20306=DIRECTION ( 'NONE',  ( 0.8660512985181134660, 0.4999551463232372317, 0.000000000000000000 ) ) ;
#20309=CARTESIAN_POINT ( 'NONE',  ( 0.5743670735733531485, -1.499265677782189332, 0.5819334991045758132 ) ) ;
#20317=CARTESIAN_POINT ( 'NONE',  ( 0.2153918940804837590, -1.242713953115129666, 0.4559406856927734619 ) ) ;
#20321=CARTESIAN_POINT ( 'NONE',  ( 0.2978499211271074532, -0.7548715063715667473, 0.6844903506759184575 ) ) ;
#20324=ADVANCED_FACE ( 'NONE', ( #18109, #37630 ), #21615, .F. ) ;
#20329=CARTESIAN_POINT ( 'NONE',  ( 0.6960330676580404052, -1.427191473012519918, 0.4398509372606123069 ) ) ;
#20330=B_SPLINE_CURVE_WITH_KNOTS ( 'NONE', 3,
 ( #27250, #5403, #39780, #36496 ),
 .UNSPECIFIED., .F., .F.,
 ( 4, 4 ),
 ( 3.469446951953614189E-18, 0.0007111050983136056993 ),
 .UNSPECIFIED. ) ;
#20332=DIRECTION ( 'NONE',  ( -0.9574652249354426159, 0.000000000000000000, -0.2885486840020622390 ) ) ;
#20338=EDGE_CURVE ( 'NONE', #6171, #28384, #11964, .T. ) ;
#20341=CARTESIAN_POINT ( 'NONE',  ( 0.07043814880410684265, -1.334972480813831242, 0.5056242588139928662 ) ) ;
#20343=EDGE_LOOP ( 'NONE', ( #37841, #27571, #35223, #37898, #5662, #31870 ) ) ;
#20347=CARTESIAN_POINT ( 'NONE',  ( 0.5380213988856127338, -1.358208888136053005, 0.7378845647473735170 ) ) ;
#20350=CARTESIAN_POINT ( 'NONE',  ( 0.1874843899254543811, -0.7932266022496337055, 0.2338244398510780642 ) ) ;
#20354=CARTESIAN_POINT ( 'NONE',  ( 0.3266909551894673913, -1.639055458000120868, 0.5694230527446741963 ) ) ;
#20355=CARTESIAN_POINT ( 'NONE',  ( 0.7015756474355604455, -1.490181709399133858, 0.5009006423618302950 ) ) ;
#20356=CARTESIAN_POINT ( 'NONE',  ( 0.1873251789708756665, -0.5721470344398987828, 0.02377237672441944241 ) ) ;
#20357=CARTESIAN_POINT ( 'NONE',  ( 0.05563540667800927902, -1.335270441939011121, 0.5197417262808780025 ) ) ;
#20363=CARTESIAN_POINT ( 'NONE',  ( 0.4366195600600660254, -1.227215273123700712, 0.6046990178492395174 ) ) ;
#20374=CARTESIAN_POINT ( 'NONE',  ( 0.03449693227200471141, -1.144353617540043722, 0.6732275831407835698 ) ) ;
#20375=CARTESIAN_POINT ( 'NONE',  ( 0.1804100887215605853, -0.4972044085177187989, 0.1208670693178307276 ) ) ;
#20384=AXIS2_PLACEMENT_3D ( 'NONE', #29435, #32508, #16477 ) ;
#20385=CARTESIAN_POINT ( 'NONE',  ( 0.1882052571625662252, -0.5110766197885958650, 0.09799269069308937097 ) ) ;
#20388=CARTESIAN_POINT ( 'NONE',  ( 0.6019577307062530247, -1.483131278876760550, 0.5728282478110194864 ) ) ;
#20389=CARTESIAN_POINT ( 'NONE',  ( -0.0001062047391421509833, -0.6980687014391792067, -0.01370441279489919249 ) ) ;
#20392=CARTESIAN_POINT ( 'NONE',  ( 0.3100641407756268286, -1.188533344716862006, 0.5383015422848057563 ) ) ;
#20394=CARTESIAN_POINT ( 'NONE',  ( -0.01398755374478900804, -0.5253281656772126329, 0.1457185332388696575 ) ) ;
#20399=CARTESIAN_POINT ( 'NONE',  ( -0.001266333596127353555, -0.7404579356088998310, -0.06462206035643762447 ) ) ;
#20400=ORIENTED_EDGE ( 'NONE', *, *, #35353, .F. ) ;
#20402=CARTESIAN_POINT ( 'NONE',  ( 0.08704056524540265682, -0.8139669836441042472, 0.2169878034514332588 ) ) ;
#20403=CARTESIAN_POINT ( 'NONE',  ( 0.1188311809963038257, -1.413182374742705028, 0.5829798790863079949 ) ) ;
#20404=CARTESIAN_POINT ( 'NONE',  ( 0.09049813587943421334, -0.5721903250205445657, 0.1963611786150708527 ) ) ;
#20405=CARTESIAN_POINT ( 'NONE',  ( 0.5530767995133970549, -1.511202523187898272, 0.5748300795346157344 ) ) ;
#20406=CARTESIAN_POINT ( 'NONE',  ( 0.02528307276850410429, -1.032232763260760411, 0.5721851376505144859 ) ) ;
#20410=CARTESIAN_POINT ( 'NONE',  ( 0.7428087118830455360, -1.516422422578568074, 0.5574800764447178647 ) ) ;
#20411=DIRECTION ( 'NONE',  ( 0.9998941247116546194, -0.01455087607601020239, 0.0001066420868422379362 ) ) ;
#20413=VECTOR ( 'NONE', #15215, 39.37007874015748143 ) ;
#20415=CARTESIAN_POINT ( 'NONE',  ( -0.0003284294498005900943, -0.9127994026214639733, 0.03813321986937860675 ) ) ;
#20416=CARTESIAN_POINT ( 'NONE',  ( 0.4529039210267923887, -1.253808424768705354, 0.8185038725021189787 ) ) ;
#20419=CARTESIAN_POINT ( 'NONE',  ( -0.002083146443013342720, -0.8967360763018593639, 0.1136267619940960899 ) ) ;
#20420=CARTESIAN_POINT ( 'NONE',  ( 0.4793721953524077151, -1.080656662118478328, 0.6419491832934718367 ) ) ;
#20422=CARTESIAN_POINT ( 'NONE',  ( 0.1983812210006687116, -0.5262237738225362671, 0.3723155052761787376 ) ) ;
#20424=CARTESIAN_POINT ( 'NONE',  ( 0.3110598971219385445, -1.761560204844608624, 0.5688280639540626016 ) ) ;
#20427=CARTESIAN_POINT ( 'NONE',  ( 0.05790745537833989764, -0.8938553282252756915, 0.7578938048666139515 ) ) ;
#20431=ORIENTED_EDGE ( 'NONE', *, *, #4694, .T. ) ;
#20432=CARTESIAN_POINT ( 'NONE',  ( 0.3204139389452045905, -1.755336229099436318, 0.4849083929475462296 ) ) ;
#20433=CARTESIAN_POINT ( 'NONE',  ( 0.1895831464430141056, -0.5047047246472137205, 0.1457185332388698518 ) ) ;
#20438=EDGE_LOOP ( 'NONE', ( #32972, #3130, #32122, #22897 ) ) ;
#20447=CARTESIAN_POINT ( 'NONE',  ( 0.1045684668339736112, -0.6803636310989321645, 0.3644625957350271506 ) ) ;
#20448=CARTESIAN_POINT ( 'NONE',  ( 0.2160733736694307461, -1.306826138754803912, 1.030613714223332256 ) ) ;
#20449=CARTESIAN_POINT ( 'NONE',  ( 0.4974923246832697599, -1.542513320629801843, 0.5739867662333766329 ) ) ;
#20450=CARTESIAN_POINT ( 'NONE',  ( 0.2465969332363348310, -1.554578480253843153, 0.8932696627654338473 ) ) ;
#20451=DIRECTION ( 'NONE',  ( -0.9998941247116546194, 0.01455087607601020239, -0.0001066420868422379362 ) ) ;
#20452=CARTESIAN_POINT ( 'NONE',  ( 0.07874391045642013809, -1.016202677645668073, 0.5597170535595098473 ) ) ;
#20457=CARTESIAN_POINT ( 'NONE',  ( 0.1155307545216270604, -0.4504370356409115317, 0.1913358126256027025 ) ) ;
#20464=CARTESIAN_POINT ( 'NONE',  ( 0.1042976598065218086, -1.410862685333503563, 0.5472972531283946118 ) ) ;
#20465=CARTESIAN_POINT ( 'NONE',  ( 0.6053747664524671279, -1.274130884506152084, 0.6672623879134867986 ) ) ;
#20467=DIRECTION ( 'NONE',  ( 0.8917998487739612345, 0.000000000000000000, 0.4524301379514188426 ) ) ;
#20472=CARTESIAN_POINT ( 'NONE',  ( 0.4351562478787889821, -1.231973398409348830, 0.5773826741853494982 ) ) ;
#20477=CARTESIAN_POINT ( 'NONE',  ( 0.4309721705498754107, -1.026644649581611279, 0.7159381971572771342 ) ) ;
#20481=CARTESIAN_POINT ( 'NONE',  ( 0.04328149986045663061, -0.8653222245068001861, 0.4300052425544355073 ) ) ;
#20482=ORIENTED_EDGE ( 'NONE', *, *, #38809, .F. ) ;
#20489=CARTESIAN_POINT ( 'NONE',  ( 0.4623201946560837050, -1.229771743025807051, 0.6528049022507957933 ) ) ;
#20493=EDGE_CURVE ( 'NONE', #25362, #755, #29164, .T. ) ;
#20494=CARTESIAN_POINT ( 'NONE',  ( 0.1875000000000000833, -0.9151275355372969766, 0.1556228124470683261 ) ) ;
#20495=ORIENTED_EDGE ( 'NONE', *, *, #23573, .T. ) ;
#20502=CARTESIAN_POINT ( 'NONE',  ( 0.4157541982092135546, -1.583937682242001044, 0.6612602235990290289 ) ) ;
#20503=CARTESIAN_POINT ( 'NONE',  ( 0.06924492911542678986, -0.5400501729053300837, 0.1493934372158857438 ) ) ;
#20509=CARTESIAN_POINT ( 'NONE',  ( 0.5059976415411798767, -1.396705590786084361, 0.7971529581759053684 ) ) ;
#20511=CARTESIAN_POINT ( 'NONE',  ( 0.3259879919981947261, -1.767950897709274605, 0.5312986935551964329 ) ) ;
#20516=CARTESIAN_POINT ( 'NONE',  ( 0.2201243784102229206, -1.228421504212272142, 0.5037550799415064784 ) ) ;
#20519=CARTESIAN_POINT ( 'NONE',  ( 0.4361655066743588827, -1.002659119010890665, 0.8380844301937150354 ) ) ;
#20525=CARTESIAN_POINT ( 'NONE',  ( 0.6475726312330142287, -1.570798523461287122, 0.6204058447896725337 ) ) ;
#20527=CARTESIAN_POINT ( 'NONE',  ( 0.09884054835556708996, -1.311923263315395882, 0.4413102268934767647 ) ) ;
#20530=CARTESIAN_POINT ( 'NONE',  ( 0.2556072607908594918, -1.486118078215695082, 1.019147448260280475 ) ) ;
#20533=CARTESIAN_POINT ( 'NONE',  ( 0.1301343169317701887, -1.291588712062315070, 0.5482363898924115242 ) ) ;
#20534=CARTESIAN_POINT ( 'NONE',  ( 0.3047917819195049005, -1.756872408949714082, 0.5682440848926118004 ) ) ;
#20536=ORIENTED_EDGE ( 'NONE', *, *, #36363, .T. ) ;
#20537=B_SPLINE_SURFACE_WITH_KNOTS ( 'NONE', 3, 3, ( 
 ( #37720, #34826, #28458, #6634 ),
 ( #27656, #9544, #28074, #6248 ),
 ( #334, #22122, #2973, #25399 ),
 ( #37931, #15311, #34639, #6436 ),
 ( #15708, #37312, #9122, #31157 ),
 ( #2763, #28255, #12839, #3167 ),
 ( #18818, #30741, #118, #21508 ) ),
 .UNSPECIFIED., .F., .F., .F.,
 ( 4, 3, 4 ),
 ( 4, 4 ),
 ( -0.3148221902048737308, 1.762024255024811303, 3.838870700254496171 ),
 ( -2.028463316011129169, -1.118706456288100393 ),
 .UNSPECIFIED. ) ;
#20542=ORIENTED_EDGE ( 'NONE', *, *, #16933, .F. ) ;
#20546=CARTESIAN_POINT ( 'NONE',  ( 0.4650199496164343360, -1.240973784595583052, 0.7347874889090585393 ) ) ;
#20549=CARTESIAN_POINT ( 'NONE',  ( 0.5132401252193277141, -1.118795806750195077, 0.5530176081283582068 ) ) ;
#20552=ORIENTED_EDGE ( 'NONE', *, *, #26768, .T. ) ;
#20555=CARTESIAN_POINT ( 'NONE',  ( 0.3269969022841393569, -1.639178607059557757, 0.5737397447481697998 ) ) ;
#20556=CARTESIAN_POINT ( 'NONE',  ( 0.6699226625680384517, -1.527762541135565311, 0.4380289821314772292 ) ) ;
#20557=CARTESIAN_POINT ( 'NONE',  ( 0.1766991223480313400, -0.5033111013864854932, 0.007072260541898520332 ) ) ;
#20558=CARTESIAN_POINT ( 'NONE',  ( 0.4970758107849645446, -1.079867600816170059, 0.3667417262808778666 ) ) ;
#20563=B_SPLINE_CURVE_WITH_KNOTS ( 'NONE', 3,
 ( #17119, #5355, #8873, #2701, #15050, #6185 ),
 .UNSPECIFIED., .F., .F.,
 ( 4, 2, 4 ),
 ( -1.278175275817475656E-05, 0.001487059793246534858, 0.002986901339251244424 ),
 .UNSPECIFIED. ) ;
#20568=CARTESIAN_POINT ( 'NONE',  ( 0.3294235031038280637, -1.286857108956994233, 0.6092337535398641979 ) ) ;
#20573=CARTESIAN_POINT ( 'NONE',  ( 0.3533729702181945265, -1.079803932887578588, 0.6392005906009133875 ) ) ;
#20575=EDGE_CURVE ( 'NONE', #7215, #17240, #26555, .T. ) ;
#20580=CARTESIAN_POINT ( 'NONE',  ( 0.3511079287476752686, -1.164805985122750132, 0.4335040596137048619 ) ) ;
#20583=CARTESIAN_POINT ( 'NONE',  ( 0.0004301618663383071674, -0.4396629486604707315, 0.1172979280922971101 ) ) ;
#20592=CARTESIAN_POINT ( 'NONE',  ( 0.1727619635060002046, -0.5231396776924384096, 0.1880568578134374502 ) ) ;
#20596=CARTESIAN_POINT ( 'NONE',  ( 0.1344311301205933229, -0.5616928836434232908, 0.2071304835220897644 ) ) ;
#20598=CARTESIAN_POINT ( 'NONE',  ( -0.0005234781679937302191, -0.7395155989349303516, -0.005349842773564665935 ) ) ;
#20603=CARTESIAN_POINT ( 'NONE',  ( 0.3461980321613498668, -1.167639817428515858, 0.4367330521527788556 ) ) ;
#20605=CARTESIAN_POINT ( 'NONE',  ( -0.01173968894115999702, -0.5704551753217745880, 0.3127573418170750408 ) ) ;
#20607=CARTESIAN_POINT ( 'NONE',  ( 0.1861578656809604604, -1.253385901324051144, 0.5940953843551290969 ) ) ;
#20608=CARTESIAN_POINT ( 'NONE',  ( 0.5965761245944036784, -1.493465029535157029, 0.5182417262812423209 ) ) ;
#20613=CARTESIAN_POINT ( 'NONE',  ( 0.01131643751578586751, -0.9461934511605994969, 0.1286063635815848094 ) ) ;
#20614=CARTESIAN_POINT ( 'NONE',  ( 0.1105467269751546355, -1.363254696163590518, 0.6837916529716010494 ) ) ;
#20615=CARTESIAN_POINT ( 'NONE',  ( 0.09483622992911115712, -0.6024812608924786650, 0.2828265107361390696 ) ) ;
#20616=CARTESIAN_POINT ( 'NONE',  ( 0.5524544392347628952, -1.511033082563104424, 0.5634634827593720807 ) ) ;
#20618=CARTESIAN_POINT ( 'NONE',  ( 0.4778170654558047126, -1.668016138613298560, 0.5682417262808788783 ) ) ;
#20622=CARTESIAN_POINT ( 'NONE',  ( 0.3981089169560373398, -1.724261708826889228, 0.4259583991113702339 ) ) ;
#20629=CARTESIAN_POINT ( 'NONE',  ( -0.0004024309093390212992, -0.9356036818533377541, 0.1173018208859672590 ) ) ;
#20630=CARTESIAN_POINT ( 'NONE',  ( 0.4353877174700542807, -1.231365710109779910, 0.5832408271660066701 ) ) ;
#20632=CARTESIAN_POINT ( 'NONE',  ( 0.06257380981966247091, -1.147456929947968884, 0.7547943717889301629 ) ) ;
#20634=CARTESIAN_POINT ( 'NONE',  ( 0.3711835952353229051, -0.9982156264046870842, 0.6339317236198600547 ) ) ;
#20636=CARTESIAN_POINT ( 'NONE',  ( 0.2506904587504640847, -0.6594178163634784040, 0.5852584525479398447 ) ) ;
#20638=DIRECTION ( 'NONE',  ( 0.4999551463232372317, -0.8660512985181135770, 0.000000000000000000 ) ) ;
#20642=CARTESIAN_POINT ( 'NONE',  ( 0.08275655485679608847, -0.9821269456125771846, 0.8324652710739945949 ) ) ;
#20645=CARTESIAN_POINT ( 'NONE',  ( 0.3008812400416732702, -1.193811035676025645, 0.5682417262808779901 ) ) ;
#20648=CARTESIAN_POINT ( 'NONE',  ( 0.6053747664524671279, -1.274130884506152084, 0.6672623879134867986 ) ) ;
#20653=VERTEX_POINT ( 'NONE', #1245 ) ;
#20663=CARTESIAN_POINT ( 'NONE',  ( 0.2067711592739439608, -0.8738170338164513717, 0.6440652579052440485 ) ) ;
#20665=CARTESIAN_POINT ( 'NONE',  ( 0.2950888954987143098, -1.594460040844208226, 0.9601565580101251163 ) ) ;
#20666=CARTESIAN_POINT ( 'NONE',  ( 0.1013562098727056604, -0.5836111280376300448, 0.2907278789027847310 ) ) ;
#20668=CARTESIAN_POINT ( 'NONE',  ( 0.2698039524218523999, -1.685703698922064842, 0.6459807199062099770 ) ) ;
#20670=CARTESIAN_POINT ( 'NONE',  ( 0.05563666494323122463, -0.9593727281709375498, 0.3928659522660303272 ) ) ;
#20674=CARTESIAN_POINT ( 'NONE',  ( 0.1948345289757165422, -0.5719942820726408028, 0.2877997954568007333 ) ) ;
#20678=CARTESIAN_POINT ( 'NONE',  ( 0.07196704047461272014, -1.314327500870678733, 0.4956894008401456220 ) ) ;
#20682=CARTESIAN_POINT ( 'NONE',  ( 0.3136710858027207949, -0.8676775186001693951, 0.6334163436129683911 ) ) ;
#20690=CARTESIAN_POINT ( 'NONE',  ( 0.4113447267721775380, -1.199437961476878867, 0.6795061555269068521 ) ) ;
#20695=CARTESIAN_POINT ( 'NONE',  ( 0.2819449068958458371, -0.8989038099100304935, 0.5575401372502252206 ) ) ;
#20698=CARTESIAN_POINT ( 'NONE',  ( 0.1710813352435040513, -1.228829274190828880, 0.7416658143285672633 ) ) ;
#20705=CARTESIAN_POINT ( 'NONE',  ( 0.4384245533723877819, -1.193668192789114402, 0.6617654306343142556 ) ) ;
#20709=VERTEX_POINT ( 'NONE', #26730 ) ;
#20715=CARTESIAN_POINT ( 'NONE',  ( 0.09248278889685218607, -0.7035006267299489524, 0.5252844283285661442 ) ) ;
#20716=CARTESIAN_POINT ( 'NONE',  ( 0.7071069014570956490, -1.521634513519168452, 0.5617257377400114438 ) ) ;
#20721=CARTESIAN_POINT ( 'NONE',  ( 0.5602799925893692246, -1.505597493397644149, 0.5182417262812344383 ) ) ;
#20722=CARTESIAN_POINT ( 'NONE',  ( 0.5734050883652083153, -1.499117349616238881, 0.5634239076586705641 ) ) ;
#20723=EDGE_LOOP ( 'NONE', ( #24874, #2525, #12583, #26119, #9176 ) ) ;
#20725=CARTESIAN_POINT ( 'NONE',  ( 0.3221170355888270387, -1.758120817819334158, 0.5423541406307321733 ) ) ;
#20729=CARTESIAN_POINT ( 'NONE',  ( 0.2219243583429411082, -1.238942616970301280, 0.4663869545833551622 ) ) ;
#20733=CARTESIAN_POINT ( 'NONE',  ( 0.7224934542336318710, -1.479659627397842403, 0.5766931279523788145 ) ) ;
#20745=CARTESIAN_POINT ( 'NONE',  ( 0.6693573925625662113, -1.453639881720312443, 0.4440174721139349967 ) ) ;
#20749=CARTESIAN_POINT ( 'NONE',  ( 0.1180550382625277506, -1.031362315377588157, 0.9291368297579983837 ) ) ;
#20751=CARTESIAN_POINT ( 'NONE',  ( 0.1825913591765910837, -1.261380122499173639, 0.5231355524944251156 ) ) ;
#20753=VERTEX_POINT ( 'NONE', #15165 ) ;
#20756=CARTESIAN_POINT ( 'NONE',  ( 0.1438070510857625550, -1.283988175806205723, 0.3667417262808778111 ) ) ;
#20759=CARTESIAN_POINT ( 'NONE',  ( 0.3480912466186250054, -1.075785438362978574, 0.7514184427825739698 ) ) ;
#20762=CARTESIAN_POINT ( 'NONE',  ( 0.5240142186908230970, -1.141661684775556296, 0.6661746706671649587 ) ) ;
#20766=CARTESIAN_POINT ( 'NONE',  ( 0.1571208352139699116, -1.056369343299222052, 0.8465988816176888143 ) ) ;
#20767=CARTESIAN_POINT ( 'NONE',  ( 0.7052075302012132951, -1.496959223845125697, 0.5106402777884315736 ) ) ;
#20768=CARTESIAN_POINT ( 'NONE',  ( 0.1874708175093220963, -0.5603066453311646988, 0.03565836971681755896 ) ) ;
#20775=CARTESIAN_POINT ( 'NONE',  ( 0.7053410326410682885, -1.513865973459305625, 0.5669051209305092653 ) ) ;
#20777=CARTESIAN_POINT ( 'NONE',  ( 0.3127911584666093203, -1.259356820209954320, 0.6734448273910310645 ) ) ;
#20780=B_SPLINE_CURVE_WITH_KNOTS ( 'NONE', 3,
 ( #4681, #36586, #4295, #16862, #35770, #29404 ),
 .UNSPECIFIED., .F., .F.,
 ( 4, 2, 4 ),
 ( 0.3856337156884760975, 0.6928168578442379655, 1.000000000000000000 ),
 .UNSPECIFIED. ) ;
#20781=DIRECTION ( 'NONE',  ( 0.000000000000000000, 0.000000000000000000, -1.000000000000000000 ) ) ;
#20783=CARTESIAN_POINT ( 'NONE',  ( 0.3590089656256109651, -1.084402299286110205, 0.6388604778428618181 ) ) ;
#20790=B_SPLINE_CURVE_WITH_KNOTS ( 'NONE', 3,
 ( #22967, #28526, #19481, #185, #22367, #25239, #35102, #19666, #15979, #7292, #25647, #25861, #37986, #32203 ),
 .UNSPECIFIED., .F., .F.,
 ( 4, 2, 2, 2, 2, 2, 4 ),
 ( 0.000000000000000000, 0.0003496075178145187368, 0.0006992150356290374735, 0.001398430071258081019, 0.002097645106887124564, 0.002447252624701651974, 0.002796860142516178951 ),
 .UNSPECIFIED. ) ;
#20794=CARTESIAN_POINT ( 'NONE',  ( 0.4610664102433212341, -1.239956099693821923, 0.6057417262809809966 ) ) ;
#20795=CARTESIAN_POINT ( 'NONE',  ( 0.7079468961844166408, -1.501371341494817990, 0.5260067408216857476 ) ) ;
#20796=CARTESIAN_POINT ( 'NONE',  ( 0.01205697956425911578, -0.4614203675330614818, 0.01888062949785454178 ) ) ;
#20798=CARTESIAN_POINT ( 'NONE',  ( 0.004450193950484558972, -0.5028013914547208030, 0.3755358887046206795 ) ) ;
#20804=CARTESIAN_POINT ( 'NONE',  ( 0.1869757914927797082, -0.5054508214312307679, 0.1434178755068601097 ) ) ;
#20805=ORIENTED_EDGE ( 'NONE', *, *, #37409, .F. ) ;
#20806=LINE ( 'NONE', #12470, #22664 ) ;
#20810=CARTESIAN_POINT ( 'NONE',  ( 0.0004931007904724790366, -0.6328789585674243767, -0.01332374601334393796 ) ) ;
#20813=CARTESIAN_POINT ( 'NONE',  ( 0.1153471662232078698, -0.4465907064269051263, 0.1457432652200511269 ) ) ;
#20814=ORIENTED_EDGE ( 'NONE', *, *, #26110, .F. ) ;
#20815=CARTESIAN_POINT ( 'NONE',  ( -0.01401648950443899755, -0.5294816969626192638, 0.1867042317857136313 ) ) ;
#20817=CARTESIAN_POINT ( 'NONE',  ( 0.1397034525758832912, -1.246271773685439843, 0.6054699798243167175 ) ) ;
#20823=CARTESIAN_POINT ( 'NONE',  ( 0.01149267591286579245, -0.8822181097163754870, -0.02549007114653972436 ) ) ;
#20824=CARTESIAN_POINT ( 'NONE',  ( 0.02668311692182204556, -0.9302189178724024066, 0.5981466358412875772 ) ) ;
#20825=CARTESIAN_POINT ( 'NONE',  ( 0.1577241720307761830, -0.7737101317851643456, 0.5597104839991265957 ) ) ;
#20826=CARTESIAN_POINT ( 'NONE',  ( 0.1855202466758043289, -0.8222115594753283130, 0.1007574222658992741 ) ) ;
#20828=CARTESIAN_POINT ( 'NONE',  ( 0.06022125200248988619, -1.332505749032950604, 0.5527776638144757948 ) ) ;
#20835=CARTESIAN_POINT ( 'NONE',  ( 0.3985140155258163341, -1.105590023491421769, 0.6028892103598463281 ) ) ;
#20841=CARTESIAN_POINT ( 'NONE',  ( 0.2565019309081923438, -1.535068652515254151, 0.9594965307338887417 ) ) ;
#20842=CARTESIAN_POINT ( 'NONE',  ( 0.4929465528686918230, -1.082715557938388029, 0.5668025781570900090 ) ) ;
#20843=CARTESIAN_POINT ( 'NONE',  ( -0.002208084152283221538, -0.8485876746239671142, 0.2367784268410296489 ) ) ;
#20845=CARTESIAN_POINT ( 'NONE',  ( 0.1876258513389257310, -0.4649338269308297966, 0.1998821562507554217 ) ) ;
#20847=CARTESIAN_POINT ( 'NONE',  ( 0.5264113014007820723, -1.640729993778254014, 0.5682417262808777680 ) ) ;
#20849=ORIENTED_EDGE ( 'NONE', *, *, #14451, .T. ) ;
#20851=CARTESIAN_POINT ( 'NONE',  ( 0.02401934354094946433, -0.7133339170399575213, 0.5802934023308400358 ) ) ;
#20852=EDGE_CURVE ( 'NONE', #26173, #7024, #28137, .T. ) ;
#20854=CARTESIAN_POINT ( 'NONE',  ( 0.5873107854097197045, -1.491061893667417371, 0.5610701424334307852 ) ) ;
#20859=EDGE_CURVE ( 'NONE', #39668, #9404, #999, .T. ) ;
#20861=CARTESIAN_POINT ( 'NONE',  ( 0.1989132775362471572, -0.6135140644431382739, 0.3133236772439795259 ) ) ;
#20867=CARTESIAN_POINT ( 'NONE',  ( 0.1826134026666640653, -1.261648033191452134, 0.4282186462236581836 ) ) ;
#20871=CARTESIAN_POINT ( 'NONE',  ( 0.2066366444374464761, -1.235973243786347542, 0.5699631943058273142 ) ) ;
#20872=CARTESIAN_POINT ( 'NONE',  ( 0.09426521933953035948, -0.7368835468627613627, 0.2937654492271515871 ) ) ;
#20873=CARTESIAN_POINT ( 'NONE',  ( 0.2183274780194145726, -1.352241882189698652, 1.036399751412596437 ) ) ;
#20874=CARTESIAN_POINT ( 'NONE',  ( 0.2927782761540232426, -1.083998813092891700, 0.8148780714178450735 ) ) ;
#20875=CARTESIAN_POINT ( 'NONE',  ( 0.3410005206520395626, -1.758673451842764246, 0.4621779736240644310 ) ) ;
#20877=CARTESIAN_POINT ( 'NONE',  ( 0.09805242145838190260, -1.310054031134215036, 0.5682417262808774350 ) ) ;
#20881=CARTESIAN_POINT ( 'NONE',  ( 0.3158993119317616283, -0.7784124716426810142, 0.7037675960530900277 ) ) ;
#20886=CARTESIAN_POINT ( 'NONE',  ( 0.3931095016817222065, -1.150926721643386497, 0.4182417262808778569 ) ) ;
#20888=CARTESIAN_POINT ( 'NONE',  ( 0.3149931741451680312, -1.174162082499039084, 0.5426465745000428331 ) ) ;
#20889=CARTESIAN_POINT ( 'NONE',  ( 0.4727414870697744798, -1.078201156678013639, 0.7478468640933467748 ) ) ;
#20903=CARTESIAN_POINT ( 'NONE',  ( 0.2171196146447029740, -1.332674774804728290, 0.6488356689647567510 ) ) ;
#20904=ORIENTED_EDGE ( 'NONE', *, *, #24114, .T. ) ;
#20905=CARTESIAN_POINT ( 'NONE',  ( 0.2572301429339545198, -1.333641270216179286, 0.5682417262808723279 ) ) ;
#20909=CARTESIAN_POINT ( 'NONE',  ( 0.4690544269859369675, -1.240261309394489642, 0.5870667310821602314 ) ) ;
#20916=CARTESIAN_POINT ( 'NONE',  ( 0.3948505749141573151, -1.157343825514034918, 0.4182417262808776903 ) ) ;
#20918=( BOUNDED_SURFACE ( )  B_SPLINE_SURFACE ( 3, 2, ( 
 ( #13375, #38668, #19956 ),
 ( #4314, #16272, #1077 ),
 ( #16667, #31903, #7178 ),
 ( #32488, #38476, #28812 ),
 ( #7380, #16878, #7598 ),
 ( #13162, #3905, #32283 ),
 ( #38062, #20172, #32698 ),
 ( #16071, #486, #9874 ),
 ( #4102, #10486, #1266 ),
 ( #25949, #26333, #10307 ) ),
 .UNSPECIFIED., .F., .F., .T. ) 
 B_SPLINE_SURFACE_WITH_KNOTS ( ( 4, 2, 2, 2, 4 ),
 ( 3, 3 ),
 ( 0.001615335599980216629, 0.002812013140722832618, 0.003111182525908486561, 0.003410351911094140938, 0.004008690681465448824 ),
 ( 0.000000000000000000, 1.000000000000000000 ),
 .UNSPECIFIED. ) 
 GEOMETRIC_REPRESENTATION_ITEM ( )  RATIONAL_B_SPLINE_SURFACE ( (
 ( 1.000000000000000000, 0.8170441014559525206, 1.000000000000000000),
 ( 1.000000000000000000, 0.8398996753289208472, 1.000000000000000000),
 ( 1.000000000000000000, 0.8580894509173602192, 1.000000000000000000),
 ( 1.000000000000000000, 0.8737185627151831113, 1.000000000000000000),
 ( 1.000000000000000000, 0.8764984143296298269, 1.000000000000000000),
 ( 1.000000000000000000, 0.8812237365503433617, 1.000000000000000000),
 ( 1.000000000000000000, 0.8832013687233702948, 1.000000000000000000),
 ( 1.000000000000000000, 0.8880237859985680160, 1.000000000000000000),
 ( 1.000000000000000000, 0.8897420245345738499, 1.000000000000000000),
 ( 1.000000000000000000, 0.8897565210025812910, 1.000000000000000000) ) ) 
 REPRESENTATION_ITEM ( '' )  SURFACE ( )  );
#20919=CARTESIAN_POINT ( 'NONE',  ( 0.1917248655069789809, -0.6407273034312881421, 0.1015045423513593059 ) ) ;
#20920=CARTESIAN_POINT ( 'NONE',  ( 0.4438802985545475810, -1.570449409196589041, 0.6444032079186845507 ) ) ;
#20921=CARTESIAN_POINT ( 'NONE',  ( 0.06831379255928186900, -0.5749909519026226157, 0.04969217839999666431 ) ) ;
#20923=CARTESIAN_POINT ( 'NONE',  ( 0.4838398748940612726, -1.167039897535582682, 0.4225238715116874655 ) ) ;
#20926=CARTESIAN_POINT ( 'NONE',  ( 0.1240259653398129713, -0.5782917783936175615, 0.2638625179588850456 ) ) ;
#20927=FACE_OUTER_BOUND ( 'NONE', #1836, .T. ) ;
#20929=CARTESIAN_POINT ( 'NONE',  ( 0.6350751079694297863, -1.569022301146391962, 0.4218919778450955782 ) ) ;
#20930=CARTESIAN_POINT ( 'NONE',  ( 0.1372793408763309797, -1.276325292378077236, 0.4310377198975363089 ) ) ;
#20931=CARTESIAN_POINT ( 'NONE',  ( 0.003157924493107725546, -0.5245024639201223415, 0.1457192838223093367 ) ) ;
#20932=CARTESIAN_POINT ( 'NONE',  ( 0.08861584565946885317, -0.6039893155899630495, 0.02242969405406716743 ) ) ;
#20933=CARTESIAN_POINT ( 'NONE',  ( 0.1878356035704684124, -0.4698003021450733452, 0.2206963598966235063 ) ) ;
#20934=CARTESIAN_POINT ( 'NONE',  ( 0.08222542156927244161, -1.327483614382554800, 0.4683366274854123823 ) ) ;
#20935=CARTESIAN_POINT ( 'NONE',  ( 0.01128729522791821309, -0.9461985897322298111, 0.1806064185212560014 ) ) ;
#20937=DIRECTION ( 'NONE',  ( 0.5113178712883763577, 0.8593916653663353777, -8.996534555025795202E-14 ) ) ;
#20938=CARTESIAN_POINT ( 'NONE',  ( 0.5675929565786681508, -1.617839747320475086, 0.5725551038798919468 ) ) ;
#20940=CARTESIAN_POINT ( 'NONE',  ( 0.5991966895601555931, -1.596821569857824752, 0.4287152735839648843 ) ) ;
#20941=CARTESIAN_POINT ( 'NONE',  ( 0.05109603825399443300, -0.7331182637548316894, 0.7465514741729609716 ) ) ;
#20942=DIRECTION ( 'NONE',  ( -0.4999551463232372317, 0.8660512985181135770, -0.000000000000000000 ) ) ;
#20944=CARTESIAN_POINT ( 'NONE',  ( 0.4332356878749745177, -1.705790429466398583, 0.6052722225822104729 ) ) ;
#20945=CONICAL_SURFACE ( 'NONE', #28814, 0.1762268159172233339, 0.7853981633974500554 ) ;
#20946=VERTEX_POINT ( 'NONE', #32210 ) ;
#20948=CARTESIAN_POINT ( 'NONE',  ( 0.3918182118607618225, -1.107073211027153725, 0.6042946153017961786 ) ) ;
#20951=CARTESIAN_POINT ( 'NONE',  ( 0.4842931683238080320, -1.270018078534612904, 0.7216184661905129527 ) ) ;
#20954=CARTESIAN_POINT ( 'NONE',  ( 0.5067209442253272078, -1.108407892246341175, 0.6081930138323172752 ) ) ;
#20962=CARTESIAN_POINT ( 'NONE',  ( 0.3558919305822700330, -1.622312069902127840, 0.5706928582630780289 ) ) ;
#20963=CARTESIAN_POINT ( 'NONE',  ( 0.7057303773600904773, -1.512934555508332668, 0.5564953324639242416 ) ) ;
#20964=CARTESIAN_POINT ( 'NONE',  ( 0.1773295416277048953, -0.4575625385501337350, 0.1501579634321036083 ) ) ;
#20970=CARTESIAN_POINT ( 'NONE',  ( 0.1648393044702914367, -1.273995379727181021, 0.4182417262808778569 ) ) ;
#20972=CARTESIAN_POINT ( 'NONE',  ( 0.2054732354593832022, -1.060600144931224342, 0.7368794145240139537 ) ) ;
#20974=DIRECTION ( 'NONE',  ( -0.4999551463232371762, 0.8660512985181134660, -0.000000000000000000 ) ) ;
#20975=CARTESIAN_POINT ( 'NONE',  ( 0.1597138714205091625, -0.9558088324725364515, 0.4497724057842478751 ) ) ;
#20977=CARTESIAN_POINT ( 'NONE',  ( 0.3534995746758727853, -1.163432996101295025, 0.4351399550592107701 ) ) ;
#20979=CARTESIAN_POINT ( 'NONE',  ( 0.4012199348250638509, -1.136392022378372113, 0.4815844951853371358 ) ) ;
#20980=CARTESIAN_POINT ( 'NONE',  ( 0.03852435536883173223, -1.195394391876414719, 0.6677169776219902264 ) ) ;
#20983=CARTESIAN_POINT ( 'NONE',  ( 0.4437585245673965617, -1.132310435069097565, 0.4450710391304853464 ) ) ;
#20985=CARTESIAN_POINT ( 'NONE',  ( 0.7087227687136311571, -1.504650563340975022, 0.5335643800121802061 ) ) ;
#20987=CARTESIAN_POINT ( 'NONE',  ( 0.0001866439489153905271, -0.5339630687492940009, -0.05105682221463851006 ) ) ;
#20989=CARTESIAN_POINT ( 'NONE',  ( 0.03892492223551621139, -0.6940895124628043700, 0.6890254284164284426 ) ) ;
#20993=CARTESIAN_POINT ( 'NONE',  ( 0.2948640431575899057, -1.208698857598578869, 0.4182417262808778013 ) ) ;
#20997=CARTESIAN_POINT ( 'NONE',  ( 0.001011648560469348857, -0.5841484436987858242, 0.01311714344844475653 ) ) ;
#20998=ORIENTED_EDGE ( 'NONE', *, *, #35891, .F. ) ;
#21004=CARTESIAN_POINT ( 'NONE',  ( 0.006823764970969815359, -0.6154038265784372852, 0.4059195148818033339 ) ) ;
#21006=CARTESIAN_POINT ( 'NONE',  ( 0.2186880164441438179, -1.240563195108393080, 0.5774983274694442947 ) ) ;
#21016=CARTESIAN_POINT ( 'NONE',  ( 0.2705165854423337013, -0.9635601006052144646, 0.7153668490100312249 ) ) ;
#21017=CARTESIAN_POINT ( 'NONE',  ( 0.1874317355884921321, -0.6912902591703241617, 0.04192882835670527081 ) ) ;
#21018=CARTESIAN_POINT ( 'NONE',  ( -0.01736481776669303659, -0.5247326629091749739, 0.1457185332388703236 ) ) ;
#21023=CARTESIAN_POINT ( 'NONE',  ( 0.4584370907333497058, -1.110107490588079671, 0.5683196366401116473 ) ) ;
#21028=CARTESIAN_POINT ( 'NONE',  ( 0.2142493868227219878, -1.379310565402303457, 1.003739045973664368 ) ) ;
#21029=CARTESIAN_POINT ( 'NONE',  ( 0.4003901567941702822, -1.031933045472551269, 0.6312919426632347397 ) ) ;
#21030=CARTESIAN_POINT ( 'NONE',  ( 0.03340947221881906959, -0.9865371011752580577, 0.6764581597365023624 ) ) ;
#21032=CARTESIAN_POINT ( 'NONE',  ( 0.3279357908889724005, -0.8116789304350262579, 0.7312476538325396458 ) ) ;
#21039=CARTESIAN_POINT ( 'NONE',  ( 0.07380144035736982411, -0.9240663959273383021, 0.7785025519333340638 ) ) ;
#21040=CARTESIAN_POINT ( 'NONE',  ( 0.1299497688713388832, -0.5790410954462047455, 0.2626379361186624850 ) ) ;
#21044=CARTESIAN_POINT ( 'NONE',  ( 0.2529714763052502979, -0.7233805682233873657, 0.5452257223911994855 ) ) ;
#21045=ORIENTED_EDGE ( 'NONE', *, *, #8886, .T. ) ;
#21053=AXIS2_PLACEMENT_3D ( 'NONE', #3041, #6501, #9798 ) ;
#21058=CARTESIAN_POINT ( 'NONE',  ( 0.2639495433093203558, -0.9686959132792163363, 0.6974367203216930156 ) ) ;
#21059=CARTESIAN_POINT ( 'NONE',  ( 0.2030024116509572818, -1.310890633394409033, 1.024740945452946361 ) ) ;
#21060=CARTESIAN_POINT ( 'NONE',  ( 0.1094109803698096878, -0.6218279727836852899, 0.3761239768809111483 ) ) ;
#21061=FACE_OUTER_BOUND ( 'NONE', #11453, .T. ) ;
#21062=CARTESIAN_POINT ( 'NONE',  ( 0.0009970652039437085962, -0.5853685308490127470, 0.01218434430457844379 ) ) ;
#21063=CARTESIAN_POINT ( 'NONE',  ( 0.003383243044336568025, -0.9698986547711589967, 0.4010568066359272987 ) ) ;
#21068=CARTESIAN_POINT ( 'NONE',  ( 0.2686022046095623006, -0.8300817956324447744, 0.7674347935952442468 ) ) ;
#21070=EDGE_CURVE ( 'NONE', #21929, #5559, #23408, .T. ) ;
#21072=LENGTH_MEASURE_WITH_UNIT ( LENGTH_MEASURE( 0.02539999999999999897 ), #24780 );
#21075=EDGE_CURVE ( 'NONE', #24709, #38007, #34081, .T. ) ;
#21077=CARTESIAN_POINT ( 'NONE',  ( 0.2089316498445973613, -0.7245868578893045475, 0.3779356710034222910 ) ) ;
#21093=CARTESIAN_POINT ( 'NONE',  ( 0.07311138962147617493, -0.9435636872638024641, 0.6307374715929325859 ) ) ;
#21094=ORIENTED_EDGE ( 'NONE', *, *, #36821, .T. ) ;
#21099=CARTESIAN_POINT ( 'NONE',  ( 0.4381232881540311208, -1.195278502452886915, 0.6782187811958457768 ) ) ;
#21102=CARTESIAN_POINT ( 'NONE',  ( 0.0003671528708184450067, -0.4356477474403453454, 0.1457185332388686860 ) ) ;
#21109=CARTESIAN_POINT ( 'NONE',  ( 0.1857207782009835662, -0.9735509886838665805, 0.7778221052609431974 ) ) ;
#21111=CARTESIAN_POINT ( 'NONE',  ( 0.1925852169268471858, -0.7535752542798960230, 0.3142616005574464522 ) ) ;
#21112=CARTESIAN_POINT ( 'NONE',  ( 0.4926894108487032131, -1.176944786191506109, 0.4224236931107097637 ) ) ;
#21115=B_SPLINE_CURVE_WITH_KNOTS ( 'NONE', 3,
 ( #30146, #1975, #20905, #33427 ),
 .UNSPECIFIED., .F., .F.,
 ( 4, 4 ),
 ( 0.01696221039300578257, 0.4968750736215113428 ),
 .UNSPECIFIED. ) ;
#21119=CARTESIAN_POINT ( 'NONE',  ( 0.5735257847173089729, -1.499153090709115510, 0.5657782871807620628 ) ) ;
#21120=CARTESIAN_POINT ( 'NONE',  ( 0.4194453228269892642, -1.699896402126472195, 0.4182417262805759317 ) ) ;
#21123=CIRCLE ( 'NONE', #13211, 0.009999999999999995004 ) ;
#21124=CARTESIAN_POINT ( 'NONE',  ( 0.2094458608486971796, -1.234382894204292702, 0.5645286332426232567 ) ) ;
#21125=VECTOR ( 'NONE', #27222, 39.37007874015748143 ) ;
#21127=CARTESIAN_POINT ( 'NONE',  ( 0.2161540139445707054, -1.242273860952007203, 0.4569645709156981428 ) ) ;
#21128=CARTESIAN_POINT ( 'NONE',  ( 0.2120163453477715010, -0.5915265038663817254, 0.4276896445164236615 ) ) ;
#21129=CARTESIAN_POINT ( 'NONE',  ( 0.07958551560962270899, -1.322831287755755758, 0.4682677590956452196 ) ) ;
#21134=CARTESIAN_POINT ( 'NONE',  ( 0.6672263256166468537, -1.559577713309568292, 0.6159734170043985602 ) ) ;
#21135=CARTESIAN_POINT ( 'NONE',  ( 0.6795582604384902137, -1.448051739356461365, 0.4670391094899577489 ) ) ;
#21138=CARTESIAN_POINT ( 'NONE',  ( 0.01707166242847063184, -0.6102210326195973700, 0.5232503585198154950 ) ) ;
#21145=AXIS2_PLACEMENT_3D ( 'NONE', #3543, #28651, #6820 ) ;
#21148=CARTESIAN_POINT ( 'NONE',  ( 0.3227141990867507526, -1.181380599211185212, 0.5734485983774162410 ) ) ;
#21149=DIRECTION ( 'NONE',  ( 0.9998941247116547304, -0.01455087607601020412, 0.0001066420868422379633 ) ) ;
#21152=CARTESIAN_POINT ( 'NONE',  ( 0.4773756200668168859, -1.258275737217217527, 0.7110155661270410876 ) ) ;
#21154=ORIENTED_EDGE ( 'NONE', *, *, #2658, .T. ) ;
#21155=CARTESIAN_POINT ( 'NONE',  ( 0.4718294406633598559, -1.074170765704426822, 0.6461978756939577018 ) ) ;
#21160=CARTESIAN_POINT ( 'NONE',  ( 0.3587861683550780389, -1.611959099284976160, 0.6979777834575303652 ) ) ;
#21161=CARTESIAN_POINT ( 'NONE',  ( 0.06536555028605087192, -0.7987193142509114718, 0.04805781248889415963 ) ) ;
#21166=CARTESIAN_POINT ( 'NONE',  ( 0.4492966705992636478, -1.050346012740955626, 0.6361637604917406152 ) ) ;
#21170=CARTESIAN_POINT ( 'NONE',  ( 0.1424399877835745010, -0.9312767937703616550, 0.6301790181337186825 ) ) ;
#21175=CARTESIAN_POINT ( 'NONE',  ( 0.7476847780466161497, -1.513986987551942498, 0.3667417262808780887 ) ) ;
#21178=CARTESIAN_POINT ( 'NONE',  ( 0.6498387395261646660, -1.464631408770378673, 0.4182417262808778013 ) ) ;
#21179=DIRECTION ( 'NONE',  ( 0.4999551463232372317, -0.8660512985181135770, 0.000000000000000000 ) ) ;
#21182=CARTESIAN_POINT ( 'NONE',  ( 0.4707877201786100918, -1.135202906000321921, 0.4619518047902346214 ) ) ;
#21183=CARTESIAN_POINT ( 'NONE',  ( 0.4581693818450407463, -1.241628499769009020, 0.6057417262809811076 ) ) ;
#21184=CARTESIAN_POINT ( 'NONE',  ( 0.3121393770295847747, -1.175762900167912184, 0.5260634940794319814 ) ) ;
#21185=CARTESIAN_POINT ( 'NONE',  ( 0.01201275324683169846, -0.4797197884825873393, -0.009968709375361768654 ) ) ;
#21187=CARTESIAN_POINT ( 'NONE',  ( 0.05241514471239613199, -0.7522610373340221646, 0.7518993562137571418 ) ) ;
#21188=CARTESIAN_POINT ( 'NONE',  ( 0.3224586748600002384, -1.296590453040780799, 0.4182417262808783009 ) ) ;
#21196=CARTESIAN_POINT ( 'NONE',  ( 0.002371010564581027980, -0.5282417084461772383, 0.1487601318397159811 ) ) ;
#21204=CARTESIAN_POINT ( 'NONE',  ( 0.2705629139958489748, -1.674023155731529711, 0.6420758730732996078 ) ) ;
#21206=CARTESIAN_POINT ( 'NONE',  ( 0.1128228149019921550, -1.274631681149367646, 0.6181115705952207051 ) ) ;
#21210=CARTESIAN_POINT ( 'NONE',  ( 0.7112185359115762440, -1.490287028582105711, 0.5669016283713388393 ) ) ;
#21213=CARTESIAN_POINT ( 'NONE',  ( 0.3225054573102290600, -1.181499395378165174, 0.5729696959891698027 ) ) ;
#21214=CARTESIAN_POINT ( 'NONE',  ( 0.1852697703518005889, -0.8388889655799410816, 0.1423358669777717023 ) ) ;
#21217=CARTESIAN_POINT ( 'NONE',  ( 0.4235708306963869574, -1.181282221097477381, 0.7940044402252741662 ) ) ;
#21218=CARTESIAN_POINT ( 'NONE',  ( 0.1868970225581818301, -0.7280982606231287679, 0.03318949868953756377 ) ) ;
#21223=CARTESIAN_POINT ( 'NONE',  ( 0.4067032487861790280, -1.709706946175272080, 0.4220675772687526028 ) ) ;
#21226=CARTESIAN_POINT ( 'NONE',  ( 0.4802217237380822512, -1.662726879635128219, 0.3667417262808781442 ) ) ;
#21228=CARTESIAN_POINT ( 'NONE',  ( 0.01127691157594227882, -0.9461533502836454446, 0.1506559775778698596 ) ) ;
#21231=VECTOR ( 'NONE', #38026, 39.37007874015748143 ) ;
#21234=CARTESIAN_POINT ( 'NONE',  ( 0.2493678129588278725, -1.619726033520551667, 0.7664167198318853069 ) ) ;
#21235=CARTESIAN_POINT ( 'NONE',  ( 0.06977928302938717076, -1.183750997490756296, 0.7568106749872303141 ) ) ;
#21239=CARTESIAN_POINT ( 'NONE',  ( 0.2433107440384445208, -0.6632537007949954599, 0.5455544552538778014 ) ) ;
#21243=CARTESIAN_POINT ( 'NONE',  ( 0.6964549535019117776, -1.533417755710658081, 0.5924443473190263987 ) ) ;
#21247=( GEOMETRIC_REPRESENTATION_CONTEXT ( 3 ) GLOBAL_UNCERTAINTY_ASSIGNED_CONTEXT ( ( #19042 ) ) GLOBAL_UNIT_ASSIGNED_CONTEXT ( ( #12411, #5214, #15298 ) ) REPRESENTATION_CONTEXT ( 'NONE', 'WORKASPACE' ) );
#21251=CARTESIAN_POINT ( 'NONE',  ( 0.09341372340922594886, -1.037589379625932784, 0.8542603175731292575 ) ) ;
#21252=CARTESIAN_POINT ( 'NONE',  ( 0.1856961636715741826, -0.7498557161068394317, 0.5589214599598529842 ) ) ;
#21253=LINE ( 'NONE', #33183, #21125 ) ;
#21255=CARTESIAN_POINT ( 'NONE',  ( 0.1906247196645203257, -0.5843772811062373229, 0.1513679272151527977 ) ) ;
#21258=CARTESIAN_POINT ( 'NONE',  ( 0.2927257310821322900, -0.8050081238773644232, 0.6220914005605751029 ) ) ;
#21266=CARTESIAN_POINT ( 'NONE',  ( 0.1238647415275516556, -0.7604388772436289079, 0.4528127954481608319 ) ) ;
#21267=AXIS2_PLACEMENT_3D ( 'NONE', #33068, #4874, #27112 ) ;
#21268=CARTESIAN_POINT ( 'NONE',  ( 0.3239698234882238959, -1.727951091942375728, 0.7867494264257975933 ) ) ;
#21270=CARTESIAN_POINT ( 'NONE',  ( 0.09764433117057039202, -0.5450118788951329174, 0.1457185332388695742 ) ) ;
#21272=CARTESIAN_POINT ( 'NONE',  ( 0.002290818369124609372, -0.5198888459286679087, 0.1457185332388686583 ) ) ;
#21273=CARTESIAN_POINT ( 'NONE',  ( 0.05908521160031481728, -1.327330609165742192, 0.5935265463149500542 ) ) ;
#21274=VERTEX_POINT ( 'NONE', #29353 ) ;
#21277=CARTESIAN_POINT ( 'NONE',  ( 0.2762174934205044452, -0.8433163854438798790, 0.7765387688752221074 ) ) ;
#21283=CARTESIAN_POINT ( 'NONE',  ( 0.6624296566318823576, -1.373680494012689435, 0.6057417262805894209 ) ) ;
#21284=CARTESIAN_POINT ( 'NONE',  ( 0.2711464003948310664, -1.672220156048179751, 0.5055462609045281441 ) ) ;
#21285=CARTESIAN_POINT ( 'NONE',  ( 0.3122204723728539411, -1.175715471473605778, 0.5253545403616187714 ) ) ;
#21286=CARTESIAN_POINT ( 'NONE',  ( 0.1874999999999996669, -0.6872203660140437931, 0.1457185332388695742 ) ) ;
#21293=CARTESIAN_POINT ( 'NONE',  ( 0.4466550410545370164, -1.204244029663398496, 0.6473101387276720686 ) ) ;
#21305=CARTESIAN_POINT ( 'NONE',  ( 0.008503815048826473752, -0.8451467311994962373, 0.1457185332388719889 ) ) ;
#21315=CARTESIAN_POINT ( 'NONE',  ( 0.4682349133427387566, -1.238864133684273394, 0.6416901653891257107 ) ) ;
#21317=CARTESIAN_POINT ( 'NONE',  ( 0.1536596445529307131, -1.277574755431481579, 0.4245438548657216038 ) ) ;
#21325=CARTESIAN_POINT ( 'NONE',  ( 0.4393559444842871642, -1.556801234278946122, 0.7099263403775109005 ) ) ;
#21327=CARTESIAN_POINT ( 'NONE',  ( 0.5642073033013602634, -1.616444467847912847, 0.4682437291146816505 ) ) ;
#21328=CARTESIAN_POINT ( 'NONE',  ( 0.4497778021248119984, -1.147640960188543113, 0.4232850839822800415 ) ) ;
#21334=CARTESIAN_POINT ( 'NONE',  ( 0.1367182587715192466, -0.6335969605309247354, 0.3882801499301780646 ) ) ;
#21335=CARTESIAN_POINT ( 'NONE',  ( 0.4231979350574381904, -1.697322476885489762, 0.4297746138276614114 ) ) ;
#21336=CARTESIAN_POINT ( 'NONE',  ( 0.4517177305807006937, -1.568671020668126914, 0.6057417262804751790 ) ) ;
#21344=CARTESIAN_POINT ( 'NONE',  ( 0.5633425123490871655, -1.213831759034801561, 0.8533915188341715252 ) ) ;
#21351=CARTESIAN_POINT ( 'NONE',  ( 0.5913213363384987042, -1.604640830199632662, 0.6017661975466599422 ) ) ;
#21365=CARTESIAN_POINT ( 'NONE',  ( 0.3398061633079089705, -1.151650735656065461, 0.5895292019541952255 ) ) ;
#21370=CARTESIAN_POINT ( 'NONE',  ( 0.5004679210847464699, -1.293934441700709037, 0.6841144912013866763 ) ) ;
#21374=CARTESIAN_POINT ( 'NONE',  ( 0.3074110389119673048, -0.9534851582863556052, 0.5796648297427198226 ) ) ;
#21378=CIRCLE ( 'NONE', #3615, 0.03749999999977554621 ) ;
#21382=CARTESIAN_POINT ( 'NONE',  ( 0.03580802019661705193, -0.5461554526729558434, 0.2169286433324936203 ) ) ;
#21384=CARTESIAN_POINT ( 'NONE',  ( 0.1759602538404660133, -0.6574070655985931877, -0.08278933279227815301 ) ) ;
#21388=CARTESIAN_POINT ( 'NONE',  ( 0.5327020933798468638, -1.151343754938154218, 0.6263913407894506902 ) ) ;
#21389=CARTESIAN_POINT ( 'NONE',  ( 0.1463340742998959498, -0.7013816541812762928, 0.5029480910574282149 ) ) ;
#21390=ORIENTED_EDGE ( 'NONE', *, *, #33893, .F. ) ;
#21393=CARTESIAN_POINT ( 'NONE',  ( -1.920933771635442211, -2.937918075995054945, 0.4182417262808775238 ) ) ;
#21394=VECTOR ( 'NONE', #38744, 39.37007874015748143 ) ;
#21396=B_SPLINE_CURVE_WITH_KNOTS ( 'NONE', 3,
 ( #28372, #40513, #31659, #9652, #37619, #15626, #31868, #12528 ),
 .UNSPECIFIED., .F., .F.,
 ( 4, 2, 2, 4 ),
 ( 1.602656041417568188E-11, 0.001966995538234637009, 0.002950493299338675587, 0.003933991060442713732 ),
 .UNSPECIFIED. ) ;
#21397=DIRECTION ( 'NONE',  ( -0.9998941303973200023, 0.01455087615875037474, 0.000000000000000000 ) ) ;
#21398=CARTESIAN_POINT ( 'NONE',  ( 0.3922353094782703997, -1.714330012172307294, 0.4177417262808784115 ) ) ;
#21399=CARTESIAN_POINT ( 'NONE',  ( 0.3518999744609554448, -1.164331320867108444, 0.4249471546789464482 ) ) ;
#21401=CARTESIAN_POINT ( 'NONE',  ( 0.003421962176364201202, -0.9701471101739370662, 0.4009549150280219965 ) ) ;
#21405=B_SPLINE_CURVE_WITH_KNOTS ( 'NONE', 3,
 ( #12442, #5664, #8958, #15548, #37526, #3190, #21531, #18410, #27893, #12050 ),
 .UNSPECIFIED., .F., .F.,
 ( 4, 2, 2, 2, 4 ),
 ( 0.000000000000000000, 0.0005029730322535831428, 0.001005946064507166286, 0.001508919096760749428, 0.002011892129014332571 ),
 .UNSPECIFIED. ) ;
#21406=CARTESIAN_POINT ( 'NONE',  ( 0.4823781031358342353, -1.129173803219876149, 0.4907471721780757856 ) ) ;
#21407=CARTESIAN_POINT ( 'NONE',  ( 0.4639634386416064404, -1.238283699618621725, 0.6057417262809811076 ) ) ;
#21411=CARTESIAN_POINT ( 'NONE',  ( 3.839896904129604577E-06, -0.6023364376982222046, -0.1016634491690118630 ) ) ;
#21420=CARTESIAN_POINT ( 'NONE',  ( 0.3222810527215910215, -1.758570551863011922, 0.4849083929475443422 ) ) ;
#21429=CARTESIAN_POINT ( 'NONE',  ( 0.2665270026871217612, -1.675380026011078716, 0.5755890425476034578 ) ) ;
#21430=CARTESIAN_POINT ( 'NONE',  ( 0.1972680329291656987, -0.9306160649008226038, 0.6420804189482948177 ) ) ;
#21433=CARTESIAN_POINT ( 'NONE',  ( 0.6065454785784598624, -1.479009159021363207, 0.5747789317403434461 ) ) ;
#21439=CARTESIAN_POINT ( 'NONE',  ( 0.01142787841204725117, -0.9119713417645858300, 0.01598648563123014274 ) ) ;
#21443=CARTESIAN_POINT ( 'NONE',  ( 0.4624398381476410025, -1.269083403305113489, 0.8176449397995606549 ) ) ;
#21445=CARTESIAN_POINT ( 'NONE',  ( 0.2599034962623482659, -1.582350648323867182, 0.8549863447754705303 ) ) ;
#21446=CARTESIAN_POINT ( 'NONE',  ( 0.01240358949466654342, -0.4404738072168086216, 0.2329760197377778452 ) ) ;
#21447=CARTESIAN_POINT ( 'NONE',  ( 0.4196259286637142871, -1.711435686544057644, 0.4273953198980491863 ) ) ;
#21450=CARTESIAN_POINT ( 'NONE',  ( 0.4676789493019616883, -1.559177855287317005, 0.5735223705611400824 ) ) ;
#21451=CARTESIAN_POINT ( 'NONE',  ( -0.0003736070913198792057, -0.9292939094275918244, 0.08502934550331207875 ) ) ;
#21455=CARTESIAN_POINT ( 'NONE',  ( 0.2426062050407847281, -1.584949062848913348, 0.8214247301831154591 ) ) ;
#21456=CARTESIAN_POINT ( 'NONE',  ( 0.04678374077078594623, -1.010183413244198469, 0.6999868061010977582 ) ) ;
#21458=CARTESIAN_POINT ( 'NONE',  ( 0.4805300281521128203, -1.080349003257709439, 0.8405881438443104647 ) ) ;
#21460=CARTESIAN_POINT ( 'NONE',  ( 0.7071864311907015699, -1.521274929146462673, 0.5612556364004261944 ) ) ;
#21463=ORIENTED_EDGE ( 'NONE', *, *, #25749, .F. ) ;
#21464=CARTESIAN_POINT ( 'NONE',  ( -0.002282498291095993656, -0.8555267327002353817, 0.1457185332388701293 ) ) ;
#21465=CARTESIAN_POINT ( 'NONE',  ( 0.2722157990050696474, -1.638612347704280658, 0.7745732599775748684 ) ) ;
#21466=CARTESIAN_POINT ( 'NONE',  ( 0.1282641000242639162, -0.5556219276664670081, 0.1881736293549454153 ) ) ;
#21467=DIRECTION ( 'NONE',  ( -0.4999551463232372317, 0.8660512985181134660, -0.000000000000000000 ) ) ;
#21469=CARTESIAN_POINT ( 'NONE',  ( 0.5847200959167868639, -1.241056950120674518, 0.7055318339491533086 ) ) ;
#21478=TOROIDAL_SURFACE ( 'NONE', #26091, 0.04749999999977554815, 0.01000000000000000021 ) ;
#21481=CARTESIAN_POINT ( 'NONE',  ( 0.09608046277552639847, -0.7200274365782738384, 0.3052469828618230019 ) ) ;
#21484=CARTESIAN_POINT ( 'NONE',  ( 0.5236732281772086273, -1.517283060796150718, 0.6742510201405766956 ) ) ;
#21485=CARTESIAN_POINT ( 'NONE',  ( 0.3251375141011914049, -1.768545959953308877, 0.5240463964343101688 ) ) ;
#21486=CARTESIAN_POINT ( 'NONE',  ( -0.002282498291095993656, -0.8555267327002353817, 0.1457185332388701293 ) ) ;
#21487=CARTESIAN_POINT ( 'NONE',  ( 0.0003805203522013556679, -0.9506305917533103278, 0.2426406003428543956 ) ) ;
#21490=ADVANCED_FACE ( 'NONE', ( #3374 ), #36871, .T. ) ;
#21492=CARTESIAN_POINT ( 'NONE',  ( 0.5838512187896826022, -1.247881422114380801, 0.8761440252600439793 ) ) ;
#21499=CARTESIAN_POINT ( 'NONE',  ( 0.2607589496226037640, -1.678824709164980833, 0.5052740673131734805 ) ) ;
#21500=CARTESIAN_POINT ( 'NONE',  ( 0.3554163599750466140, -1.162345695606875173, 0.4422132562362467434 ) ) ;
#21501=CARTESIAN_POINT ( 'NONE',  ( 0.4873263706924592098, -1.095012774062378513, 0.6880473194844076712 ) ) ;
#21503=CARTESIAN_POINT ( 'NONE',  ( 0.5654596793231598806, -1.618818539163461301, 0.5682417262808788783 ) ) ;
#21508=CARTESIAN_POINT ( 'NONE',  ( 0.6078349182483022695, -1.478587231578513572, 0.5349676189723107100 ) ) ;
#21517=CARTESIAN_POINT ( 'NONE',  ( 0.01144005434401617304, -0.8535789549361010309, 0.3246971777977655793 ) ) ;
#21518=ORIENTED_EDGE ( 'NONE', *, *, #14433, .T. ) ;
#21520=CARTESIAN_POINT ( 'NONE',  ( 0.3047936848243344432, -1.756875962071034580, 0.5682417262361116883 ) ) ;
#21522=CARTESIAN_POINT ( 'NONE',  ( 0.7390121836339409445, -1.515703229308124955, 0.4860421661703527851 ) ) ;
#21524=CARTESIAN_POINT ( 'NONE',  ( 0.3416500515225935897, -1.080402072964486315, 0.7068558125486118504 ) ) ;
#21525=CARTESIAN_POINT ( 'NONE',  ( 0.1957946853229683704, -1.369086038819396389, 0.5557458681356171049 ) ) ;
#21528=CARTESIAN_POINT ( 'NONE',  ( 0.1482405220709307747, -0.7090401843242698510, 0.5530575512909489122 ) ) ;
#21531=CARTESIAN_POINT ( 'NONE',  ( 0.6990116478510675080, -1.529268566928075002, 0.5876553814873258785 ) ) ;
#21532=CARTESIAN_POINT ( 'NONE',  ( 0.06090235255802147613, -0.5536121331843190108, 0.2259376826350176226 ) ) ;
#21534=CARTESIAN_POINT ( 'NONE',  ( 0.5538295395026971990, -1.622802647202313819, 0.5051661404396670108 ) ) ;
#21542=CARTESIAN_POINT ( 'NONE',  ( 0.1221917373669615114, -0.5546197540517507907, 0.1887439894328808709 ) ) ;
#21543=CARTESIAN_POINT ( 'NONE',  ( 0.4503526376543276477, -1.692732021471400339, 0.4426110423297867635 ) ) ;
#21544=DIRECTION ( 'NONE',  ( -0.8660512985181135770, -0.4999551463232371207, 0.000000000000000000 ) ) ;
#21547=CARTESIAN_POINT ( 'NONE',  ( 0.3663975874019590462, -1.157438136726378408, 0.4269148889825721827 ) ) ;
#21548=CARTESIAN_POINT ( 'NONE',  ( 0.3446155261768803491, -0.8529094429884808148, 0.7348996499020890028 ) ) ;
#21551=CARTESIAN_POINT ( 'NONE',  ( 0.001320963519262947179, -0.9568487245275125730, 0.3190620996948075327 ) ) ;
#21554=CARTESIAN_POINT ( 'NONE',  ( 0.1212526918783438795, -0.8711807980328569734, 0.4983147516987611048 ) ) ;
#21555=CARTESIAN_POINT ( 'NONE',  ( 0.2672157584620782345, -1.674897712893493429, 0.5728500076325480084 ) ) ;
#21564=CARTESIAN_POINT ( 'NONE',  ( 0.3295209608565876636, -1.174482601001649362, 0.5872793224613557239 ) ) ;
#21567=CARTESIAN_POINT ( 'NONE',  ( 0.4621666676022437859, -1.234211826098466913, 0.7071490788379034553 ) ) ;
#21570=CARTESIAN_POINT ( 'NONE',  ( 0.4515156439561487933, -1.057718100141998407, 0.6525781907329395448 ) ) ;
#21578=CARTESIAN_POINT ( 'NONE',  ( 0.03743733038894521414, -0.5670480389072934946, 0.2780609670579947124 ) ) ;
#21579=CARTESIAN_POINT ( 'NONE',  ( 0.06558781334581398337, -0.7848964240899376499, 0.03428501785215255782 ) ) ;
#21580=CARTESIAN_POINT ( 'NONE',  ( 0.1861909972232556609, -0.6993559402776449163, -0.02127579158555052696 ) ) ;
#21584=CARTESIAN_POINT ( 'NONE',  ( 0.3036438813139882842, -1.041601470818427799, 0.6258450271758987382 ) ) ;
#21585=CARTESIAN_POINT ( 'NONE',  ( 0.5469705670084967775, -1.495816971338993495, 0.6906149559573403485 ) ) ;
#21593=CARTESIAN_POINT ( 'NONE',  ( 0.5694934407712974878, -1.613350223101006620, 0.4177417262808785781 ) ) ;
#21594=CARTESIAN_POINT ( 'NONE',  ( 0.1117288206367789555, -1.275843495540134320, 0.6175638907962521795 ) ) ;
#21597=CARTESIAN_POINT ( 'NONE',  ( 1.365923996832131609E-16, -0.9481888444201339583, 0.1457185332388703791 ) ) ;
#21601=CARTESIAN_POINT ( 'NONE',  ( 0.4743695099260452075, -1.117357713078968695, 0.5498565627795439781 ) ) ;
#21602=CARTESIAN_POINT ( 'NONE',  ( 0.4444931384256880502, -1.226103329170601386, 0.5856983068965044836 ) ) ;
#21605=CARTESIAN_POINT ( 'NONE',  ( 0.05086546246741921462, -1.198860143930047473, 0.7015125153497857591 ) ) ;
#21612=VERTEX_POINT ( 'NONE', #22038 ) ;
#21615=PLANE ( 'NONE',  #14706 ) ;
#21616=ORIENTED_EDGE ( 'NONE', *, *, #1771, .T. ) ;
#21618=ORIENTED_EDGE ( 'NONE', *, *, #11163, .T. ) ;
#21621=CARTESIAN_POINT ( 'NONE',  ( 0.01818706982255626978, -0.6782422388700252158, 0.5155022423221341521 ) ) ;
#21622=CARTESIAN_POINT ( 'NONE',  ( 0.06444297064315794576, -0.8352831487901670737, 0.1457185332388703236 ) ) ;
#21625=EDGE_CURVE ( 'NONE', #40154, #35767, #38464, .T. ) ;
#21631=CARTESIAN_POINT ( 'NONE',  ( 0.2625973931889362678, -0.6796768235205253861, 0.1477649966949237115 ) ) ;
#21633=CARTESIAN_POINT ( 'NONE',  ( 0.5182059338286948424, -1.328740440620357344, 0.7997488878819424274 ) ) ;
#21634=FACE_OUTER_BOUND ( 'NONE', #31560, .T. ) ;
#21635=CARTESIAN_POINT ( 'NONE',  ( 0.2289168280753887674, -1.471836432603705669, 0.9194637683477111523 ) ) ;
#21636=CARTESIAN_POINT ( 'NONE',  ( 0.1486919001366245052, -1.066606737835706253, 0.9727470820782289085 ) ) ;
#21640=CARTESIAN_POINT ( 'NONE',  ( 0.6589703859825570831, -1.564329074718757484, 0.3667417262808780887 ) ) ;
#21646=CARTESIAN_POINT ( 'NONE',  ( 0.003124719664520368614, -0.5686731593868924461, 0.1457185332388688526 ) ) ;
#21647=CARTESIAN_POINT ( 'NONE',  ( 0.08392504549576879080, -1.205435068169474988, 0.7615968429824111485 ) ) ;
#21649=CARTESIAN_POINT ( 'NONE',  ( 0.3234650319091952331, -0.8156164872106268504, 0.7066254915499745604 ) ) ;
#21650=CARTESIAN_POINT ( 'NONE',  ( 0.6704502323737214775, -1.558777008743201353, 0.6054797769067454816 ) ) ;
#21655=CARTESIAN_POINT ( 'NONE',  ( 0.2642540606809890558, -1.625850527579886018, 0.8231221639007153534 ) ) ;
#21656=CARTESIAN_POINT ( 'NONE',  ( 0.1291821447933259592, -0.5731434977924334540, 0.2461200965963110388 ) ) ;
#21657=CARTESIAN_POINT ( 'NONE',  ( 0.1133170741025229245, -1.391401617297857163, 0.5182417262812423209 ) ) ;
#21659=CARTESIAN_POINT ( 'NONE',  ( 0.2766509774079478068, -0.8188515361471339071, 0.5743688119339978027 ) ) ;
#21662=CARTESIAN_POINT ( 'NONE',  ( 0.2628562773071145275, -0.7496856360161251454, 0.5667459045074426660 ) ) ;
#21664=CARTESIAN_POINT ( 'NONE',  ( 0.5264113014007820723, -1.640729993778254014, 0.5682417262808777680 ) ) ;
#21668=CARTESIAN_POINT ( 'NONE',  ( 0.09800014303332876819, -0.7423468218336800595, 0.3236582407429515196 ) ) ;
#21670=CARTESIAN_POINT ( 'NONE',  ( 0.1091101412475568994, -0.5932495664807553304, 0.3114501276851988631 ) ) ;
#21671=CARTESIAN_POINT ( 'NONE',  ( 0.3259879919982053287, -1.767950897709265945, 0.5312986935552727052 ) ) ;
#21672=CARTESIAN_POINT ( 'NONE',  ( 0.001904821466202900188, -0.5284344570646690720, 0.09157858422922257602 ) ) ;
#21673=CARTESIAN_POINT ( 'NONE',  ( 0.04300737265183255525, -1.224161303901022180, 0.6631612324643675338 ) ) ;
#21675=CARTESIAN_POINT ( 'NONE',  ( 0.4488584268620961493, -1.696961260237186409, 0.5959601211048285441 ) ) ;
#21676=CARTESIAN_POINT ( 'NONE',  ( 0.6140150280136293937, -1.296280020069253469, 0.8682680789332258842 ) ) ;
#21680=CARTESIAN_POINT ( 'NONE',  ( 0.5972608898831076596, -1.261123752139667875, 0.6057417262808246772 ) ) ;
#21682=PLANE ( 'NONE',  #23182 ) ;
#21683=CARTESIAN_POINT ( 'NONE',  ( 0.4299297405268334149, -1.031605064505895619, 0.6882246241152528698 ) ) ;
#21686=B_SPLINE_CURVE_WITH_KNOTS ( 'NONE', 3,
 ( #21503, #15306, #3163, #5634, #21901, #12417, #31152, #39986, #11808, #6029, #34021, #18597 ),
 .UNSPECIFIED., .F., .F.,
 ( 4, 2, 2, 2, 2, 4 ),
 ( -5.999999998893646056E-08, 0.0004327397255088311447, 0.0008655394510176511996, 0.001731138902035301826, 0.002596738353052953103, 0.003462337804070603729 ),
 .UNSPECIFIED. ) ;
#21688=CARTESIAN_POINT ( 'NONE',  ( 0.4000099798367696691, -1.704638381955406734, 0.4182417262808776903 ) ) ;
#21690=ORIENTED_EDGE ( 'NONE', *, *, #260, .F. ) ;
#21691=CARTESIAN_POINT ( 'NONE',  ( 0.4670213778778394831, -1.236191465557153757, 0.6057417262809817737 ) ) ;
#21697=CARTESIAN_POINT ( 'NONE',  ( 0.06001981139707002200, -1.214044704396488594, 0.7646275528860384529 ) ) ;
#21707=DIRECTION ( 'NONE',  ( -0.4999551463232372317, 0.8660512985181134660, -0.000000000000000000 ) ) ;
#21710=CARTESIAN_POINT ( 'NONE',  ( 0.1090682129762271801, -0.6262447015380825377, 0.4004099436828046366 ) ) ;
#21712=CARTESIAN_POINT ( 'NONE',  ( 0.7071069014570956490, -1.521634513519168452, 0.5617257377400114438 ) ) ;
#21713=CARTESIAN_POINT ( 'NONE',  ( 0.2830252135639645394, -1.159611347306545470, 0.8504159276851470661 ) ) ;
#21716=CARTESIAN_POINT ( 'NONE',  ( 0.5766475765793911412, -1.620807927452676767, 0.4730587198120521641 ) ) ;
#21722=CARTESIAN_POINT ( 'NONE',  ( 0.5804045214929907104, -1.495121667922066910, 0.5634096241211530298 ) ) ;
#21723=CARTESIAN_POINT ( 'NONE',  ( 0.4343371540759652372, -1.702447133182462435, 0.4323261742870332935 ) ) ;
#21727=CARTESIAN_POINT ( 'NONE',  ( 0.2101951102887192890, -1.233953443661628846, 0.5631135429232324574 ) ) ;
#21729=CARTESIAN_POINT ( 'NONE',  ( 0.6277259471038021399, -1.316916163187945799, 0.8316945246157878557 ) ) ;
#21734=CARTESIAN_POINT ( 'NONE',  ( 0.003994112659391831251, -0.9740337013070538008, 0.4215942553239714341 ) ) ;
#21737=CARTESIAN_POINT ( 'NONE',  ( 0.1897018898765783779, -0.7780637555336420430, 0.2978648193278307654 ) ) ;
#21747=CARTESIAN_POINT ( 'NONE',  ( 0.6527381947427340902, -1.527960125101692768, 0.4182417262808776903 ) ) ;
#21748=CARTESIAN_POINT ( 'NONE',  ( 0.08298671528866649605, -0.8222748340196127659, 0.1457185332388708787 ) ) ;
#21749=EDGE_CURVE ( 'NONE', #1874, #26668, #11483, .T. ) ;
#21751=ADVANCED_FACE ( 'NONE', ( #38654 ), #418, .F. ) ;
#21754=CARTESIAN_POINT ( 'NONE',  ( 0.3660523240620164875, -1.128919933506183471, 0.6218697989683404925 ) ) ;
#21755=DIRECTION ( 'NONE',  ( 0.8660512985181133550, 0.4999551463232373982, 0.000000000000000000 ) ) ;
#21757=CARTESIAN_POINT ( 'NONE',  ( 0.5082032253465859073, -1.306217543967353123, 0.6299990673569597632 ) ) ;
#21761=CARTESIAN_POINT ( 'NONE',  ( 0.5117280326951013647, -1.115088012504228621, 0.5923667439031021775 ) ) ;
#21764=CARTESIAN_POINT ( 'NONE',  ( 0.09908208500843325439, -1.366949803050675261, 0.6729494607312549448 ) ) ;
#21766=AXIS2_PLACEMENT_3D ( 'NONE', #11683, #21149, #33679 ) ;
#21767=CARTESIAN_POINT ( 'NONE',  ( 0.06532065983977884682, -0.7045720426608378384, 0.5366528578034658326 ) ) ;
#21769=CARTESIAN_POINT ( 'NONE',  ( 0.06477686075188948678, -0.8276703782281517041, 0.09804374420191747097 ) ) ;
#21770=CARTESIAN_POINT ( 'NONE',  ( 0.1118013512516233404, -0.8708971820562737554, -0.01152571254326707761 ) ) ;
#21778=CARTESIAN_POINT ( 'NONE',  ( 0.4760996380614069823, -1.068744558855534432, 0.6220588924540169096 ) ) ;
#21779=CARTESIAN_POINT ( 'NONE',  ( 0.1377143472285344561, -0.6768556682296630322, 0.4686332729017968490 ) ) ;
#21786=CARTESIAN_POINT ( 'NONE',  ( 0.4345963605075027769, -1.690632822822775827, 0.4263932049186950901 ) ) ;
#21787=CARTESIAN_POINT ( 'NONE',  ( 0.07279096728935340044, -1.323295152996974977, 0.4931969685770185019 ) ) ;
#21790=CARTESIAN_POINT ( 'NONE',  ( 0.05796715499547382133, -1.320156192035571774, 0.6033327867956804758 ) ) ;
#21793=CARTESIAN_POINT ( 'NONE',  ( 0.3845716336272441138, -1.023253965646789831, 0.6260147105531964629 ) ) ;
#21794=CARTESIAN_POINT ( 'NONE',  ( 0.4815930311117895823, -1.120787884457994599, 0.5308384764438787151 ) ) ;
#21795=CARTESIAN_POINT ( 'NONE',  ( 0.5565267853031266032, -1.184521675161833043, 0.6057417262809816627 ) ) ;
#21799=CARTESIAN_POINT ( 'NONE',  ( -0.002175845014896822093, -0.8193767622554530838, 0.2897257274743089139 ) ) ;
#21804=CARTESIAN_POINT ( 'NONE',  ( 0.3417290234946780969, -1.631754028364875264, 0.4817266676845163853 ) ) ;
#21805=EDGE_CURVE ( 'NONE', #35767, #32520, #15869, .T. ) ;
#21813=CARTESIAN_POINT ( 'NONE',  ( 0.5116187330526053012, -1.317947182177965804, 0.7954296552626618499 ) ) ;
#21819=ORIENTED_EDGE ( 'NONE', *, *, #21825, .T. ) ;
#21820=CARTESIAN_POINT ( 'NONE',  ( 0.01251345383894142578, -0.5638626234200834197, 0.2823644336484513739 ) ) ;
#21823=CARTESIAN_POINT ( 'NONE',  ( 0.08016089217752186968, -1.309201107948811504, 0.5631135211526980822 ) ) ;
#21825=EDGE_CURVE ( 'NONE', #10513, #30976, #32550, .T. ) ;
#21826=VECTOR ( 'NONE', #17065, 39.37007874015748143 ) ;
#21834=CARTESIAN_POINT ( 'NONE',  ( 0.4881568739066119433, -1.310886444036855947, 0.8120130285850476470 ) ) ;
#21838=CARTESIAN_POINT ( 'NONE',  ( 0.2496972935526009241, -0.9635046127537866267, 0.6859288853639479155 ) ) ;
#21839=CARTESIAN_POINT ( 'NONE',  ( 0.2746970422698945535, -1.662148702819467694, 0.7072477570165817129 ) ) ;
#21841=CARTESIAN_POINT ( 'NONE',  ( 0.08540438715202058884, -0.8281466500289427213, 0.8274849438104245891 ) ) ;
#21843=CARTESIAN_POINT ( 'NONE',  ( 0.06843411546424661707, -1.327640554429453168, 0.5682417262808774350 ) ) ;
#21844=CARTESIAN_POINT ( 'NONE',  ( 0.3091361241754520539, -1.774399086135407533, 0.3157417262808776548 ) ) ;
#21845=CARTESIAN_POINT ( 'NONE',  ( 0.4414599527244874033, -1.202236957499543069, 0.6968917936656464640 ) ) ;
#21849=CARTESIAN_POINT ( 'NONE',  ( 0.002083146443013472390, -0.4777046557262296100, 0.1109577558998209867 ) ) ;
#21850=CARTESIAN_POINT ( 'NONE',  ( 0.06667927146718531650, -1.148330793516402881, 0.7614259873238805598 ) ) ;
#21852=CARTESIAN_POINT ( 'NONE',  ( 0.3043431798205027405, -0.7811398438223191576, 0.6771279187310788039 ) ) ;
#21859=CIRCLE ( 'NONE', #4095, 0.03749999999977554621 ) ;
#21862=ORIENTED_EDGE ( 'NONE', *, *, #26344, .T. ) ;
#21864=CARTESIAN_POINT ( 'NONE',  ( 0.2238418704740615384, -1.454669764064490778, 0.9245064154499356146 ) ) ;
#21866=CARTESIAN_POINT ( 'NONE',  ( 0.5949972485239248821, -1.483920380426879682, 0.6302736613771389163 ) ) ;
#21867=CARTESIAN_POINT ( 'NONE',  ( 0.3486080135059020368, -1.166240872638638182, 0.4316577372902974941 ) ) ;
#21869=CARTESIAN_POINT ( 'NONE',  ( 0.4727414870697744798, -1.078201156678013639, 0.7478468640933467748 ) ) ;
#21872=CARTESIAN_POINT ( 'NONE',  ( 0.5737815958547760609, -1.229766092225264673, 0.8180618760404326784 ) ) ;
#21875=DIRECTION ( 'NONE',  ( 1.000000000000000000, 0.000000000000000000, 0.000000000000000000 ) ) ;
#21877=CARTESIAN_POINT ( 'NONE',  ( 0.3048982267989290840, -1.756746414302342796, 0.5594309555313056181 ) ) ;
#21880=CARTESIAN_POINT ( 'NONE',  ( 0.1200857017990378389, -0.7890252880104620115, 0.4347573559404794841 ) ) ;
#21882=CARTESIAN_POINT ( 'NONE',  ( 0.5104467154061602674, -1.495435902464579803, 0.7328012557383771775 ) ) ;
#21883=EDGE_CURVE ( 'NONE', #1876, #24913, #36984, .T. ) ;
#21889=CARTESIAN_POINT ( 'NONE',  ( 0.7436037172534608608, -1.516441821114285382, 0.5740297838107625283 ) ) ;
#21896=CARTESIAN_POINT ( 'NONE',  ( 0.2319960710055803677, -1.232736008543062090, 0.4687417262808780127 ) ) ;
#21898=CARTESIAN_POINT ( 'NONE',  ( 0.0006292437964357017102, -0.9180166443092167006, 0.3683461522897012452 ) ) ;
#21899=CARTESIAN_POINT ( 'NONE',  ( 0.5440395270977919084, -1.170651503450800268, 0.6371399293509031336 ) ) ;
#21901=CARTESIAN_POINT ( 'NONE',  ( 0.5806656507430593139, -1.610816081966196078, 0.5908874216888502229 ) ) ;
#21904=CARTESIAN_POINT ( 'NONE',  ( 0.3870879061362800799, -1.718823008802655927, 0.4198165928321926366 ) ) ;
#21907=CARTESIAN_POINT ( 'NONE',  ( 0.4775505920942409444, -1.133805584195902494, 0.4714299366448774786 ) ) ;
#21910=B_SPLINE_CURVE_WITH_KNOTS ( 'NONE', 3,
 ( #33461, #24425, #17828, #24037, #8166, #1620, #21135, #20745, #27512, #40035 ),
 .UNSPECIFIED., .F., .F.,
 ( 4, 2, 2, 2, 4 ),
 ( 0.000000000000000000, 0.0009922644452961607020, 0.001984528890592321404, 0.002976793335888482106, 0.003969057781184642808 ),
 .UNSPECIFIED. ) ;
#21911=CARTESIAN_POINT ( 'NONE',  ( 0.1872551924900081322, -0.8472677374427307617, 0.2151649526408891677 ) ) ;
#21914=CARTESIAN_POINT ( 'NONE',  ( 0.1214394166101126354, -1.245726820615419062, 0.7465128526039198631 ) ) ;
#21915=ORIENTED_EDGE ( 'NONE', *, *, #13178, .T. ) ;
#21917=CARTESIAN_POINT ( 'NONE',  ( 0.1536596445529307131, -1.277574755431481579, 0.4245438548657216038 ) ) ;
#21923=CARTESIAN_POINT ( 'NONE',  ( 0.2260509237186448805, -1.351684612934085372, 0.5412798235273647007 ) ) ;
#21926=CARTESIAN_POINT ( 'NONE',  ( 0.2629928857398323716, -0.9282033514108480876, 0.7349524644010387853 ) ) ;
#21929=VERTEX_POINT ( 'NONE', #31836 ) ;
#21931=CARTESIAN_POINT ( 'NONE',  ( 0.07342862190203788830, -0.5555273798011833852, 0.2245834878394794565 ) ) ;
#21936=CARTESIAN_POINT ( 'NONE',  ( 0.1880425571213318880, -0.9154252179768241904, 0.1909967134266482292 ) ) ;
#21940=CARTESIAN_POINT ( 'NONE',  ( 0.1367236663606709313, -0.6234998906017088505, 0.3678473249437352322 ) ) ;
#21941=CARTESIAN_POINT ( 'NONE',  ( 0.4876229533068589528, -1.660624946139342084, 0.5317207588342793834 ) ) ;
#21945=AXIS2_PLACEMENT_3D ( 'NONE', #6446, #16534, #943 ) ;
#21948=B_SPLINE_CURVE_WITH_KNOTS ( 'NONE', 3,
 ( #25082, #28172, #5745, #9043 ),
 .UNSPECIFIED., .F., .F.,
 ( 4, 4 ),
 ( 3.324383805864000793E-17, 2.394154788142702125E-05 ),
 .UNSPECIFIED. ) ;
#21949=CARTESIAN_POINT ( 'NONE',  ( 0.5297859054048726923, -1.159963375372088823, 0.8529160106009885389 ) ) ;
#21953=CARTESIAN_POINT ( 'NONE',  ( 0.05954239774771610122, -1.330287657886653596, 0.5843365015712381760 ) ) ;
#21956=CARTESIAN_POINT ( 'NONE',  ( 0.1898061597842229664, -0.8838521600963774594, 0.6041132961182806849 ) ) ;
#21957=CARTESIAN_POINT ( 'NONE',  ( 0.06972317538281022631, -1.315496003368490152, 0.5114807970970258744 ) ) ;
#21958=CARTESIAN_POINT ( 'NONE',  ( 0.6047538891612445067, -1.605163873594933843, 0.4396382108053981108 ) ) ;
#21962=CARTESIAN_POINT ( 'NONE',  ( 0.3336325236675090067, -1.050835064020409160, 0.7593003920438236021 ) ) ;
#21969=CARTESIAN_POINT ( 'NONE',  ( 0.07135087575717259656, -1.325947744100555603, 0.5536768997389298619 ) ) ;
#21972=CARTESIAN_POINT ( 'NONE',  ( 0.3632587558834509123, -1.098712390806521499, 0.7441976441039135359 ) ) ;
#21974=EDGE_LOOP ( 'NONE', ( #15598, #23510, #6255, #20542 ) ) ;
#21975=CARTESIAN_POINT ( 'NONE',  ( 0.4813782568983027699, -1.076368431653871971, 0.6093178202591913450 ) ) ;
#21976=ORIENTED_EDGE ( 'NONE', *, *, #30675, .T. ) ;
#21978=CARTESIAN_POINT ( 'NONE',  ( 0.01358700006623634465, -0.9214419153559146869, 0.5592488618034630043 ) ) ;
#21982=CARTESIAN_POINT ( 'NONE',  ( 0.3852639964463288047, -1.605627256116679336, 0.5745209014822190152 ) ) ;
#21984=CARTESIAN_POINT ( 'NONE',  ( 0.1853660027032721369, -0.7908266843905505938, 0.01465295923235358268 ) ) ;
#21985=DIRECTION ( 'NONE',  ( -0.7432310347629357272, -0.4120354308901564844, 0.5271000214915373405 ) ) ;
#21989=EDGE_LOOP ( 'NONE', ( #22518, #32622, #21976, #31516, #35374, #29695, #4739 ) ) ;
#21990=CARTESIAN_POINT ( 'NONE',  ( 0.3426012929402474372, -0.9387369744000205740, 0.6409010290876834270 ) ) ;
#21992=CARTESIAN_POINT ( 'NONE',  ( 0.5097106194861918960, -1.415068235197837199, 0.7887110192874389192 ) ) ;
#21995=CARTESIAN_POINT ( 'NONE',  ( 0.1873082927213247373, -0.6998484496557862977, 0.03162329823462053241 ) ) ;
#22002=ADVANCED_FACE ( 'NONE', ( #6927 ), #5863, .F. ) ;
#22005=CARTESIAN_POINT ( 'NONE',  ( 0.2106403741462083423, -1.241433952965754539, 0.5874914036943872375 ) ) ;
#22007=CARTESIAN_POINT ( 'NONE',  ( 0.08492870897506230032, -1.322602396236127520, 0.7244794688457697474 ) ) ;
#22010=CARTESIAN_POINT ( 'NONE',  ( 0.4508097189255980131, -1.059596525805123202, 0.6314750327306427602 ) ) ;
#22012=CARTESIAN_POINT ( 'NONE',  ( 0.1838304123260658118, -1.376269861257182203, 0.4854672772329559072 ) ) ;
#22013=CARTESIAN_POINT ( 'NONE',  ( 0.4857959727310743325, -1.202259978777793226, 0.5856983068965045947 ) ) ;
#22017=EDGE_CURVE ( 'NONE', #7249, #38394, #29128, .T. ) ;
#22020=CARTESIAN_POINT ( 'NONE',  ( -0.003124719664520040317, -0.8057675726412020234, 0.1293934913668264852 ) ) ;
#22021=CARTESIAN_POINT ( 'NONE',  ( -0.0001502531655640915837, -0.8192210497105464340, -0.06580348057302833065 ) ) ;
#22023=CARTESIAN_POINT ( 'NONE',  ( 0.3338768636023082270, -1.636289205640462541, 0.4854925386805667986 ) ) ;
#22028=ORIENTED_EDGE ( 'NONE', *, *, #17013, .F. ) ;
#22031=CARTESIAN_POINT ( 'NONE',  ( 0.5974902904423020633, -1.460252601885912327, 0.6227098129790233916 ) ) ;
#22032=CARTESIAN_POINT ( 'NONE',  ( 0.002302760697785899424, -0.5199223015690960237, 0.1489253775790380097 ) ) ;
#22035=CARTESIAN_POINT ( 'NONE',  ( 0.2033348128484126494, -0.6878582300498709001, 0.3466453153493967432 ) ) ;
#22037=CARTESIAN_POINT ( 'NONE',  ( 0.03806478327246554799, -0.7058754152494622902, 0.5484913812544711664 ) ) ;
#22038=CARTESIAN_POINT ( 'NONE',  ( 0.3862110256088818194, -1.731934476144515900, 0.4282538419479027247 ) ) ;
#22044=ORIENTED_EDGE ( 'NONE', *, *, #12763, .F. ) ;
#22048=FACE_OUTER_BOUND ( 'NONE', #22330, .T. ) ;
#22052=CARTESIAN_POINT ( 'NONE',  ( 0.5832544884196250168, -1.433562627639882292, 0.6981186852435199430 ) ) ;
#22057=CARTESIAN_POINT ( 'NONE',  ( 0.01378518146509891129, -0.4682930211632502782, 0.3166968367138670026 ) ) ;
#22062=CARTESIAN_POINT ( 'NONE',  ( 0.4590722942007692264, -1.224561879564241673, 0.6545337212731852095 ) ) ;
#22065=CARTESIAN_POINT ( 'NONE',  ( 0.3165138724069220255, -1.757609964495261190, 0.6990733182572979043 ) ) ;
#22067=CARTESIAN_POINT ( 'NONE',  ( 0.09763382290327969615, -1.358444063574388183, 0.6820618144092522872 ) ) ;
#22072=CARTESIAN_POINT ( 'NONE',  ( 0.6990213974170155220, -1.529262631747053902, 0.5876538509318743886 ) ) ;
#22078=CARTESIAN_POINT ( 'NONE',  ( 0.2194110478981629864, -1.459085012964730810, 0.9363139587045151702 ) ) ;
#22079=CARTESIAN_POINT ( 'NONE',  ( 0.5946750165716045977, -1.487132221806371390, 0.5679954418029664609 ) ) ;
#22080=B_SPLINE_CURVE_WITH_KNOTS ( 'NONE', 3,
 ( #15884, #1102, #32126, #13403, #16698, #9906, #303, #517, #23084, #7025, #13010, #3930, #25558, #19590, #38505, #32311, #29246, #13610, #14003, #20198, #36425, #17299, #23896, #13796, #29643, #26361, #4943, #4530, #32521, #1483, #39306, #8236, #24107, #32920, #1289, #30057, #7411, #1694, #32723, #36212, #39496, #11325, #10939, #38893, #26963, #10723, #14604, #7821, #11127, #11545, #23500, #20813 ),
 .UNSPECIFIED., .F., .F.,
 ( 4, 2, 2, 2, 2, 2, 2, 2, 2, 2, 2, 2, 2, 2, 2, 2, 2, 2, 2, 2, 2, 2, 2, 2, 2, 4 ),
 ( 0.001215176597727166043, 0.002640180933026298367, 0.003352683100675868649, 0.004065185268325438930, 0.005490189603624587300, 0.006915193938923737405, 0.008340198274222885774, 0.009052700441872457357, 0.009765202609522028940, 0.01119020694482118945, 0.01261521128012034997, 0.01546521995071867446, 0.01689022428601783324, 0.01831522862131699722, 0.02116523729191532519, 0.02401524596251365662, 0.02686525463311198805, 0.02971526330371031602, 0.03256527197430864745, 0.03541528064490696848, 0.03684028498020613940, 0.03826528931550530338, 0.04111529798610363828, 0.04254030232140279533, 0.04396530665670195931, 0.04681531532730028033 ),
 .UNSPECIFIED. ) ;
#22085=CARTESIAN_POINT ( 'NONE',  ( 0.3991878447057942703, -0.9797369418029474586, 0.7176166460480870590 ) ) ;
#22094=ORIENTED_EDGE ( 'NONE', *, *, #28191, .T. ) ;
#22095=CARTESIAN_POINT ( 'NONE',  ( 0.08744249762914983737, -0.7479857328945178629, 0.2113153514082470319 ) ) ;
#22097=CARTESIAN_POINT ( 'NONE',  ( 0.1038539065874188316, -0.5467874247544137756, 0.1622444650650389786 ) ) ;
#22102=CARTESIAN_POINT ( 'NONE',  ( 0.4224071670835765624, -1.711981311311245646, 0.6086670734470306376 ) ) ;
#22104=CARTESIAN_POINT ( 'NONE',  ( 0.6657490759106345912, -1.561538255549536736, 0.5663076794875994135 ) ) ;
#22107=CARTESIAN_POINT ( 'NONE',  ( 0.1361552210536516039, -0.5798312371597438286, 0.2613271312737237007 ) ) ;
#22111=CARTESIAN_POINT ( 'NONE',  ( 0.05563540667800927902, -1.335270441939011121, 0.5197417262808780025 ) ) ;
#22114=CARTESIAN_POINT ( 'NONE',  ( 0.03852435536883173223, -1.195394391876414719, 0.6677169776219902264 ) ) ;
#22115=CARTESIAN_POINT ( 'NONE',  ( 0.2858575041057334065, -0.8891697324286316206, 0.5691962326423758434 ) ) ;
#22119=EDGE_CURVE ( 'NONE', #39497, #1588, #19130, .T. ) ;
#22122=CARTESIAN_POINT ( 'NONE',  ( 0.5140974934605563318, -1.532472854630404946, 0.5610796881895311339 ) ) ;
#22126=DIRECTION ( 'NONE',  ( -0.4999551463232359549, 0.8660512985181140211, 0.000000000000000000 ) ) ;
#22127=CARTESIAN_POINT ( 'NONE',  ( 0.1906473341773986807, -0.8225591132712883891, 0.2611071221664287845 ) ) ;
#22129=VECTOR ( 'NONE', #5075, 39.37007874015748143 ) ;
#22130=CARTESIAN_POINT ( 'NONE',  ( 0.2316917763911649497, -1.232208891764917880, 0.5707417262808780478 ) ) ;
#22131=CARTESIAN_POINT ( 'NONE',  ( 0.03213308919446983269, -1.082564143163080805, 0.7440698363395104042 ) ) ;
#22134=CYLINDRICAL_SURFACE ( 'NONE', #19211, 0.03749999999977557397 ) ;
#22135=DIRECTION ( 'NONE',  ( -0.4999551463232372317, 0.8660512985181135770, -0.000000000000000000 ) ) ;
#22145=CARTESIAN_POINT ( 'NONE',  ( 0.09046525539546303174, -0.5659545125636742391, 0.1933820889497062101 ) ) ;
#22148=CARTESIAN_POINT ( 'NONE',  ( 0.07284975538018015340, -0.5413571526563850655, 0.1629110515435110984 ) ) ;
#22152=CARTESIAN_POINT ( 'NONE',  ( 0.2233957848829526416, -0.9348223186165968146, 0.4130400850522266687 ) ) ;
#22155=CARTESIAN_POINT ( 'NONE',  ( 0.1897112079047663935, -0.5340520988485693010, 0.1365881794216592948 ) ) ;
#22156=CARTESIAN_POINT ( 'NONE',  ( 0.1255523023994105369, -0.5499328071996130163, 0.1534195410746523047 ) ) ;
#22160=CARTESIAN_POINT ( 'NONE',  ( 0.07039376183350297411, -0.5541924008705879645, 0.2222877572371358135 ) ) ;
#22162=B_SPLINE_CURVE_WITH_KNOTS ( 'NONE', 3,
 ( #2526, #14868, #27428, #27616 ),
 .UNSPECIFIED., .F., .F.,
 ( 4, 4 ),
 ( 1.309687503460227108E-17, 0.0002394164927460790192 ),
 .UNSPECIFIED. ) ;
#22164=CARTESIAN_POINT ( 'NONE',  ( 0.5016144086874707586, -1.117686766064061255, 0.8075564334577929326 ) ) ;
#22166=CARTESIAN_POINT ( 'NONE',  ( 0.04593167833806930528, -1.243000510969585415, 0.6581084539110385601 ) ) ;
#22170=CARTESIAN_POINT ( 'NONE',  ( 0.1207196391192309343, -0.8326872279821241341, 0.4345446219756442519 ) ) ;
#22171=CARTESIAN_POINT ( 'NONE',  ( 0.06955161396059786338, -1.315588549135835894, 0.5148643997387302162 ) ) ;
#22173=EDGE_LOOP ( 'NONE', ( #31720, #14153, #37019, #1832 ) ) ;
#22181=CARTESIAN_POINT ( 'NONE',  ( 0.3316311659535515766, -1.291330680059900260, 0.4674458267467086481 ) ) ;
#22184=CARTESIAN_POINT ( 'NONE',  ( 0.5066646123182778627, -1.303543819055811515, 0.6363843823558122947 ) ) ;
#22186=CARTESIAN_POINT ( 'NONE',  ( 0.3806788393426449035, -1.717835445135155625, 0.4208877479360482732 ) ) ;
#22187=CARTESIAN_POINT ( 'NONE',  ( 0.4579382962256918765, -1.063507731091402952, 0.6287285752299462960 ) ) ;
#22193=CARTESIAN_POINT ( 'NONE',  ( 0.3615071206352756805, -1.531905561232253188, 0.8175632647814430332 ) ) ;
#22194=CARTESIAN_POINT ( 'NONE',  ( 0.08634205943466652378, -0.7634307173544517822, 0.04861706834207135675 ) ) ;
#22195=CARTESIAN_POINT ( 'NONE',  ( 0.1861028475561006812, -0.7105372532307299149, -0.02003343372011650789 ) ) ;
#22197=ORIENTED_EDGE ( 'NONE', *, *, #4728, .T. ) ;
#22199=CARTESIAN_POINT ( 'NONE',  ( 0.5672310176675520177, -1.503268715516413945, 0.5784013901591326112 ) ) ;
#22201=CARTESIAN_POINT ( 'NONE',  ( 0.1868122149958911793, -0.7339159750268756666, 0.03456946681538086014 ) ) ;
#22207=CARTESIAN_POINT ( 'NONE',  ( 0.08668499250304141646, -0.7271995642927178150, 0.06208601679367901915 ) ) ;
#22208=CARTESIAN_POINT ( 'NONE',  ( 0.4136294883733457883, -1.694877849074676091, 0.4182417262808776903 ) ) ;
#22209=CARTESIAN_POINT ( 'NONE',  ( 0.07497864282572899719, -1.322056043867073427, 0.4862695133534066794 ) ) ;
#22210=CARTESIAN_POINT ( 'NONE',  ( 0.2011421443510955920, -1.242285083301493120, 0.5974872228881977776 ) ) ;
#22214=CARTESIAN_POINT ( 'NONE',  ( 0.2370370725713593918, -0.9423068241879761775, 0.4501375130042485906 ) ) ;
#22215=CARTESIAN_POINT ( 'NONE',  ( 0.3392508469782434810, -1.160100971070933795, 0.4507252195672304951 ) ) ;
#22216=LINE ( 'NONE', #12945, #13295 ) ;
#22217=CARTESIAN_POINT ( 'NONE',  ( 0.2615233978049238406, -1.678084768816710648, 0.5373352594323992371 ) ) ;
#22218=CARTESIAN_POINT ( 'NONE',  ( -0.001215370517532385992, -0.9049306443239834019, 0.2850616817831099770 ) ) ;
#22219=CARTESIAN_POINT ( 'NONE',  ( -0.0003249894700343514218, -0.9114069365513199905, 0.03530629958352291681 ) ) ;
#22221=CARTESIAN_POINT ( 'NONE',  ( 0.3434800707737146741, -1.169184835483404905, 0.4282596159937968605 ) ) ;
#22222=EDGE_CURVE ( 'NONE', #15271, #22420, #31593, .T. ) ;
#22225=ORIENTED_EDGE ( 'NONE', *, *, #30335, .T. ) ;
#22231=CARTESIAN_POINT ( 'NONE',  ( 0.5621458515759424346, -1.398487943849158199, 0.7472131749405318546 ) ) ;
#22234=B_SPLINE_CURVE_WITH_KNOTS ( 'NONE', 3,
 ( #39994, #2171, #12029, #37318, #33616, #12425, #2567, #2768, #17991, #9127, #18197, #37508, #24376, #5643 ),
 .UNSPECIFIED., .F., .F.,
 ( 4, 2, 2, 2, 2, 2, 4 ),
 ( -6.000000003697073285E-08, 0.004089234075588695644, 0.008178528151177427361, 0.01226782222676616081, 0.01329014574566334157, 0.01431246926456052233, 0.01635711630235487865 ),
 .UNSPECIFIED. ) ;
#22239=CARTESIAN_POINT ( 'NONE',  ( 0.05196760682231239825, -0.7635565754909066083, 0.6226813947830622809 ) ) ;
#22240=CARTESIAN_POINT ( 'NONE',  ( 0.4104656799765715736, -1.198377304174871316, 0.6811348502778500347 ) ) ;
#22241=CARTESIAN_POINT ( 'NONE',  ( 0.2397435495978002262, -1.344164646061327462, 0.4182417262808770797 ) ) ;
#22243=CARTESIAN_POINT ( 'NONE',  ( 0.1864213255783573886, -0.8266995537623093027, -0.03797464539687132185 ) ) ;
#22244=CARTESIAN_POINT ( 'NONE',  ( 0.4136294883733860894, -1.694877849074643228, 0.4182417262808776903 ) ) ;
#22248=CARTESIAN_POINT ( 'NONE',  ( 0.1886409489414842822, -0.8408369741812754539, 0.2375134434870870004 ) ) ;
#22250=CARTESIAN_POINT ( 'NONE',  ( 0.5780881571870869484, -1.425136765289637841, 0.7439213802220401295 ) ) ;
#22251=( BOUNDED_SURFACE ( )  B_SPLINE_SURFACE ( 3, 2, ( 
 ( #15506, #15692, #28242 ),
 ( #31734, #34415, #529 ),
 ( #18373, #9109, #2744 ),
 ( #37296, #30921, #40388 ),
 ( #37916, #34623, #12603 ),
 ( #15293, #18581, #2955 ),
 ( #21675, #40584, #28444 ),
 ( #9726, #37702, #317 ),
 ( #6015, #9525, #31139 ),
 ( #22102, #28060, #12406 ),
 ( #24958, #6424, #31524 ),
 ( #3339, #12822, #22295 ),
 ( #34810, #6615, #16122 ),
 ( #7224, #19411, #1116 ),
 ( #32741, #35840, #26188 ),
 ( #3765, #16318, #13215 ),
 ( #7652, #13623, #4151 ),
 ( #16920, #10350, #38712 ),
 ( #32142, #20216, #38912 ),
 ( #714, #7435, #25996 ),
 ( #16509, #22492, #26385 ),
 ( #35017, #10742, #4548 ),
 ( #10533, #20010, #35239 ),
 ( #14021, #23316, #38518 ) ),
 .UNSPECIFIED., .F., .F., .F. ) 
 B_SPLINE_SURFACE_WITH_KNOTS ( ( 4, 2, 2, 2, 2, 2, 2, 2, 2, 2, 2, 4 ),
 ( 3, 3 ),
 ( 0.008433819124337599629, 0.009129665800632340289, 0.009477589138779709751, 0.009825512476927079214, 0.01052135915322181987, 0.01086928249136918934, 0.01121720582951656053, 0.01191305250581130119, 0.01260889918210604185, 0.01295682252025341305, 0.01330474585840078251, 0.01400059253469552317 ),
 ( 0.000000000000000000, 1.000000000000000000 ),
 .UNSPECIFIED. ) 
 GEOMETRIC_REPRESENTATION_ITEM ( )  RATIONAL_B_SPLINE_SURFACE ( (
 ( 1.000000000000000000, 0.6948880044713926507, 1.000000000000000000),
 ( 1.000000000000000000, 0.6960840624298344492, 1.000000000000000000),
 ( 1.000000000000000000, 0.6983799194115379860, 1.000000000000000000),
 ( 1.000000000000000000, 0.7023957980309022409, 1.000000000000000000),
 ( 1.000000000000000000, 0.7038384642190140816, 1.000000000000000000),
 ( 1.000000000000000000, 0.7066519844213186019, 1.000000000000000000),
 ( 1.000000000000000000, 0.7080301531803978587, 1.000000000000000000),
 ( 1.000000000000000000, 0.7118414011448579437, 1.000000000000000000),
 ( 1.000000000000000000, 0.7139388523227178096, 1.000000000000000000),
 ( 1.000000000000000000, 0.7156078395921124935, 1.000000000000000000),
 ( 1.000000000000000000, 0.7159334618363153435, 1.000000000000000000),
 ( 1.000000000000000000, 0.7160867862248367910, 1.000000000000000000),
 ( 1.000000000000000000, 0.7159093286432843817, 1.000000000000000000),
 ( 1.000000000000000000, 0.7146582677834552033, 1.000000000000000000),
 ( 1.000000000000000000, 0.7128727118445921107, 1.000000000000000000),
 ( 1.000000000000000000, 0.7079968471081192760, 1.000000000000000000),
 ( 1.000000000000000000, 0.7050215538929806014, 1.000000000000000000),
 ( 1.000000000000000000, 0.7005626529068207375, 1.000000000000000000),
 ( 1.000000000000000000, 0.6990679116423534900, 1.000000000000000000),
 ( 1.000000000000000000, 0.6963021034989965719, 1.000000000000000000),
 ( 1.000000000000000000, 0.6950231705106640900, 1.000000000000000000),
 ( 1.000000000000000000, 0.6916869647287414713, 1.000000000000000000),
 ( 1.000000000000000000, 0.6899239366554796860, 1.000000000000000000),
 ( 1.000000000000000000, 0.6900227658400107655, 1.000000000000000000) ) ) 
 REPRESENTATION_ITEM ( '' )  SURFACE ( )  );
#22252=EDGE_CURVE ( 'NONE', #13794, #18202, #18877, .T. ) ;
#22253=CARTESIAN_POINT ( 'NONE',  ( 0.3364639209793421348, -1.089988309885336681, 0.7406982884823408719 ) ) ;
#22254=CARTESIAN_POINT ( 'NONE',  ( 0.1859432605888821921, -0.7573098151843028480, 0.1022962920937455361 ) ) ;
#22256=CARTESIAN_POINT ( 'NONE',  ( 0.2959710460089218231, -1.597927643852713464, 0.9577133037227931744 ) ) ;
#22262=DIRECTION ( 'NONE',  ( -1.000000000000000000, -0.000000000000000000, -0.000000000000000000 ) ) ;
#22263=CARTESIAN_POINT ( 'NONE',  ( 0.002083146443013521830, -0.4777046557262296100, 0.1638349238242636507 ) ) ;
#22264=CARTESIAN_POINT ( 'NONE',  ( 0.1169578367557221887, -1.398407385406643222, 0.6329296710379738178 ) ) ;
#22270=CARTESIAN_POINT ( 'NONE',  ( 0.4831567767736278385, -1.121977757481035010, 0.5105939270972588151 ) ) ;
#22273=CARTESIAN_POINT ( 'NONE',  ( 0.2439840020134950993, -1.523895357778563664, 0.8969720475523240699 ) ) ;
#22274=EDGE_CURVE ( 'NONE', #11170, #19917, #3633, .T. ) ;
#22275=CARTESIAN_POINT ( 'NONE',  ( 0.5954621451176055347, -1.487120967891011114, 0.5849300529686594086 ) ) ;
#22276=EDGE_CURVE ( 'NONE', #17780, #34098, #11008, .T. ) ;
#22277=CARTESIAN_POINT ( 'NONE',  ( 0.3511079287476752686, -1.164805985122749687, 0.4335040596137051394 ) ) ;
#22288=CARTESIAN_POINT ( 'NONE',  ( 0.1029610634938303709, -0.7684373263134592902, 0.3557047774870934487 ) ) ;
#22290=CARTESIAN_POINT ( 'NONE',  ( 0.5266619910787769809, -1.525087864311528429, 0.6234923701237724547 ) ) ;
#22295=CARTESIAN_POINT ( 'NONE',  ( 0.4074647527740007380, -1.709076545307301798, 0.6202421242740956409 ) ) ;
#22296=CARTESIAN_POINT ( 'NONE',  ( 0.7005072418814222157, -1.435918383503960394, 0.7932214653155064132 ) ) ;
#22299=CARTESIAN_POINT ( 'NONE',  ( 0.5900193846650280127, -1.451085630206152999, 0.7130590060845574119 ) ) ;
#22302=CARTESIAN_POINT ( 'NONE',  ( 0.4952488905928916774, -1.196841907270136840, 0.4182417262808778013 ) ) ;
#22304=CARTESIAN_POINT ( 'NONE',  ( 0.02115399423329476433, -1.083931147575175613, 0.6303919839426973537 ) ) ;
#22305=CARTESIAN_POINT ( 'NONE',  ( 0.5043207191046787941, -1.105492587439252494, 0.6133613128836958861 ) ) ;
#22316=CARTESIAN_POINT ( 'NONE',  ( 0.08955701898351196844, -0.5706670494699135343, 0.1066062274051425146 ) ) ;
#22320=CARTESIAN_POINT ( 'NONE',  ( 0.005103737174765597510, -0.9529501791669972022, 0.6308053658798797869 ) ) ;
#22324=EDGE_LOOP ( 'NONE', ( #39395, #10502 ) ) ;
#22326=CYLINDRICAL_SURFACE ( 'NONE', #35752, 0.03749999999977551152 ) ;
#22330=EDGE_LOOP ( 'NONE', ( #24244, #18889, #28528, #39998, #10767, #27874, #2126, #16798, #1474 ) ) ;
#22332=ORIENTED_EDGE ( 'NONE', *, *, #39615, .T. ) ;
#22333=CARTESIAN_POINT ( 'NONE',  ( 0.08992510688325772161, -0.6057077997829167781, 0.1553500322290060354 ) ) ;
#22335=CARTESIAN_POINT ( 'NONE',  ( 0.004323292021450524797, -0.5016872349303481693, 0.3729438605722754096 ) ) ;
#22336=CARTESIAN_POINT ( 'NONE',  ( 0.4314429043751959458, -1.476193151465878595, 0.8070760231935298901 ) ) ;
#22338=CARTESIAN_POINT ( 'NONE',  ( 0.004308327751199931069, -0.5715689420563186962, 0.3310798223114407302 ) ) ;
#22341=CARTESIAN_POINT ( 'NONE',  ( 0.2561730234726187216, -0.9528060625594280131, 0.4936757400543403396 ) ) ;
#22342=ADVANCED_FACE ( 'NONE', ( #21061 ), #15623, .F. ) ;
#22347=CARTESIAN_POINT ( 'NONE',  ( 0.5809782845877130564, -1.495266891998359382, 0.5744612900028297497 ) ) ;
#22350=CARTESIAN_POINT ( 'NONE',  ( 0.1204904522838102926, -0.7160080108176953839, 0.5344870570319224523 ) ) ;
#22351=CARTESIAN_POINT ( 'NONE',  ( 0.5255575159092462645, -1.179369731138129040, 0.4666486945702073563 ) ) ;
#22352=CARTESIAN_POINT ( 'NONE',  ( 0.6778058174389349766, -1.398346805643282620, 0.6444391890521875554 ) ) ;
#22353=CARTESIAN_POINT ( 'NONE',  ( 0.4209353462971754944, -1.136818033495635261, 0.4445034551534702283 ) ) ;
#22354=CARTESIAN_POINT ( 'NONE',  ( 0.06015859323110296641, -1.307383187822563020, 0.6320855273814715014 ) ) ;
#22358=CARTESIAN_POINT ( 'NONE',  ( 0.09719910960680759604, -0.8177032743061471987, 0.3260758418614409515 ) ) ;
#22364=CARTESIAN_POINT ( 'NONE',  ( 0.1746104702851725143, -0.8080234154602033980, 0.5960121186932698656 ) ) ;
#22367=CARTESIAN_POINT ( 'NONE',  ( 0.3332916228607076259, -1.159868621030426983, 0.5808959208038069200 ) ) ;
#22374=CARTESIAN_POINT ( 'NONE',  ( 0.4828762206425698533, -1.264095418145567251, 0.6661113250919497020 ) ) ;
#22376=CARTESIAN_POINT ( 'NONE',  ( 0.5744493500335104974, -1.624687623158924232, 0.5560814181295907765 ) ) ;
#22377=CARTESIAN_POINT ( 'NONE',  ( 0.4835150722484384267, -1.077540828773440484, 0.6059843185820091849 ) ) ;
#22380=DIRECTION ( 'NONE',  ( -0.8660512985181423318, -0.4999551463231871051, 0.000000000000000000 ) ) ;
#22382=CARTESIAN_POINT ( 'NONE',  ( 0.08947281526746891922, -0.7905738690218343523, 0.6404966654700502415 ) ) ;
#22384=CARTESIAN_POINT ( 'NONE',  ( 0.1109460505795314550, -0.9288804736197510126, 0.1344306538234449899 ) ) ;
#22388=EDGE_LOOP ( 'NONE', ( #27483, #36477, #40274, #39884 ) ) ;
#22390=CARTESIAN_POINT ( 'NONE',  ( 0.4930915531067465718, -1.082784575164420726, 0.5786337965014383133 ) ) ;
#22391=CARTESIAN_POINT ( 'NONE',  ( 0.1440976411593163087, -0.6767727035454040863, 0.4660634794818891424 ) ) ;
#22393=FACE_OUTER_BOUND ( 'NONE', #23935, .T. ) ;
#22397=CARTESIAN_POINT ( 'NONE',  ( 0.1855153659605877081, -0.8219892960459125320, 0.1767872597970533977 ) ) ;
#22398=FACE_OUTER_BOUND ( 'NONE', #38704, .T. ) ;
#22399=CARTESIAN_POINT ( 'NONE',  ( 0.3922565764085018114, -1.717990344284888060, 0.6205140842479107688 ) ) ;
#22400=CARTESIAN_POINT ( 'NONE',  ( 0.08833238169483845215, -0.6441912979656407856, 0.06334869283158285624 ) ) ;
#22401=CARTESIAN_POINT ( 'NONE',  ( 0.7394099696849650849, -1.503374687208528737, 0.6698237402283935271 ) ) ;
#22403=CARTESIAN_POINT ( 'NONE',  ( 0.1099113005465149340, -1.419268643255550355, 0.5685633924154458452 ) ) ;
#22405=CARTESIAN_POINT ( 'NONE',  ( 0.1003432527060652141, -1.374243440585479981, 0.6783211582849573151 ) ) ;
#22411=CARTESIAN_POINT ( 'NONE',  ( -8.537024980200822558E-17, -0.6872203660140397963, 0.1457185332388691301 ) ) ;
#22417=ORIENTED_EDGE ( 'NONE', *, *, #37555, .F. ) ;
#22420=VERTEX_POINT ( 'NONE', #19408 ) ;
#22425=CARTESIAN_POINT ( 'NONE',  ( 0.5935870542470136346, -1.451877841075679632, 0.6599787284733793502 ) ) ;
#22426=B_SPLINE_CURVE_WITH_KNOTS ( 'NONE', 3,
 ( #25494, #12523, #18704, #12726 ),
 .UNSPECIFIED., .F., .F.,
 ( 4, 4 ),
 ( 0.000000000000000000, 0.0005928691263773363217 ),
 .UNSPECIFIED. ) ;
#22429=ORIENTED_EDGE ( 'NONE', *, *, #18790, .F. ) ;
#22430=CARTESIAN_POINT ( 'NONE',  ( 0.5546634778460078907, -1.622195262996998233, 0.4988266963081158800 ) ) ;
#22432=CARTESIAN_POINT ( 'NONE',  ( 0.01967356235354560112, -0.6161222107093594635, 0.4019596896130384622 ) ) ;
#22434=CARTESIAN_POINT ( 'NONE',  ( 0.1123349855930559915, -0.8080303305208232922, -0.06315017404710350502 ) ) ;
#22438=CARTESIAN_POINT ( 'NONE',  ( 0.4047092701292824279, -1.701611041320455708, 0.4182417262808776903 ) ) ;
#22442=CARTESIAN_POINT ( 'NONE',  ( 0.1109778970610976606, -0.9286704811356188971, 0.1599727523405532759 ) ) ;
#22444=CARTESIAN_POINT ( 'NONE',  ( 0.5633198742680586291, -1.401022841391578400, 0.7649915433844801660 ) ) ;
#22445=CARTESIAN_POINT ( 'NONE',  ( 0.3523921359471319237, -1.112685253907127247, 0.7380400840877293644 ) ) ;
#22447=VECTOR ( 'NONE', #35717, 39.37007874015748854 ) ;
#22450=CARTESIAN_POINT ( 'NONE',  ( 0.4342919329069486190, -1.232046631451992225, 0.5547567841613109119 ) ) ;
#22451=CARTESIAN_POINT ( 'NONE',  ( 0.3254773505639530495, -1.768308184846890452, 0.5269442850043757343 ) ) ;
#22457=CARTESIAN_POINT ( 'NONE',  ( -0.01736481776669303659, -0.6872203660140440151, 0.1457185332388702681 ) ) ;
#22462=CARTESIAN_POINT ( 'NONE',  ( 0.3316976289008216061, -1.758220054772660745, 0.5638205628752049892 ) ) ;
#22466=CARTESIAN_POINT ( 'NONE',  ( 0.4830778208102094462, -1.123855190747131472, 0.5028193722743440341 ) ) ;
#22468=CARTESIAN_POINT ( 'NONE',  ( 0.1056036318510553268, -1.411794347249417880, 0.5652933847224521635 ) ) ;
#22470=CARTESIAN_POINT ( 'NONE',  ( 0.2709457873140602158, -1.674456041952191887, 0.6046742933308183465 ) ) ;
#22471=CARTESIAN_POINT ( 'NONE',  ( 0.1358503106379023995, -0.5959801875305653640, 0.3049145827815397669 ) ) ;
#22473=EDGE_LOOP ( 'NONE', ( #23730, #32181, #31506 ) ) ;
#22475=ORIENTED_EDGE ( 'NONE', *, *, #28545, .F. ) ;
#22483=CARTESIAN_POINT ( 'NONE',  ( 0.3048157867855714742, -1.756814508404978215, 0.5624209259133406968 ) ) ;
#22485=CARTESIAN_POINT ( 'NONE',  ( 0.1593808023014779141, -0.8351711200615056230, 0.5495798524048867151 ) ) ;
#22486=CARTESIAN_POINT ( 'NONE',  ( 0.08990954768171793843, -0.5436503405977816117, 0.1466997848779070523 ) ) ;
#22487=CARTESIAN_POINT ( 'NONE',  ( 0.4534567705953844730, -1.373683393137863584, 0.8250533907914637810 ) ) ;
#22490=CARTESIAN_POINT ( 'NONE',  ( 0.6947424619376043609, -1.490652314882815688, 0.4500177634849870101 ) ) ;
#22492=CARTESIAN_POINT ( 'NONE',  ( 0.3447343635093774172, -1.745799762367185926, 0.5848968271157334309 ) ) ;
#22493=CARTESIAN_POINT ( 'NONE',  ( 0.6290611267951696783, -1.457193995254231433, 0.8259264861884191289 ) ) ;
#22496=CARTESIAN_POINT ( 'NONE',  ( 0.1353763015934749681, -0.5739868718191323271, 0.2449457213022636637 ) ) ;
#22505=CARTESIAN_POINT ( 'NONE',  ( 0.2247355409086003175, -0.8309010600190726015, 0.4364284219733364223 ) ) ;
#22514=EDGE_LOOP ( 'NONE', ( #26026, #11419, #1941, #30665, #27085, #36424, #18796 ) ) ;
#22517=CARTESIAN_POINT ( 'NONE',  ( 0.08760676156666630243, -0.6788582240935653322, 0.02273922730970788161 ) ) ;
#22518=ORIENTED_EDGE ( 'NONE', *, *, #36623, .T. ) ;
#22520=CARTESIAN_POINT ( 'NONE',  ( 0.1482163224994231254, -1.323752227822259542, 0.6994010967223863728 ) ) ;
#22523=CARTESIAN_POINT ( 'NONE',  ( 0.1625982857068778153, -0.6782215948270849948, 0.2386756342038218459 ) ) ;
#22531=CARTESIAN_POINT ( 'NONE',  ( 0.008654831750343138300, -0.6462809503128671418, -0.007129606758741551496 ) ) ;
#22535=CARTESIAN_POINT ( 'NONE',  ( 0.09006073176016128612, -0.5638610315313903332, 0.1703137466647555442 ) ) ;
#22538=FACE_OUTER_BOUND ( 'NONE', #11832, .T. ) ;
#22540=CARTESIAN_POINT ( 'NONE',  ( 0.09462334978017705733, -0.6107534901994555732, 0.3586568835318235116 ) ) ;
#22543=CARTESIAN_POINT ( 'NONE',  ( 0.01364417761961938744, -0.8803303390833581155, 0.4681144232289236040 ) ) ;
#22544=CARTESIAN_POINT ( 'NONE',  ( 0.3576271336300551607, -1.040820894166447630, 0.6313593842330901262 ) ) ;
#22547=CARTESIAN_POINT ( 'NONE',  ( 0.1153471661799955333, -0.4465907051537503225, 0.1446142472693831005 ) ) ;
#22553=EDGE_CURVE ( 'NONE', #16305, #16916, #28717, .T. ) ;
#22555=EDGE_CURVE ( 'NONE', #33041, #990, #19400, .T. ) ;
#22556=CARTESIAN_POINT ( 'NONE',  ( 0.5385451171429854744, -1.174625208511617114, 0.8096455807874475274 ) ) ;
#22557=CARTESIAN_POINT ( 'NONE',  ( 0.5112813987709829977, -1.114248626770950823, 0.5535915447156093405 ) ) ;
#22558=CARTESIAN_POINT ( 'NONE',  ( 0.02968583136207634046, -1.058910347371198268, 0.6069042338158797678 ) ) ;
#22561=CARTESIAN_POINT ( 'NONE',  ( 0.1954870513704480839, -0.7169417872080507959, 0.3287089370885468154 ) ) ;
#22562=CARTESIAN_POINT ( 'NONE',  ( 0.3385785554808135034, -1.058259937818618379, 0.7608351996376890858 ) ) ;
#22567=EDGE_CURVE ( 'NONE', #4940, #22989, #31147, .T. ) ;
#22569=CARTESIAN_POINT ( 'NONE',  ( 0.4657365369423695500, -1.116270101206942922, 0.5666720171803257822 ) ) ;
#22570=CARTESIAN_POINT ( 'NONE',  ( 0.5953303036072959964, -1.457508885835639978, 0.6057417262805095959 ) ) ;
#22573=CARTESIAN_POINT ( 'NONE',  ( 0.09075956982381812310, -1.322849663306714829, 0.4537812744180037550 ) ) ;
#22574=ADVANCED_FACE ( 'NONE', ( #22393 ), #7685, .T. ) ;
#22576=ORIENTED_EDGE ( 'NONE', *, *, #20493, .T. ) ;
#22579=CARTESIAN_POINT ( 'NONE',  ( 0.1835632973924980760, -0.5276942279169911654, 0.2392151530743482357 ) ) ;
#22582=CARTESIAN_POINT ( 'NONE',  ( 0.4235506502418905916, -1.177630414603479281, 0.7006544390589145577 ) ) ;
#22585=B_SPLINE_CURVE_WITH_KNOTS ( 'NONE', 3,
 ( #13184, #295, #25754, #23449, #691, #508, #3741, #35967, #16294, #22468, #28422, #25139, #32117, #13942, #7773, #3922 ),
 .UNSPECIFIED., .F., .F.,
 ( 4, 2, 2, 2, 2, 2, 2, 4 ),
 ( 0.000000000000000000, 0.0008266127476143557374, 0.001239919121421530299, 0.001446572308325117526, 0.001549898901776911465, 0.001601562198502808326, 0.001627393846865756539, 0.001653225495228704970 ),
 .UNSPECIFIED. ) ;
#22586=CARTESIAN_POINT ( 'NONE',  ( 0.4471380481896147785, -1.057582006303192657, 0.6325253032963528144 ) ) ;
#22587=ORIENTED_EDGE ( 'NONE', *, *, #20039, .F. ) ;
#22589=CARTESIAN_POINT ( 'NONE',  ( 0.09351869311172626709, -1.333801252570538942, 0.7037513887513892064 ) ) ;
#22591=CARTESIAN_POINT ( 'NONE',  ( 0.03978348861078892518, -0.5859180147546816375, 0.3261096058830926236 ) ) ;
#22593=CARTESIAN_POINT ( 'NONE',  ( 0.2008473531602258111, -0.6365206772495614063, 0.3321400968866717318 ) ) ;
#22595=ORIENTED_EDGE ( 'NONE', *, *, #33089, .T. ) ;
#22597=ORIENTED_EDGE ( 'NONE', *, *, #22732, .F. ) ;
#22598=DIRECTION ( 'NONE',  ( 0.8543860900384366852, 0.5196387294542549329, -1.017227249256228896E-13 ) ) ;
#22599=CARTESIAN_POINT ( 'NONE',  ( 0.1167732631504307256, -0.5657854654953510254, 0.2312607435301864134 ) ) ;
#22601=CARTESIAN_POINT ( 'NONE',  ( 0.07043814880409834944, -1.334972480813817031, 0.5056242588139941985 ) ) ;
#22604=AXIS2_PLACEMENT_3D ( 'NONE', #29579, #24045, #17237 ) ;
#22609=CARTESIAN_POINT ( 'NONE',  ( 0.4079495573748788129, -1.708779812455338165, 0.6204884880800459745 ) ) ;
#22613=DIRECTION ( 'NONE',  ( -0.4999551463232372317, 0.8660512985181135770, -0.000000000000000000 ) ) ;
#22616=CARTESIAN_POINT ( 'NONE',  ( 0.1034728371066890584, -1.383544289075226974, 0.6669953293747845624 ) ) ;
#22618=DIRECTION ( 'NONE',  ( 0.9998941247116546194, -0.01455087607601020412, 0.0001066420868422379362 ) ) ;
#22620=CARTESIAN_POINT ( 'NONE',  ( 0.7062706752423565382, -1.445327451526715823, 0.7203384021836691797 ) ) ;
#22621=CARTESIAN_POINT ( 'NONE',  ( 0.2590435573837815419, -1.679512851806065576, 0.5266323208858617599 ) ) ;
#22623=CARTESIAN_POINT ( 'NONE',  ( 0.01037466073212112323, -0.7737952308255096057, 0.4846566707863347867 ) ) ;
#22624=CARTESIAN_POINT ( 'NONE',  ( -1.643206837334582843E-05, -0.7039665126479284218, -0.1033155573469211747 ) ) ;
#22627=CARTESIAN_POINT ( 'NONE',  ( 0.4115766028365042128, -1.733048369835246794, 0.5182417262812423209 ) ) ;
#22638=CARTESIAN_POINT ( 'NONE',  ( 0.5982972540623748836, -1.463353734898567238, 0.5950316300567694006 ) ) ;
#22643=CARTESIAN_POINT ( 'NONE',  ( 0.1996512133853552973, -0.6037243375952904278, 0.3287643322477424301 ) ) ;
#22646=CARTESIAN_POINT ( 'NONE',  ( 0.2811029688069974775, -1.576922886774730026, 0.8430380186458928948 ) ) ;
#22649=FACE_OUTER_BOUND ( 'NONE', #9856, .T. ) ;
#22655=CARTESIAN_POINT ( 'NONE',  ( 0.1863396098874236240, -0.9154215460517445280, 0.1638900048413362009 ) ) ;
#22657=CARTESIAN_POINT ( 'NONE',  ( 0.5952542337618718093, -1.458258124885792872, 0.5925654897410345123 ) ) ;
#22658=CARTESIAN_POINT ( 'NONE',  ( 0.2663031117850838680, -1.076423138501223509, 0.7428620000047612137 ) ) ;
#22660=AXIS2_PLACEMENT_3D ( 'NONE', #18361, #9297, #21875 ) ;
#22662=CARTESIAN_POINT ( 'NONE',  ( 0.1840595033465176056, -0.8547675690073376353, 0.1457166466292989515 ) ) ;
#22664=VECTOR ( 'NONE', #25025, 39.37007874015748143 ) ;
#22665=CARTESIAN_POINT ( 'NONE',  ( 0.005980720888701209978, -0.8455916207747946611, 0.1457185332388707122 ) ) ;
#22671=CARTESIAN_POINT ( 'NONE',  ( 0.2920835003669574048, -1.623987781970284594, 0.9481157836879084977 ) ) ;
#22673=CARTESIAN_POINT ( 'NONE',  ( 0.1102619990977181802, -1.417135361233744728, 0.5934404726580401190 ) ) ;
#22683=CARTESIAN_POINT ( 'NONE',  ( 0.2687519046691748126, -1.687296055496309677, 0.6251195327720597827 ) ) ;
#22684=CIRCLE ( 'NONE', #10830, 0.03749999999977554621 ) ;
#22685=CARTESIAN_POINT ( 'NONE',  ( 0.5948985926855137052, -1.487191034969570502, 0.5724586774276513301 ) ) ;
#22687=DIRECTION ( 'NONE',  ( -0.4999551463232372317, 0.8660512985181134660, 6.869252350113302335E-17 ) ) ;
#22698=CARTESIAN_POINT ( 'NONE',  ( 0.0001922330474179282408, -0.9534082139883226503, 0.1483282180229331948 ) ) ;
#22700=CARTESIAN_POINT ( 'NONE',  ( 0.1642392807452758841, -0.8691899957643679508, 0.5538582745929433448 ) ) ;
#22702=CARTESIAN_POINT ( 'NONE',  ( 0.08990936761269098521, -0.5436479961250846316, 0.1460913089649385210 ) ) ;
#22703=CARTESIAN_POINT ( 'NONE',  ( 0.1112219432785723217, -0.5687467704934952017, 0.2435113322008175263 ) ) ;
#22704=EDGE_LOOP ( 'NONE', ( #8499, #2438, #35817, #29148 ) ) ;
#22708=CARTESIAN_POINT ( 'NONE',  ( 0.1048591973540500683, -1.410537849644770025, 0.5682417262808777680 ) ) ;
#22709=CARTESIAN_POINT ( 'NONE',  ( 0.6944912789943821219, -1.426234547408998354, 0.6673110007802252053 ) ) ;
#22711=CARTESIAN_POINT ( 'NONE',  ( 0.5955909224605128172, -1.457896359989123480, 0.6966997756915641604 ) ) ;
#22712=CARTESIAN_POINT ( 'NONE',  ( 0.01176895705049121714, -0.6529346896220689089, -0.1114654361404705807 ) ) ;
#22714=CARTESIAN_POINT ( 'NONE',  ( 0.2322138788700108258, -1.233113307957229177, 0.3157417262808777658 ) ) ;
#22717=CARTESIAN_POINT ( 'NONE',  ( 0.04965997019300262549, -1.266850117287420696, 0.6475152895583352608 ) ) ;
#22718=CARTESIAN_POINT ( 'NONE',  ( 0.2182827306251404198, -0.8246641648518335810, 0.4150641157079975052 ) ) ;
#22725=( BOUNDED_SURFACE ( )  B_SPLINE_SURFACE ( 3, 2, ( 
 ( #5875, #15755, #28306 ),
 ( #18437, #30988, #12664 ),
 ( #2812, #27918, #15360 ),
 ( #22358, #37362, #31407 ),
 ( #37771, #24639, #9592 ),
 ( #22170, #34683, #6690 ),
 ( #9173, #25021, #6080 ),
 ( #6488, #8986, #21554 ),
 ( #36560, #28727, #31209 ),
 ( #3028, #15572, #12889 ),
 ( #34882, #37552, #9376 ),
 ( #21956, #19059, #34483 ),
 ( #25446, #37977, #19267 ),
 ( #31807, #3622, #16186 ),
 ( #588, #29117, #25851 ),
 ( #35297, #38764, #19862 ),
 ( #20080, #7090, #10208 ),
 ( #23168, #775, #4601 ),
 ( #979, #16787, #32397 ),
 ( #16981, #6897, #20279 ),
 ( #7285, #26445, #10813 ),
 ( #35480, #9993, #13493 ),
 ( #13281, #26059, #29521 ),
 ( #3814, #17177, #19470 ),
 ( #32195, #28909, #32609 ),
 ( #22775, #35093, #35697 ),
 ( #22562, #16370, #38169 ),
 ( #7501, #10397, #38369 ),
 ( #19659, #32003, #23388 ),
 ( #29723, #4010, #4220 ),
 ( #38578, #13082, #16573 ),
 ( #38981, #29334, #26243 ),
 ( #13680, #22960, #1180 ),
 ( #32800, #10595, #4421 ),
 ( #35904, #1361, #13870 ),
 ( #7712, #25637, #20690 ),
 ( #14907, #1567, #24370 ),
 ( #39796, #27465, #33222 ),
 ( #36096, #21293, #1966 ),
 ( #14702, #33004, #8110 ),
 ( #39582, #36708, #17595 ),
 ( #7901, #5226, #20472 ) ),
 .UNSPECIFIED., .F., .F., .T. ) 
 B_SPLINE_SURFACE_WITH_KNOTS ( ( 4, 2, 2, 2, 2, 2, 2, 2, 2, 2, 2, 2, 2, 2, 2, 2, 2, 2, 2, 2, 4 ),
 ( 3, 3 ),
 ( 0.007479710391323436854, 0.01100368895397634515, 0.01452766751662925432, 0.01628965679795570803, 0.01805164607928216175, 0.01981363536060861547, 0.02069463000127184232, 0.02157562464193507265, 0.02333761392326152984, 0.02421860856392475669, 0.02509960320458798355, 0.02598059784525121041, 0.02686159248591443727, 0.02774258712657766413, 0.02862358176724089098, 0.02950457640790411784, 0.03038557104856734470, 0.03214756032989379841, 0.03302855497055702527, 0.03390954961122025213, 0.03567153889254670585 ),
 ( 0.000000000000000000, 1.000000000000000000 ),
 .UNSPECIFIED. ) 
 GEOMETRIC_REPRESENTATION_ITEM ( )  RATIONAL_B_SPLINE_SURFACE ( (
 ( 1.000000000000000000, 0.7659916417601224659, 1.000000000000000000),
 ( 1.000000000000000000, 0.7660618423663158039, 1.000000000000000000),
 ( 1.000000000000000000, 0.7663819230775843483, 1.000000000000000000),
 ( 1.000000000000000000, 0.7675928100430011725, 1.000000000000000000),
 ( 1.000000000000000000, 0.7687294063333358629, 1.000000000000000000),
 ( 1.000000000000000000, 0.7716951888074965460, 1.000000000000000000),
 ( 1.000000000000000000, 0.7729019889268164967, 1.000000000000000000),
 ( 1.000000000000000000, 0.7757527099395760128, 1.000000000000000000),
 ( 1.000000000000000000, 0.7773719702424962685, 1.000000000000000000),
 ( 1.000000000000000000, 0.7807403279777797023, 1.000000000000000000),
 ( 1.000000000000000000, 0.7824602495331657304, 1.000000000000000000),
 ( 1.000000000000000000, 0.7843589238246971851, 1.000000000000000000),
 ( 1.000000000000000000, 0.7848581668868191974, 1.000000000000000000),
 ( 1.000000000000000000, 0.7852721754964663292, 1.000000000000000000),
 ( 1.000000000000000000, 0.7851778104893205601, 1.000000000000000000),
 ( 1.000000000000000000, 0.7835785179914779297, 1.000000000000000000),
 ( 1.000000000000000000, 0.7804117671199929385, 1.000000000000000000),
 ( 1.000000000000000000, 0.7725400516492265668, 1.000000000000000000),
 ( 1.000000000000000000, 0.7694933636094736240, 1.000000000000000000),
 ( 1.000000000000000000, 0.7633371169485945185, 1.000000000000000000),
 ( 1.000000000000000000, 0.7602722165944099109, 1.000000000000000000),
 ( 1.000000000000000000, 0.7547023054668801079, 1.000000000000000000),
 ( 1.000000000000000000, 0.7521850639428176999, 1.000000000000000000),
 ( 1.000000000000000000, 0.7476002769756485700, 1.000000000000000000),
 ( 1.000000000000000000, 0.7455123382604045279, 1.000000000000000000),
 ( 1.000000000000000000, 0.7415958813887417733, 1.000000000000000000),
 ( 1.000000000000000000, 0.7397619986562821159, 1.000000000000000000),
 ( 1.000000000000000000, 0.7361471414609971342, 1.000000000000000000),
 ( 1.000000000000000000, 0.7343594884252070409, 1.000000000000000000),
 ( 1.000000000000000000, 0.7309782830180014956, 1.000000000000000000),
 ( 1.000000000000000000, 0.7293746573561863400, 1.000000000000000000),
 ( 1.000000000000000000, 0.7264315972118717823, 1.000000000000000000),
 ( 1.000000000000000000, 0.7250888023308159624, 1.000000000000000000),
 ( 1.000000000000000000, 0.7216279031333409089, 1.000000000000000000),
 ( 1.000000000000000000, 0.7203114455652043224, 1.000000000000000000),
 ( 1.000000000000000000, 0.7183868100543469026, 1.000000000000000000),
 ( 1.000000000000000000, 0.7177772480437595304, 1.000000000000000000),
 ( 1.000000000000000000, 0.7162016412217627748, 1.000000000000000000),
 ( 1.000000000000000000, 0.7153339323267929872, 1.000000000000000000),
 ( 1.000000000000000000, 0.7125888713840239364, 1.000000000000000000),
 ( 1.000000000000000000, 0.7104034760854559538, 1.000000000000000000),
 ( 1.000000000000000000, 0.7083861251860454900, 1.000000000000000000) ) ) 
 REPRESENTATION_ITEM ( '' )  SURFACE ( )  );
#22727=CARTESIAN_POINT ( 'NONE',  ( 0.4517177305807006937, -1.568671020668126914, 0.6057417262804751790 ) ) ;
#22728=CARTESIAN_POINT ( 'NONE',  ( 0.002297679438261008168, -0.5200315581813911292, 0.1541446757893583930 ) ) ;
#22731=CARTESIAN_POINT ( 'NONE',  ( 0.1223045647424210181, -1.412159682085746271, 0.4849083929475432320 ) ) ;
#22732=EDGE_CURVE ( 'NONE', #38394, #4902, #23793, .T. ) ;
#22733=CARTESIAN_POINT ( 'NONE',  ( 0.6674886243000348607, -1.379560724353076306, 0.6935688206045713677 ) ) ;
#22737=FACE_OUTER_BOUND ( 'NONE', #25840, .T. ) ;
#22741=VECTOR ( 'NONE', #18619, 39.37007874015748143 ) ;
#22744=CARTESIAN_POINT ( 'NONE',  ( 0.09375000000000012490, -0.4427825420493726183, 0.1457185332388693244 ) ) ;
#22746=CARTESIAN_POINT ( 'NONE',  ( 0.09028630236563642275, -0.6068359833129397529, 0.1815368149905945694 ) ) ;
#22747=B_SPLINE_CURVE_WITH_KNOTS ( 'NONE', 3,
 ( #6072, #34261, #9165, #40026, #40641, #21727 ),
 .UNSPECIFIED., .F., .F.,
 ( 4, 2, 4 ),
 ( 0.000000000000000000, 0.5000000000000000000, 1.000000000000000000 ),
 .UNSPECIFIED. ) ;
#22748=CARTESIAN_POINT ( 'NONE',  ( 0.004052029362975025431, -0.4904197722336705589, 0.3777681374143450621 ) ) ;
#22749=CARTESIAN_POINT ( 'NONE',  ( 0.08534804946041728291, -0.5449560838406929397, 0.1719968967555055850 ) ) ;
#22752=CARTESIAN_POINT ( 'NONE',  ( 0.02261441518021851602, -0.9148528262931132637, 0.5668782753494319149 ) ) ;
#22753=CARTESIAN_POINT ( 'NONE',  ( 0.1478010146435930483, -0.9292797905990020091, 0.2962792169381038287 ) ) ;
#22758=CARTESIAN_POINT ( 'NONE',  ( 0.3762269255763664999, -1.611863304361743854, 0.5413035033958920605 ) ) ;
#22766=CARTESIAN_POINT ( 'NONE',  ( 0.5394647426574938898, -1.171356344921436365, 0.5164463399402798860 ) ) ;
#22768=CARTESIAN_POINT ( 'NONE',  ( 0.5691520580847880817, -1.222151117369431939, 0.8040585553043922973 ) ) ;
#22770=CARTESIAN_POINT ( 'NONE',  ( 0.05183675104700934816, -1.280743812480995780, 0.6394744559116233296 ) ) ;
#22775=CARTESIAN_POINT ( 'NONE',  ( 0.3323313641875296764, -1.048848748898059124, 0.7591878350141942899 ) ) ;
#22777=CARTESIAN_POINT ( 'NONE',  ( 0.6894585631977647733, -1.505591693816618282, 0.4630974732098093738 ) ) ;
#22785=CARTESIAN_POINT ( 'NONE',  ( 0.1497070752459234155, -1.041491121288300681, 0.7282887345088536746 ) ) ;
#22793=CARTESIAN_POINT ( 'NONE',  ( 0.4740991274768489583, -1.249207495721872840, 0.6570441671156094232 ) ) ;
#22795=CARTESIAN_POINT ( 'NONE',  ( 0.3247324306351095924, -1.759421949583082734, 0.4854534786567432647 ) ) ;
#22796=CARTESIAN_POINT ( 'NONE',  ( 0.4929433234940127639, -1.082713786091526353, 0.5692160337251114255 ) ) ;
#22803=CARTESIAN_POINT ( 'NONE',  ( 0.05410802736446353872, -0.5974446213890977075, 0.3459503305939781725 ) ) ;
#22804=CARTESIAN_POINT ( 'NONE',  ( 0.06602991763110438450, -0.7534794085705573963, 0.01325795176106262310 ) ) ;
#22805=CARTESIAN_POINT ( 'NONE',  ( 0.01128677947712186484, -0.9461986806730106059, 0.1457185332388702959 ) ) ;
#22806=CARTESIAN_POINT ( 'NONE',  ( 0.06727760473923048712, -0.6490144398117091429, 0.002857611472789892224 ) ) ;
#22809=CIRCLE ( 'NONE', #30689, 0.04749999999977550652 ) ;
#22810=CARTESIAN_POINT ( 'NONE',  ( 0.4931437851155135443, -1.083180748979025498, 0.5665107511466522805 ) ) ;
#22811=CARTESIAN_POINT ( 'NONE',  ( 0.1718176880793481076, -0.7513250685104085891, 0.5656676516626540918 ) ) ;
#22812=EDGE_LOOP ( 'NONE', ( #17288, #6170, #36622, #29806 ) ) ;
#22813=CARTESIAN_POINT ( 'NONE',  ( 0.06896958704128998419, -1.329019900465761905, 0.4989856710699280273 ) ) ;
#22815=ADVANCED_FACE ( 'NONE', ( #23613 ), #3015, .F. ) ;
#22820=CARTESIAN_POINT ( 'NONE',  ( 0.08750868709893994124, -0.6856954311291793003, 0.06271735481263093770 ) ) ;
#22822=CARTESIAN_POINT ( 'NONE',  ( 0.7370562124357561418, -1.515684240363464941, 0.4449423861150900716 ) ) ;
#22824=CARTESIAN_POINT ( 'NONE',  ( 0.06690724611807970235, -1.340115547279100428, 0.5315811339006457636 ) ) ;
#22825=DIRECTION ( 'NONE',  ( 0.1010117037271631713, 0.05706541553526763705, -0.9932472874666826712 ) ) ;
#22829=CARTESIAN_POINT ( 'NONE',  ( 0.1685272260733683414, -1.385079421489360474, 0.5084237370591300209 ) ) ;
#22830=CARTESIAN_POINT ( 'NONE',  ( 0.1850180133982991526, -0.7563345632739647550, -0.01070758755936668249 ) ) ;
#22832=CARTESIAN_POINT ( 'NONE',  ( 0.2646723247128293655, -1.687375416948911244, 0.5682417262808783232 ) ) ;
#22833=CARTESIAN_POINT ( 'NONE',  ( 0.09565263806948612335, -1.148840486724431953, 0.8358535653919648700 ) ) ;
#22834=CARTESIAN_POINT ( 'NONE',  ( -0.0001800219140582012974, -0.8396310703285838617, -0.05215014162539268611 ) ) ;
#22835=B_SPLINE_CURVE_WITH_KNOTS ( 'NONE', 3,
 ( #31415, #3217, #21748, #28916, #15765, #10000 ),
 .UNSPECIFIED., .F., .F.,
 ( 4, 2, 4 ),
 ( 0.000000000000000000, 0.5000000000000002220, 1.000000000000000000 ),
 .UNSPECIFIED. ) ;
#22839=CARTESIAN_POINT ( 'NONE',  ( 0.2073148280362371032, -1.247401114506933917, 0.4282226788861551725 ) ) ;
#22842=ADVANCED_FACE ( 'NONE', ( #20927 ), #7181, .F. ) ;
#22848=CARTESIAN_POINT ( 'NONE',  ( 0.5184242004029562256, -1.327098421978155640, 0.7590059521294971745 ) ) ;
#22851=CARTESIAN_POINT ( 'NONE',  ( 0.3219050788564604137, -0.8784703629548025194, 0.6443316309767920247 ) ) ;
#22856=CARTESIAN_POINT ( 'NONE',  ( 0.3272817739344252574, -1.639265242723384697, 0.5775048433984611984 ) ) ;
#22857=CARTESIAN_POINT ( 'NONE',  ( 0.6119653131825866232, -1.588158183054942496, 0.4221774592016356298 ) ) ;
#22858=DIRECTION ( 'NONE',  ( 1.000000000000000000, 0.000000000000000000, 0.000000000000000000 ) ) ;
#22859=CARTESIAN_POINT ( 'NONE',  ( 0.3066658489686008293, -1.757170713505755710, 0.5393683295168898439 ) ) ;
#22865=CARTESIAN_POINT ( 'NONE',  ( 0.2666607338143368588, -0.9575770305785957781, 0.5134922487128943391 ) ) ;
#22867=CARTESIAN_POINT ( 'NONE',  ( 0.5965761245944036784, -1.493465029535157029, 0.5182417262812423209 ) ) ;
#22869=CARTESIAN_POINT ( 'NONE',  ( 0.1391441241210990831, -0.8698021353542626510, 0.5024695666797485138 ) ) ;
#22870=CARTESIAN_POINT ( 'NONE',  ( 0.01057097757788910339, -0.5312311850581503681, 0.1694607747591961866 ) ) ;
#22871=ADVANCED_FACE ( 'NONE', ( #23939 ), #35554, .T. ) ;
#22873=EDGE_CURVE ( 'NONE', #5090, #8849, #39987, .T. ) ;
#22880=CARTESIAN_POINT ( 'NONE',  ( 0.1835961851041346959, -0.5126270562563732813, 0.08826789480522242992 ) ) ;
#22885=CARTESIAN_POINT ( 'NONE',  ( 0.4820730268389710194, -1.120100422993975275, 0.5182417262812748504 ) ) ;
#22887=CARTESIAN_POINT ( 'NONE',  ( 0.2613660211529243438, -1.686120988816170119, 0.5257579584705852627 ) ) ;
#22889=CARTESIAN_POINT ( 'NONE',  ( 0.1380264030324899749, -0.6050966432626355695, 0.3254296826921013741 ) ) ;
#22890=VERTEX_POINT ( 'NONE', #26819 ) ;
#22893=EDGE_CURVE ( 'NONE', #17370, #1876, #21253, .T. ) ;
#22895=ORIENTED_EDGE ( 'NONE', *, *, #6998, .F. ) ;
#22897=ORIENTED_EDGE ( 'NONE', *, *, #15988, .F. ) ;
#22901=CARTESIAN_POINT ( 'NONE',  ( 0.0003981076881877283497, -0.5275076572294771227, -0.1178596299512809226 ) ) ;
#22902=ORIENTED_EDGE ( 'NONE', *, *, #20575, .F. ) ;
#22903=CARTESIAN_POINT ( 'NONE',  ( 0.08507626058706400929, -0.7891241300377995760, 0.1593484486019202950 ) ) ;
#22904=CIRCLE ( 'NONE', #32734, 0.01000000000000002970 ) ;
#22905=CARTESIAN_POINT ( 'NONE',  ( 0.08991945692117814248, -0.5437780353368280029, 0.1532396220041035706 ) ) ;
#22906=CARTESIAN_POINT ( 'NONE',  ( 0.1110044217621600354, -0.5667795212461463894, 0.2377383413596886597 ) ) ;
#22908=CARTESIAN_POINT ( 'NONE',  ( 0.1766140053765036799, -0.4884607529735562892, 0.1457336358543773192 ) ) ;
#22909=CARTESIAN_POINT ( 'NONE',  ( 0.5848508152300195828, -1.486263022089187036, 0.6467108361231791447 ) ) ;
#22911=CARTESIAN_POINT ( 'NONE',  ( 0.4142925369596769380, -1.705023740597148008, 0.4226190609429597567 ) ) ;
#22913=CARTESIAN_POINT ( 'NONE',  ( 0.4368279861777725204, -1.677667223885754844, 0.4182417262808776903 ) ) ;
#22915=CARTESIAN_POINT ( 'NONE',  ( 0.1390279997722746186, -0.5963079674089665216, 0.3040810692042346108 ) ) ;
#22916=CARTESIAN_POINT ( 'NONE',  ( 1.598725267176023850E-05, -0.6709277514742212345, -0.1033257619575898290 ) ) ;
#22920=CARTESIAN_POINT ( 'NONE',  ( 0.1120276941441372132, -1.367097346105948130, 0.7195291715619951400 ) ) ;
#22921=CARTESIAN_POINT ( 'NONE',  ( 0.2122887247597850247, -0.8188226314918697346, 0.3927370908608381339 ) ) ;
#22924=DIRECTION ( 'NONE',  ( 0.000000000000000000, -0.9804888279246389837, -0.1965748160751215334 ) ) ;
#22927=CARTESIAN_POINT ( 'NONE',  ( 0.002367394983765751248, -0.5282119844061630154, 0.1467999231854355824 ) ) ;
#22928=CARTESIAN_POINT ( 'NONE',  ( 0.1029498318846682331, -1.296234522660387967, 0.4455275691814166161 ) ) ;
#22929=ORIENTED_EDGE ( 'NONE', *, *, #28342, .F. ) ;
#22930=CARTESIAN_POINT ( 'NONE',  ( 0.1438070510857625550, -1.283988175806205723, 0.3667417262808778111 ) ) ;
#22931=CARTESIAN_POINT ( 'NONE',  ( 0.6265937217076796850, -1.312621381056858993, 0.7675331558851111735 ) ) ;
#22941=CARTESIAN_POINT ( 'NONE',  ( 0.000000000000000000, -0.4262518876079541830, 0.1457185332388689636 ) ) ;
#22942=CARTESIAN_POINT ( 'NONE',  ( 0.09222453600979922672, -0.6532506521049682435, 0.2501001928013826259 ) ) ;
#22943=CARTESIAN_POINT ( 'NONE',  ( 0.01375146018318225069, -0.4678462169232188161, 0.3154892069967682455 ) ) ;
#22944=CARTESIAN_POINT ( 'NONE',  ( 0.3831456390985862326, -1.321512013252764906, 0.8548773317760315349 ) ) ;
#22946=CARTESIAN_POINT ( 'NONE',  ( 0.3512175092685453359, -1.737626439724724303, 0.4368660991148545780 ) ) ;
#22947=CARTESIAN_POINT ( 'NONE',  ( 0.06593013508327637273, -0.9837097893939223958, 0.4880478824260481852 ) ) ;
#22949=B_SPLINE_CURVE_WITH_KNOTS ( 'NONE', 3,
 ( #29302, #16542, #13250, #25817, #26028, #11596, #32773, #7868, #1754, #1938 ),
 .UNSPECIFIED., .F., .F.,
 ( 4, 2, 2, 2, 4 ),
 ( 9.931801139967757520E-05, 0.0004520544377635757880, 0.0008047908641274740009, 0.001157527290491372268, 0.001510263716855270427 ),
 .UNSPECIFIED. ) ;
#22951=CARTESIAN_POINT ( 'NONE',  ( 0.1922391936362386755, -0.4904811663640207819, 0.2844517592273411721 ) ) ;
#22954=CARTESIAN_POINT ( 'NONE',  ( 0.4845724100169539472, -1.091512197975673670, 0.8037230719241761356 ) ) ;
#22956=CARTESIAN_POINT ( 'NONE',  ( 0.5043831596453355326, -1.118121868638674687, 0.5040939098466322710 ) ) ;
#22960=CARTESIAN_POINT ( 'NONE',  ( 0.3894760245852240677, -1.134673749242862018, 0.7271684844242152224 ) ) ;
#22967=CARTESIAN_POINT ( 'NONE',  ( 0.3229289876128840775, -1.169687821100875658, 0.5631135379446852163 ) ) ;
#22968=CARTESIAN_POINT ( 'NONE',  ( 0.1213752263504523504, -0.9708261959865926993, 0.6725932955394058332 ) ) ;
#22976=CARTESIAN_POINT ( 'NONE',  ( 0.4058008863267686395, -1.155685782444805687, 0.7188585313195411386 ) ) ;
#22984=CARTESIAN_POINT ( 'NONE',  ( 0.04882066477899291851, -0.5577723668033041093, 0.2454755323597881955 ) ) ;
#22985=CARTESIAN_POINT ( 'NONE',  ( 0.06568576414414206699, -0.7783668077490022430, 0.02890612836029912355 ) ) ;
#22986=CARTESIAN_POINT ( 'NONE',  ( 0.2018873067935590404, -0.6340018868387371498, 0.3403718512341859515 ) ) ;
#22989=VERTEX_POINT ( 'NONE', #36673 ) ;
#22990=CARTESIAN_POINT ( 'NONE',  ( 0.4163860380882642431, -1.242336163338821464, 0.5827596682515493454 ) ) ;
#22991=CARTESIAN_POINT ( 'NONE',  ( 0.1282033164738295428, -0.6133254681109230333, 0.3496213826538958624 ) ) ;
#22996=CARTESIAN_POINT ( 'NONE',  ( 0.1858438793772869690, -0.7993314817513539339, 0.1881562487493555480 ) ) ;
#22997=ORIENTED_EDGE ( 'NONE', *, *, #13923, .T. ) ;
#22998=CARTESIAN_POINT ( 'NONE',  ( 0.3621582553283898553, -1.735977488954054904, 0.6111894207627336373 ) ) ;
#22999=CARTESIAN_POINT ( 'NONE',  ( 0.08596614173211629406, -0.8123625242870818886, 0.06126983391297252668 ) ) ;
#23001=CARTESIAN_POINT ( 'NONE',  ( 0.5961566725213064410, -1.266700452128206367, 0.8733730542187856383 ) ) ;
#23007=EDGE_CURVE ( 'NONE', #10513, #3992, #34574, .T. ) ;
#23008=ADVANCED_FACE ( 'NONE', ( #40149 ), #18354, .T. ) ;
#23009=B_SPLINE_CURVE_WITH_KNOTS ( 'NONE', 3,
 ( #39111, #1888, #36016, #16905, #20392, #23686, #33331, #19990, #4730, #29854, #14399, #29447, #14213, #8024, #20603, #5138 ),
 .UNSPECIFIED., .F., .F.,
 ( 4, 2, 2, 2, 2, 2, 2, 4 ),
 ( 0.000000000000000000, 0.0004900782238211935865, 0.0009801564476423871731, 0.001470234671463580651, 0.001960312895284774346, 0.002940469342927169976, 0.003430547566748366490, 0.003920625790569563437 ),
 .UNSPECIFIED. ) ;
#23013=ADVANCED_FACE ( 'NONE', ( #12582 ), #30641, .F. ) ;
#23014=CARTESIAN_POINT ( 'NONE',  ( 0.6960133515994678666, -1.427157319712460959, 0.5654899826020431952 ) ) ;
#23017=CARTESIAN_POINT ( 'NONE',  ( 0.001061621656357588511, -0.7083572002807602130, 0.2962098885571950446 ) ) ;
#23024=EDGE_CURVE ( 'NONE', #32680, #12748, #8894, .T. ) ;
#23025=CARTESIAN_POINT ( 'NONE',  ( 0.4970273525888077026, -1.079783658718535877, 0.3157417262808778213 ) ) ;
#23026=ORIENTED_EDGE ( 'NONE', *, *, #3181, .T. ) ;
#23029=CARTESIAN_POINT ( 'NONE',  ( 0.4164969987651618299, -1.171307339976814799, 0.7723814282107528406 ) ) ;
#23033=CARTESIAN_POINT ( 'NONE',  ( 0.1860214731903934160, -0.7916887388224913558, 0.2098883466634208494 ) ) ;
#23037=EDGE_LOOP ( 'NONE', ( #40519, #3422, #1845, #13106 ) ) ;
#23039=CARTESIAN_POINT ( 'NONE',  ( 0.3262830249888155620, -1.638891270961440272, 0.5636674631656366508 ) ) ;
#23042=CARTESIAN_POINT ( 'NONE',  ( 0.05567535398968421340, -1.335339640988971288, 0.4687417262808780127 ) ) ;
#23045=CARTESIAN_POINT ( 'NONE',  ( 0.3211485391366948883, -1.297382044030143344, 0.5018407269173935648 ) ) ;
#23046=CARTESIAN_POINT ( 'NONE',  ( 0.1880962557479734509, -0.9163805599553175307, 0.2154166370166123168 ) ) ;
#23049=CARTESIAN_POINT ( 'NONE',  ( 0.2226181049683592650, -0.9993126311397080297, 0.7099361533374629607 ) ) ;
#23050=CARTESIAN_POINT ( 'NONE',  ( 0.05236818520811117178, -0.8281183987458714535, 0.6957665626363849221 ) ) ;
#23060=CARTESIAN_POINT ( 'NONE',  ( 0.05838938100891326310, -1.295898982425970125, 0.6424779078687598011 ) ) ;
#23062=CARTESIAN_POINT ( 'NONE',  ( 0.1766140053765036799, -0.4884607529735562892, 0.1457336358543773192 ) ) ;
#23063=CARTESIAN_POINT ( 'NONE',  ( 0.1013956804831029068, -1.380631438172658543, 0.6556088357230328567 ) ) ;
#23069=CARTESIAN_POINT ( 'NONE',  ( 0.3086540466703007191, -1.716681333513715657, 0.8049923379735365314 ) ) ;
#23078=CARTESIAN_POINT ( 'NONE',  ( 0.6027046940806113362, -1.482916138156018748, 0.5916400363227261039 ) ) ;
#23082=ORIENTED_EDGE ( 'NONE', *, *, #39169, .T. ) ;
#23084=CARTESIAN_POINT ( 'NONE',  ( 0.6539706967335917609, -1.516592165152658822, 0.7560619644851708232 ) ) ;
#23086=FACE_OUTER_BOUND ( 'NONE', #24642, .T. ) ;
#23091=CARTESIAN_POINT ( 'NONE',  ( 0.001266334362739574958, -0.6339827964191881993, -0.06462206035643804081 ) ) ;
#23093=VERTEX_POINT ( 'NONE', #25144 ) ;
#23095=CARTESIAN_POINT ( 'NONE',  ( 0.09694425764873422502, -0.8015933583696732700, 0.3191342905503998240 ) ) ;
#23098=CARTESIAN_POINT ( 'NONE',  ( 0.1102974682193811340, -0.5579282852749359867, 0.2100915847438293294 ) ) ;
#23105=CARTESIAN_POINT ( 'NONE',  ( 0.4092943692574704251, -1.708139270546744415, 0.4222004656856017113 ) ) ;
#23110=CARTESIAN_POINT ( 'NONE',  ( 0.01175246436738983276, -0.6702937331852513170, -0.1131883302235354855 ) ) ;
#23111=CARTESIAN_POINT ( 'NONE',  ( 0.5246674523321896988, -1.372085926420510971, 0.7928523263102306151 ) ) ;
#23112=( NAMED_UNIT ( * ) SI_UNIT ( $, .STERADIAN. ) SOLID_ANGLE_UNIT ( ) );
#23113=EDGE_CURVE ( 'NONE', #6212, #28462, #19355, .T. ) ;
#23118=CARTESIAN_POINT ( 'NONE',  ( -0.003124719664520032511, -0.8057675726412022454, 0.1130684494947832019 ) ) ;
#23119=CARTESIAN_POINT ( 'NONE',  ( 0.3472154721327633808, -0.9812419721698063535, 0.6178014265861627718 ) ) ;
#23122=CARTESIAN_POINT ( 'NONE',  ( 0.6929208297549553919, -1.429122597532291650, 0.5682417262808779901 ) ) ;
#23127=CARTESIAN_POINT ( 'NONE',  ( 0.01117138305292090204, -0.5571624402049411007, 0.2649020760849408185 ) ) ;
#23132=CARTESIAN_POINT ( 'NONE',  ( 0.3323167458231998661, -1.749637683294404056, 0.4593311801905495262 ) ) ;
#23133=CARTESIAN_POINT ( 'NONE',  ( 0.5893014856854912331, -1.253657609334210665, 0.7958531859040811618 ) ) ;
#23135=ORIENTED_EDGE ( 'NONE', *, *, #37835, .F. ) ;
#23142=FACE_OUTER_BOUND ( 'NONE', #15939, .T. ) ;
#23143=CARTESIAN_POINT ( 'NONE',  ( 0.08789236658728763474, -0.6851542995134042302, 0.1774356670165384287 ) ) ;
#23144=CARTESIAN_POINT ( 'NONE',  ( 0.01825373427587153111, -0.5918760537899200314, 0.5452743738062094669 ) ) ;
#23145=CARTESIAN_POINT ( 'NONE',  ( 0.1049701980345018326, -0.6534432861451462404, 0.4406655119813854826 ) ) ;
#23146=CARTESIAN_POINT ( 'NONE',  ( 0.1145253369699427703, -0.4958736430966769193, -0.001267178298959518697 ) ) ;
#23148=CARTESIAN_POINT ( 'NONE',  ( 0.2135674535618494740, -1.112065761644619233, 0.6472873446657533281 ) ) ;
#23152=DIRECTION ( 'NONE',  ( 0.8406598760563539496, 0.5415634522278213181, 1.230192937850935930E-12 ) ) ;
#23153=CARTESIAN_POINT ( 'NONE',  ( 0.1159518160055648672, -0.4567671116231432071, 0.2228320516541739127 ) ) ;
#23161=DIRECTION ( 'NONE',  ( 0.4999551463232372317, -0.8660512985181135770, 0.000000000000000000 ) ) ;
#23162=CARTESIAN_POINT ( 'NONE',  ( 0.1906247196645203257, -0.5843772811062373229, 0.1513679272151527977 ) ) ;
#23163=CARTESIAN_POINT ( 'NONE',  ( 0.4133723901694114633, -1.141160002464131962, 0.4339463194546827607 ) ) ;
#23164=CARTESIAN_POINT ( 'NONE',  ( 0.007518266030304054416, -0.8543892252648230823, 0.3273543424587478379 ) ) ;
#23168=CARTESIAN_POINT ( 'NONE',  ( 0.2579846408969476701, -0.9486487916598037584, 0.7016806324682074436 ) ) ;
#23172=ORIENTED_EDGE ( 'NONE', *, *, #31529, .F. ) ;
#23178=CARTESIAN_POINT ( 'NONE',  ( 0.1669756386256049108, -1.085067953939178764, 0.7439077123735935437 ) ) ;
#23182=AXIS2_PLACEMENT_3D ( 'NONE', #6024, #2967, #328 ) ;
#23187=CARTESIAN_POINT ( 'NONE',  ( 0.4039508790787581516, -1.152909626704288204, 0.7080790044088270951 ) ) ;
#23188=EDGE_CURVE ( 'NONE', #10339, #1246, #38888, .T. ) ;
#23191=CARTESIAN_POINT ( 'NONE',  ( 0.2870562969094627714, -0.9697506529368410400, 0.5438065585693926396 ) ) ;
#23195=CARTESIAN_POINT ( 'NONE',  ( 0.3268282208471015582, -1.379742495938673930, 0.8813508202197246622 ) ) ;
#23197=CARTESIAN_POINT ( 'NONE',  ( 0.08863201702724371467, -0.6115582155368344264, 0.04856835249286290540 ) ) ;
#23198=CARTESIAN_POINT ( 'NONE',  ( 0.2005880444173030741, -0.7283351547258000158, 0.3314209756853015443 ) ) ;
#23199=CARTESIAN_POINT ( 'NONE',  ( 0.1217997580153728360, -1.296604091693217553, 0.4993402295728919804 ) ) ;
#23203=CARTESIAN_POINT ( 'NONE',  ( 0.5159274993618521155, -1.411867277967620238, 0.7865152916356047408 ) ) ;
#23207=B_SPLINE_CURVE_WITH_KNOTS ( 'NONE', 3,
 ( #4053, #22824, #7329, #35144 ),
 .UNSPECIFIED., .F., .F.,
 ( 4, 4 ),
 ( 1.748223473168675632E-18, 0.001015713385322552413 ),
 .UNSPECIFIED. ) ;
#23208=CARTESIAN_POINT ( 'NONE',  ( 0.6328777722953394802, -1.566953138837623882, 0.4182417262808777458 ) ) ;
#23209=CARTESIAN_POINT ( 'NONE',  ( 0.1422768683044231819, -1.284954004962210128, 0.4310363220745050405 ) ) ;
#23211=CARTESIAN_POINT ( 'NONE',  ( 0.008270684066414063854, -0.5292528935463532980, 0.1457206007561614447 ) ) ;
#23222=CARTESIAN_POINT ( 'NONE',  ( 0.1847224921572867273, -0.8249592463731384440, 0.04913026459056606815 ) ) ;
#23224=CARTESIAN_POINT ( 'NONE',  ( 0.1180873783825124868, -1.300942055715428758, 0.4272205016256891419 ) ) ;
#23226=CARTESIAN_POINT ( 'NONE',  ( 0.2142493868227219878, -1.379310565402303457, 1.003739045973664368 ) ) ;
#23229=DIRECTION ( 'NONE',  ( -0.9848077530122080203, -0.1736481776669303589, 2.792475675812634297E-17 ) ) ;
#23233=CARTESIAN_POINT ( 'NONE',  ( 0.05583995664670776682, -1.335624775257321817, 0.3157417262808777658 ) ) ;
#23234=ORIENTED_EDGE ( 'NONE', *, *, #22732, .T. ) ;
#23238=CARTESIAN_POINT ( 'NONE',  ( 0.3636646492274219766, -1.094494851808226699, 0.7706032642260752796 ) ) ;
#23241=CARTESIAN_POINT ( 'NONE',  ( 0.3816662009041032477, -0.9823246188028521564, 0.6672886469660396225 ) ) ;
#23248=CARTESIAN_POINT ( 'NONE',  ( 0.3305191838506285618, -1.637725477021584553, 0.6377116139030889475 ) ) ;
#23249=CARTESIAN_POINT ( 'NONE',  ( 0.2625973931889362678, -0.6796768235205253861, 0.1477649966949237115 ) ) ;
#23251=DIRECTION ( 'NONE',  ( 0.4849077135392313997, -0.8745653259477845776, 0.000000000000000000 ) ) ;
#23260=CARTESIAN_POINT ( 'NONE',  ( 0.1814429951780466566, -0.9296868405956840720, 0.6374604447006659846 ) ) ;
#23261=CARTESIAN_POINT ( 'NONE',  ( 0.01155947731736221493, -0.5664951642967490653, 0.2915036740642469870 ) ) ;
#23262=CARTESIAN_POINT ( 'NONE',  ( 0.4673063575290828386, -1.111595057335264647, 0.5567563882193511393 ) ) ;
#23264=CARTESIAN_POINT ( 'NONE',  ( 0.6632248500530988355, -1.473733142766466386, 0.4224342954051147347 ) ) ;
#23271=CARTESIAN_POINT ( 'NONE',  ( 0.01088233830205680326, -1.005040962621902345, 0.5452311825355896646 ) ) ;
#23272=CARTESIAN_POINT ( 'NONE',  ( 0.1637488714925408873, -0.5994898440788770655, 0.1932149833450298726 ) ) ;
#23277=ORIENTED_EDGE ( 'NONE', *, *, #36700, .T. ) ;
#23280=CARTESIAN_POINT ( 'NONE',  ( 0.4529143664019396609, -1.108999136783218153, 0.5738870192722926866 ) ) ;
#23286=CARTESIAN_POINT ( 'NONE',  ( 0.1776121323683093056, -0.4901272394318858527, 0.1210201606631986920 ) ) ;
#23287=VERTEX_POINT ( 'NONE', #10328 ) ;
#23288=CARTESIAN_POINT ( 'NONE',  ( 0.2580628395236652106, -1.678234314258598925, 0.5461929056667225169 ) ) ;
#23289=CARTESIAN_POINT ( 'NONE',  ( 0.3750645785205684035, -1.122292824651612397, 0.8025833334800251961 ) ) ;
#23290=CARTESIAN_POINT ( 'NONE',  ( 0.006933825066843425124, -0.8076031261048381982, 0.04254292565515345459 ) ) ;
#23296=CARTESIAN_POINT ( 'NONE',  ( -0.006114502025653725630, -0.6147594159447776763, 0.4101266738532061695 ) ) ;
#23303=CARTESIAN_POINT ( 'NONE',  ( 0.001051957896761219601, -0.5275076572294767896, -0.06462206035643838775 ) ) ;
#23305=ORIENTED_EDGE ( 'NONE', *, *, #37637, .F. ) ;
#23307=CARTESIAN_POINT ( 'NONE',  ( 0.1399519254280139069, -0.8623850441597388228, 0.4929895343781093842 ) ) ;
#23309=CARTESIAN_POINT ( 'NONE',  ( 0.1213787196452971867, -0.7177200554198521765, 0.5360780237648733459 ) ) ;
#23311=CARTESIAN_POINT ( 'NONE',  ( 0.1100557636787395099, -0.5505741347682650000, 0.1801202379966963252 ) ) ;
#23315=CARTESIAN_POINT ( 'NONE',  ( 0.6615779634392502384, -1.540590691117124322, 0.4334491422028962648 ) ) ;
#23316=CARTESIAN_POINT ( 'NONE',  ( 0.3293809238194490563, -1.753471329581329119, 0.5621866716956569476 ) ) ;
#23317=CARTESIAN_POINT ( 'NONE',  ( 0.6937322149078435363, -1.428803319834411001, 0.5909098324580162043 ) ) ;
#23323=CARTESIAN_POINT ( 'NONE',  ( 0.01180359879124304526, -0.6193534279860481995, -0.1047011498718341121 ) ) ;
#23325=CARTESIAN_POINT ( 'NONE',  ( 0.09245883518616107577, -0.6465694857495450920, 0.4344858352814658375 ) ) ;
#23328=CARTESIAN_POINT ( 'NONE',  ( -0.0004320282599767403219, -0.9107381779821550616, 0.3274798035714688860 ) ) ;
#23329=CARTESIAN_POINT ( 'NONE',  ( 0.4924424051965485827, -1.082438949443123688, 0.5780025781777323735 ) ) ;
#23331=CARTESIAN_POINT ( 'NONE',  ( 0.3390826044135689665, -0.8321809361840178942, 0.7462327844847882474 ) ) ;
#23333=AXIS2_PLACEMENT_3D ( 'NONE', #34418, #25577, #12605 ) ;
#23335=CARTESIAN_POINT ( 'NONE',  ( 0.3084895503185087207, -1.760900578822133467, 0.5693513805774124137 ) ) ;
#23337=CIRCLE ( 'NONE', #2301, 0.04749999999977556897 ) ;
#23344=CARTESIAN_POINT ( 'NONE',  ( 0.06486042810549992599, -1.341249661891149803, 0.5682417262808776570 ) ) ;
#23345=AXIS2_PLACEMENT_3D ( 'NONE', #17021, #36133, #4647 ) ;
#23346=CARTESIAN_POINT ( 'NONE',  ( 0.5385451171429854744, -1.174625208511617114, 0.8096455807874475274 ) ) ;
#23347=ORIENTED_EDGE ( 'NONE', *, *, #4454, .T. ) ;
#23357=ORIENTED_EDGE ( 'NONE', *, *, #10546, .F. ) ;
#23358=CARTESIAN_POINT ( 'NONE',  ( 0.05153374671598465878, -0.6956169804826777270, 0.7932021015506084405 ) ) ;
#23359=CARTESIAN_POINT ( 'NONE',  ( 0.1445017185149053141, -0.7748226788906442675, 0.5206329989080951126 ) ) ;
#23360=CARTESIAN_POINT ( 'NONE',  ( 0.1921532005765090867, -1.222151250233040942, 1.020715813206927614 ) ) ;
#23361=CARTESIAN_POINT ( 'NONE',  ( 0.4713144649729504865, -1.557651269372687608, 0.6044819294908458929 ) ) ;
#23362=CARTESIAN_POINT ( 'NONE',  ( 0.2398555970347700794, -1.530130166554039439, 0.9080419457258624982 ) ) ;
#23363=CARTESIAN_POINT ( 'NONE',  ( 0.2687203115727492264, -1.674044157977605529, 0.5754666865148680976 ) ) ;
#23364=CARTESIAN_POINT ( 'NONE',  ( 0.2565301720564582832, -1.029081863103397554, 0.6124915876908022527 ) ) ;
#23370=CARTESIAN_POINT ( 'NONE',  ( 0.1907289319405431338, -0.5457051035001712069, 0.2140866037401576716 ) ) ;
#23380=VECTOR ( 'NONE', #10490, 39.37007874015748854 ) ;
#23381=CARTESIAN_POINT ( 'NONE',  ( 0.1175190731393374044, -1.414871271504619221, 0.5257910806408424564 ) ) ;
#23382=CARTESIAN_POINT ( 'NONE',  ( 0.5536319580448211264, -1.193555294463456873, 0.7337749688435845075 ) ) ;
#23384=CARTESIAN_POINT ( 'NONE',  ( 0.02317288298003269270, -0.9573509765991652376, 0.6276687800861534550 ) ) ;
#23386=CARTESIAN_POINT ( 'NONE',  ( 0.3245308759113119113, -1.295391163961464365, 0.5682442948123348492 ) ) ;
#23388=CARTESIAN_POINT ( 'NONE',  ( 0.3351423068873352062, -1.099926675622169725, 0.7404414555003379084 ) ) ;
#23398=DIMENSIONAL_EXPONENTS ( 1.000000000000000000, 0.000000000000000000, 0.000000000000000000, 0.000000000000000000, 0.000000000000000000, 0.000000000000000000, 0.000000000000000000 ) ;
#23399=CARTESIAN_POINT ( 'NONE',  ( 0.06321419030197487909, -0.8491159278358076934, 0.3547255550195697049 ) ) ;
#23406=CARTESIAN_POINT ( 'NONE',  ( 0.4799179709319398857, -1.259100254504656569, 0.5857027040861966238 ) ) ;
#23408=LINE ( 'NONE', #36111, #18674 ) ;
#23410=CARTESIAN_POINT ( 'NONE',  ( 0.1885390680155161480, -0.9156976364345736918, 0.1977769869421455440 ) ) ;
#23415=ORIENTED_EDGE ( 'NONE', *, *, #13551, .T. ) ;
#23416=CARTESIAN_POINT ( 'NONE',  ( 0.01188899208819103881, -0.5504388812625971017, -0.07422846483693842923 ) ) ;
#23417=CARTESIAN_POINT ( 'NONE',  ( 0.4146543403318773691, -1.589641078845216882, 0.5897920107734272444 ) ) ;
#23418=CARTESIAN_POINT ( 'NONE',  ( 0.06900019283952113502, -0.5439056195324916132, 0.1104857819084973242 ) ) ;
#23423=CARTESIAN_POINT ( 'NONE',  ( 0.5423765350489757608, -1.450385248195758647, 0.7501209832966719837 ) ) ;
#23428=CARTESIAN_POINT ( 'NONE',  ( 0.2246977112670445476, -1.237341369623786269, 0.4719027293363190489 ) ) ;
#23432=CARTESIAN_POINT ( 'NONE',  ( 0.1952857665188987568, -0.5148003437455072051, 0.3467747870930740217 ) ) ;
#23438=CARTESIAN_POINT ( 'NONE',  ( 0.1849765250084728363, -0.7825370905210525807, 0.005108896899734703331 ) ) ;
#23440=AXIS2_PLACEMENT_3D ( 'NONE', #31959, #16136, #26008 ) ;
#23442=CARTESIAN_POINT ( 'NONE',  ( 0.01602427940967538628, -0.5690816651727684805, 0.5319142476028417832 ) ) ;
#23445=CARTESIAN_POINT ( 'NONE',  ( 0.5848508152300195828, -1.486263022089187036, 0.6467108361231791447 ) ) ;
#23449=CARTESIAN_POINT ( 'NONE',  ( 0.1091517887402940062, -1.415340451669741872, 0.5420629516186480368 ) ) ;
#23454=CARTESIAN_POINT ( 'NONE',  ( 0.5572041907646198000, -1.389387165738231067, 0.7048252436811164312 ) ) ;
#23456=EDGE_LOOP ( 'NONE', ( #28270, #28130 ) ) ;
#23457=CARTESIAN_POINT ( 'NONE',  ( 0.3223305689799217388, -0.9241512680936796453, 0.6167986945225242268 ) ) ;
#23462=( BOUNDED_SURFACE ( )  B_SPLINE_SURFACE ( 3, 2, ( 
 ( #8393, #20964, #1651 ),
 ( #30416, #14786, #14363 ),
 ( #23852, #33291, #14566 ),
 ( #10893, #18071, #7787 ),
 ( #27347, #17465, #32877 ),
 ( #36377, #33484, #36774 ),
 ( #4899, #7981, #8196 ),
 ( #17257, #20557, #30018 ),
 ( #20768, #2448, #33091 ),
 ( #20356, #26738, #33692 ),
 ( #30623, #39878, #14986 ),
 ( #26927, #11091, #23651 ),
 ( #30204, #5100, #39067 ),
 ( #2035, #5506, #27133 ),
 ( #39664, #24252, #8587 ),
 ( #12494, #34102, #5905 ),
 ( #12, #27734, #25051 ),
 ( #28147, #2640, #2839 ),
 ( #11886, #18277, #27948 ),
 ( #9201, #21384, #33920 ),
 ( #5719, #40269, #25260 ),
 ( #21580, #37199, #24452 ),
 ( #22195, #31626, #6515 ),
 ( #19087, #37802, #3441 ),
 ( #27539, #18895, #30820 ),
 ( #6110, #9621, #6322 ),
 ( #34710, #40060, #36985 ),
 ( #24671, #12698, #15391 ),
 ( #15176, #9019, #12105 ),
 ( #21984, #18466, #40486 ),
 ( #34512, #31019, #8806 ),
 ( #12312, #24868, #21770 ),
 ( #37388, #34303, #31433 ),
 ( #15785, #18677, #31240 ),
 ( #3056, #37585, #15601 ),
 ( #9407, #3239, #28335 ),
 ( #206, #16394, #19891 ),
 ( #3653, #12915, #26274 ),
 ( #25882, #16214, #35721 ),
 ( #3837, #15999, #28749 ),
 ( #7117, #38790, #22384 ),
 ( #28547, #35124, #31837 ) ),
 .UNSPECIFIED., .F., .F., .T. ) 
 B_SPLINE_SURFACE_WITH_KNOTS ( ( 4, 2, 2, 2, 2, 2, 2, 2, 2, 2, 2, 2, 2, 2, 2, 2, 2, 2, 2, 2, 4 ),
 ( 3, 3 ),
 ( 0.005950481707744588282, 0.006716259263195396498, 0.007482036818646203846, 0.008247814374097012929, 0.009013591929547820278, 0.009396480707273224819, 0.009779369484998627626, 0.01016225826272403217, 0.01054514704044943671, 0.01131092459590024579, 0.01207670215135105314, 0.01284247970680186049, 0.01360825726225266957, 0.01399114603997807238, 0.01437403481770347692, 0.01513981237315428427, 0.01590558992860509335, 0.01628847870633049616, 0.01667136748405589897, 0.01743714503950670805, 0.01820292259495751713 ),
 ( 0.1244524664081657073, 1.000000000000000000 ),
 .UNSPECIFIED. ) 
 GEOMETRIC_REPRESENTATION_ITEM ( )  RATIONAL_B_SPLINE_SURFACE ( (
 ( 0.9499063442391089129, 0.7987438208070558598, 1.000000000000000000),
 ( 0.9499101753461761666, 0.7987592126557592209, 1.000000000000000000),
 ( 0.9498996626311451141, 0.7987169767911981300, 1.000000000000000000),
 ( 0.9498647205990344844, 0.7985765937472975029, 1.000000000000000000),
 ( 0.9498406268971775201, 0.7984797949350583846, 1.000000000000000000),
 ( 0.9497859433926709727, 0.7982600985879926281, 1.000000000000000000),
 ( 0.9497549696405049868, 0.7981356584982937097, 1.000000000000000000),
 ( 0.9496882370548647145, 0.7978675537850399291, 1.000000000000000000),
 ( 0.9496520408222892673, 0.7977221318676597228, 1.000000000000000000),
 ( 0.9495915405754780103, 0.7974790661874149311, 1.000000000000000000),
 ( 0.9495703971913793673, 0.7973941205663723775, 1.000000000000000000),
 ( 0.9495268132974180597, 0.7972190179942053589, 1.000000000000000000),
 ( 0.9495042694130420013, 0.7971284457258256406, 1.000000000000000000),
 ( 0.9494576496633018170, 0.7969411463050679600, 1.000000000000000000),
 ( 0.9494335756765570622, 0.7968444267002283699, 1.000000000000000000),
 ( 0.9493838834922390113, 0.7966447834719645460, 1.000000000000000000),
 ( 0.9493581158244890350, 0.7965412593374354699, 1.000000000000000000),
 ( 0.9492798676385878487, 0.7962268895697659499, 1.000000000000000000),
 ( 0.9492263787684320775, 0.7960119927834690134, 1.000000000000000000),
 ( 0.9491168155290150565, 0.7955718117144263690, 1.000000000000000000),
 ( 0.9490603055549355904, 0.7953447773465653903, 1.000000000000000000),
 ( 0.9489483632414097425, 0.7948950381137618315, 1.000000000000000000),
 ( 0.9488921165716348582, 0.7946690615967901827, 1.000000000000000000),
 ( 0.9487835679013090218, 0.7942329566586614487, 1.000000000000000000),
 ( 0.9487309736807549854, 0.7940216542149569623, 1.000000000000000000),
 ( 0.9486547899165758135, 0.7937155784641993783, 1.000000000000000000),
 ( 0.9486297387484154964, 0.7936149329371018357, 1.000000000000000000),
 ( 0.9485816243033379225, 0.7934216284311081946, 1.000000000000000000),
 ( 0.9485584661661164985, 0.7933285883416276718, 1.000000000000000000),
 ( 0.9484916720352057906, 0.7930602363642083041, 1.000000000000000000),
 ( 0.9484506837745732000, 0.7928955620037245744, 1.000000000000000000),
 ( 0.9483757353755084551, 0.7925944494535770435, 1.000000000000000000),
 ( 0.9483428265590246875, 0.7924622350530370340, 1.000000000000000000),
 ( 0.9482982329828737456, 0.7922830759835624015, 1.000000000000000000),
 ( 0.9482841625340747704, 0.7922265465743627555, 1.000000000000000000),
 ( 0.9482574280669420208, 0.7921191382284120674, 1.000000000000000000),
 ( 0.9482447675118421682, 0.7920682732055432940, 1.000000000000000000),
 ( 0.9482098218232999365, 0.7919278754715699531, 1.000000000000000000),
 ( 0.9481899903031330012, 0.7918482003926456958, 1.000000000000000000),
 ( 0.9481627597725135193, 0.7917387990629434213, 1.000000000000000000),
 ( 0.9481555257785727608, 0.7917097357822004966, 1.000000000000000000),
 ( 0.9481610290116149198, 0.7917318455611419559, 1.000000000000000000) ) ) 
 REPRESENTATION_ITEM ( '' )  SURFACE ( )  );
#23463=CARTESIAN_POINT ( 'NONE',  ( 0.02395668684128875181, -0.5542051941014292105, 0.2488759775346758019 ) ) ;
#23464=CARTESIAN_POINT ( 'NONE',  ( 0.6845627961534704875, -1.503898997149517580, 0.4557198836646339513 ) ) ;
#23470=AXIS2_PLACEMENT_3D ( 'NONE', #34714, #22598, #25474 ) ;
#23473=CARTESIAN_POINT ( 'NONE',  ( 0.3806020551634139437, -1.255922899846727558, 0.6160997750454292321 ) ) ;
#23474=CARTESIAN_POINT ( 'NONE',  ( 0.5923740993416417577, -1.483515408114672418, 0.6326167027179712132 ) ) ;
#23478=CARTESIAN_POINT ( 'NONE',  ( 0.4266844285874258902, -1.124162052474312334, 0.5132868267961471220 ) ) ;
#23479=DIRECTION ( 'NONE',  ( 0.8614903136912356318, 0.5077740042737285409, 1.079459829625176262E-11 ) ) ;
#23482=CARTESIAN_POINT ( 'NONE',  ( 0.4009842110195314113, -1.137333063945437095, 0.4310421439394608312 ) ) ;
#23483=CARTESIAN_POINT ( 'NONE',  ( 0.4138729472876766513, -1.128955312352843965, 0.5470489658417444501 ) ) ;
#23486=CARTESIAN_POINT ( 'NONE',  ( 0.5989748564488622806, -1.469694812953115548, 0.6043986940112930917 ) ) ;
#23487=CARTESIAN_POINT ( 'NONE',  ( 0.1798183621851980052, -1.228826535827538757, 1.015400663858992081 ) ) ;
#23489=EDGE_CURVE ( 'NONE', #1703, #35767, #22835, .T. ) ;
#23492=CARTESIAN_POINT ( 'NONE',  ( 0.1755412408656793488, -0.5236575430993549718, 0.09909328031171654727 ) ) ;
#23495=CARTESIAN_POINT ( 'NONE',  ( 0.6020063251545132443, -1.483136369781559383, 0.5737255376849879074 ) ) ;
#23497=CARTESIAN_POINT ( 'NONE',  ( -0.0001984217570695264842, -0.7096501419610361516, -0.02101570025487809953 ) ) ;
#23498=VERTEX_POINT ( 'NONE', #28313 ) ;
#23499=ORIENTED_EDGE ( 'NONE', *, *, #36363, .F. ) ;
#23500=CARTESIAN_POINT ( 'NONE',  ( 0.1153472973656773787, -0.4465945704133856831, 0.1832744267750886502 ) ) ;
#23503=CARTESIAN_POINT ( 'NONE',  ( 0.004648077331195073561, -0.6786668696663772371, 0.5213953154864034989 ) ) ;
#23509=CARTESIAN_POINT ( 'NONE',  ( 0.004042983189834512686, -0.6339827964191876442, 0.09509064842808945262 ) ) ;
#23510=ORIENTED_EDGE ( 'NONE', *, *, #17720, .F. ) ;
#23512=CARTESIAN_POINT ( 'NONE',  ( 0.08690321595024325108, -0.7908715706426733272, 0.2150688980104960291 ) ) ;
#23513=CARTESIAN_POINT ( 'NONE',  ( 0.03292036658315200537, -0.9539746468707878124, 0.6379772252982135461 ) ) ;
#23514=CARTESIAN_POINT ( 'NONE',  ( 0.07425324393167602455, -0.5797589466047996520, 0.2935359610363197369 ) ) ;
#23515=CARTESIAN_POINT ( 'NONE',  ( 0.4275179515708005251, -1.300593502282117564, 0.8352946709572205419 ) ) ;
#23516=CARTESIAN_POINT ( 'NONE',  ( 0.05301051884385669932, -1.209477745581631680, 0.6633383430279803372 ) ) ;
#23518=CARTESIAN_POINT ( 'NONE',  ( 0.06936654275850007156, -1.327133429011322141, 0.5458395137742464431 ) ) ;
#23520=CARTESIAN_POINT ( 'NONE',  ( 0.6867864222940462948, -1.415806215839816140, 0.6057417262805012692 ) ) ;
#23522=CARTESIAN_POINT ( 'NONE',  ( 0.07043814880410806389, -1.334972480813829021, 0.5056242588139847616 ) ) ;
#23524=CARTESIAN_POINT ( 'NONE',  ( -0.0001820817997102400665, -0.8409590828520395744, -0.05113895155038358786 ) ) ;
#23525=CARTESIAN_POINT ( 'NONE',  ( 0.4776172972151280782, -1.293649847444084289, 0.8149156285371210728 ) ) ;
#23529=CARTESIAN_POINT ( 'NONE',  ( 0.05848126963139189949, -0.9969932945501481791, 0.7623047753129613691 ) ) ;
#23530=CARTESIAN_POINT ( 'NONE',  ( 0.4927680500253098783, -1.082617619565096723, 0.5740975660237009892 ) ) ;
#23533=CARTESIAN_POINT ( 'NONE',  ( 0.2020777887685438201, -0.5385241820806814239, 0.3979124043150588097 ) ) ;
#23541=CARTESIAN_POINT ( 'NONE',  ( 0.03395086281050493232, -0.7332833338886608487, 0.5887985628043005404 ) ) ;
#23542=CARTESIAN_POINT ( 'NONE',  ( 0.1136746601619137848, -1.290010351664979016, 0.4385763861344814663 ) ) ;
#23545=CARTESIAN_POINT ( 'NONE',  ( 0.3253942984295454255, -1.752804437849984076, 0.4715143984075212402 ) ) ;
#23546=CARTESIAN_POINT ( 'NONE',  ( 0.5484444682544461491, -1.189958873811490347, 0.8086343185444866410 ) ) ;
#23555=VERTEX_POINT ( 'NONE', #38378 ) ;
#23557=CARTESIAN_POINT ( 'NONE',  ( 0.08875147084456934399, -0.6445117467991269278, 0.1562688198774206394 ) ) ;
#23558=CARTESIAN_POINT ( 'NONE',  ( 0.2811027414035134897, -1.594431497873851189, 0.9549070678298874348 ) ) ;
#23559=CARTESIAN_POINT ( 'NONE',  ( 0.4989807694161794704, -1.541666567615755490, 0.6106768752493882957 ) ) ;
#23560=CARTESIAN_POINT ( 'NONE',  ( 0.1139602419629163615, -0.5599708880517814125, -0.05895036679083177911 ) ) ;
#23561=FACE_OUTER_BOUND ( 'NONE', #9867, .T. ) ;
#23562=CARTESIAN_POINT ( 'NONE',  ( 0.07287665493537502648, -1.000988532525567631, 0.5315438341818862211 ) ) ;
#23564=VERTEX_POINT ( 'NONE', #25860 ) ;
#23565=CARTESIAN_POINT ( 'NONE',  ( 0.3303481907406706219, -1.638360797784888190, 0.5482645839017932232 ) ) ;
#23566=CARTESIAN_POINT ( 'NONE',  ( 0.2248424822466164874, -0.6656341711533926286, 0.4617182395505510795 ) ) ;
#23570=CARTESIAN_POINT ( 'NONE',  ( 0.07300061029741421181, -1.320382841123569628, 0.5080970089286546143 ) ) ;
#23572=CARTESIAN_POINT ( 'NONE',  ( 0.6159793682513172719, -1.299209393623256492, 0.5257027981018284057 ) ) ;
#23573=EDGE_CURVE ( 'NONE', #507, #24616, #34087, .T. ) ;
#23579=EDGE_CURVE ( 'NONE', #7024, #7215, #12593, .T. ) ;
#23583=CARTESIAN_POINT ( 'NONE',  ( 0.4475429125754209481, -1.047523227676938173, 0.7185146543629753468 ) ) ;
#23586=CARTESIAN_POINT ( 'NONE',  ( 0.2791220714032659478, -1.321220139306267471, 0.5682417262808748815 ) ) ;
#23594=CARTESIAN_POINT ( 'NONE',  ( 0.4540954970294862059, -1.215799341954577395, 0.6428014875294941755 ) ) ;
#23600=CARTESIAN_POINT ( 'NONE',  ( 0.5860257985473389386, -1.592810714289445650, 0.4182417262808776903 ) ) ;
#23604=CARTESIAN_POINT ( 'NONE',  ( 0.4144077979564601555, -1.589676522203103959, 0.5854317008102997155 ) ) ;
#23605=CARTESIAN_POINT ( 'NONE',  ( 0.06873388849150627311, -0.5537460360556609729, 0.08262749772200221610 ) ) ;
#23611=CARTESIAN_POINT ( 'NONE',  ( 0.3556566238030725580, -1.130358669023453722, 0.8129044222785481999 ) ) ;
#23613=FACE_OUTER_BOUND ( 'NONE', #5644, .T. ) ;
#23616=CARTESIAN_POINT ( 'NONE',  ( 0.2037257193243683095, -1.237902000685740633, 0.4623145460830584974 ) ) ;
#23619=CARTESIAN_POINT ( 'NONE',  ( 0.6565177652365870031, -1.363219716956428407, 0.8083140950016142190 ) ) ;
#23624=CARTESIAN_POINT ( 'NONE',  ( 0.2326005804937198163, -1.348008995865297432, 0.5133468128822303855 ) ) ;
#23625=CARTESIAN_POINT ( 'NONE',  ( 0.1844128417485024762, -0.6074837269968395015, -0.01383500138692834829 ) ) ;
#23627=CARTESIAN_POINT ( 'NONE',  ( 0.3690965330173307524, -1.099411688709415413, 0.5182417262812423209 ) ) ;
#23629=CARTESIAN_POINT ( 'NONE',  ( 0.002083146443013504916, -0.4777046557262296100, 0.1457185332388684640 ) ) ;
#23632=CARTESIAN_POINT ( 'NONE',  ( 0.5977452740392612540, -1.597648098397363547, 0.4278779530986268620 ) ) ;
#23636=DIRECTION ( 'NONE',  ( 0.4999551463232372317, -0.8660512985181135770, 0.000000000000000000 ) ) ;
#23637=CARTESIAN_POINT ( 'NONE',  ( 0.3207919832889619127, -1.182535135427784878, 0.4177417262808780229 ) ) ;
#23638=ORIENTED_EDGE ( 'NONE', *, *, #12490, .F. ) ;
#23641=CARTESIAN_POINT ( 'NONE',  ( 0.5550199683367226244, -1.387812963830668211, 0.6052661460963145723 ) ) ;
#23645=CARTESIAN_POINT ( 'NONE',  ( 0.1971950993027475063, -0.8036775079564704161, 0.3187204964795984363 ) ) ;
#23649=CARTESIAN_POINT ( 'NONE',  ( 0.02340052157832292826, -0.5442089205427294019, 0.2181755822959388913 ) ) ;
#23650=CARTESIAN_POINT ( 'NONE',  ( 0.6570310456701250468, -1.541036513631718785, 0.4253474239190344064 ) ) ;
#23651=CARTESIAN_POINT ( 'NONE',  ( 0.1141259082751814175, -0.5391003347981141447, -0.04436171186494073521 ) ) ;
#23652=CARTESIAN_POINT ( 'NONE',  ( 0.3207919832889619127, -1.182535135427784878, 0.4177417262808780229 ) ) ;
#23658=CARTESIAN_POINT ( 'NONE',  ( 0.08269480835304590660, -0.8371205904093916850, 0.2823278632619380391 ) ) ;
#23661=CARTESIAN_POINT ( 'NONE',  ( 0.3203156827224240555, -1.053479473948887080, 0.6335618240576057492 ) ) ;
#23663=FACE_BOUND ( 'NONE', #32827, .T. ) ;
#23667=CARTESIAN_POINT ( 'NONE',  ( 0.009587871238832338869, -0.9974913955574146174, 0.5289707807213344104 ) ) ;
#23668=CARTESIAN_POINT ( 'NONE',  ( 0.5594945947431219091, -1.182971886111896964, 0.6057417262809814407 ) ) ;
#23672=CARTESIAN_POINT ( 'NONE',  ( 0.1142751706468553285, -0.9924943110554562686, 0.9292056703508084770 ) ) ;
#23673=AXIS2_PLACEMENT_3D ( 'NONE', #16429, #25921, #19719 ) ;
#23676=ORIENTED_EDGE ( 'NONE', *, *, #4989, .F. ) ;
#23677=CARTESIAN_POINT ( 'NONE',  ( 0.1870046356540934207, -0.5056247393092100362, 0.1384337335614591047 ) ) ;
#23681=CARTESIAN_POINT ( 'NONE',  ( 0.6013823673879303833, -1.482980318010622911, 0.5610683146295102341 ) ) ;
#23683=CARTESIAN_POINT ( 'NONE',  ( -0.001060993694459935396, -0.7858254716106745086, 0.01975934941180707005 ) ) ;
#23686=CARTESIAN_POINT ( 'NONE',  ( 0.3084843299837661257, -1.189417664086780846, 0.5254903229641211260 ) ) ;
#23688=CARTESIAN_POINT ( 'NONE',  ( 0.2616305944698923969, -1.623119320148453726, 0.8135356459590667999 ) ) ;
#23697=CARTESIAN_POINT ( 'NONE',  ( 0.07318559350598305424, -1.141632816824696750, 0.7599663268781896575 ) ) ;
#23698=CARTESIAN_POINT ( 'NONE',  ( 0.07117412038449888456, -0.5606254895656045401, 0.2415125051803064526 ) ) ;
#23699=CARTESIAN_POINT ( 'NONE',  ( 0.5523264011633536308, -1.510993508513732930, 0.5610637926937284137 ) ) ;
#23700=CARTESIAN_POINT ( 'NONE',  ( 0.1837552442763759619, -0.5219052425814498797, 0.2609841535793563927 ) ) ;
#23702=FACE_OUTER_BOUND ( 'NONE', #1108, .T. ) ;
#23704=CARTESIAN_POINT ( 'NONE',  ( 0.6982435741820434139, -1.438800902438351459, 0.5626105661469322783 ) ) ;
#23709=CARTESIAN_POINT ( 'NONE',  ( 0.4107682604834280715, -1.110406771794815395, 0.6170034175396635900 ) ) ;
#23710=DIRECTION ( 'NONE',  ( 0.8660512985181134660, 0.4999551463232371762, 0.000000000000000000 ) ) ;
#23712=CARTESIAN_POINT ( 'NONE',  ( 0.4567198261210261845, -1.219045092035883293, 0.5856983068965102568 ) ) ;
#23713=CARTESIAN_POINT ( 'NONE',  ( 0.002392376194700432737, -0.7211561054371403712, 0.3442605867753443794 ) ) ;
#23714=CARTESIAN_POINT ( 'NONE',  ( 0.4922096163030106331, -1.082311226180449504, 0.5799505941865350511 ) ) ;
#23716=CARTESIAN_POINT ( 'NONE',  ( 0.2114022633412600827, -0.5658596150412534831, 0.4491712673773823883 ) ) ;
#23719=CARTESIAN_POINT ( 'NONE',  ( 0.3061274744420098282, -1.759189183208312413, 0.5682166201788007021 ) ) ;
#23722=CARTESIAN_POINT ( 'NONE',  ( 0.1171733338514413247, -1.124504233628559779, 0.8957213136541929410 ) ) ;
#23726=ORIENTED_EDGE ( 'NONE', *, *, #34113, .F. ) ;
#23729=CARTESIAN_POINT ( 'NONE',  ( 0.6117231882494743589, -1.284912631992666254, 0.6460020013211499323 ) ) ;
#23730=ORIENTED_EDGE ( 'NONE', *, *, #22276, .F. ) ;
#23737=PLANE ( 'NONE',  #19996 ) ;
#23743=CARTESIAN_POINT ( 'NONE',  ( 0.2317368684993577621, -0.9096491609996487648, 0.6759228893237037017 ) ) ;
#23745=CARTESIAN_POINT ( 'NONE',  ( 0.1346410849617742378, -1.067092216287955697, 0.9652224197926299043 ) ) ;
#23746=CARTESIAN_POINT ( 'NONE',  ( 0.4970208778649962134, -1.542363045560136037, 0.5660616863803898946 ) ) ;
#23747=CARTESIAN_POINT ( 'NONE',  ( 0.2580594912783656381, -1.598602451500839683, 0.8570735393225172860 ) ) ;
#23749=CARTESIAN_POINT ( 'NONE',  ( 0.1941099092474980470, -0.9693953940917349188, 0.5071542142353313576 ) ) ;
#23755=CIRCLE ( 'NONE', #34929, 0.01000000000000001582 ) ;
#23756=CARTESIAN_POINT ( 'NONE',  ( 0.2578022185847296810, -0.7392430535719961560, 0.5549718881115695002 ) ) ;
#23757=ADVANCED_FACE ( 'NONE', ( #18968 ), #27426, .F. ) ;
#23765=DIRECTION ( 'NONE',  ( 0.4999551463232371762, -0.8660512985181134660, 0.000000000000000000 ) ) ;
#23766=CARTESIAN_POINT ( 'NONE',  ( 0.3392765801623501276, -0.9012043381553855870, 0.6651284465457234507 ) ) ;
#23769=EDGE_CURVE ( 'NONE', #27736, #2583, #275, .T. ) ;
#23778=CARTESIAN_POINT ( 'NONE',  ( 0.3199600894486596125, -0.9236621663148832928, 0.6127110118620351376 ) ) ;
#23781=CARTESIAN_POINT ( 'NONE',  ( 0.08749854297545196780, -0.9854861971012113253, 0.6823029913621244669 ) ) ;
#23782=ORIENTED_EDGE ( 'NONE', *, *, #29831, .F. ) ;
#23785=CARTESIAN_POINT ( 'NONE',  ( 0.5382307432915078849, -1.161159458769174257, 0.5682417262808779901 ) ) ;
#23787=CARTESIAN_POINT ( 'NONE',  ( 0.3774258077853776538, -1.121343430727174795, 0.7058894445193834022 ) ) ;
#23788=CIRCLE ( 'NONE', #19809, 0.07749999999977555398 ) ;
#23790=CARTESIAN_POINT ( 'NONE',  ( 0.3174226411910346934, -1.752965763378658393, 0.5310945280258847490 ) ) ;
#23791=CARTESIAN_POINT ( 'NONE',  ( 0.2098534808732534784, -0.9273921219866952947, 0.3620977009047463002 ) ) ;
#23793=B_SPLINE_CURVE_WITH_KNOTS ( 'NONE', 3,
 ( #27306, #14740, #17624, #39233, #8548, #29759, #17422, #11454, #39834, #2199 ),
 .UNSPECIFIED., .F., .F.,
 ( 4, 2, 2, 2, 4 ),
 ( 0.000000000000000000, 0.0007867799123170480082, 0.001573559824634096016, 0.002360339736951139796, 0.003147119649268183793 ),
 .UNSPECIFIED. ) ;
#23794=CARTESIAN_POINT ( 'NONE',  ( 0.5926726610113466354, -1.589034138814389374, 0.4182417262808776903 ) ) ;
#23798=( BOUNDED_SURFACE ( )  B_SPLINE_SURFACE ( 3, 2, ( 
 ( #36230, #8044, #23518 ),
 ( #33156, #20828, #4961 ),
 ( #36444, #1904, #14416 ),
 ( #26978, #27193, #23913 ) ),
 .UNSPECIFIED., .F., .F., .F. ) 
 B_SPLINE_SURFACE_WITH_KNOTS ( ( 4, 4 ),
 ( 3, 3 ),
 ( -1.546505978833323525E-15, 0.0005696895415557860689 ),
 ( 0.000000000000000000, 1.000000000000000000 ),
 .UNSPECIFIED. ) 
 GEOMETRIC_REPRESENTATION_ITEM ( )  RATIONAL_B_SPLINE_SURFACE ( (
 ( 1.000000000000000000, 0.7101913118100382505, 1.000000000000000000),
 ( 1.000000000000000000, 0.7102645811962934319, 1.000000000000000000),
 ( 1.000000000000000000, 0.7103277044789075845, 1.000000000000000000),
 ( 1.000000000000000000, 0.7103763540285419342, 1.000000000000000000) ) ) 
 REPRESENTATION_ITEM ( '' )  SURFACE ( )  );
#23801=CARTESIAN_POINT ( 'NONE',  ( 0.1377409401209249984, -0.8452087646918974295, 0.6880418428642343098 ) ) ;
#23802=CARTESIAN_POINT ( 'NONE',  ( 0.08759928954965089110, -0.6793946942812071343, 0.02269552198566341175 ) ) ;
#23803=CARTESIAN_POINT ( 'NONE',  ( 0.1897655176910530150, -0.7785539449726521788, 0.2985823049966282450 ) ) ;
#23804=CARTESIAN_POINT ( 'NONE',  ( 0.1459220268477366689, -1.282677086676273337, 0.4807434598447087870 ) ) ;
#23811=CARTESIAN_POINT ( 'NONE',  ( 0.2982777979521030742, -1.009191457843666040, 0.7688872764601440979 ) ) ;
#23812=ORIENTED_EDGE ( 'NONE', *, *, #9495, .F. ) ;
#23816=CARTESIAN_POINT ( 'NONE',  ( 0.1941405844127271907, -1.254956905737245609, 0.4467041655102085840 ) ) ;
#23819=CARTESIAN_POINT ( 'NONE',  ( 0.6491914112794352487, -1.351404041023776204, 0.8153926641961858346 ) ) ;
#23826=CARTESIAN_POINT ( 'NONE',  ( 0.5727340295961615979, -1.614449106656711708, 0.5626663476171955836 ) ) ;
#23828=CARTESIAN_POINT ( 'NONE',  ( 0.1060996949738549772, -1.304465968667597675, 0.4400741763124171313 ) ) ;
#23831=CARTESIAN_POINT ( 'NONE',  ( 0.2920835003669574048, -1.623987781970284594, 0.9481157836879084977 ) ) ;
#23834=CARTESIAN_POINT ( 'NONE',  ( 0.3048131552638332353, -1.756863458444712700, 0.5686633310820135012 ) ) ;
#23839=CARTESIAN_POINT ( 'NONE',  ( 0.4093611158985690501, -1.131941421409890403, 0.5197417262808780025 ) ) ;
#23840=DIRECTION ( 'NONE',  ( 0.8660512985181133550, 0.4999551463232371207, 0.000000000000000000 ) ) ;
#23842=CARTESIAN_POINT ( 'NONE',  ( 0.5042534145799544287, -1.300931244380588714, 0.7003810967224629591 ) ) ;
#23844=ORIENTED_EDGE ( 'NONE', *, *, #20575, .T. ) ;
#23845=CARTESIAN_POINT ( 'NONE',  ( 0.3550363906115478474, -0.9559691138050746551, 0.6482402363088731745 ) ) ;
#23847=ORIENTED_EDGE ( 'NONE', *, *, #10752, .T. ) ;
#23850=CARTESIAN_POINT ( 'NONE',  ( 0.3578840571904184364, -1.622517175314822202, 0.6005136135349141702 ) ) ;
#23851=CARTESIAN_POINT ( 'NONE',  ( 0.6889712424111062994, -1.498443914574956848, 0.4645504256959663847 ) ) ;
#23852=CARTESIAN_POINT ( 'NONE',  ( 0.1882261734610965742, -0.5202158445490479011, 0.1262989087885288408 ) ) ;
#23857=ORIENTED_EDGE ( 'NONE', *, *, #13643, .F. ) ;
#23863=CARTESIAN_POINT ( 'NONE',  ( 0.1863649894376638305, -1.020275744783735838, 0.7192912599071568103 ) ) ;
#23864=CARTESIAN_POINT ( 'NONE',  ( 0.3540817610093318635, -1.633452470505663667, 0.5182417262812423209 ) ) ;
#23868=CARTESIAN_POINT ( 'NONE',  ( 0.1501646858415086605, -0.9504056024928764224, 0.4235331231779344008 ) ) ;
#23870=FACE_OUTER_BOUND ( 'NONE', #30959, .T. ) ;
#23877=CARTESIAN_POINT ( 'NONE',  ( 0.01555240294579989489, -1.032170008678823470, 0.5911815370100742539 ) ) ;
#23880=CARTESIAN_POINT ( 'NONE',  ( 0.0003443436031621042938, -0.4626201699786359756, 0.03852669977424470066 ) ) ;
#23886=VERTEX_POINT ( 'NONE', #15873 ) ;
#23888=CARTESIAN_POINT ( 'NONE',  ( 0.1871418833521726888, -0.5093494604625196098, 0.1906562654118973132 ) ) ;
#23892=CARTESIAN_POINT ( 'NONE',  ( 0.0003935148711146671356, -0.6434531841869496338, -0.01657467902959560910 ) ) ;
#23896=CARTESIAN_POINT ( 'NONE',  ( 0.5070565638186045332, -1.226247237694178427, 0.9020276881305223649 ) ) ;
#23899=CARTESIAN_POINT ( 'NONE',  ( 0.1990087807486831672, -1.411128265896168799, 0.9384327408913899493 ) ) ;
#23900=CARTESIAN_POINT ( 'NONE',  ( 0.5934537061017988169, -1.599883771062468041, 0.4225983487168387120 ) ) ;
#23901=CARTESIAN_POINT ( 'NONE',  ( 0.1831969519479068331, -1.238078994650575249, 0.5906457657967459918 ) ) ;
#23904=ADVANCED_FACE ( 'NONE', ( #7014 ), #3824, .T. ) ;
#23906=ORIENTED_EDGE ( 'NONE', *, *, #37063, .T. ) ;
#23907=VERTEX_POINT ( 'NONE', #1281 ) ;
#23908=CARTESIAN_POINT ( 'NONE',  ( 0.01165244542177405231, -0.7705269947053657864, -0.09957348361509645029 ) ) ;
#23909=CARTESIAN_POINT ( 'NONE',  ( 0.09220195039318782038, -1.256385609540978443, 0.7507312887929911138 ) ) ;
#23910=CARTESIAN_POINT ( 'NONE',  ( 0.09649107927482511449, -0.5884850972898393318, 0.3050835042885340354 ) ) ;
#23911=CARTESIAN_POINT ( 'NONE',  ( 0.01141274522673730620, -0.9470863358862970927, 0.2134741291574251409 ) ) ;
#23913=CARTESIAN_POINT ( 'NONE',  ( 0.06843884545124433172, -1.327631889387169473, 0.5684120120348994387 ) ) ;
#23914=CONICAL_SURFACE ( 'NONE', #21945, 0.2609684784060898322, 0.1745329251994329756 ) ;
#23919=DIRECTION ( 'NONE',  ( 0.01455087615875041117, 0.9998941303973198913, 0.000000000000000000 ) ) ;
#23922=CARTESIAN_POINT ( 'NONE',  ( 0.3965913301904485655, -1.111811593118467778, 0.6217369508112342569 ) ) ;
#23925=CARTESIAN_POINT ( 'NONE',  ( 0.05992416651567116642, -0.8828589634183678925, 0.7642515975180658172 ) ) ;
#23927=CARTESIAN_POINT ( 'NONE',  ( 0.1856290495283919040, -0.8698730627085041744, 0.1722928722954065184 ) ) ;
#23929=CARTESIAN_POINT ( 'NONE',  ( 0.1878356035704684124, -0.4698003021450733452, 0.2206963598966235063 ) ) ;
#23935=EDGE_LOOP ( 'NONE', ( #14202, #6445, #23638, #32428 ) ) ;
#23937=CARTESIAN_POINT ( 'NONE',  ( 0.1570928595072558498, -1.231659055714347417, 0.9252356148029357019 ) ) ;
#23939=FACE_OUTER_BOUND ( 'NONE', #12357, .T. ) ;
#23941=CARTESIAN_POINT ( 'NONE',  ( 0.06619202177789897112, -1.328973388337416406, 0.5682286961285595295 ) ) ;
#23942=CARTESIAN_POINT ( 'NONE',  ( 0.2055745749294108637, -0.6303510842867390274, 0.3631342511460070033 ) ) ;
#23956=CARTESIAN_POINT ( 'NONE',  ( 0.1293727182780175788, -1.251705868455923243, 0.6057490510025627106 ) ) ;
#23957=CARTESIAN_POINT ( 'NONE',  ( 0.2094105298161792195, -0.8866733143744640611, 0.6435963268220464828 ) ) ;
#23959=CARTESIAN_POINT ( 'NONE',  ( 0.2857211247607547855, -1.599410745080646956, 0.9638650573196021476 ) ) ;
#23960=CARTESIAN_POINT ( 'NONE',  ( 0.09909590748669688809, -0.5670311656315165649, 0.2451387329811758886 ) ) ;
#23962=CARTESIAN_POINT ( 'NONE',  ( 0.1141128553655777061, -0.5404361383069915536, -0.04587327521813978209 ) ) ;
#23964=CARTESIAN_POINT ( 'NONE',  ( 0.08997777199038561879, -1.272785463024103558, 0.6309002601239589447 ) ) ;
#23966=ORIENTED_EDGE ( 'NONE', *, *, #17544, .F. ) ;
#23968=CARTESIAN_POINT ( 'NONE',  ( 0.2783458387688289570, -0.7789938178757523923, 0.5967641912780569102 ) ) ;
#23969=DIRECTION ( 'NONE',  ( 0.8660512985181139101, 0.4999551463232366766, 0.000000000000000000 ) ) ;
#23974=CARTESIAN_POINT ( 'NONE',  ( 0.3193812180522301869, -1.183103643414081807, 0.4697888944849939463 ) ) ;
#23975=CARTESIAN_POINT ( 'NONE',  ( 0.4795791402848185725, -1.087578995800233095, 0.7487995513514865698 ) ) ;
#23985=CARTESIAN_POINT ( 'NONE',  ( 0.5739612213088449710, -1.639306779899527555, 0.5182417262812423209 ) ) ;
#23986=EDGE_CURVE ( 'NONE', #21612, #19731, #27686, .T. ) ;
#23990=CARTESIAN_POINT ( 'NONE',  ( 0.3720834698793197837, -0.9620146622799481406, 0.6738924748705610313 ) ) ;
#23992=DIRECTION ( 'NONE',  ( 0.8660512985181135770, 0.4999551463232372317, 0.000000000000000000 ) ) ;
#23994=CARTESIAN_POINT ( 'NONE',  ( 0.1849629421863227541, -1.262760559472479116, 0.7247380077052344438 ) ) ;
#24000=CARTESIAN_POINT ( 'NONE',  ( 0.4501467687945732710, -1.211961921974989753, 0.6678290789428007468 ) ) ;
#24007=CARTESIAN_POINT ( 'NONE',  ( 0.3764383192846859627, -1.163784862039349388, 0.4182417262808778569 ) ) ;
#24011=CARTESIAN_POINT ( 'NONE',  ( 0.4060240284916718512, -1.489574581569751199, 0.8154449424633511967 ) ) ;
#24013=CARTESIAN_POINT ( 'NONE',  ( 0.6754688192570067473, -1.566413995319801522, 0.6053351715126479293 ) ) ;
#24014=CARTESIAN_POINT ( 'NONE',  ( 0.1945633475659577505, -0.8045315353305676487, 0.2954283631093154727 ) ) ;
#24015=CARTESIAN_POINT ( 'NONE',  ( 0.5763712271873797643, -1.496301764669956569, 0.4854925386805672427 ) ) ;
#24021=CARTESIAN_POINT ( 'NONE',  ( 0.5738576967776770621, -1.499251410920260152, 0.5722528306968517331 ) ) ;
#24022=CIRCLE ( 'NONE', #23345, 0.009999999999999960310 ) ;
#24024=CARTESIAN_POINT ( 'NONE',  ( 0.3621729297631758326, -1.619675390324748498, 0.6057417262804762892 ) ) ;
#24025=CARTESIAN_POINT ( 'NONE',  ( 0.6510214958982905031, -1.549214841228496065, 0.4232660966085758369 ) ) ;
#24026=CARTESIAN_POINT ( 'NONE',  ( 0.1669810943094347522, -1.270657801378861418, 0.4327140572190054102 ) ) ;
#24029=CARTESIAN_POINT ( 'NONE',  ( 0.7167626400851214719, -1.479603991551655895, 0.4558490598962456342 ) ) ;
#24031=CARTESIAN_POINT ( 'NONE',  ( -0.0004424791507732762593, -0.9367167129038181939, 0.1457185332388704069 ) ) ;
#24035=DIRECTION ( 'NONE',  ( 0.01254811300245564816, 0.8659344938869285579, 0.4999999971568664936 ) ) ;
#24037=CARTESIAN_POINT ( 'NONE',  ( 0.6936858524652079749, -1.440596496979289265, 0.5164693539546609813 ) ) ;
#24038=CARTESIAN_POINT ( 'NONE',  ( 0.08972986647850272890, -1.313679858983815230, 0.4566612845758172279 ) ) ;
#24041=CARTESIAN_POINT ( 'NONE',  ( 0.2750825180155820338, -1.558163865710181728, 0.9909808761736236260 ) ) ;
#24043=ADVANCED_FACE ( 'NONE', ( #28177 ), #31272, .F. ) ;
#24045=DIRECTION ( 'NONE',  ( 0.9998941247116546194, -0.01455087607601020239, 0.0001066420868422379362 ) ) ;
#24048=ORIENTED_EDGE ( 'NONE', *, *, #2991, .T. ) ;
#24049=CARTESIAN_POINT ( 'NONE',  ( 0.4039231983721676134, -1.110675651203401948, 0.6196059181502108215 ) ) ;
#24051=CARTESIAN_POINT ( 'NONE',  ( 0.3643718150905314035, -1.122313172052715968, 0.6044674227507519371 ) ) ;
#24054=CARTESIAN_POINT ( 'NONE',  ( 0.4958217342451587406, -1.286626739914629614, 0.6909901939486514655 ) ) ;
#24057=CARTESIAN_POINT ( 'NONE',  ( 0.5017447040277105419, -1.102516469585429260, 0.6180670868896422920 ) ) ;
#24061=CARTESIAN_POINT ( 'NONE',  ( 0.009884248493598344482, -0.5504904132058388022, 0.06650783079932308384 ) ) ;
#24062=CARTESIAN_POINT ( 'NONE',  ( 0.3563132181259857645, -1.622456743041318594, 0.5765765839559005013 ) ) ;
#24064=CARTESIAN_POINT ( 'NONE',  ( 0.7086437989906794188, -1.516288493585639330, 0.5545215044661631065 ) ) ;
#24067=VERTEX_POINT ( 'NONE', #2876 ) ;
#24070=ORIENTED_EDGE ( 'NONE', *, *, #22274, .F. ) ;
#24073=CARTESIAN_POINT ( 'NONE',  ( 0.3229734859516730783, -1.276098296144065225, 0.6443918083873608760 ) ) ;
#24079=CARTESIAN_POINT ( 'NONE',  ( 0.1160572313976696857, -0.9313940905863343778, 0.2591244526804493131 ) ) ;
#24081=DIRECTION ( 'NONE',  ( 0.9998941247116546194, -0.01455087607601020239, 0.0001066420868422379362 ) ) ;
#24082=CARTESIAN_POINT ( 'NONE',  ( 0.6581239351981619246, -1.508981307375971026, 0.4182417262808776903 ) ) ;
#24085=CARTESIAN_POINT ( 'NONE',  ( 0.4752902067229345384, -1.128721034250735444, 0.4769721126355153107 ) ) ;
#24086=CARTESIAN_POINT ( 'NONE',  ( 0.4091955671835494357, -1.131682303504549347, 0.5515612239602755151 ) ) ;
#24088=CARTESIAN_POINT ( 'NONE',  ( 0.01216095678309696802, -0.4295234428450211972, 0.1161211177829335195 ) ) ;
#24091=CARTESIAN_POINT ( 'NONE',  ( 0.007789957077748424150, -0.5295643729319113868, 0.4348223727464700650 ) ) ;
#24094=EDGE_CURVE ( 'NONE', #22420, #20653, #13483, .T. ) ;
#24097=CARTESIAN_POINT ( 'NONE',  ( 0.1726814644796534071, -0.5193392427952403523, 0.1436262120076541027 ) ) ;
#24098=ORIENTED_EDGE ( 'NONE', *, *, #19209, .F. ) ;
#24104=CARTESIAN_POINT ( 'NONE',  ( 0.009274569113454507810, -0.5902431952254217906, 0.02081147810894002498 ) ) ;
#24105=ORIENTED_EDGE ( 'NONE', *, *, #22873, .T. ) ;
#24106=ORIENTED_EDGE ( 'NONE', *, *, #4932, .F. ) ;
#24107=CARTESIAN_POINT ( 'NONE',  ( 0.2859601836109825213, -0.8602919011690969286, 0.7882872347711364913 ) ) ;
#24110=CARTESIAN_POINT ( 'NONE',  ( 0.2658579063097570860, -1.675104683681777340, 0.5666873703055449463 ) ) ;
#24114=EDGE_CURVE ( 'NONE', #32978, #29236, #9446, .T. ) ;
#24120=CARTESIAN_POINT ( 'NONE',  ( 0.01133266107010722987, -0.9445109682311131349, 0.1117785243345983531 ) ) ;
#24122=CARTESIAN_POINT ( 'NONE',  ( 0.09236582558789477315, -0.5663732494358152403, 0.2468274383348227075 ) ) ;
#24124=CARTESIAN_POINT ( 'NONE',  ( 0.1874263242844142752, -0.6916738960414681170, 0.04030299999698908758 ) ) ;
#24127=CARTESIAN_POINT ( 'NONE',  ( 0.01220502636281931008, -0.4284498256520046788, 0.1513327638351227855 ) ) ;
#24128=CARTESIAN_POINT ( 'NONE',  ( 0.3869965781225513934, -1.721508965229717969, 0.4224448655611768855 ) ) ;
#24130=CARTESIAN_POINT ( 'NONE',  ( 0.3965913301904470112, -1.111811593118468666, 0.6217369508112339238 ) ) ;
#24132=CARTESIAN_POINT ( 'NONE',  ( 0.3056347003372518745, -1.768333716703696323, 0.5707417262808793801 ) ) ;
#24133=CARTESIAN_POINT ( 'NONE',  ( 0.4495844847086868379, -1.113559791644742836, 0.5920747722683810110 ) ) ;
#24134=CARTESIAN_POINT ( 'NONE',  ( -2.070859481142756309, -2.678208067297373152, 0.4182417262808778013 ) ) ;
#24136=CARTESIAN_POINT ( 'NONE',  ( 0.003124719664520466192, -0.5686731593868933343, 0.09441483597926585147 ) ) ;
#24137=CARTESIAN_POINT ( 'NONE',  ( 0.4813782568983027699, -1.076368431653871971, 0.6093178202591913450 ) ) ;
#24138=CARTESIAN_POINT ( 'NONE',  ( -0.002132486385545492077, -0.8570572293951210785, 0.2363897508679551895 ) ) ;
#24140=CARTESIAN_POINT ( 'NONE',  ( 0.4199384557880279645, -0.9749410087210258480, 0.8268343460595501959 ) ) ;
#24141=EDGE_CURVE ( 'NONE', #356, #38533, #28906, .T. ) ;
#24148=CARTESIAN_POINT ( 'NONE',  ( 0.03323571768382589664, -0.7628981867746865708, 0.6419652344973219016 ) ) ;
#24149=CARTESIAN_POINT ( 'NONE',  ( 0.1286531880915040282, -0.5504795770112219655, 0.1533591383774981221 ) ) ;
#24153=CARTESIAN_POINT ( 'NONE',  ( 0.1918124086860224231, -0.5891232155910660628, 0.2119633080407007653 ) ) ;
#24163=CARTESIAN_POINT ( 'NONE',  ( 0.1619021036549118109, -1.239954387664122804, 0.6006692075211629289 ) ) ;
#24164=CARTESIAN_POINT ( 'NONE',  ( 0.1868433879157239408, -0.8567470366939088366, 0.6079207818232758020 ) ) ;
#24165=CARTESIAN_POINT ( 'NONE',  ( 0.3076776373462946079, -1.692203703971726148, 0.8683076824790618709 ) ) ;
#24166=CARTESIAN_POINT ( 'NONE',  ( 0.09958715870559087247, -0.5710702051975550253, 0.2566525979842094185 ) ) ;
#24167=CARTESIAN_POINT ( 'NONE',  ( 0.3224073211681580675, -1.764214325044133780, 0.5172595626481488740 ) ) ;
#24168=CARTESIAN_POINT ( 'NONE',  ( -0.001716626588588560445, -0.8384702095208486083, 0.07132058285942260989 ) ) ;
#24169=CARTESIAN_POINT ( 'NONE',  ( 6.320982786526573478E-21, -0.9481888444201335142, 0.1628301291833881004 ) ) ;
#24172=CARTESIAN_POINT ( 'NONE',  ( 0.3768783096114195486, -1.720370743462858343, 0.4222122349756301518 ) ) ;
#24173=CARTESIAN_POINT ( 'NONE',  ( 0.3074793524532691835, -0.8298883473507410180, 0.6448015414277138424 ) ) ;
#24176=CARTESIAN_POINT ( 'NONE',  ( 0.06936654275873489761, -1.327133429011184917, 0.5458395137742713121 ) ) ;
#24178=CARTESIAN_POINT ( 'NONE',  ( 0.3144318060873547704, -1.185957278504782941, 0.4815581988605170949 ) ) ;
#24179=CARTESIAN_POINT ( 'NONE',  ( 0.1880247778135462344, -0.6881053353252821747, 0.1842137475136224611 ) ) ;
#24186=CARTESIAN_POINT ( 'NONE',  ( 0.6064900336555086868, -1.480007000944690398, 0.5584290337526855996 ) ) ;
#24187=EDGE_LOOP ( 'NONE', ( #25306, #13565 ) ) ;
#24192=CARTESIAN_POINT ( 'NONE',  ( 0.2234517780780992391, -1.345597857905709294, 0.6134231468698841949 ) ) ;
#24198=CARTESIAN_POINT ( 'NONE',  ( 0.4351441434883658310, -1.191296924415893965, 0.6803100719843556687 ) ) ;
#24204=CARTESIAN_POINT ( 'NONE',  ( 0.07443973040452947498, -1.324188178367487145, 0.5273133236568789961 ) ) ;
#24206=CARTESIAN_POINT ( 'NONE',  ( 0.1853096727063575921, -0.4547550531002670371, -0.03797464539687132878 ) ) ;
#24207=CARTESIAN_POINT ( 'NONE',  ( 0.3152971339881030510, -1.290423043535891656, 0.8808430741779670337 ) ) ;
#24209=CARTESIAN_POINT ( 'NONE',  ( 0.2003689620726051279, -0.7510051162810029712, 0.3312793566268386614 ) ) ;
#24214=CARTESIAN_POINT ( 'NONE',  ( 0.5818144595221569348, -1.494326653636363522, 0.6059908575948350640 ) ) ;
#24217=FACE_OUTER_BOUND ( 'NONE', #33519, .T. ) ;
#24222=CARTESIAN_POINT ( 'NONE',  ( 0.2366026829857577063, -0.6283501033379368383, 0.5457308484972661633 ) ) ;
#24223=CARTESIAN_POINT ( 'NONE',  ( 0.08146015332400657893, -1.318321297778866308, 0.4704503523288177669 ) ) ;
#24226=CARTESIAN_POINT ( 'NONE',  ( 0.6340757229130811190, -1.590406591614232479, 0.6099564950747226044 ) ) ;
#24231=CARTESIAN_POINT ( 'NONE',  ( 0.006340579314978117206, -0.5092170189304694450, 0.4201425565785884553 ) ) ;
#24234=CARTESIAN_POINT ( 'NONE',  ( 0.3532546603346390923, -1.752899160574764137, 0.5887449090255344464 ) ) ;
#24237=CARTESIAN_POINT ( 'NONE',  ( 0.3523703943677440331, -1.135285113435899884, 0.5996270292805977453 ) ) ;
#24240=CARTESIAN_POINT ( 'NONE',  ( 0.3321123081999855509, -1.047335542731505420, 0.7624713745059377157 ) ) ;
#24243=CARTESIAN_POINT ( 'NONE',  ( 0.5030539720840632167, -1.104010818905506675, 0.6157662270679344907 ) ) ;
#24244=ORIENTED_EDGE ( 'NONE', *, *, #4254, .T. ) ;
#24250=CARTESIAN_POINT ( 'NONE',  ( 0.2272720996045521635, -1.257744579346037561, 0.9080304507863062868 ) ) ;
#24251=CARTESIAN_POINT ( 'NONE',  ( 0.6611561708455119257, -1.539609889559191869, 0.4316073648859315437 ) ) ;
#24252=CARTESIAN_POINT ( 'NONE',  ( 0.1762911760445602105, -0.5715213023984071494, -0.05307465194668001957 ) ) ;
#24255=CARTESIAN_POINT ( 'NONE',  ( 0.4591084281630142261, -1.062138763103065875, 0.7175457429786104013 ) ) ;
#24256=EDGE_CURVE ( 'NONE', #8281, #13526, #713, .T. ) ;
#24261=CARTESIAN_POINT ( 'NONE',  ( 0.07907905168991602451, -0.8327024128097892941, 0.1796145744779967246 ) ) ;
#24262=DIRECTION ( 'NONE',  ( 0.8660512985181135770, 0.4999551463232368431, 0.000000000000000000 ) ) ;
#24271=CARTESIAN_POINT ( 'NONE',  ( 0.4258872143332720350, -1.124793373273393682, 0.5082973339379032174 ) ) ;
#24272=CARTESIAN_POINT ( 'NONE',  ( 0.05992090360963518020, -1.332693131100006312, 0.5739722883257112329 ) ) ;
#24274=CARTESIAN_POINT ( 'NONE',  ( 0.4852819058807865682, -1.130531678747876967, 0.4902071956013302478 ) ) ;
#24275=CARTESIAN_POINT ( 'NONE',  ( 0.4958658331358156701, -1.219703574955436576, 0.6057417262809811076 ) ) ;
#24278=( BOUNDED_SURFACE ( )  B_SPLINE_SURFACE ( 3, 2, ( 
 ( #24696, #37228, #34130 ),
 ( #28174, #38228, #31461 ),
 ( #29182, #3268, #19121 ),
 ( #31661, #16245, #3478 ) ),
 .UNSPECIFIED., .F., .F., .F. ) 
 B_SPLINE_SURFACE_WITH_KNOTS ( ( 4, 4 ),
 ( 3, 3 ),
 ( -7.975391180803370617E-16, 0.0006271655702608574731 ),
 ( 0.000000000000000000, 1.000000000000000000 ),
 .UNSPECIFIED. ) 
 GEOMETRIC_REPRESENTATION_ITEM ( )  RATIONAL_B_SPLINE_SURFACE ( (
 ( 1.000000000000000000, 0.7064740011966007538, 1.000000000000000000),
 ( 1.000000000000000000, 0.7219955957196710905, 1.000000000000000000),
 ( 1.000000000000000000, 0.7376221875044689513, 1.000000000000000000),
 ( 1.000000000000000000, 0.7525568848367699681, 1.000000000000000000) ) ) 
 REPRESENTATION_ITEM ( '' )  SURFACE ( )  );
#24286=DIRECTION ( 'NONE',  ( -0.01455087615875037474, -0.9998941303973200023, -4.739223851275271008E-17 ) ) ;
#24295=CARTESIAN_POINT ( 'NONE',  ( 0.2661946161772972275, -1.675245939826407016, 0.5712008051485940596 ) ) ;
#24297=CARTESIAN_POINT ( 'NONE',  ( 0.1293833808128240226, -1.251700972679722357, 0.6057482417128505769 ) ) ;
#24303=CARTESIAN_POINT ( 'NONE',  ( 0.01159594543348162025, -0.8166607006614792219, -0.07868870078605369467 ) ) ;
#24306=CARTESIAN_POINT ( 'NONE',  ( 0.2950454914726564071, -0.9974602440063756736, 0.7344975353665614826 ) ) ;
#24307=CARTESIAN_POINT ( 'NONE',  ( 0.1859701558446418823, -0.7915647177415402469, 0.06398500588167709002 ) ) ;
#24308=FACE_BOUND ( 'NONE', #25098, .T. ) ;
#24310=ADVANCED_FACE ( 'NONE', ( #29584 ), #8711, .T. ) ;
#24313=ADVANCED_FACE ( 'NONE', ( #37183 ), #26434, .F. ) ;
#24315=CARTESIAN_POINT ( 'NONE',  ( 0.4787764723021453728, -1.660223331282874915, 0.4687417262808790119 ) ) ;
#24316=CARTESIAN_POINT ( 'NONE',  ( -1.501945623848432731E-05, -0.9404952636685606215, 0.08221629722440988719 ) ) ;
#24320=CARTESIAN_POINT ( 'NONE',  ( 0.01707166242847063184, -0.6102210326195973700, 0.5232503585198154950 ) ) ;
#24321=CARTESIAN_POINT ( 'NONE',  ( 0.05627171146895854764, -1.105186018705181406, 0.7448477350381816908 ) ) ;
#24323=CARTESIAN_POINT ( 'NONE',  ( 0.7205914100055046401, -1.471989004879187490, 0.6461535000039996257 ) ) ;
#24330=VERTEX_POINT ( 'NONE', #27931 ) ;
#24332=CARTESIAN_POINT ( 'NONE',  ( 0.08536974246100553776, -0.9712496366881051557, 0.8111207091837429051 ) ) ;
#24333=CARTESIAN_POINT ( 'NONE',  ( 0.4692603364931002274, -1.311301443745613193, 0.8202886701068771158 ) ) ;
#24336=CARTESIAN_POINT ( 'NONE',  ( 0.3050116026255210722, -0.8112037691066587008, 0.6500339927034136656 ) ) ;
#24339=CARTESIAN_POINT ( 'NONE',  ( 0.1978587402095111636, -0.5849795632145003976, 0.3178455878192510409 ) ) ;
#24346=CARTESIAN_POINT ( 'NONE',  ( 0.1570735404638902155, -0.8185203973244239428, 0.5474549588355609453 ) ) ;
#24349=CARTESIAN_POINT ( 'NONE',  ( 0.4975257062221719595, -1.542520066884107477, 0.5745007069453309523 ) ) ;
#24350=CARTESIAN_POINT ( 'NONE',  ( 0.3228300096166880628, -1.762500210627791830, 0.5312294313579276617 ) ) ;
#24351=CARTESIAN_POINT ( 'NONE',  ( -0.001003582044002233756, -0.7901068500879731005, 0.01239078819350922581 ) ) ;
#24352=CARTESIAN_POINT ( 'NONE',  ( 0.04506684102745490278, -1.071221704980362732, 0.6225836480969521025 ) ) ;
#24357=CARTESIAN_POINT ( 'NONE',  ( 0.3490285838404457164, -0.8930994557897173891, 0.6976986907528974768 ) ) ;
#24361=CARTESIAN_POINT ( 'NONE',  ( 0.2649651584399684845, -1.675931921620917420, 0.5387030096079383767 ) ) ;
#24363=CARTESIAN_POINT ( 'NONE',  ( 0.5392338747517343434, -1.163405467613477295, 0.6464276897500325081 ) ) ;
#24370=CARTESIAN_POINT ( 'NONE',  ( 0.4154866155576192877, -1.204292224885589402, 0.6716659532497037954 ) ) ;
#24373=DIRECTION ( 'NONE',  ( 0.01455087615875041117, 0.9998941303973198913, 0.000000000000000000 ) ) ;
#24376=CARTESIAN_POINT ( 'NONE',  ( 0.2554305435801562107, -0.9452134505148684918, 0.6994406939077150165 ) ) ;
#24379=CARTESIAN_POINT ( 'NONE',  ( 0.008503815048827287337, -0.8451467311994965703, 0.1811066047224641762 ) ) ;
#24385=CARTESIAN_POINT ( 'NONE',  ( 0.7429241260303105499, -1.515741207197444762, 0.5682417262808782121 ) ) ;
#24387=CARTESIAN_POINT ( 'NONE',  ( 0.3518875961510150585, -1.091088960822164555, 0.7123828146467774403 ) ) ;
#24391=ORIENTED_EDGE ( 'NONE', *, *, #23024, .F. ) ;
#24395=CARTESIAN_POINT ( 'NONE',  ( 0.1832751269464030219, -0.7337134285967986669, 0.1015045423513593059 ) ) ;
#24396=CARTESIAN_POINT ( 'NONE',  ( 0.4258307314927392007, -1.528964036469551369, 0.7696345003288364017 ) ) ;
#24399=CARTESIAN_POINT ( 'NONE',  ( 0.3047823188150395324, -1.756856274844342147, 0.5653043665036784349 ) ) ;
#24401=CONICAL_SURFACE ( 'NONE', #28965, 0.1624877031048690135, 0.1745329251994329756 ) ;
#24409=CARTESIAN_POINT ( 'NONE',  ( 0.5009665901131933330, -1.376049689205368187, 0.8038812696496657750 ) ) ;
#24410=CARTESIAN_POINT ( 'NONE',  ( 0.4664189868188083898, -1.671521195344378041, 0.4684108820178269350 ) ) ;
#24419=CARTESIAN_POINT ( 'NONE',  ( 0.1946137278002632309, -0.5377497569806550803, 0.3020257395598471839 ) ) ;
#24421=CARTESIAN_POINT ( 'NONE',  ( 0.01141983555232837372, -0.9471369104752583867, 0.2153783958211964722 ) ) ;
#24424=CARTESIAN_POINT ( 'NONE',  ( 0.1186103394390872201, -1.414144848331978510, 0.5683298932114988489 ) ) ;
#24425=CARTESIAN_POINT ( 'NONE',  ( 0.6983652742124539792, -1.438553779962960188, 0.5551970221657683835 ) ) ;
#24427=ORIENTED_EDGE ( 'NONE', *, *, #20338, .T. ) ;
#24429=CARTESIAN_POINT ( 'NONE',  ( 0.5640895105453352931, -1.503407492374277510, 0.5358556994421860287 ) ) ;
#24432=ADVANCED_FACE ( 'NONE', ( #37569, #28530 ), #14620, .F. ) ;
#24438=FACE_OUTER_BOUND ( 'NONE', #10067, .T. ) ;
#24441=CARTESIAN_POINT ( 'NONE',  ( 0.4793721387301719816, -1.262504312832766651, 0.7257340988765215162 ) ) ;
#24444=CARTESIAN_POINT ( 'NONE',  ( 0.4930347527585871026, -1.093336683456308078, 0.6301225560750347565 ) ) ;
#24450=CARTESIAN_POINT ( 'NONE',  ( 0.3556005243248319680, -1.622197365539165936, 0.5664687466889557488 ) ) ;
#24452=CARTESIAN_POINT ( 'NONE',  ( 0.1130246885457655975, -0.7035223855512272584, -0.09530233752769670663 ) ) ;
#24453=DIRECTION ( 'NONE',  ( 0.000000000000000000, -0.8660477418057305199, 0.4999613074160784154 ) ) ;
#24454=ORIENTED_EDGE ( 'NONE', *, *, #15554, .T. ) ;
#24455=ORIENTED_EDGE ( 'NONE', *, *, #38942, .T. ) ;
#24456=CARTESIAN_POINT ( 'NONE',  ( 0.3793161018499474069, -0.9685596994469443111, 0.6812625861292541662 ) ) ;
#24457=CARTESIAN_POINT ( 'NONE',  ( 0.3111660121705961957, -1.077154095635142417, 0.8049933954744191711 ) ) ;
#24466=CARTESIAN_POINT ( 'NONE',  ( 0.5714515714113984624, -1.616742210554280135, 0.5707417262808793801 ) ) ;
#24470=DIRECTION ( 'NONE',  ( 0.8660512985181133550, 0.4999551463232370652, 0.000000000000000000 ) ) ;
#24473=CARTESIAN_POINT ( 'NONE',  ( 0.4808682371952084367, -1.130070160517919753, 0.4859207442516079722 ) ) ;
#24474=CARTESIAN_POINT ( 'NONE',  ( 0.4510981778992304569, -1.245710572978114161, 0.6057417262809815517 ) ) ;
#24476=CARTESIAN_POINT ( 'NONE',  ( 0.0003542010310559907385, -0.4591614539952885155, 0.04612386700675097373 ) ) ;
#24477=CARTESIAN_POINT ( 'NONE',  ( 0.0004750592482352814579, -0.4386115460793976739, 0.1457185332388683252 ) ) ;
#24478=CARTESIAN_POINT ( 'NONE',  ( 0.0004755335033020558909, -0.4388027427473707998, 0.1568150681250891076 ) ) ;
#24479=CARTESIAN_POINT ( 'NONE',  ( 0.5953303036072959964, -1.457508885835639978, 0.6057417262805095959 ) ) ;
#24480=EDGE_CURVE ( 'NONE', #10169, #35222, #7223, .T. ) ;
#24482=EDGE_CURVE ( 'NONE', #5559, #35870, #10532, .T. ) ;
#24483=ORIENTED_EDGE ( 'NONE', *, *, #30346, .F. ) ;
#24487=EDGE_CURVE ( 'NONE', #9452, #37238, #5519, .T. ) ;
#24488=AXIS2_PLACEMENT_3D ( 'NONE', #13626, #39136, #35430 ) ;
#24490=CARTESIAN_POINT ( 'NONE',  ( 0.01056578810015139022, -0.5296855280550349931, 0.1486859626770064002 ) ) ;
#24495=CIRCLE ( 'NONE', #34991, 0.02499999999999998404 ) ;
#24498=CARTESIAN_POINT ( 'NONE',  ( 0.2654089594124767748, -1.674916358741208144, 0.5606694567451773192 ) ) ;
#24499=CARTESIAN_POINT ( 'NONE',  ( 0.3538654265270187449, -1.126342156508903791, 0.7354529254703474628 ) ) ;
#24500=CARTESIAN_POINT ( 'NONE',  ( 0.1691312463165446367, -1.239161314218422127, 0.5978938133338337346 ) ) ;
#24504=CARTESIAN_POINT ( 'NONE',  ( 0.5382316988408143432, -1.161161114027098318, 0.5682417262808693303 ) ) ;
#24508=CARTESIAN_POINT ( 'NONE',  ( 0.3424415908864473779, -1.747937484235617012, 0.4483338674949445268 ) ) ;
#24510=B_SPLINE_SURFACE_WITH_KNOTS ( 'NONE', 3, 3, ( 
 ( #22638, #3275, #25704, #22031, #40523, #19339, #34746, #22425, #34552, #2880, #248, #12538, #12961, #22231, #37425, #19543, #15830, #25093, #19131, #9238, #21813, #16253, #38235, #16046, #6157, #649, #6364, #12746, #37847, #18721, #18933, #31669, #34953, #463, #31277, #31878, #10064 ),
 ( #15634, #28181, #46, #3486, #28592, #37629, #31468, #6971, #15433, #29589, #38448, #23454, #7778, #1244, #20347, #10282, #13563, #22848, #1434, #29192, #16433, #29798, #32866, #35972, #19723, #16857, #25925, #13948, #32075, #26310, #4076, #20150, #4675, #1640, #35367, #29400, #26130 ),
 ( #17247, #26729, #23641, #10884, #36161, #1054, #35556, #38644, #32678, #13745, #26517, #14159, #7576, #39258, #32256, #17048, #11081, #4484, #16643, #38837, #4291, #39053, #10666, #10463, #3881, #7972, #28977, #842, #13350, #23029, #19930, #7157, #7353, #32466, #23238, #35765, #24240 ),
 ( #17456, #27723, #11275, #14554, #5278, #17844, #33079, #30807, #8383, #40258, #12091, #24657, #8185, #1838, #23842, #36364, #37187, #26918, #20951, #24441, #33681, #30403, #20546, #14354, #2234, #5492, #4889, #18060, #39652, #8574, #2436, #30005, #33473, #11489, #39448, #20759, #14774 ),
 ( #30611, #27336, #33281, #5088, #39865, #30194, #11686, #17648, #2024, #33908, #15163, #14973, #27122, #21370, #24054, #36580, #36763, #40049, #21152, #27527, #11871, #36973, #8793, #5705, #18263, #2628, #25248, #37992, #9189, #34697, #31823, #9609, #37376, #31423, #21972, #37789, #3225 ),
 ( #31007, #195, #28320, #34501, #16204, #12687, #2828, #410, #21757, #22184, #40475, #18453, #25653, #6312, #5893, #28739, #12297, #3044, #18884, #15774, #21567, #19283, #37573, #601, #13095, #9005, #34292, #15379, #24856, #6097, #34090, #27935, #9396, #12905, #6504, #19075, #18666 ),
 ( #31229, #31613, #15589, #3430, #3642, #28136, #1, #25460, #15989, #28534, #12481, #25036, #9801, #22374, #34896, #6708, #32020, #14107, #10415, #7106, #16806, #6915, #19489, #10831, #32815, #10610, #3828, #38999, #4024, #22976, #35495, #16383, #13512, #7301, #32629, #35712, #28924 ),
 ( #29352, #789, #13299, #25871, #38386, #35109, #29741, #10224, #4238, #4436, #38594, #1193, #17193, #22793, #19880, #32415, #13696, #35316, #19673, #16590, #32209, #29136, #10012, #13888, #1584, #38184, #22582, #26463, #998, #23187, #26075, #26263, #20099, #38781, #7520, #16996, #29538 ),
 ( #1379, #23406, #35923, #7730, #20295, #4619, #39599, #36309, #5237, #36110, #7916, #40004, #21315, #39815, #20489, #27479, #33237, #11434, #24000, #33026, #1979, #36529, #21099, #24198, #4829, #18001, #2384, #8340, #14924, #17400, #8130, #29960, #36721, #23787, #11035, #24387, #11826 ),
 ( #5655, #14309, #20909, #27066, #30350, #11221, #26871, #5044, #1796, #17606, #39214, #36922, #30758, #2577, #23594, #8737, #33853, #30561, #2181, #8530, #20705, #39402, #26681, #18210, #14501, #30151, #33431, #14719, #17792, #33625, #27284, #11640, #5439, #24987, #7027, #40618, #21524 ) ),
 .UNSPECIFIED., .F., .F., .F.,
 ( 4, 3, 3, 4 ),
 ( 4, 3, 3, 3, 3, 3, 3, 3, 3, 3, 3, 3, 4 ),
 ( 0.2346684314605614330, 0.4922368959575419423, 0.6210211282060321691, 0.7498053604545223960 ),
 ( 0.002735921434322369401, 0.006796569813770247936, 0.01085721819321812734, 0.01897851495211388614, 0.03522110846990540028, 0.05146370198769691096, 0.06770629550548842857, 0.08394888902327994618, 0.1001914825410714638, 0.1326766695766544990, 0.1651618566122375342, 0.1976470436478205417, 0.2626174177189866121 ),
 .UNSPECIFIED. ) ;
#24511=CARTESIAN_POINT ( 'NONE',  ( 0.4662195773891402162, -1.247030207462705986, 0.8121041408566435083 ) ) ;
#24515=CARTESIAN_POINT ( 'NONE',  ( 0.1266021694322588542, -1.239399129679921829, 0.5182417262812423209 ) ) ;
#24517=CARTESIAN_POINT ( 'NONE',  ( 0.3218125531527813998, -1.760402285594251159, 0.6125947341875596086 ) ) ;
#24518=CARTESIAN_POINT ( 'NONE',  ( 0.3830298086532948343, -1.726706798021515610, 0.4282875075352186034 ) ) ;
#24521=CARTESIAN_POINT ( 'NONE',  ( 0.5714515714113984624, -1.616742210554280135, 0.5707417262808793801 ) ) ;
#24522=( BOUNDED_SURFACE ( )  B_SPLINE_SURFACE ( 3, 2, ( 
 ( #12393, #24950, #21877 ),
 ( #6415, #25564, #22483 ),
 ( #34405, #308, #6221 ),
 ( #31339, #12203, #37904 ) ),
 .UNSPECIFIED., .F., .F., .F. ) 
 B_SPLINE_SURFACE_WITH_KNOTS ( ( 4, 4 ),
 ( 3, 3 ),
 ( -3.035766082959412415E-18, 0.0002157631431912795808 ),
 ( 0.000000000000000000, 1.000000000000000000 ),
 .UNSPECIFIED. ) 
 GEOMETRIC_REPRESENTATION_ITEM ( )  RATIONAL_B_SPLINE_SURFACE ( (
 ( 1.000000000000000000, 0.6984366549430296445, 1.000000000000000000),
 ( 1.000000000000000000, 0.6988655720237708646, 1.000000000000000000),
 ( 1.000000000000000000, 0.6993079394701908758, 1.000000000000000000),
 ( 1.000000000000000000, 0.6997606559984659302, 1.000000000000000000) ) ) 
 REPRESENTATION_ITEM ( '' )  SURFACE ( )  );
#24523=CARTESIAN_POINT ( 'NONE',  ( 0.4051897154098655363, -1.104944129929064101, 0.6010342342611436628 ) ) ;
#24528=CARTESIAN_POINT ( 'NONE',  ( 0.01197363197122058853, -0.5805133742323803636, 0.4689902101802463363 ) ) ;
#24529=CARTESIAN_POINT ( 'NONE',  ( 0.04888454729359380940, -1.019292185716472732, 0.7074266517341860627 ) ) ;
#24532=CARTESIAN_POINT ( 'NONE',  ( 0.7168528728721502707, -1.464418552067108470, 0.6746166867755808427 ) ) ;
#24542=CARTESIAN_POINT ( 'NONE',  ( 0.2585116059216619466, -1.600704214304080608, 0.8541279405034801764 ) ) ;
#24544=CARTESIAN_POINT ( 'NONE',  ( 0.5884674137009996420, -1.491157991441193209, 0.5851315895956400448 ) ) ;
#24545=CARTESIAN_POINT ( 'NONE',  ( 0.3441766385685567364, -1.748888513973746228, 0.4490806875465770398 ) ) ;
#24548=CARTESIAN_POINT ( 'NONE',  ( 0.2254586261693722060, -0.6723955984770768612, 0.4589204916406527945 ) ) ;
#24557=CARTESIAN_POINT ( 'NONE',  ( 0.08982948562931099279, -0.7300237816344226083, 0.2455375391678501773 ) ) ;
#24561=CARTESIAN_POINT ( 'NONE',  ( 0.1038461025547566530, -0.5461054185183505938, 0.1537531581841332651 ) ) ;
#24563=CARTESIAN_POINT ( 'NONE',  ( 0.07044958284825096617, -1.315011783116714073, 0.5339628106424040288 ) ) ;
#24565=CARTESIAN_POINT ( 'NONE',  ( 0.02056819537566472247, -1.080172155999248318, 0.6281642683093259238 ) ) ;
#24566=VERTEX_POINT ( 'NONE', #13508 ) ;
#24569=CARTESIAN_POINT ( 'NONE',  ( 0.2465799821153819571, -0.7910269351804194438, 0.7388407842391677693 ) ) ;
#24575=CARTESIAN_POINT ( 'NONE',  ( 0.3184462859233389564, -1.172215077377981585, 0.5535637004880700207 ) ) ;
#24576=CARTESIAN_POINT ( 'NONE',  ( 0.1886295724182434630, -0.6892155111403490686, 0.2012867199884409153 ) ) ;
#24594=CARTESIAN_POINT ( 'NONE',  ( 0.05336070580022266724, -1.000409524100160485, 0.6919889636817496692 ) ) ;
#24597=CARTESIAN_POINT ( 'NONE',  ( 0.3163627804571104707, -1.761805152290217613, 0.5682287416806770519 ) ) ;
#24603=CARTESIAN_POINT ( 'NONE',  ( 0.005475248526801685008, -0.9459170876539717554, 0.1457173627829773666 ) ) ;
#24606=CARTESIAN_POINT ( 'NONE',  ( 0.2003523658259203089, -0.8065114950566329988, 0.6680553503048993758 ) ) ;
#24607=VERTEX_POINT ( 'NONE', #29956 ) ;
#24609=CARTESIAN_POINT ( 'NONE',  ( 0.06157545530246535254, -0.5616945561363291262, 0.2499708142322518700 ) ) ;
#24612=FACE_OUTER_BOUND ( 'NONE', #17545, .T. ) ;
#24616=VERTEX_POINT ( 'NONE', #11823 ) ;
#24622=CARTESIAN_POINT ( 'NONE',  ( 0.1787419356640313761, -0.7505968874023245530, 0.5623186377554705295 ) ) ;
#24623=CARTESIAN_POINT ( 'NONE',  ( 0.4764753233885406503, -1.665949717495130766, 0.4947212307176814261 ) ) ;
#24630=CARTESIAN_POINT ( 'NONE',  ( 0.2144086742444059612, -1.243025793896146869, 0.5645655484585248018 ) ) ;
#24634=CARTESIAN_POINT ( 'NONE',  ( 0.6791962457086077043, -1.401251971513146621, 0.6322342638419099492 ) ) ;
#24636=CARTESIAN_POINT ( 'NONE',  ( 0.01276022671919619343, -1.030438920969866334, 0.5664345702674732363 ) ) ;
#24639=CARTESIAN_POINT ( 'NONE',  ( 0.1044625578173912356, -0.8429083989444113856, 0.3673943131971453835 ) ) ;
#24640=CARTESIAN_POINT ( 'NONE',  ( 0.2681719626984005456, -1.674357821296572846, 0.5749781514038686536 ) ) ;
#24642=EDGE_LOOP ( 'NONE', ( #7150, #2286, #2533, #30170, #19271, #3596, #13461, #5701 ) ) ;
#24651=VERTEX_POINT ( 'NONE', #40202 ) ;
#24655=CYLINDRICAL_SURFACE ( 'NONE', #21766, 0.1762268159172277748 ) ;
#24657=CARTESIAN_POINT ( 'NONE',  ( 0.5188837243650441522, -1.324382180592332148, 0.6742563569798550871 ) ) ;
#24660=CARTESIAN_POINT ( 'NONE',  ( 0.2317493251130877951, -0.9016848682509819302, 0.4453502113744062241 ) ) ;
#24669=CARTESIAN_POINT ( 'NONE',  ( 0.03696608829255258744, -0.5625377656374845881, 0.2658259557143141660 ) ) ;
#24671=CARTESIAN_POINT ( 'NONE',  ( 0.1855568200014149904, -0.7725989946471569780, 0.002349788420466783143 ) ) ;
#24675=CARTESIAN_POINT ( 'NONE',  ( 0.3744491522119342553, -1.096499884473891129, 0.6351544032997803457 ) ) ;
#24676=CARTESIAN_POINT ( 'NONE',  ( 0.3711814119498326736, -1.195443994201320415, 0.8360198855415841290 ) ) ;
#24684=CARTESIAN_POINT ( 'NONE',  ( 0.3931005117246323399, -1.715828765679402679, 0.3667417262808779777 ) ) ;
#24690=CARTESIAN_POINT ( 'NONE',  ( 0.4878316403371781851, -1.125113395602889810, 0.5164237391570506430 ) ) ;
#24691=CARTESIAN_POINT ( 'NONE',  ( 0.4609248481599033109, -1.239710877643270814, 0.6057417262809816627 ) ) ;
#24693=CARTESIAN_POINT ( 'NONE',  ( 0.1233923337978296703, -1.433947342477501108, 0.6209663710929820279 ) ) ;
#24695=DIRECTION ( 'NONE',  ( -0.4999551463232372317, 0.8660512985181134660, -0.000000000000000000 ) ) ;
#24696=CARTESIAN_POINT ( 'NONE',  ( 0.3434800707738534520, -1.169184835483325857, 0.4282596159935431746 ) ) ;
#24701=CARTESIAN_POINT ( 'NONE',  ( 0.2637112460222606480, -1.676801009589977465, 0.5217148786151403206 ) ) ;
#24704=CARTESIAN_POINT ( 'NONE',  ( 0.002012706044603155327, -0.5245499851267817482, 0.1047619216058349734 ) ) ;
#24705=ORIENTED_EDGE ( 'NONE', *, *, #18335, .T. ) ;
#24707=B_SPLINE_CURVE_WITH_KNOTS ( 'NONE', 3,
 ( #39536, #33566, #8285, #11369, #33378, #5181, #30285, #27221, #5381, #39284, #4321, #32893, #38866, #10699 ),
 .UNSPECIFIED., .F., .F.,
 ( 4, 2, 2, 2, 2, 2, 4 ),
 ( 1.262897753262582698E-17, 0.0007771926555927994576, 0.001554385311185586338, 0.001942981638981979833, 0.002331577966778373111, 0.002720174294574766605, 0.003108770622371160100 ),
 .UNSPECIFIED. ) ;
#24708=CIRCLE ( 'NONE', #6944, 0.009999999999999894390 ) ;
#24709=VERTEX_POINT ( 'NONE', #11429 ) ;
#24712=CARTESIAN_POINT ( 'NONE',  ( 0.008877318523083597632, -0.6275083649376383965, 0.4284230457359336497 ) ) ;
#24713=CARTESIAN_POINT ( 'NONE',  ( 0.3720203041987413806, -1.150922219009145042, 0.7251981425757600963 ) ) ;
#24714=CARTESIAN_POINT ( 'NONE',  ( 0.08830248264660876811, -1.300195518436201514, 0.5784869194914967760 ) ) ;
#24722=FACE_OUTER_BOUND ( 'NONE', #5670, .T. ) ;
#24724=CARTESIAN_POINT ( 'NONE',  ( 0.4998018223844837848, -1.298799938538372167, 0.7895654180778867159 ) ) ;
#24725=DIRECTION ( 'NONE',  ( 0.8660512985181133550, 0.4999551463232373982, 0.000000000000000000 ) ) ;
#24727=B_SPLINE_CURVE_WITH_KNOTS ( 'NONE', 3,
 ( #19275, #31815, #3632, #28917 ),
 .UNSPECIFIED., .F., .F.,
 ( 4, 4 ),
 ( 6.254634441385501517E-18, 0.0006271655702610368002 ),
 .UNSPECIFIED. ) ;
#24730=CARTESIAN_POINT ( 'NONE',  ( 0.6586301574024518990, -1.563739711041315816, 0.4687417262808791230 ) ) ;
#24737=CARTESIAN_POINT ( 'NONE',  ( 0.2936473109780965429, -1.729059834919730809, 0.6366410771178455663 ) ) ;
#24738=CARTESIAN_POINT ( 'NONE',  ( 0.04400829994862880817, -1.043756151267425603, 0.7156344331538354586 ) ) ;
#24740=CARTESIAN_POINT ( 'NONE',  ( 0.6786648513340227673, -1.399193080605451334, 0.7803980693475389696 ) ) ;
#24742=DIRECTION ( 'NONE',  ( 0.8660512985181133550, 0.4999551463232373982, 0.000000000000000000 ) ) ;
#24745=EDGE_CURVE ( 'NONE', #15727, #34759, #29570, .T. ) ;
#24748=CARTESIAN_POINT ( 'NONE',  ( 0.1901695884102587719, -0.5023773489605858344, 0.1477569985384105666 ) ) ;
#24750=CARTESIAN_POINT ( 'NONE',  ( 0.2292083863995310611, -1.502172107109858379, 0.9124160356758439505 ) ) ;
#24751=CARTESIAN_POINT ( 'NONE',  ( 0.5699498466869539204, -1.462345630761733739, 0.7181541738695536026 ) ) ;
#24753=ORIENTED_EDGE ( 'NONE', *, *, #16465, .T. ) ;
#24754=CARTESIAN_POINT ( 'NONE',  ( 0.5463261744266250108, -1.174184195093048277, 0.6317594707774240037 ) ) ;
#24757=LINE ( 'NONE', #37279, #13273 ) ;
#24764=CARTESIAN_POINT ( 'NONE',  ( 0.09262515131973823868, -0.7343695447130378362, 0.2782437690132907315 ) ) ;
#24766=( BOUNDED_SURFACE ( )  B_SPLINE_SURFACE ( 3, 2, ( 
 ( #27398, #4947, #11131 ),
 ( #21006, #18118, #14404 ),
 ( #29858, #2491, #14831 ),
 ( #17513, #11935, #1698 ),
 ( #4734, #20607, #23901 ),
 ( #27581, #39310, #24500 ),
 ( #26967, #36429, #39922 ),
 ( #36818, #30062, #1892 ),
 ( #40107, #11740, #2073 ),
 ( #37032, #14217, #20817 ),
 ( #5144, #17697, #36636 ),
 ( #39712, #26785, #24297 ),
 ( #14610, #30243, #8852 ),
 ( #27182, #11549, #5554 ),
 ( #8440, #36215, #8633 ),
 ( #21206, #33743, #30672 ),
 ( #24910, #18941, #34353 ),
 ( #37641, #28389, #33962 ),
 ( #5762, #12149, #12756 ),
 ( #15226, #37434, #18730 ),
 ( #19139, #9246, #27993 ),
 ( #27784, #40322, #24714 ),
 ( #34147, #31678, #30862 ),
 ( #12352, #18320, #6167 ),
 ( #9672, #34564, #54 ),
 ( #25317, #37245, #21823 ) ),
 .UNSPECIFIED., .F., .F., .F. ) 
 B_SPLINE_SURFACE_WITH_KNOTS ( ( 4, 2, 2, 2, 2, 2, 2, 2, 2, 2, 2, 2, 4 ),
 ( 3, 3 ),
 ( 0.000000000000000000, 0.0006596057055745040533, 0.001319211411149008107, 0.001978817116723512268, 0.002308619969510764241, 0.002638422822298016213, 0.002968225675085268619, 0.003298028527872520592, 0.003627831380659772564, 0.003957634233447024537, 0.004617239939021528482, 0.004947042791808780454, 0.005276845644596032427 ),
 ( 0.000000000000000000, 1.000000000000000000 ),
 .UNSPECIFIED. ) 
 GEOMETRIC_REPRESENTATION_ITEM ( )  RATIONAL_B_SPLINE_SURFACE ( (
 ( 1.000000000000000000, 0.7087361850990782086, 1.000000000000000000),
 ( 1.000000000000000000, 0.6765739502726043630, 1.000000000000000000),
 ( 1.000000000000000000, 0.6402241378258116677, 1.000000000000000000),
 ( 1.000000000000000000, 0.5685252139047779485, 1.000000000000000000),
 ( 1.000000000000000000, 0.5311641938883238101, 1.000000000000000000),
 ( 1.000000000000000000, 0.4614670254680833250, 1.000000000000000000),
 ( 1.000000000000000000, 0.4296915687615939228, 1.000000000000000000),
 ( 1.000000000000000000, 0.3941419833073060430, 1.000000000000000000),
 ( 1.000000000000000000, 0.3843396926333228492, 1.000000000000000000),
 ( 1.000000000000000000, 0.3710601004298905159, 1.000000000000000000),
 ( 1.000000000000000000, 0.3677117356413553417, 1.000000000000000000),
 ( 1.000000000000000000, 0.3678937320958496904, 1.000000000000000000),
 ( 1.000000000000000000, 0.3715092472210990704, 1.000000000000000000),
 ( 1.000000000000000000, 0.3844660984943514825, 1.000000000000000000),
 ( 1.000000000000000000, 0.3936923856040987491, 1.000000000000000000),
 ( 1.000000000000000000, 0.4158998654390018701, 1.000000000000000000),
 ( 1.000000000000000000, 0.4289333015709035357, 1.000000000000000000),
 ( 1.000000000000000000, 0.4565842304191866652, 1.000000000000000000),
 ( 1.000000000000000000, 0.4712877118585055980, 1.000000000000000000),
 ( 1.000000000000000000, 0.5188537258417635911, 1.000000000000000000),
 ( 1.000000000000000000, 0.5552410424637538311, 1.000000000000000000),
 ( 1.000000000000000000, 0.6097807446480927318, 1.000000000000000000),
 ( 1.000000000000000000, 0.6288539315404778618, 1.000000000000000000),
 ( 1.000000000000000000, 0.6690853270610633841, 1.000000000000000000),
 ( 1.000000000000000000, 0.6898774606012713084, 1.000000000000000000),
 ( 1.000000000000000000, 0.7100124105822595011, 1.000000000000000000) ) ) 
 REPRESENTATION_ITEM ( '' )  SURFACE ( )  );
#24767=CARTESIAN_POINT ( 'NONE',  ( 0.1579296938348824231, -0.7527599258947673677, 0.5723136178885942504 ) ) ;
#24768=CARTESIAN_POINT ( 'NONE',  ( 0.3263566400396368250, -1.758504154136070863, 0.4800462819687809080 ) ) ;
#24769=CARTESIAN_POINT ( 'NONE',  ( 0.002222032174280575301, -0.5198793158962575767, 0.1346323604582328748 ) ) ;
#24774=CARTESIAN_POINT ( 'NONE',  ( 0.3251954281970569904, -0.9255269374606153177, 0.8255160753196725265 ) ) ;
#24775=ADVANCED_FACE ( 'NONE', ( #38134 ), #25604, .T. ) ;
#24779=CARTESIAN_POINT ( 'NONE',  ( 0.4685502202651029569, -1.116536938686066183, 0.5688043585934901003 ) ) ;
#24780=( LENGTH_UNIT ( ) NAMED_UNIT ( * ) SI_UNIT ( $, .METRE. ) );
#24782=CARTESIAN_POINT ( 'NONE',  ( 0.07014435923142441076, -1.325199841737237261, 0.5075297796642793680 ) ) ;
#24787=CARTESIAN_POINT ( 'NONE',  ( 0.4556718857535577705, -1.059138143784118302, 0.6919068033735837897 ) ) ;
#24800=VERTEX_POINT ( 'NONE', #35053 ) ;
#24802=CARTESIAN_POINT ( 'NONE',  ( 0.01407560669633875494, -0.9971709087417149897, 0.6860632370118421308 ) ) ;
#24807=CARTESIAN_POINT ( 'NONE',  ( 0.7371735653322752935, -1.498976209023650696, 0.6847608182276055944 ) ) ;
#24810=CARTESIAN_POINT ( 'NONE',  ( 0.01128677947712186484, -0.9461986806730106059, 0.1457185332388702959 ) ) ;
#24816=CARTESIAN_POINT ( 'NONE',  ( 0.1328749367006503146, -0.7849577211208300653, 0.6191913765737894204 ) ) ;
#24818=CARTESIAN_POINT ( 'NONE',  ( 0.5771924405437491856, -1.609115206908811047, 0.4469232899498119527 ) ) ;
#24823=CARTESIAN_POINT ( 'NONE',  ( 0.1822190496678027793, -0.7502263017545820478, 0.5606200488576618124 ) ) ;
#24824=CARTESIAN_POINT ( 'NONE',  ( 0.4446621238095426754, -1.684612092570755726, 0.4299412632484984620 ) ) ;
#24826=EDGE_CURVE ( 'NONE', #24994, #37890, #11431, .T. ) ;
#24828=CARTESIAN_POINT ( 'NONE',  ( 0.08058916068514494768, -1.309220013881624123, 0.4727703015479320370 ) ) ;
#24829=CARTESIAN_POINT ( 'NONE',  ( 0.5908959048872451936, -1.601544548465861695, 0.4282886817583847483 ) ) ;
#24834=CARTESIAN_POINT ( 'NONE',  ( 0.4224057990199354684, -0.9849677903659747047, 0.8092447908785728172 ) ) ;
#24836=CARTESIAN_POINT ( 'NONE',  ( 0.01259362679367681710, -0.9548954960245769064, 0.3190520231937701845 ) ) ;
#24847=CARTESIAN_POINT ( 'NONE',  ( 0.6623769754396896525, -1.516903808842391177, 0.4182417262808777458 ) ) ;
#24853=CARTESIAN_POINT ( 'NONE',  ( 0.3968636464328635372, -1.134397982594676613, 0.6056963140804544343 ) ) ;
#24856=CARTESIAN_POINT ( 'NONE',  ( 0.4151592125368772646, -1.168422792391130116, 0.7279282713727704968 ) ) ;
#24859=CARTESIAN_POINT ( 'NONE',  ( 0.2246580631734754474, -0.8968525156641222740, 0.4249663362035034364 ) ) ;
#24866=CARTESIAN_POINT ( 'NONE',  ( 0.3857633994507903008, -1.605746613796385391, 0.5814654401004829554 ) ) ;
#24868=CARTESIAN_POINT ( 'NONE',  ( 0.1750730331674688889, -0.8628421928542436836, -0.003741419850515158470 ) ) ;
#24869=DIRECTION ( 'NONE',  ( 0.4999551463232371762, -0.8660512985181134660, 0.000000000000000000 ) ) ;
#24871=ORIENTED_EDGE ( 'NONE', *, *, #3444, .F. ) ;
#24872=CARTESIAN_POINT ( 'NONE',  ( 0.3960837959415427489, -1.111483722700696397, 0.6223813603130625705 ) ) ;
#24873=CARTESIAN_POINT ( 'NONE',  ( 0.1303976270792735204, -0.6539453279429289223, 0.4317581259434655760 ) ) ;
#24874=ORIENTED_EDGE ( 'NONE', *, *, #35628, .F. ) ;
#24881=CARTESIAN_POINT ( 'NONE',  ( 0.1637585665034339832, -0.5994899851647166322, 0.1022936816274461203 ) ) ;
#24884=CARTESIAN_POINT ( 'NONE',  ( 0.4206426192640880246, -1.125420795136339747, 0.5391101744456719969 ) ) ;
#24885=CARTESIAN_POINT ( 'NONE',  ( 0.0003547581337898165674, -0.9504652791025145486, 0.2394745140284491591 ) ) ;
#24887=CARTESIAN_POINT ( 'NONE',  ( 0.1991581284650917050, -0.9215239498232444815, 0.3071336240427082753 ) ) ;
#24888=CARTESIAN_POINT ( 'NONE',  ( 0.4312022151739950404, -1.138629288109622273, 0.4375280249474818306 ) ) ;
#24889=CARTESIAN_POINT ( 'NONE',  ( 0.5465277059400872606, -1.167200690009414510, 0.5856983068965131434 ) ) ;
#24891=CARTESIAN_POINT ( 'NONE',  ( -0.002783323111321702164, -0.8122190247268278318, 0.2436509486217987297 ) ) ;
#24900=LINE ( 'NONE', #21420, #20413 ) ;
#24908=CARTESIAN_POINT ( 'NONE',  ( 0.2407897211441908936, -1.453152299343511755, 0.9165384340539985963 ) ) ;
#24909=CARTESIAN_POINT ( 'NONE',  ( 0.1221059964993554542, -0.8717596041297476228, 0.5005114288050678262 ) ) ;
#24910=CARTESIAN_POINT ( 'NONE',  ( 0.1100434532894998957, -1.277816772219506625, 0.6166110354182127162 ) ) ;
#24912=CARTESIAN_POINT ( 'NONE',  ( 0.4026370839150480996, -1.708716391613833041, 0.4182417262808775793 ) ) ;
#24913=VERTEX_POINT ( 'NONE', #17145 ) ;
#24916=CARTESIAN_POINT ( 'NONE',  ( 0.3555645034559717366, -1.742873732338575898, 0.4378062404383618045 ) ) ;
#24918=CARTESIAN_POINT ( 'NONE',  ( 0.3202064935259268941, -1.032063384080334822, 0.7518809291558405938 ) ) ;
#24919=CARTESIAN_POINT ( 'NONE',  ( 0.1874578000378240850, -0.6893444085712847613, 0.06304793604024336307 ) ) ;
#24921=CARTESIAN_POINT ( 'NONE',  ( 0.01226325382937903420, -0.4335986999190264979, 0.2007874243352632537 ) ) ;
#24923=CARTESIAN_POINT ( 'NONE',  ( 0.7472694261237929902, -1.513267490863592135, 0.4687417262808789009 ) ) ;
#24924=CARTESIAN_POINT ( 'NONE',  ( 0.1850349610749611740, -0.7952146172061540508, 0.1457185332388699905 ) ) ;
#24925=CARTESIAN_POINT ( 'NONE',  ( 0.1850841550199354701, -0.8515884040318244530, 0.1812164098636643572 ) ) ;
#24928=CARTESIAN_POINT ( 'NONE',  ( 0.0003038568743942667081, -0.4444331504931744448, 0.2553847410507332771 ) ) ;
#24929=CARTESIAN_POINT ( 'NONE',  ( 0.08174454493327279470, -1.241495247832560489, 0.7557354517501940760 ) ) ;
#24931=CARTESIAN_POINT ( 'NONE',  ( 0.6491914112794352487, -1.351404041023776204, 0.8153926641961858346 ) ) ;
#24936=EDGE_LOOP ( 'NONE', ( #30101, #18903, #23847, #1448 ) ) ;
#24938=CARTESIAN_POINT ( 'NONE',  ( 0.2454656089401869856, -1.560133056456860290, 0.8800177669848034956 ) ) ;
#24939=CARTESIAN_POINT ( 'NONE',  ( 0.5878865232721811607, -1.491222718801129776, 0.5725363768365727690 ) ) ;
#24943=CARTESIAN_POINT ( 'NONE',  ( 0.1876168051218740918, -0.6873969840233377093, 0.1659352930446481023 ) ) ;
#24944=ORIENTED_EDGE ( 'NONE', *, *, #904, .F. ) ;
#24946=CARTESIAN_POINT ( 'NONE',  ( 0.3539056426437465763, -0.9003241868202508380, 0.7035817311501109117 ) ) ;
#24947=CARTESIAN_POINT ( 'NONE',  ( 0.1856533569311497323, -0.7573055082216308964, 0.1457185332388697685 ) ) ;
#24950=CARTESIAN_POINT ( 'NONE',  ( 0.3100229871264634229, -1.765619355789175282, 0.5593676469398397577 ) ) ;
#24951=ORIENTED_EDGE ( 'NONE', *, *, #16543, .T. ) ;
#24952=CARTESIAN_POINT ( 'NONE',  ( 0.2533938263156997883, -0.9611212520725127550, 0.6837618949440756877 ) ) ;
#24953=CARTESIAN_POINT ( 'NONE',  ( 0.3245437662617405850, -1.759079744317569860, 0.6570495871072389305 ) ) ;
#24954=CARTESIAN_POINT ( 'NONE',  ( 0.4817671749021297245, -1.450000170275026479, 0.7905690555072178993 ) ) ;
#24955=CARTESIAN_POINT ( 'NONE',  ( 0.3165945761936767022, -1.762959260158723840, 0.5320016251091660431 ) ) ;
#24958=CARTESIAN_POINT ( 'NONE',  ( 0.4189016656849444686, -1.713998620513816018, 0.6094645527338905522 ) ) ;
#24959=CARTESIAN_POINT ( 'NONE',  ( 0.7359799699820096519, -1.496616301705748997, 0.6950498515647415276 ) ) ;
#24960=CARTESIAN_POINT ( 'NONE',  ( 0.1163334220414616871, -1.415481480104449741, 0.5683323772858765999 ) ) ;
#24962=LINE ( 'NONE', #22302, #14855 ) ;
#24964=CARTESIAN_POINT ( 'NONE',  ( 0.002346242718065488699, -0.9632443647534850717, 0.3631189922238501344 ) ) ;
#24965=CARTESIAN_POINT ( 'NONE',  ( 0.5463261744266250108, -1.174184195093048277, 0.6317594707774240037 ) ) ;
#24968=CARTESIAN_POINT ( 'NONE',  ( 0.3947704391985938921, -1.713677448712424445, 0.4185425205145197336 ) ) ;
#24971=CARTESIAN_POINT ( 'NONE',  ( 0.4673214953140302219, -1.236749788148563400, 0.6057417262809804415 ) ) ;
#24978=CARTESIAN_POINT ( 'NONE',  ( -0.01318839431724684423, -0.8581597300867446210, 0.3276449317425384478 ) ) ;
#24979=ORIENTED_EDGE ( 'NONE', *, *, #37059, .T. ) ;
#24986=ADVANCED_FACE ( 'NONE', ( #29301, #1753 ), #38338, .T. ) ;
#24987=CARTESIAN_POINT ( 'NONE',  ( 0.3782534879241810644, -1.123019940516551740, 0.6966012497027646022 ) ) ;
#24989=CARTESIAN_POINT ( 'NONE',  ( 0.2325938614944302874, -1.347997356825076487, 0.5182417262812506475 ) ) ;
#24991=ORIENTED_EDGE ( 'NONE', *, *, #30152, .T. ) ;
#24993=CARTESIAN_POINT ( 'NONE',  ( 0.09191803790759442427, -0.5734812623173219936, 0.2369789867951458406 ) ) ;
#24994=VERTEX_POINT ( 'NONE', #1335 ) ;
#24995=CARTESIAN_POINT ( 'NONE',  ( 0.7053080889764471451, -1.513942001867420339, 0.5667347313869608438 ) ) ;
#24996=CARTESIAN_POINT ( 'NONE',  ( 0.4143629965670120319, -1.443116486983128111, 0.8306079842001903302 ) ) ;
#24997=DIRECTION ( 'NONE',  ( -0.8662449985352328463, -0.4996194577002526782, 4.774657901377541008E-15 ) ) ;
#24998=CARTESIAN_POINT ( 'NONE',  ( 0.5856637561180031426, -1.604417808857893535, 0.4379681301762496926 ) ) ;
#25000=CARTESIAN_POINT ( 'NONE',  ( 0.3634081991604131701, -1.011642316747166870, 0.6166164155041838901 ) ) ;
#25002=CARTESIAN_POINT ( 'NONE',  ( 0.1175254897578254243, -1.414866947670519570, 0.5260415310556526558 ) ) ;
#25003=CARTESIAN_POINT ( 'NONE',  ( 0.1887433770899517860, -0.4595573870411951978, 0.1492066213800052610 ) ) ;
#25004=CARTESIAN_POINT ( 'NONE',  ( 0.1319611972603651762, -0.6045625464573930463, 0.3271665123075399584 ) ) ;
#25005=CARTESIAN_POINT ( 'NONE',  ( 0.4452565618721048835, -1.695813388727355653, 0.4387187260761371554 ) ) ;
#25013=CARTESIAN_POINT ( 'NONE',  ( 0.2335251464432007984, -1.232233318504470043, 0.5010574213731815441 ) ) ;
#25014=CARTESIAN_POINT ( 'NONE',  ( 0.2791332027808016703, -0.7342173681784933681, 0.6310308052199803397 ) ) ;
#25017=CARTESIAN_POINT ( 'NONE',  ( 0.05037753678752365100, -1.191647567912915040, 0.6657367322637173235 ) ) ;
#25021=CARTESIAN_POINT ( 'NONE',  ( 0.1263930849240390564, -0.8569068895757016024, 0.4518561175853242906 ) ) ;
#25022=CARTESIAN_POINT ( 'NONE',  ( 0.2631236827724738325, -1.677172619524047947, 0.5509572661685944173 ) ) ;
#25025=DIRECTION ( 'NONE',  ( 0.4999551463232372317, -0.8660512985181134660, 0.000000000000000000 ) ) ;
#25026=CARTESIAN_POINT ( 'NONE',  ( 0.4415664673242307714, -1.208588400238274740, 0.7960777065921241791 ) ) ;
#25032=CARTESIAN_POINT ( 'NONE',  ( 0.1514213231021494244, -1.394936281994370697, 0.5181495499691263218 ) ) ;
#25033=CARTESIAN_POINT ( 'NONE',  ( 0.3249649890265327024, -1.766762640835898290, 0.5057684568561345850 ) ) ;
#25036=CARTESIAN_POINT ( 'NONE',  ( 0.4901888945983902679, -1.275704295442520397, 0.6511736332760663659 ) ) ;
#25041=CARTESIAN_POINT ( 'NONE',  ( 0.1874346505856443745, -0.8710952576279675785, 0.2160754816401605771 ) ) ;
#25042=VERTEX_POINT ( 'NONE', #8079 ) ;
#25049=CARTESIAN_POINT ( 'NONE',  ( 0.3135982152475476070, -1.415948938436505822, 0.8853364428893668592 ) ) ;
#25051=CARTESIAN_POINT ( 'NONE',  ( 0.1137653586930576638, -0.5867251212695386853, -0.07337486296685742648 ) ) ;
#25058=CARTESIAN_POINT ( 'NONE',  ( 0.4084715984908769415, -1.024951146690285642, 0.6323129096802421190 ) ) ;
#25059=CARTESIAN_POINT ( 'NONE',  ( 0.4998774473189910861, -1.399813891400437216, 0.7994217634795599547 ) ) ;
#25061=CARTESIAN_POINT ( 'NONE',  ( 0.1870184603604498619, -0.7197645011776521162, 0.03166985066965816165 ) ) ;
#25070=CARTESIAN_POINT ( 'NONE',  ( 0.07779920321647403048, -1.322114474344633583, 0.5682417262808776570 ) ) ;
#25075=CARTESIAN_POINT ( 'NONE',  ( 0.4903202831852248589, -1.081274614053407523, 0.5895842322316532380 ) ) ;
#25077=CARTESIAN_POINT ( 'NONE',  ( 0.4669205535706663635, -1.236249669535754103, 0.6057417262809816627 ) ) ;
#25080=AXIS2_PLACEMENT_3D ( 'NONE', #17851, #30411, #2242 ) ;
#25081=CARTESIAN_POINT ( 'NONE',  ( -0.0004320282599767403219, -0.9107381779821550616, 0.3274798035714688860 ) ) ;
#25082=CARTESIAN_POINT ( 'NONE',  ( 0.2615233978049238406, -1.678084768816710648, 0.5373352594323992371 ) ) ;
#25084=FACE_OUTER_BOUND ( 'NONE', #16390, .T. ) ;
#25093=CARTESIAN_POINT ( 'NONE',  ( 0.5328035064341107852, -1.351445797141976213, 0.7805622800820304352 ) ) ;
#25096=ORIENTED_EDGE ( 'NONE', *, *, #31101, .F. ) ;
#25097=CARTESIAN_POINT ( 'NONE',  ( 0.5532309630114417009, -1.623494765793418670, 0.5182130042910411127 ) ) ;
#25098=EDGE_LOOP ( 'NONE', ( #10363, #16871 ) ) ;
#25099=CARTESIAN_POINT ( 'NONE',  ( 0.01228388642712701859, -0.5615114497096570512, 0.2760925587857833707 ) ) ;
#25100=CARTESIAN_POINT ( 'NONE',  ( 0.3780826364363035208, -1.158814516788133409, 0.7205068528634307468 ) ) ;
#25106=CARTESIAN_POINT ( 'NONE',  ( 0.4092767628406372982, -1.698388671139740680, 0.4182417262808776903 ) ) ;
#25112=CARTESIAN_POINT ( 'NONE',  ( 0.2042467818395008738, -0.8389012776653698156, 0.6553572424280913467 ) ) ;
#25116=CARTESIAN_POINT ( 'NONE',  ( 0.6984807982178791175, -1.438753897344778432, 0.5682417262808779901 ) ) ;
#25117=CARTESIAN_POINT ( 'NONE',  ( 0.2731127878045417900, -1.644505663937311013, 0.7612257175765594353 ) ) ;
#25120=CARTESIAN_POINT ( 'NONE',  ( 0.01524602687849146640, -0.4843663032112671130, 0.3577232613832507790 ) ) ;
#25124=CARTESIAN_POINT ( 'NONE',  ( 0.1856533569311497323, -0.7573055082216308964, 0.1457185332388697685 ) ) ;
#25128=CARTESIAN_POINT ( 'NONE',  ( 0.001298983775798597754, -0.4632363948272406606, 0.3098607539948510792 ) ) ;
#25129=CARTESIAN_POINT ( 'NONE',  ( 0.09875757964952747159, -1.346375778014429425, 0.7038248674981169017 ) ) ;
#25131=B_SPLINE_CURVE_WITH_KNOTS ( 'NONE', 3,
 ( #5571, #1505, #14231, #14019, #26594, #5158, #39132, #26796 ),
 .UNSPECIFIED., .F., .F.,
 ( 4, 2, 2, 4 ),
 ( 1.734723475976807094E-18, 0.0009467803671446852441, 0.001420170550717034155, 0.001893560734289383065 ),
 .UNSPECIFIED. ) ;
#25132=CIRCLE ( 'NONE', #38271, 0.009999999999999986330 ) ;
#25135=AXIS2_PLACEMENT_3D ( 'NONE', #2693, #12162, #24725 ) ;
#25139=CARTESIAN_POINT ( 'NONE',  ( 0.1053303053968787928, -1.411347232757804271, 0.5669086859767527020 ) ) ;
#25140=CARTESIAN_POINT ( 'NONE',  ( 0.2248388864219118266, -1.477604057314256369, 0.9308881366616725828 ) ) ;
#25143=CARTESIAN_POINT ( 'NONE',  ( 0.5956979317618377179, -1.486985939769752241, 0.5919158884504209794 ) ) ;
#25144=CARTESIAN_POINT ( 'NONE',  ( 0.4362155086522900849, -1.060665164869476929, 0.5182417262812423209 ) ) ;
#25146=CARTESIAN_POINT ( 'NONE',  ( 0.5537997781288683807, -1.186498928682228504, 0.6031466697272260813 ) ) ;
#25149=CARTESIAN_POINT ( 'NONE',  ( 0.6993646500685410938, -1.437698798162368341, 0.6034325323896145843 ) ) ;
#25152=LINE ( 'NONE', #3322, #25948 ) ;
#25154=DIRECTION ( 'NONE',  ( 1.060606950627616897E-16, 6.122684696619992497E-17, 1.000000000000000000 ) ) ;
#25156=CARTESIAN_POINT ( 'NONE',  ( 0.08659262626681933639, -0.7684511726617067051, 0.2033331541635994277 ) ) ;
#25157=DIRECTION ( 'NONE',  ( 0.4999551463232372317, -0.8660512985181135770, 0.000000000000000000 ) ) ;
#25158=CARTESIAN_POINT ( 'NONE',  ( 0.5250024315009472753, -1.526804064326204413, 0.5696525905436546910 ) ) ;
#25161=ORIENTED_EDGE ( 'NONE', *, *, #21075, .F. ) ;
#25164=CARTESIAN_POINT ( 'NONE',  ( 0.7431085294082976356, -1.516429236334945196, 0.5637232355900747560 ) ) ;
#25166=CARTESIAN_POINT ( 'NONE',  ( 0.6088915796500192767, -1.479003135906368227, 0.5701753227515949929 ) ) ;
#25171=CARTESIAN_POINT ( 'NONE',  ( 0.05579155178881651383, -1.335540925555324332, 0.3667417262808778111 ) ) ;
#25173=CARTESIAN_POINT ( 'NONE',  ( 0.04695358122948785351, -1.249483587492180581, 0.6552810377283075915 ) ) ;
#25175=CARTESIAN_POINT ( 'NONE',  ( 0.3550363906115478474, -0.9559691138050746551, 0.6482402363088731745 ) ) ;
#25178=ORIENTED_EDGE ( 'NONE', *, *, #28513, .F. ) ;
#25182=CARTESIAN_POINT ( 'NONE',  ( 0.4139939964727673005, -1.143890656390630367, 0.4261699876408763799 ) ) ;
#25185=CARTESIAN_POINT ( 'NONE',  ( 0.1911258005295297935, -0.8295430315077879646, 0.2652737953583465536 ) ) ;
#25187=CARTESIAN_POINT ( 'NONE',  ( 0.2321526281619643584, -1.233007205928619232, 0.3667417262808778111 ) ) ;
#25188=CARTESIAN_POINT ( 'NONE',  ( 0.007912233754840233141, -0.9669037819151463653, 0.6493826208389911203 ) ) ;
#25192=AXIS2_PLACEMENT_3D ( 'NONE', #34685, #19061, #37773 ) ;
#25201=CARTESIAN_POINT ( 'NONE',  ( 0.09836942906952807208, -0.6323750885681652667, 0.3152165718758609958 ) ) ;
#25205=CARTESIAN_POINT ( 'NONE',  ( 0.4416675145290221427, -1.573766806705525489, 0.5734788493934752651 ) ) ;
#25208=CARTESIAN_POINT ( 'NONE',  ( 0.06936654275873489761, -1.327133429011184917, 0.5458395137742713121 ) ) ;
#25209=CARTESIAN_POINT ( 'NONE',  ( 0.4912014431318024732, -1.081758076222086862, 0.5909367962944523933 ) ) ;
#25212=CARTESIAN_POINT ( 'NONE',  ( 0.5805227504890819734, -1.495156126203962987, 0.5657488023295393909 ) ) ;
#25220=CARTESIAN_POINT ( 'NONE',  ( 0.4378619693737221819, -1.010538247186560268, 0.8194577876302902020 ) ) ;
#25221=VECTOR ( 'NONE', #23229, 39.37007874015748854 ) ;
#25224=CARTESIAN_POINT ( 'NONE',  ( 0.01419313219423278850, -1.039704043814793755, 0.5807212468082825207 ) ) ;
#25230=CARTESIAN_POINT ( 'NONE',  ( 0.2676415634711663549, -1.674658064059759033, 0.5739467722781522729 ) ) ;
#25231=AXIS2_PLACEMENT_3D ( 'NONE', #27325, #20942, #30393 ) ;
#25236=CARTESIAN_POINT ( 'NONE',  ( 0.5010411840214703538, -1.300757910890522062, 0.7890095542399213624 ) ) ;
#25239=CARTESIAN_POINT ( 'NONE',  ( 0.3398313727135623963, -1.151616092976642136, 0.5895549894284093373 ) ) ;
#25240=ORIENTED_EDGE ( 'NONE', *, *, #37185, .F. ) ;
#25244=CARTESIAN_POINT ( 'NONE',  ( 0.1859093133543100740, -0.7573093211699954974, 0.1754562816741712661 ) ) ;
#25248=CARTESIAN_POINT ( 'NONE',  ( 0.4340226251431142934, -1.195050833747549834, 0.7346307913083539587 ) ) ;
#25251=CARTESIAN_POINT ( 'NONE',  ( 0.1920143701880955289, -0.8743002769911518701, 0.2704752137325454608 ) ) ;
#25255=VERTEX_POINT ( 'NONE', #31512 ) ;
#25258=CARTESIAN_POINT ( 'NONE',  ( 0.05827439840305041058, -0.6775244079679950682, 0.4991996434535173055 ) ) ;
#25259=CARTESIAN_POINT ( 'NONE',  ( 0.08569141848276186357, -0.7951378289679750244, 0.08553711018156767709 ) ) ;
#25260=CARTESIAN_POINT ( 'NONE',  ( 0.1132202721956721558, -0.6714642036273535952, -0.09530415291956083335 ) ) ;
#25265=VERTEX_POINT ( 'NONE', #24947 ) ;
#25266=CARTESIAN_POINT ( 'NONE',  ( 0.4152142928025790991, -1.128277177651309193, 0.5697251069065648599 ) ) ;
#25267=CARTESIAN_POINT ( 'NONE',  ( 0.1176201142355292467, -0.5735051211531788651, 0.2538439209176449607 ) ) ;
#25269=AXIS2_PLACEMENT_3D ( 'NONE', #33492, #20974, #32888 ) ;
#25270=CARTESIAN_POINT ( 'NONE',  ( 0.1874127487346899379, -0.6926261066621903772, 0.03768796299198888533 ) ) ;
#25275=CARTESIAN_POINT ( 'NONE',  ( 0.07779920321647403048, -1.322114474344633583, 0.5682417262808776570 ) ) ;
#25277=CARTESIAN_POINT ( 'NONE',  ( 0.08693421129271258763, -0.7278123032406825788, 0.02060656405704834257 ) ) ;
#25288=CARTESIAN_POINT ( 'NONE',  ( 0.4862843069642890925, -1.079060212656593798, 0.6007065101366493298 ) ) ;
#25290=CARTESIAN_POINT ( 'NONE',  ( 0.2086414000262838409, -1.361922069228335364, 0.4817113886979867421 ) ) ;
#25292=CARTESIAN_POINT ( 'NONE',  ( 0.4474210138429077221, -1.247506387532115735, 0.6057417262809816627 ) ) ;
#25297=CARTESIAN_POINT ( 'NONE',  ( -0.003075981321608621880, -0.8070878537792822716, 0.1960017582677906212 ) ) ;
#25298=CARTESIAN_POINT ( 'NONE',  ( 8.402003333010158955E-05, -0.6075279228541787813, -0.09071442693374498489 ) ) ;
#25301=TOROIDAL_SURFACE ( 'NONE', #29906, 0.04749999999977554815, 0.01000000000000000021 ) ;
#25305=CARTESIAN_POINT ( 'NONE',  ( 0.3704391661570882177, -1.756796239285488337, 0.5182417262812423209 ) ) ;
#25306=ORIENTED_EDGE ( 'NONE', *, *, #1735, .F. ) ;
#25309=DIRECTION ( 'NONE',  ( -0.8660512985181135770, -0.4999551463232368431, 0.000000000000000000 ) ) ;
#25315=CARTESIAN_POINT ( 'NONE',  ( 0.1177973440672865080, -0.9935853818565597573, 0.8155281618166205782 ) ) ;
#25316=CARTESIAN_POINT ( 'NONE',  ( 0.07530787293288457307, -0.8414947218206061397, 0.3166737376759417022 ) ) ;
#25317=CARTESIAN_POINT ( 'NONE',  ( 0.07780827639779400173, -1.322105357709411733, 0.5682417262808776570 ) ) ;
#25318=CARTESIAN_POINT ( 'NONE',  ( 0.3100229871264633674, -1.765619355789175948, 0.5593676469398386475 ) ) ;
#25319=CARTESIAN_POINT ( 'NONE',  ( 0.1881312614525582350, -0.9196856789278203825, 0.05501147976861575639 ) ) ;
#25326=CARTESIAN_POINT ( 'NONE',  ( 0.1862143093560568174, -0.9153542374865832887, 0.1410250186500938141 ) ) ;
#25329=CARTESIAN_POINT ( 'NONE',  ( 0.5480184601717554838, -1.413123777809382364, 0.7684874893864968026 ) ) ;
#25330=CARTESIAN_POINT ( 'NONE',  ( 0.3071154694917676009, -1.047539419770983304, 0.7367026581941298335 ) ) ;
#25332=CARTESIAN_POINT ( 'NONE',  ( 0.2130547489620155110, -1.418506719972717489, 0.9320990850557395735 ) ) ;
#25333=CARTESIAN_POINT ( 'NONE',  ( 0.1596578019756997591, -1.106139421783004062, 0.9882459099239285782 ) ) ;
#25337=CARTESIAN_POINT ( 'NONE',  ( 0.1566196390284286255, -1.366403859981695224, 0.5182417262812423209 ) ) ;
#25341=EDGE_CURVE ( 'NONE', #16916, #11170, #20780, .T. ) ;
#25342=B_SPLINE_CURVE_WITH_KNOTS ( 'NONE', 3,
 ( #11472, #8370, #29780, #2420 ),
 .UNSPECIFIED., .F., .F.,
 ( 4, 4 ),
 ( 3.469446951953613804E-18, 0.0002990235347002869089 ),
 .UNSPECIFIED. ) ;
#25346=CARTESIAN_POINT ( 'NONE',  ( 0.1040330991377019648, -1.397689221518311653, 0.6251921974533098947 ) ) ;
#25349=AXIS2_PLACEMENT_3D ( 'NONE', #1981, #4438, #14110 ) ;
#25351=CARTESIAN_POINT ( 'NONE',  ( 0.7071741867143577220, -1.496830158817513023, 0.5329102775952888615 ) ) ;
#25358=CARTESIAN_POINT ( 'NONE',  ( 0.2162209611966269818, -1.457820977148307051, 0.9280216023009758564 ) ) ;
#25360=CARTESIAN_POINT ( 'NONE',  ( 0.1322362858526628659, -0.5735584538993211412, 0.2455366585897305887 ) ) ;
#25361=CARTESIAN_POINT ( 'NONE',  ( 0.3817257825202987065, -1.726009493650376259, 0.4251351636136782575 ) ) ;
#25362=VERTEX_POINT ( 'NONE', #33286 ) ;
#25375=CARTESIAN_POINT ( 'NONE',  ( 0.08538299691383864631, -0.7671892257780278390, 0.1457185332388683252 ) ) ;
#25377=CARTESIAN_POINT ( 'NONE',  ( 0.5265351747158187878, -1.525993753803500663, 0.6091402573601836234 ) ) ;
#25381=CARTESIAN_POINT ( 'NONE',  ( 0.4419048264408250715, -1.686280600454902245, 0.4284299735159858291 ) ) ;
#25383=CARTESIAN_POINT ( 'NONE',  ( 0.6879396389015977054, -1.414347470100213666, 0.6986533948158418772 ) ) ;
#25384=AXIS2_PLACEMENT_3D ( 'NONE', #12013, #2751, #5627 ) ;
#25387=CARTESIAN_POINT ( 'NONE',  ( 0.1348063704134844498, -0.5683947605430353933, 0.2284001142341055557 ) ) ;
#25391=CARTESIAN_POINT ( 'NONE',  ( 0.1435064959217801916, -1.283467536720964697, 0.5197417262808780025 ) ) ;
#25395=CARTESIAN_POINT ( 'NONE',  ( 0.008926059106093127415, -1.005466151381485762, 0.5191422350400326513 ) ) ;
#25396=CARTESIAN_POINT ( 'NONE',  ( 0.5135568109339374576, -1.117989077717415292, 0.5796127612779116145 ) ) ;
#25399=CARTESIAN_POINT ( 'NONE',  ( 0.5138082349489954126, -1.531582140144923443, 0.5361777791604406262 ) ) ;
#25401=ORIENTED_EDGE ( 'NONE', *, *, #34575, .T. ) ;
#25404=CARTESIAN_POINT ( 'NONE',  ( 0.1893571754530913309, -0.8322940459586247730, 0.2468763379997500618 ) ) ;
#25405=ORIENTED_EDGE ( 'NONE', *, *, #35525, .T. ) ;
#25407=CARTESIAN_POINT ( 'NONE',  ( 0.4971920908461615607, -1.080069027881642052, 0.4687417262808780127 ) ) ;
#25408=CARTESIAN_POINT ( 'NONE',  ( -0.002729411228280882208, -0.9128323640382212112, 0.5539659124371107968 ) ) ;
#25409=ORIENTED_EDGE ( 'NONE', *, *, #13943, .F. ) ;
#25412=DIRECTION ( 'NONE',  ( -0.8660512985181135770, -0.4999551463232370097, 0.000000000000000000 ) ) ;
#25420=ORIENTED_EDGE ( 'NONE', *, *, #38315, .T. ) ;
#25421=ORIENTED_EDGE ( 'NONE', *, *, #21749, .T. ) ;
#25423=CARTESIAN_POINT ( 'NONE',  ( 0.09255270613366611832, -0.5765971826892936081, 0.2511563476660008676 ) ) ;
#25426=CARTESIAN_POINT ( 'NONE',  ( 2.155092840285021536E-05, -0.4374981960197986131, 0.2330919378759825356 ) ) ;
#25427=CARTESIAN_POINT ( 'NONE',  ( 0.3368577323154672287, -1.280641800761222360, 0.8706439758358487380 ) ) ;
#25430=CARTESIAN_POINT ( 'NONE',  ( 0.005980720888701209978, -0.8455916207747946611, 0.1457185332388707122 ) ) ;
#25431=CARTESIAN_POINT ( 'NONE',  ( 0.4929465528686921560, -1.082715557938388029, 0.5682417262808779901 ) ) ;
#25433=CARTESIAN_POINT ( 'NONE',  ( 0.1897112079047662825, -0.5340520988485676357, 0.1406012133455345203 ) ) ;
#25434=CARTESIAN_POINT ( 'NONE',  ( 0.5814726822843937493, -1.495195014991375304, 0.5853331262226206810 ) ) ;
#25438=CARTESIAN_POINT ( 'NONE',  ( 0.07161007277227926515, -0.5641287990778131034, 0.2518656736807903807 ) ) ;
#25441=CARTESIAN_POINT ( 'NONE',  ( 0.2097017171917790468, -0.6397877375661684685, 0.3875311123790295409 ) ) ;
#25442=FACE_OUTER_BOUND ( 'NONE', #20723, .T. ) ;
#25443=CARTESIAN_POINT ( 'NONE',  ( 0.06380316775577042632, -1.284647545824749049, 0.6326371944557522831 ) ) ;
#25446=CARTESIAN_POINT ( 'NONE',  ( 0.1950551304375616468, -0.8882144403296816648, 0.6132150535162333993 ) ) ;
#25447=CARTESIAN_POINT ( 'NONE',  ( 0.3663975874019590462, -1.157438136726378408, 0.4269148889825721827 ) ) ;
#25450=CYLINDRICAL_SURFACE ( 'NONE', #25979, 0.08749999999977552123 ) ;
#25451=CARTESIAN_POINT ( 'NONE',  ( 0.2382400519805366879, -0.9170320373645088896, 0.6858731337248115123 ) ) ;
#25457=CARTESIAN_POINT ( 'NONE',  ( 0.2955290772965331048, -1.312059711113043869, 0.4171601467298353683 ) ) ;
#25460=CARTESIAN_POINT ( 'NONE',  ( 0.4990439851886846467, -1.290753470885830367, 0.6181967010847094768 ) ) ;
#25462=CARTESIAN_POINT ( 'NONE',  ( 0.3206961510659663839, -1.761846847463105714, 0.5004172992779960527 ) ) ;
#25463=CARTESIAN_POINT ( 'NONE',  ( 0.4903202831852248589, -1.081274614053407523, 0.5895842322316532380 ) ) ;
#25466=DIRECTION ( 'NONE',  ( -0.4999551463231795001, 0.8660512985181467727, -4.414622697374767230E-14 ) ) ;
#25467=ORIENTED_EDGE ( 'NONE', *, *, #26110, .T. ) ;
#25468=CARTESIAN_POINT ( 'NONE',  ( 0.1074504339463943636, -0.8508434056105943499, 0.7040215940812857287 ) ) ;
#25469=CARTESIAN_POINT ( 'NONE',  ( 0.08520265857480655014, -0.8310134553494858967, 0.1293978458592746628 ) ) ;
#25474=DIRECTION ( 'NONE',  ( -0.5196387294542602620, 0.8543860900384334656, 0.000000000000000000 ) ) ;
#25475=CARTESIAN_POINT ( 'NONE',  ( 0.1193658396322129084, -0.5857129773433993325, 0.2871785300524037909 ) ) ;
#25477=CARTESIAN_POINT ( 'NONE',  ( 0.07082949537098930104, -1.327879666565185968, 0.4918166835856172536 ) ) ;
#25481=DIRECTION ( 'NONE',  ( 0.4999551463232372317, -0.8660512985181134660, 0.000000000000000000 ) ) ;
#25483=CARTESIAN_POINT ( 'NONE',  ( 0.08509945581906654122, -0.7689446773063483009, 0.1451249978468672763 ) ) ;
#25484=CARTESIAN_POINT ( 'NONE',  ( 0.6320591615222423965, -1.324690328322339239, 0.8595101463142521547 ) ) ;
#25486=CARTESIAN_POINT ( 'NONE',  ( 0.08591898661219740663, -1.312985777298583567, 0.5876069855766993255 ) ) ;
#25487=ADVANCED_FACE ( 'NONE', ( #8580 ), #24401, .F. ) ;
#25492=CARTESIAN_POINT ( 'NONE',  ( 0.3535325904207607950, -1.006223909752091972, 0.6094712593526115940 ) ) ;
#25494=CARTESIAN_POINT ( 'NONE',  ( 0.06486042810549992599, -1.341249661891149803, 0.5682417262808776570 ) ) ;
#25495=CARTESIAN_POINT ( 'NONE',  ( 0.2626492960486415673, -1.683514498680941607, 0.5584510130552119422 ) ) ;
#25496=CARTESIAN_POINT ( 'NONE',  ( -0.003124719664520056797, -0.8057675726412014683, 0.1627348865840318737 ) ) ;
#25497=CARTESIAN_POINT ( 'NONE',  ( 0.0003398915440874476107, -0.4642088512194108563, 0.03525733416984885848 ) ) ;
#25503=DIRECTION ( 'NONE',  ( 1.000000000000000000, 0.000000000000000000, 0.000000000000000000 ) ) ;
#25507=FACE_OUTER_BOUND ( 'NONE', #33127, .T. ) ;
#25511=ORIENTED_EDGE ( 'NONE', *, *, #27649, .T. ) ;
#25515=CARTESIAN_POINT ( 'NONE',  ( 0.2970205159420773455, -1.628083574653397481, 0.7594346419547136628 ) ) ;
#25517=DIRECTION ( 'NONE',  ( 0.4999551463232372317, -0.8660512985181134660, 0.000000000000000000 ) ) ;
#25528=CARTESIAN_POINT ( 'NONE',  ( 0.1109098225493666129, -0.9286357918493259866, 0.1499897478545695051 ) ) ;
#25530=CARTESIAN_POINT ( 'NONE',  ( 0.5676195825672284423, -1.407416061909668725, 0.7341546013530008130 ) ) ;
#25531=CARTESIAN_POINT ( 'NONE',  ( 0.3607701097029427095, -1.124548115609032672, 0.7351652811684338262 ) ) ;
#25532=CARTESIAN_POINT ( 'NONE',  ( 0.01251508115950892945, -0.5804186138772022829, 0.3264740463578477137 ) ) ;
#25533=CARTESIAN_POINT ( 'NONE',  ( 0.4784772001453526657, -1.116132439391088749, 0.5343330151343557155 ) ) ;
#25536=CARTESIAN_POINT ( 'NONE',  ( 0.4647870327407357394, -1.232526483438142861, 0.6307241740363012106 ) ) ;
#25541=CARTESIAN_POINT ( 'NONE',  ( 0.02385183771220368218, -0.6100559285722760849, 0.5958381505304063408 ) ) ;
#25542=CARTESIAN_POINT ( 'NONE',  ( 0.1036797529164252135, -1.395233841299822419, 0.6304550959310950553 ) ) ;
#25549=CARTESIAN_POINT ( 'NONE',  ( 0.3777575235213288529, -1.142457055047713110, 0.4315219747622728863 ) ) ;
#25553=CARTESIAN_POINT ( 'NONE',  ( 0.5949237905379889391, -1.487194157178949094, 0.5729122955301783060 ) ) ;
#25555=EDGE_LOOP ( 'NONE', ( #15628, #27715, #29305, #22997, #37591, #6753 ) ) ;
#25558=CARTESIAN_POINT ( 'NONE',  ( 0.6233902549407862592, -1.444966001498531272, 0.8349750966499661642 ) ) ;
#25563=EDGE_CURVE ( 'NONE', #36473, #4497, #38885, .T. ) ;
#25564=CARTESIAN_POINT ( 'NONE',  ( 0.3099339588126717171, -1.765677022123078421, 0.5623500827625801390 ) ) ;
#25567=CARTESIAN_POINT ( 'NONE',  ( 0.09437040392396874033, -0.7574139486114807029, 0.2971058147919648507 ) ) ;
#25568=CARTESIAN_POINT ( 'NONE',  ( 0.08990536851188153655, -0.5646295468556791208, 0.1460913089649357455 ) ) ;
#25569=CARTESIAN_POINT ( 'NONE',  ( 0.4943412959198616452, -1.443455042774087760, 0.7864209901413284909 ) ) ;
#25572=CARTESIAN_POINT ( 'NONE',  ( 0.6806522551434478485, -1.498521771693993587, 0.4238695236950315026 ) ) ;
#25575=CARTESIAN_POINT ( 'NONE',  ( 0.7432499820993477835, -1.511365401434814570, 0.6392776140757149284 ) ) ;
#25577=DIRECTION ( 'NONE',  ( 0.4999551463232371762, -0.8660512985181134660, 0.000000000000000000 ) ) ;
#25578=CARTESIAN_POINT ( 'NONE',  ( 0.6089010132592387325, -1.475778064326142003, 0.6288872192019396845 ) ) ;
#25582=EDGE_CURVE ( 'NONE', #10550, #8335, #37797, .T. ) ;
#25586=CARTESIAN_POINT ( 'NONE',  ( 0.003677659035771949428, -0.9373694290314303901, 0.4460629830528545781 ) ) ;
#25587=CARTESIAN_POINT ( 'NONE',  ( 0.3909368226714677319, -0.9916197579736178991, 0.6726537802841677793 ) ) ;
#25589=CARTESIAN_POINT ( 'NONE',  ( 0.1626176757286639796, -0.6782218769987641283, 0.05683303076865411224 ) ) ;
#25594=ORIENTED_EDGE ( 'NONE', *, *, #8121, .F. ) ;
#25599=CARTESIAN_POINT ( 'NONE',  ( 0.3208715077212234701, -1.182672892261233732, 0.4687417262808780127 ) ) ;
#25600=CARTESIAN_POINT ( 'NONE',  ( 0.1669163231849704332, -1.368600478287528288, 0.6337086473961658362 ) ) ;
#25604=CYLINDRICAL_SURFACE ( 'NONE', #30932, 0.1000000000000000194 ) ;
#25605=DIRECTION ( 'NONE',  ( 0.8660512985181133550, 0.4999551463232373982, 0.000000000000000000 ) ) ;
#25609=ORIENTED_EDGE ( 'NONE', *, *, #8505, .F. ) ;
#25610=CARTESIAN_POINT ( 'NONE',  ( 0.3098984767712536503, -1.765718780359063267, 0.5682417262808792113 ) ) ;
#25612=CARTESIAN_POINT ( 'NONE',  ( 0.1991057831364872188, -0.8359650798049160780, 0.6453486718655260246 ) ) ;
#25614=CARTESIAN_POINT ( 'NONE',  ( 0.02277869702299618881, -0.6155849950919007885, 0.5815368015377633260 ) ) ;
#25615=CARTESIAN_POINT ( 'NONE',  ( 0.1228925711962478157, -0.7562269421748776255, 0.5887331513672725558 ) ) ;
#25619=CARTESIAN_POINT ( 'NONE',  ( 0.1875000000000002220, -0.9151275355372970877, 0.1608123706567810285 ) ) ;
#25622=CARTESIAN_POINT ( 'NONE',  ( 0.1887412855916308085, -0.4595320686313653646, 0.1436109887884128300 ) ) ;
#25623=CARTESIAN_POINT ( 'NONE',  ( 0.1718105009781868697, -0.7246503184330945757, 0.5294875450235927428 ) ) ;
#25629=EDGE_CURVE ( 'NONE', #14919, #23555, #19152, .T. ) ;
#25630=CARTESIAN_POINT ( 'NONE',  ( 0.1963745812722482442, -0.6060194383687296238, 0.2878283022669332891 ) ) ;
#25632=CARTESIAN_POINT ( 'NONE',  ( 0.5111972025864910396, -1.114343631621611763, 0.5700687535673305550 ) ) ;
#25633=CARTESIAN_POINT ( 'NONE',  ( 0.03810263172085913419, -1.166682418185958525, 0.6773769210087452475 ) ) ;
#25637=CARTESIAN_POINT ( 'NONE',  ( 0.4315008625312996560, -1.186182859931574685, 0.6815412659474554546 ) ) ;
#25640=CARTESIAN_POINT ( 'NONE',  ( 0.7031996424904172205, -1.495314321248880862, 0.5017627394515868922 ) ) ;
#25644=CARTESIAN_POINT ( 'NONE',  ( 0.5202166948571674832, -1.331060376252395816, 0.7806648288483002407 ) ) ;
#25647=CARTESIAN_POINT ( 'NONE',  ( 0.3751813939980868096, -1.114089948641664440, 0.6058345290201684330 ) ) ;
#25648=ORIENTED_EDGE ( 'NONE', *, *, #10680, .F. ) ;
#25650=CARTESIAN_POINT ( 'NONE',  ( 0.3317329491067714242, -1.291263278213948817, 0.4170592068404440633 ) ) ;
#25653=CARTESIAN_POINT ( 'NONE',  ( 0.4956954725223758351, -1.285442406743084964, 0.6670609216475702485 ) ) ;
#25656=CARTESIAN_POINT ( 'NONE',  ( 0.2632752295237112405, -1.677058126094923329, 0.5210370874354662840 ) ) ;
#25657=CARTESIAN_POINT ( 'NONE',  ( 0.4929465528686921560, -1.082715557938388029, 0.5685663778595840823 ) ) ;
#25660=CARTESIAN_POINT ( 'NONE',  ( 0.06254816942709211236, -1.140419159346305777, 0.7531148659283598557 ) ) ;
#25662=CARTESIAN_POINT ( 'NONE',  ( 0.3317989971924339421, -1.461076630628523665, 0.8685545625247669266 ) ) ;
#25663=CARTESIAN_POINT ( 'NONE',  ( 0.08572706863110483855, -0.8134827521777350245, 0.07519561625211983180 ) ) ;
#25664=CARTESIAN_POINT ( 'NONE',  ( 0.1981136876533342028, -0.5988876534399234508, 0.3156152556879199267 ) ) ;
#25666=ORIENTED_EDGE ( 'NONE', *, *, #27291, .F. ) ;
#25669=VERTEX_POINT ( 'NONE', #26876 ) ;
#25671=CARTESIAN_POINT ( 'NONE',  ( 0.5668833231537255823, -1.503228122861213878, 0.5723226605073136186 ) ) ;
#25679=AXIS2_PLACEMENT_3D ( 'NONE', #40433, #24997, #9151 ) ;
#25682=DIRECTION ( 'NONE',  ( 0.4999551463232372317, -0.8660512985181134660, 0.000000000000000000 ) ) ;
#25689=CARTESIAN_POINT ( 'NONE',  ( 0.5193158764790237747, -1.143105642405225053, 0.8514134314631569556 ) ) ;
#25692=CARTESIAN_POINT ( 'NONE',  ( 0.2190338188766751681, -1.487106827364948147, 0.9008211596871106286 ) ) ;
#25693=CARTESIAN_POINT ( 'NONE',  ( 0.0001425719452660938885, -0.5630222807798194173, -0.07015382250872513603 ) ) ;
#25697=ORIENTED_EDGE ( 'NONE', *, *, #38312, .T. ) ;
#25704=CARTESIAN_POINT ( 'NONE',  ( 0.5980105188037525554, -1.461600014062093722, 0.6143516452787856075 ) ) ;
#25710=CARTESIAN_POINT ( 'NONE',  ( 0.2971099084452207273, -1.656645455338934481, 0.5725024039952387733 ) ) ;
#25711=CARTESIAN_POINT ( 'NONE',  ( 0.6480958352246775078, -1.555737386339220762, 0.4265722068199431227 ) ) ;
#25712=CARTESIAN_POINT ( 'NONE',  ( 0.2625876981780432828, -0.6796766824346859304, 0.2386862984125060760 ) ) ;
#25713=CARTESIAN_POINT ( 'NONE',  ( 0.3174184176267851876, -1.762933076790994757, 0.5319023928052664107 ) ) ;
#25714=CARTESIAN_POINT ( 'NONE',  ( 0.1856782277538235604, -0.8266995537623093027, 0.008518417185872217273 ) ) ;
#25720=CARTESIAN_POINT ( 'NONE',  ( 0.1947361823824516613, -0.9199698176769123270, 0.2890873638243558474 ) ) ;
#25723=CARTESIAN_POINT ( 'NONE',  ( 0.5614343097231884183, -1.437874780063664426, 0.7463454611595057298 ) ) ;
#25724=CARTESIAN_POINT ( 'NONE',  ( 0.1315959483921021189, -0.8604525307240751264, 0.4681842845926359464 ) ) ;
#25727=CARTESIAN_POINT ( 'NONE',  ( 0.1810308432981227733, -0.8729890291813854342, 0.1457080207793099436 ) ) ;
#25729=DIRECTION ( 'NONE',  ( -0.6278132875326316586, 0.7783639739848378092, 0.000000000000000000 ) ) ;
#25731=CARTESIAN_POINT ( 'NONE',  ( 0.3249483201304784741, -1.768002432019315728, 0.5182417262812728520 ) ) ;
#25733=CARTESIAN_POINT ( 'NONE',  ( 0.1625982857068778153, -0.6782215948270849948, 0.2386756342038218459 ) ) ;
#25739=CARTESIAN_POINT ( 'NONE',  ( 0.01602427940967538628, -0.5690816651727684805, 0.5319142476028417832 ) ) ;
#25740=CARTESIAN_POINT ( 'NONE',  ( 0.1173773673404726187, -1.400925278984374689, 0.6274554870938690021 ) ) ;
#25743=CARTESIAN_POINT ( 'NONE',  ( 0.4226000438817392180, -1.709616762427842218, 0.4282184315516496809 ) ) ;
#25749=EDGE_CURVE ( 'NONE', #8719, #23287, #29055, .T. ) ;
#25750=B_SPLINE_CURVE_WITH_KNOTS ( 'NONE', 3,
 ( #24779, #14470, #11799, #30318, #8314, #39979, #11401 ),
 .UNSPECIFIED., .F., .F.,
 ( 4, 3, 4 ),
 ( 2.353093408709756909E-17, 3.509865184711082858E-06, 6.918258478235508878E-06 ),
 .UNSPECIFIED. ) ;
#25752=CARTESIAN_POINT ( 'NONE',  ( 0.4772201074466940196, -1.128262804531645402, 0.4802508068224435878 ) ) ;
#25754=CARTESIAN_POINT ( 'NONE',  ( 0.1121769144737377738, -1.416522762178338279, 0.5260910154307498754 ) ) ;
#25757=CARTESIAN_POINT ( 'NONE',  ( 0.5698225495787666572, -1.450209349364527389, 0.7310466856332464847 ) ) ;
#25761=ORIENTED_EDGE ( 'NONE', *, *, #21625, .T. ) ;
#25766=EDGE_CURVE ( 'NONE', #25255, #990, #39004, .T. ) ;
#25774=CARTESIAN_POINT ( 'NONE',  ( 0.2669582311511931594, -0.9789240833730817881, 0.6944203207930329524 ) ) ;
#25775=B_SPLINE_SURFACE_WITH_KNOTS ( 'NONE', 3, 3, ( 
 ( #28951, #22999, #12715, #38416 ),
 ( #34724, #31643, #28563, #25483 ),
 ( #25277, #22207, #10251, #29162 ),
 ( #38019, #22820, #32231, #35341 ),
 ( #7130, #22400, #13536, #19310 ),
 ( #20932, #36552, #13913, #36340 ),
 ( #17429, #14334, #35948, #7754 ) ),
 .UNSPECIFIED., .F., .F., .F.,
 ( 4, 3, 4 ),
 ( 4, 4 ),
 ( -3.173847279484519390, -0.01167112848645035506, 3.150505022511618680 ),
 ( -1.323227062466913795, 1.838851490560286184 ),
 .UNSPECIFIED. ) ;
#25776=CARTESIAN_POINT ( 'NONE',  ( 0.06924657340762380153, -0.5400045880099016982, 0.1389823447417335711 ) ) ;
#25777=CARTESIAN_POINT ( 'NONE',  ( 0.5386835852938653968, -1.518924006319621434, 0.5659150387024363127 ) ) ;
#25778=ORIENTED_EDGE ( 'NONE', *, *, #14283, .F. ) ;
#25783=CARTESIAN_POINT ( 'NONE',  ( 0.6835936161259937860, -1.406830003848978050, 0.7131562199467919028 ) ) ;
#25785=CARTESIAN_POINT ( 'NONE',  ( 0.1727685491708599863, -0.7001921779997841710, 0.4913863249289630031 ) ) ;
#25791=CARTESIAN_POINT ( 'NONE',  ( 6.608588869366793274E-05, -0.9486129085773968850, 0.1942756810714297844 ) ) ;
#25792=CARTESIAN_POINT ( 'NONE',  ( 0.4930347527585871026, -1.093336683456308078, 0.6301225560750347565 ) ) ;
#25800=B_SPLINE_CURVE_WITH_KNOTS ( 'NONE', 3,
 ( #9142, #12436, #18212, #21317 ),
 .UNSPECIFIED., .F., .F.,
 ( 4, 4 ),
 ( 1.058749929371489123E-17, 0.0008450547985826826515 ),
 .UNSPECIFIED. ) ;
#25804=ORIENTED_EDGE ( 'NONE', *, *, #23769, .F. ) ;
#25806=CARTESIAN_POINT ( 'NONE',  ( 0.002379513690175749652, -0.5300039046122766440, 0.1723549453226513595 ) ) ;
#25807=CARTESIAN_POINT ( 'NONE',  ( 0.1855767734282748604, -0.8171754376128953501, 0.2578515647343493922 ) ) ;
#25810=CARTESIAN_POINT ( 'NONE',  ( 0.6742391038958878147, -1.391540648348956966, 0.6661449684938977045 ) ) ;
#25817=CARTESIAN_POINT ( 'NONE',  ( 0.5902548269665799374, -1.489241228028834296, 0.5558766452402442715 ) ) ;
#25821=CARTESIAN_POINT ( 'NONE',  ( 0.6315986430998083989, -1.581773586513405716, 0.5682417262808788783 ) ) ;
#25822=CARTESIAN_POINT ( 'NONE',  ( 0.1488906047797098897, -0.7556912933748931582, 0.5388018373693193031 ) ) ;
#25824=CARTESIAN_POINT ( 'NONE',  ( 2.583436045986187992E-05, -0.4262564429027325685, 0.1457185332388686583 ) ) ;
#25825=VECTOR ( 'NONE', #24695, 39.37007874015748143 ) ;
#25826=CARTESIAN_POINT ( 'NONE',  ( 0.09071160229062831537, -0.5913197634106368561, 0.3153209778789223261 ) ) ;
#25829=CARTESIAN_POINT ( 'NONE',  ( 0.6252338399778394340, -1.468100857423625838, 0.5182417262812428760 ) ) ;
#25830=CARTESIAN_POINT ( 'NONE',  ( 0.1450424297082592573, -0.9270031065346044929, 0.2652761459977906466 ) ) ;
#25833=DIRECTION ( 'NONE',  ( -0.5415634522278134355, 0.8406598760563588346, 0.000000000000000000 ) ) ;
#25834=CARTESIAN_POINT ( 'NONE',  ( 0.1153477709767999210, -0.4466080377581258531, 0.1487152767197887637 ) ) ;
#25840=EDGE_LOOP ( 'NONE', ( #17092, #25666, #30773, #18936 ) ) ;
#25841=CARTESIAN_POINT ( 'NONE',  ( 0.6085831598237441131, -1.284018499374271371, 0.7837445821806681145 ) ) ;
#25844=CARTESIAN_POINT ( 'NONE',  ( 0.4663844447009264371, -1.139904246673989707, 0.4152358672995193900 ) ) ;
#25845=CARTESIAN_POINT ( 'NONE',  ( 0.05683680956318425820, -1.285974083448843563, 0.6485881297286527625 ) ) ;
#25847=EDGE_CURVE ( 'NONE', #23287, #13015, #11353, .T. ) ;
#25851=CARTESIAN_POINT ( 'NONE',  ( 0.1931882296960396594, -0.9271356228379165065, 0.6359237722107926594 ) ) ;
#25860=CARTESIAN_POINT ( 'NONE',  ( 0.3178512907186139547, -1.645949601790900774, 0.6057417262800831592 ) ) ;
#25861=CARTESIAN_POINT ( 'NONE',  ( 0.3832417524780237228, -1.109934760635944651, 0.6055797275786368727 ) ) ;
#25867=CARTESIAN_POINT ( 'NONE',  ( 0.1157172991699309123, -1.415943335782397616, 0.5180376455024461313 ) ) ;
#25871=CARTESIAN_POINT ( 'NONE',  ( 0.4903088652999874064, -1.276544129464578292, 0.5957393316629001623 ) ) ;
#25873=CARTESIAN_POINT ( 'NONE',  ( 0.3122977225021427161, -1.758414370883746303, 0.5144731769190049597 ) ) ;
#25874=CARTESIAN_POINT ( 'NONE',  ( 0.3310978894898223834, -0.9939147606493616838, 0.5922533870212514095 ) ) ;
#25876=ADVANCED_FACE ( 'NONE', ( #18006 ), #15373, .F. ) ;
#25878=CARTESIAN_POINT ( 'NONE',  ( -0.0007573580111799426817, -0.8643563613948842539, 0.3275742400162479084 ) ) ;
#25879=ORIENTED_EDGE ( 'NONE', *, *, #27788, .F. ) ;
#25880=CARTESIAN_POINT ( 'NONE',  ( 0.04837608321400507089, -0.5516968865674545253, 0.2272918774305557610 ) ) ;
#25881=CARTESIAN_POINT ( 'NONE',  ( 0.06467744696527351345, -0.8310922711372544791, 0.1095653288593454594 ) ) ;
#25882=CARTESIAN_POINT ( 'NONE',  ( 0.1844539022421386454, -0.8492542210929743263, 0.1057280673965992485 ) ) ;
#25885=CARTESIAN_POINT ( 'NONE',  ( 0.3291383425727634204, -1.292725137034694605, 0.5718629676982472931 ) ) ;
#25886=CARTESIAN_POINT ( 'NONE',  ( 0.2320287850415546360, -0.8916748044001994167, 0.6999815254931482933 ) ) ;
#25888=CARTESIAN_POINT ( 'NONE',  ( 0.1874542073597142144, -0.6896383861170264362, 0.05662353690727370270 ) ) ;
#25890=CARTESIAN_POINT ( 'NONE',  ( 0.5431141991461047036, -1.169197578686003824, 0.5740594486805935537 ) ) ;
#25891=AXIS2_PLACEMENT_3D ( 'NONE', #16526, #10549, #22924 ) ;
#25895=CARTESIAN_POINT ( 'NONE',  ( 0.4694587393328914504, -1.673455684603170290, 0.5834458924043449679 ) ) ;
#25896=CARTESIAN_POINT ( 'NONE',  ( 0.1223045647424210181, -1.412159682085746271, 0.4849083929475432320 ) ) ;
#25898=CARTESIAN_POINT ( 'NONE',  ( 0.6069176374591634948, -1.480164522464830990, 0.5706138896049881559 ) ) ;
#25901=CARTESIAN_POINT ( 'NONE',  ( 0.3222894045021684195, -1.758215778056678724, 0.5682417262808792113 ) ) ;
#25906=CYLINDRICAL_SURFACE ( 'NONE', #33807, 0.03749999999977545601 ) ;
#25908=EDGE_CURVE ( 'NONE', #12637, #2424, #35911, .T. ) ;
#25911=CARTESIAN_POINT ( 'NONE',  ( 0.07933644511000853550, -0.9611106349790075054, 0.8249633512138372371 ) ) ;
#25912=CARTESIAN_POINT ( 'NONE',  ( -6.654766911438814885E-05, -0.7522227857163925613, -0.09490634037222707431 ) ) ;
#25916=CARTESIAN_POINT ( 'NONE',  ( 0.3030236983578167842, -1.192445529317704978, 0.4282496583016260905 ) ) ;
#25921=DIRECTION ( 'NONE',  ( 0.000000000000000000, 0.000000000000000000, -1.000000000000000000 ) ) ;
#25925=CARTESIAN_POINT ( 'NONE',  ( 0.4528193024337852091, -1.225745371163585062, 0.7904948860725230508 ) ) ;
#25926=CARTESIAN_POINT ( 'NONE',  ( 0.5708999571285244823, -1.624164834895633236, 0.4874694594315064911 ) ) ;
#25928=CARTESIAN_POINT ( 'NONE',  ( 0.5556676709287090565, -1.190831894458023177, 0.5757950255497361614 ) ) ;
#25934=VECTOR ( 'NONE', #28565, 39.37007874015748854 ) ;
#25935=CARTESIAN_POINT ( 'NONE',  ( 0.2942755186928532329, -1.617995445140106403, 0.7842711939927167197 ) ) ;
#25936=CARTESIAN_POINT ( 'NONE',  ( 0.6462138998544783020, -1.567979845271513240, 0.4257847868880864084 ) ) ;
#25937=CARTESIAN_POINT ( 'NONE',  ( 0.1115213762701100647, -0.8962530768969190209, 0.02490635507620986289 ) ) ;
#25942=FACE_OUTER_BOUND ( 'NONE', #36813, .T. ) ;
#25943=CARTESIAN_POINT ( 'NONE',  ( 0.1893785600340663899, -0.9170734978138452842, 0.2340385483544073775 ) ) ;
#25946=CARTESIAN_POINT ( 'NONE',  ( 0.1094640939228022636, -0.8354574151733522580, 0.3143190699821967748 ) ) ;
#25947=CARTESIAN_POINT ( 'NONE',  ( 0.09725169381387938072, -1.017893544929620919, 0.8399287296596764651 ) ) ;
#25948=VECTOR ( 'NONE', #13406, 39.37007874015748143 ) ;
#25949=CARTESIAN_POINT ( 'NONE',  ( 0.4974456442574145543, -1.184401136727553094, 0.4224083929475455079 ) ) ;
#25952=CARTESIAN_POINT ( 'NONE',  ( 0.4627725426138175058, -1.215611893628281592, 0.5482364631202992777 ) ) ;
#25966=CARTESIAN_POINT ( 'NONE',  ( 0.7039831044528678250, -1.491019277299664214, 0.5110795091731726858 ) ) ;
#25967=SHAPE_REPRESENTATION ( 'Top Pivot Bracket', ( #27819 ), #21247 ) ;
#25968=DIRECTION ( 'NONE',  ( -0.8660512985181135770, -0.4999551463232369541, 0.000000000000000000 ) ) ;
#25969=ORIENTED_EDGE ( 'NONE', *, *, #15292, .F. ) ;
#25972=CARTESIAN_POINT ( 'NONE',  ( 0.5684515645774315118, -1.436290660855594314, 0.7423061315974909258 ) ) ;
#25977=EDGE_LOOP ( 'NONE', ( #6712, #8728, #1436, #23676, #37439 ) ) ;
#25979=AXIS2_PLACEMENT_3D ( 'NONE', #38769, #985, #395 ) ;
#25985=CARTESIAN_POINT ( 'NONE',  ( 0.0006767622704506771761, -0.6339827964191886434, -0.1178596299512805617 ) ) ;
#25987=CARTESIAN_POINT ( 'NONE',  ( 0.2569009810042112707, -0.9727358380243329439, 0.6816368474424655544 ) ) ;
#25989=CARTESIAN_POINT ( 'NONE',  ( 0.08990936761266832278, -0.5436479961250927362, 0.1389823447417348756 ) ) ;
#25990=CARTESIAN_POINT ( 'NONE',  ( 0.1687368033545940949, -0.7803388619690592165, 0.6016845811546662759 ) ) ;
#25992=CARTESIAN_POINT ( 'NONE',  ( 0.06773272100053760736, -1.316698543382843978, 0.6004584978572466980 ) ) ;
#25996=CARTESIAN_POINT ( 'NONE',  ( 0.3416079711831710997, -1.748037889526394384, 0.5953977406395821736 ) ) ;
#25999=CARTESIAN_POINT ( 'NONE',  ( 0.5369121333781083916, -1.380907096351134067, 0.7855338527398032511 ) ) ;
#26000=CARTESIAN_POINT ( 'NONE',  ( -9.420476929099221768E-05, -0.7761415936933997450, -0.08716077457609966439 ) ) ;
#26002=CARTESIAN_POINT ( 'NONE',  ( 0.006119849279750269946, -0.8445422014862440374, 0.1249866068643721573 ) ) ;
#26005=CARTESIAN_POINT ( 'NONE',  ( 0.07670545266435074838, -1.210239791498856521, 0.7644951083879507614 ) ) ;
#26006=CARTESIAN_POINT ( 'NONE',  ( 0.5067209442253272078, -1.108407892246341175, 0.6081930138323172752 ) ) ;
#26008=DIRECTION ( 'NONE',  ( 0.8660512985181135770, 0.4999551463232368431, 0.000000000000000000 ) ) ;
#26009=EDGE_CURVE ( 'NONE', #16210, #9524, #23788, .T. ) ;
#26013=CARTESIAN_POINT ( 'NONE',  ( 0.3844212907393982914, -1.715131551500115981, 0.4199026075312689010 ) ) ;
#26018=CARTESIAN_POINT ( 'NONE',  ( 0.002296835029420971411, -0.5198933010532057475, 0.1345257393686825342 ) ) ;
#26019=CARTESIAN_POINT ( 'NONE',  ( 0.08937458818493072832, -0.5767519040287507615, 0.09166571991850554213 ) ) ;
#26021=FACE_OUTER_BOUND ( 'NONE', #18871, .T. ) ;
#26022=CARTESIAN_POINT ( 'NONE',  ( 0.1998706582382908103, -0.5568697517490295290, 0.3524876158099713441 ) ) ;
#26026=ORIENTED_EDGE ( 'NONE', *, *, #11893, .F. ) ;
#26028=CARTESIAN_POINT ( 'NONE',  ( 0.5861528784094478528, -1.491558892450750129, 0.5551535569020163985 ) ) ;
#26030=ORIENTED_EDGE ( 'NONE', *, *, #1924, .T. ) ;
#26031=CARTESIAN_POINT ( 'NONE',  ( 0.1406250000000003053, -0.4510478692700824466, 0.1457185332388695187 ) ) ;
#26033=CARTESIAN_POINT ( 'NONE',  ( 0.1225839179203127571, -0.7429807855966490404, 0.4493094660506182225 ) ) ;
#26034=ADVANCED_FACE ( 'NONE', ( #34244 ), #11340, .F. ) ;
#26035=CARTESIAN_POINT ( 'NONE',  ( 0.02807510720231470858, -0.5716849246173629773, 0.5309397757077717328 ) ) ;
#26036=CARTESIAN_POINT ( 'NONE',  ( 0.3582932862619538916, -1.271006407676601224, 0.8606361610634840620 ) ) ;
#26037=CARTESIAN_POINT ( 'NONE',  ( 0.08855569358166180682, -1.004728779744561207, 0.8462681328029089123 ) ) ;
#26039=CARTESIAN_POINT ( 'NONE',  ( 0.1057303466113572732, -1.090484623222926608, 0.6404094407937778177 ) ) ;
#26045=CARTESIAN_POINT ( 'NONE',  ( 0.1164229267626636088, -0.4624049315941750615, 0.2417127322319602700 ) ) ;
#26048=CARTESIAN_POINT ( 'NONE',  ( 0.1625982857068778153, -0.6782215948270849948, 0.2386756342038218459 ) ) ;
#26051=CARTESIAN_POINT ( 'NONE',  ( 0.6674886243000348607, -1.379560724353076306, 0.6935688206045713677 ) ) ;
#26053=EDGE_CURVE ( 'NONE', #990, #21274, #18719, .T. ) ;
#26054=CARTESIAN_POINT ( 'NONE',  ( 0.005974781735028359547, -0.8455926680078293955, 0.1457185332388710175 ) ) ;
#26059=CARTESIAN_POINT ( 'NONE',  ( 0.3000183707936524002, -1.012959298482803305, 0.7233098648311757639 ) ) ;
#26062=CARTESIAN_POINT ( 'NONE',  ( 0.4498755731007036962, -1.064326126391425653, 0.5182417262812423209 ) ) ;
#26063=VERTEX_POINT ( 'NONE', #15233 ) ;
#26069=CARTESIAN_POINT ( 'NONE',  ( 0.1152323407702597613, -0.9559338739651589423, 0.6565232903784875562 ) ) ;
#26073=CARTESIAN_POINT ( 'NONE',  ( 0.1864550573006002465, -0.7573172630633775437, 0.1903174488078394899 ) ) ;
#26075=CARTESIAN_POINT ( 'NONE',  ( 0.3973402663755812858, -1.144813166135470350, 0.7100772268336156268 ) ) ;
#26077=CARTESIAN_POINT ( 'NONE',  ( 0.3920841177027292179, -1.709814868753107175, 0.4185788730875646957 ) ) ;
#26082=VERTEX_POINT ( 'NONE', #14840 ) ;
#26084=CARTESIAN_POINT ( 'NONE',  ( 0.4162055814956918121, -1.586242312561611634, 0.6469014666648855716 ) ) ;
#26085=CARTESIAN_POINT ( 'NONE',  ( 0.06493569881847564840, -0.8211346530322489734, 0.08200188512405065522 ) ) ;
#26086=CARTESIAN_POINT ( 'NONE',  ( 0.1963398750588821740, -0.6872747950079822754, 0.3329267309873611413 ) ) ;
#26088=ORIENTED_EDGE ( 'NONE', *, *, #6175, .T. ) ;
#26089=EDGE_CURVE ( 'NONE', #3822, #8849, #8948, .T. ) ;
#26091=AXIS2_PLACEMENT_3D ( 'NONE', #30090, #20638, #32757 ) ;
#26092=CARTESIAN_POINT ( 'NONE',  ( 0.3976745947184191499, -1.253140510797894125, 0.5816770576092088474 ) ) ;
#26094=CARTESIAN_POINT ( 'NONE',  ( 0.1752860773241999015, -0.7509627177522383290, 0.5639964784769007089 ) ) ;
#26095=ORIENTED_EDGE ( 'NONE', *, *, #18438, .F. ) ;
#26102=CARTESIAN_POINT ( 'NONE',  ( 0.3329586478011472561, -1.131820071144838069, 0.5182417262812423209 ) ) ;
#26103=CARTESIAN_POINT ( 'NONE',  ( 0.3222894045021684195, -1.758215778056678724, 0.5682417262808792113 ) ) ;
#26110=EDGE_CURVE ( 'NONE', #1874, #23886, #28000, .T. ) ;
#26111=CARTESIAN_POINT ( 'NONE',  ( 0.08197583149358347865, -1.314149287951269951, 0.5636821078433256194 ) ) ;
#26119=ORIENTED_EDGE ( 'NONE', *, *, #20039, .T. ) ;
#26120=CARTESIAN_POINT ( 'NONE',  ( 0.2949815950263163233, -1.721662039081772733, 0.6893651101351793153 ) ) ;
#26126=CARTESIAN_POINT ( 'NONE',  ( 0.4972671625857253974, -1.080199071502573771, 0.5707417262808780478 ) ) ;
#26130=CARTESIAN_POINT ( 'NONE',  ( 0.3312706671835699557, -1.040500793050076256, 0.7771620973990449599 ) ) ;
#26133=CARTESIAN_POINT ( 'NONE',  ( 0.3578995607061009054, -0.9255625346965836719, 0.6844156867609741957 ) ) ;
#26138=CARTESIAN_POINT ( 'NONE',  ( 0.3279880978169363304, -1.639400604360913949, 0.5872381464462802514 ) ) ;
#26139=CARTESIAN_POINT ( 'NONE',  ( 0.1124878519000608590, -0.7868389026292395005, -0.07401770572993009167 ) ) ;
#26140=CARTESIAN_POINT ( 'NONE',  ( 0.05579155178881651383, -1.335540925555324332, 0.3667417262808778111 ) ) ;
#26145=CARTESIAN_POINT ( 'NONE',  ( 0.5446975496317306709, -1.168323758156589953, 0.5471643355025310740 ) ) ;
#26146=CARTESIAN_POINT ( 'NONE',  ( 0.1852697703518018379, -0.8388889655799375289, 0.1462684119608197997 ) ) ;
#26149=CARTESIAN_POINT ( 'NONE',  ( 0.4113940825675456159, -1.194246046371860936, 0.6856661914167786476 ) ) ;
#26150=CARTESIAN_POINT ( 'NONE',  ( 0.2640703320512924335, -0.5784607244460839848, 0.1477649966949237115 ) ) ;
#26151=CARTESIAN_POINT ( 'NONE',  ( 0.1722267588728232657, -0.8902057077919266481, 0.1457020840065470779 ) ) ;
#26152=CARTESIAN_POINT ( 'NONE',  ( 0.4136294883733859229, -1.694877849074643450, 0.4282417262808777547 ) ) ;
#26155=CARTESIAN_POINT ( 'NONE',  ( 0.3206695962710918169, -1.761864437037726328, 0.5005377785206835961 ) ) ;
#26157=CARTESIAN_POINT ( 'NONE',  ( 0.03312451316780189864, -1.135919892802786935, 0.6708301406083743146 ) ) ;
#26158=DIRECTION ( 'NONE',  ( -0.01265474379914244447, -0.8659329421511298142, 0.4999999971568662160 ) ) ;
#26162=CARTESIAN_POINT ( 'NONE',  ( 0.2813060849845607780, -1.595222829165602763, 0.9543515313515406051 ) ) ;
#26163=CARTESIAN_POINT ( 'NONE',  ( 0.6982426364517120287, -1.490497097242356128, 0.4889590780275660520 ) ) ;
#26164=CARTESIAN_POINT ( 'NONE',  ( 0.4453503739158970465, -1.132163833841517864, 0.4458354100233239969 ) ) ;
#26167=CARTESIAN_POINT ( 'NONE',  ( 0.2241874626926840808, -0.8290071211643307292, 0.6423122159289148536 ) ) ;
#26173=VERTEX_POINT ( 'NONE', #34761 ) ;
#26180=ORIENTED_EDGE ( 'NONE', *, *, #21883, .T. ) ;
#26181=CARTESIAN_POINT ( 'NONE',  ( 0.08817979687959355550, -0.8149952009864827041, 0.2376065706799516952 ) ) ;
#26184=CARTESIAN_POINT ( 'NONE',  ( 0.1100467502016390098, -0.5492220161660857913, 0.1711048947129659437 ) ) ;
#26185=CARTESIAN_POINT ( 'NONE',  ( 0.04927849822469471119, -1.184322729783269690, 0.6652490848847384397 ) ) ;
#26188=CARTESIAN_POINT ( 'NONE',  ( 0.3837628383327942871, -1.723043414611475921, 0.6192075928247073868 ) ) ;
#26189=CARTESIAN_POINT ( 'NONE',  ( 0.6653107924583753219, -1.561504850366493669, 0.5590290280834550041 ) ) ;
#26193=CARTESIAN_POINT ( 'NONE',  ( 0.01167820585366893989, -0.7468400741294990430, -0.1063804806529143748 ) ) ;
#26194=CARTESIAN_POINT ( 'NONE',  ( 0.1801371744477150150, -0.8376302764228334974, 0.6639037816134167880 ) ) ;
#26195=( NAMED_UNIT ( * ) PLANE_ANGLE_UNIT ( ) SI_UNIT ( $, .RADIAN. ) );
#26196=CARTESIAN_POINT ( 'NONE',  ( 0.005980720888701209978, -0.8455916207747946611, 0.1457185332388707122 ) ) ;
#26198=CARTESIAN_POINT ( 'NONE',  ( -0.002175845014896822093, -0.8193767622554530838, 0.2897257274743089139 ) ) ;
#26199=CARTESIAN_POINT ( 'NONE',  ( 0.4598226378601848463, -1.064312249210862982, 0.6507415875188953258 ) ) ;
#26202=CARTESIAN_POINT ( 'NONE',  ( 0.3856987765544705460, -1.723509814865189504, 0.4239487186058908952 ) ) ;
#26203=CARTESIAN_POINT ( 'NONE',  ( 0.3048118929600290294, -1.756863971546229752, 0.5686390395660469999 ) ) ;
#26206=CARTESIAN_POINT ( 'NONE',  ( 0.002558321733063344521, -0.5432559438152800846, 0.2281836175635736930 ) ) ;
#26208=ORIENTED_EDGE ( 'NONE', *, *, #2658, .F. ) ;
#26210=CARTESIAN_POINT ( 'NONE',  ( 0.6085831598237441131, -1.284018499374271371, 0.7837445821806681145 ) ) ;
#26215=DIRECTION ( 'NONE',  ( 0.4999551463232372317, -0.8660512985181134660, 0.000000000000000000 ) ) ;
#26220=CARTESIAN_POINT ( 'NONE',  ( 0.7047926081815637511, -1.538931328977949597, 0.5682417262808784342 ) ) ;
#26221=CARTESIAN_POINT ( 'NONE',  ( 0.08841851961439690932, -0.6860782299043888255, 0.1966944432554147137 ) ) ;
#26222=CARTESIAN_POINT ( 'NONE',  ( 0.03925517826010388456, -0.6829828959353061446, 0.6939464994351529636 ) ) ;
#26223=CARTESIAN_POINT ( 'NONE',  ( 0.4701715835452702774, -1.558074627102426613, 0.5800830931470651874 ) ) ;
#26224=CARTESIAN_POINT ( 'NONE',  ( 0.2675635477756006519, -1.687710685839010960, 0.6071195368929496183 ) ) ;
#26226=CARTESIAN_POINT ( 'NONE',  ( 0.3816210699381898386, -1.147921404532277423, 0.5760534757964502761 ) ) ;
#26227=ORIENTED_EDGE ( 'NONE', *, *, #30619, .F. ) ;
#26230=B_SPLINE_CURVE_WITH_KNOTS ( 'NONE', 3,
 ( #5614, #37292, #24563, #2545, #15082, #40167 ),
 .UNSPECIFIED., .F., .F.,
 ( 4, 2, 4 ),
 ( 0.008137213426454060344, 0.008732926872069602525, 0.009328640317685142971 ),
 .UNSPECIFIED. ) ;
#26231=CARTESIAN_POINT ( 'NONE',  ( 0.1504062631728284027, -0.5880184383576758655, 0.5123281263564087862 ) ) ;
#26235=CARTESIAN_POINT ( 'NONE',  ( 0.1081859945995184841, -1.420406326327936952, 0.5048778302349400393 ) ) ;
#26236=CARTESIAN_POINT ( 'NONE',  ( 0.3520862261316686226, -0.8866190960188533587, 0.7137788081797863393 ) ) ;
#26238=CARTESIAN_POINT ( 'NONE',  ( 0.01394802180609925127, -0.9131856928993046241, 0.5601969492252886207 ) ) ;
#26243=CARTESIAN_POINT ( 'NONE',  ( 0.3642735142549751171, -1.140585997052691702, 0.7302200931181149768 ) ) ;
#26244=CARTESIAN_POINT ( 'NONE',  ( 0.2687203115727492264, -1.674044157977605529, 0.5754666865148680976 ) ) ;
#26251=CARTESIAN_POINT ( 'NONE',  ( 0.1052637591289525415, -0.6454443736156558753, 0.3793980098026691894 ) ) ;
#26254=CARTESIAN_POINT ( 'NONE',  ( 0.4062564059369914160, -1.133149177010132291, 0.4850828916047054684 ) ) ;
#26257=CARTESIAN_POINT ( 'NONE',  ( 0.1579648256015883934, -1.062633224222470973, 0.7378981056644309255 ) ) ;
#26263=CARTESIAN_POINT ( 'NONE',  ( 0.3907296536724044755, -1.136716705566652497, 0.7120754492584040474 ) ) ;
#26265=CARTESIAN_POINT ( 'NONE',  ( 0.5717376075374569488, -1.625791445033037963, 0.5487456121630054362 ) ) ;
#26268=B_SPLINE_CURVE_WITH_KNOTS ( 'NONE', 3,
 ( #475, #31679, #6772, #38050, #18943, #31289, #10076, #32086, #23416, #35180, #31478, #3498, #19350, #3893, #37643, #18731, #15643, #31888, #9462, #34567, #3285, #15840 ),
 .UNSPECIFIED., .F., .F.,
 ( 4, 2, 2, 2, 2, 2, 2, 2, 2, 2, 4 ),
 ( 0.01043159516612753024, 0.01173405610995085883, 0.01303651705377418916, 0.01368774752568585086, 0.01433897799759751256, 0.01564143894142083421, 0.01694389988524415414, 0.01759513035715581236, 0.01824636082906747059, 0.01954882177289079051, 0.02085128271671411043 ),
 .UNSPECIFIED. ) ;
#26271=CARTESIAN_POINT ( 'NONE',  ( 0.04991041250764023662, -0.5686633296565585249, 0.2759322019946101046 ) ) ;
#26273=CARTESIAN_POINT ( 'NONE',  ( 0.08825506839931913927, -0.6229187635552460023, 0.01667319878056269106 ) ) ;
#26274=CARTESIAN_POINT ( 'NONE',  ( 0.1112283632243594861, -0.9174557404464535049, 0.07156239907761412222 ) ) ;
#26279=CARTESIAN_POINT ( 'NONE',  ( 0.1865668073278461958, -0.7779540966166318405, 0.5928093434591832356 ) ) ;
#26281=CARTESIAN_POINT ( 'NONE',  ( 0.1874548549128404462, -0.6895869275214173699, 0.05757391423245525330 ) ) ;
#26283=CARTESIAN_POINT ( 'NONE',  ( 0.6159314527243455739, -1.574808447129107059, 0.4182417262808776903 ) ) ;
#26284=CARTESIAN_POINT ( 'NONE',  ( 0.1197622505559556849, -1.298029526664095101, 0.4264817069637966696 ) ) ;
#26285=CARTESIAN_POINT ( 'NONE',  ( 0.4584446980593357424, -1.679963946744034375, 0.5963570223128070724 ) ) ;
#26287=CARTESIAN_POINT ( 'NONE',  ( 0.5827378505010344378, -1.244973309454295629, 0.8759922176168969399 ) ) ;
#26293=CARTESIAN_POINT ( 'NONE',  ( 0.1849752612960278986, -0.7177878707474302233, -0.02435127109689261965 ) ) ;
#26294=CARTESIAN_POINT ( 'NONE',  ( 0.4753071910876713324, -1.208389221472485398, 0.5182417262812494263 ) ) ;
#26295=CARTESIAN_POINT ( 'NONE',  ( 0.08808183485559285819, -1.318030620364535777, 0.4536778408853885947 ) ) ;
#26297=CARTESIAN_POINT ( 'NONE',  ( 0.01618294926847982027, -0.6819691077562005654, 0.5071040197741758515 ) ) ;
#26299=ADVANCED_FACE ( 'NONE', ( #25942, #38466 ), #36966, .T. ) ;
#26301=CARTESIAN_POINT ( 'NONE',  ( 0.3048434042955683321, -1.756850910410517885, 0.5692538547013633599 ) ) ;
#26310=CARTESIAN_POINT ( 'NONE',  ( 0.4213583293965230681, -1.178187296390520444, 0.7937282009877297817 ) ) ;
#26314=CARTESIAN_POINT ( 'NONE',  ( 0.5317104447742054818, -1.152447470094080328, 0.6575248185080280194 ) ) ;
#26319=CARTESIAN_POINT ( 'NONE',  ( 0.02452063181877493087, -0.5608703732607570602, 0.2678004018634968508 ) ) ;
#26322=CARTESIAN_POINT ( 'NONE',  ( 0.1118191872339531490, -0.8690880516572517811, -0.01359164210609734025 ) ) ;
#26323=DIRECTION ( 'NONE',  ( -0.8745653259477854657, -0.4849077135392299565, 1.623341605721814605E-14 ) ) ;
#26331=CARTESIAN_POINT ( 'NONE',  ( 0.1026041305702670992, -0.8285543066798877199, 0.1457185332388695465 ) ) ;
#26333=CARTESIAN_POINT ( 'NONE',  ( 0.4948540404288629957, -1.185897220935881569, 0.4182417262808778013 ) ) ;
#26338=DIRECTION ( 'NONE',  ( 0.4999551463232372317, -0.8660512985181135770, 0.000000000000000000 ) ) ;
#26341=CARTESIAN_POINT ( 'NONE',  ( 0.03728397956324149692, -1.161596368933228263, 0.6766991317226744851 ) ) ;
#26344=EDGE_CURVE ( 'NONE', #25042, #36473, #33756, .T. ) ;
#26348=CARTESIAN_POINT ( 'NONE',  ( 0.4422952645324528809, -1.107215779629665775, 0.5826897552320002838 ) ) ;
#26350=EDGE_CURVE ( 'NONE', #8227, #30000, #25131, .T. ) ;
#26353=ORIENTED_EDGE ( 'NONE', *, *, #36610, .F. ) ;
#26354=CARTESIAN_POINT ( 'NONE',  ( 0.1883677752342057254, -0.5193258297658697176, 0.2202931123293304094 ) ) ;
#26356=CARTESIAN_POINT ( 'NONE',  ( 0.2644464953634217963, -1.687293114999279364, 0.5653706809109292353 ) ) ;
#26357=CARTESIAN_POINT ( 'NONE',  ( 0.6019347141590773997, -1.479867699914170887, 0.6295854643368259396 ) ) ;
#26361=CARTESIAN_POINT ( 'NONE',  ( 0.4506545850206880033, -1.130496563826020040, 0.8936068413349319561 ) ) ;
#26363=CARTESIAN_POINT ( 'NONE',  ( 0.1020049694779444072, -1.076130111015646040, 0.8785625650948160059 ) ) ;
#26370=CARTESIAN_POINT ( 'NONE',  ( 0.001424326983700852176, -0.9534082139883233165, -0.01138449076159441485 ) ) ;
#26373=ADVANCED_FACE ( 'NONE', ( #23702 ), #23798, .T. ) ;
#26375=CARTESIAN_POINT ( 'NONE',  ( 0.1880342618521675668, -0.9075390834704973875, 0.5937181048572924835 ) ) ;
#26377=CARTESIAN_POINT ( 'NONE',  ( 0.09001107770154211096, -0.5661368280801137853, 0.1669925442062198118 ) ) ;
#26378=AXIS2_PLACEMENT_3D ( 'NONE', #9344, #31559, #2994 ) ;
#26379=CARTESIAN_POINT ( 'NONE',  ( 0.1119770736976786057, -0.5747358184814086446, 0.2604905888496574229 ) ) ;
#26380=CARTESIAN_POINT ( 'NONE',  ( 0.02864720926977884496, -1.052608752363344946, 0.5991139217441558973 ) ) ;
#26385=CARTESIAN_POINT ( 'NONE',  ( 0.3386861991152600448, -1.749696087812495193, 0.5923449926325128345 ) ) ;
#26387=CARTESIAN_POINT ( 'NONE',  ( 0.06843998531048707534, -1.327705739214654290, 0.5337169134020078864 ) ) ;
#26390=CARTESIAN_POINT ( 'NONE',  ( -3.827020590142639815E-06, -0.7722669175349963222, -0.1011549324461909344 ) ) ;
#26391=CARTESIAN_POINT ( 'NONE',  ( 0.5759042597488219783, -1.466327531223862168, 0.7055958116420547599 ) ) ;
#26394=CARTESIAN_POINT ( 'NONE',  ( 0.1512804210101734992, -1.367800832853933501, 0.8372142429942934783 ) ) ;
#26395=CARTESIAN_POINT ( 'NONE',  ( 0.3550881284155063544, -0.9867921891001451007, 0.6236314015414725631 ) ) ;
#26397=CARTESIAN_POINT ( 'NONE',  ( 0.4361655066743588827, -1.002659119010890665, 0.8380844301937150354 ) ) ;
#26400=CARTESIAN_POINT ( 'NONE',  ( 0.6933448563160584666, -1.428940691336694435, 0.5798181663060312241 ) ) ;
#26402=CARTESIAN_POINT ( 'NONE',  ( 0.3164963388020943236, -1.761765027830636265, 0.5685543529849016453 ) ) ;
#26407=CARTESIAN_POINT ( 'NONE',  ( 0.002311413808415803493, -0.5217619077427898544, 0.1735510156824913164 ) ) ;
#26408=CARTESIAN_POINT ( 'NONE',  ( 0.09336344782360941896, -1.301801031155125576, 0.4543626096959849647 ) ) ;
#26411=CARTESIAN_POINT ( 'NONE',  ( 0.1946137278002632309, -0.5377497569806550803, 0.3020257395598471839 ) ) ;
#26417=CARTESIAN_POINT ( 'NONE',  ( 0.2411830489815006973, -1.239411181507260373, 0.4182417262808780234 ) ) ;
#26420=CARTESIAN_POINT ( 'NONE',  ( 0.2411561144159813930, -0.6701252966988756610, 0.6760123873793543181 ) ) ;
#26421=CARTESIAN_POINT ( 'NONE',  ( 0.2709626867699331254, -0.9619090970917223427, 0.7179662831592660277 ) ) ;
#26422=CARTESIAN_POINT ( 'NONE',  ( 0.2280934743446804969, -1.349410172253141083, 1.031711493552184722 ) ) ;
#26423=CARTESIAN_POINT ( 'NONE',  ( 0.08764114647180407114, -0.5715037028378165962, 0.2642098798473031529 ) ) ;
#26424=CARTESIAN_POINT ( 'NONE',  ( 0.2703307786129086066, -1.660141123700932475, 0.7591185859682896275 ) ) ;
#26426=CARTESIAN_POINT ( 'NONE',  ( 0.2764337282391635675, -1.207704344519198170, 0.5762930846214849856 ) ) ;
#26431=CARTESIAN_POINT ( 'NONE',  ( 0.1887787592512208679, -0.4599917114490411074, 0.1613286463795750858 ) ) ;
#26434=( BOUNDED_SURFACE ( )  B_SPLINE_SURFACE ( 3, 2, ( 
 ( #8381, #11868, #20948 ),
 ( #9002, #24853, #5276 ),
 ( #17840, #30400, #30608 ),
 ( #9185, #31225, #33470 ),
 ( #34288, #14550, #30804 ),
 ( #21754, #27719, #24051 ),
 ( #12087, #37373, #2231 ),
 ( #36576, #5702, #33905 ),
 ( #6094, #18259, #24237 ),
 ( #14770, #27332, #39862 ),
 ( #18663, #36760, #21365 ),
 ( #8571, #39648, #40046 ),
 ( #21564, #27119, #8788 ),
 ( #2624, #5890, #15160 ),
 ( #21148, #12294, #33678 ),
 ( #18449, #11484, #31003 ) ),
 .UNSPECIFIED., .F., .F., .T. ) 
 B_SPLINE_SURFACE_WITH_KNOTS ( ( 4, 2, 2, 2, 2, 2, 2, 4 ),
 ( 3, 3 ),
 ( -1.680513367352531873E-17, 0.0003827823838732950985, 0.0007655647677466070021, 0.001148347151619918960, 0.001531129535493230701, 0.002296694303239854400, 0.002679476687113166358, 0.003062259070986478315 ),
 ( 0.000000000000000000, 1.000000000000000000 ),
 .UNSPECIFIED. ) 
 GEOMETRIC_REPRESENTATION_ITEM ( )  RATIONAL_B_SPLINE_SURFACE ( (
 ( 1.000000000000000000, 0.3554223140987289309, 1.000000000000000000),
 ( 1.000000000000000000, 0.3396177442905202182, 1.000000000000000000),
 ( 1.000000000000000000, 0.3300690577498115452, 1.000000000000000000),
 ( 1.000000000000000000, 0.3265765077624734891, 1.000000000000000000),
 ( 1.000000000000000000, 0.3329789664787625170, 1.000000000000000000),
 ( 1.000000000000000000, 0.3573122569017027073, 1.000000000000000000),
 ( 1.000000000000000000, 0.3749106637392585761, 1.000000000000000000),
 ( 1.000000000000000000, 0.4151524565129351974, 1.000000000000000000),
 ( 1.000000000000000000, 0.4373904795482970176, 1.000000000000000000),
 ( 1.000000000000000000, 0.5060226476725440126, 1.000000000000000000),
 ( 1.000000000000000000, 0.5527513560841460505, 1.000000000000000000),
 ( 1.000000000000000000, 0.6152787851278052056, 1.000000000000000000),
 ( 1.000000000000000000, 0.6350790670704571372, 1.000000000000000000),
 ( 1.000000000000000000, 0.6725960642926860356, 1.000000000000000000),
 ( 1.000000000000000000, 0.6901810608942313685, 1.000000000000000000),
 ( 1.000000000000000000, 0.7053379087130886571, 1.000000000000000000) ) ) 
 REPRESENTATION_ITEM ( '' )  SURFACE ( )  );
#26435=AXIS2_PLACEMENT_3D ( 'NONE', #18294, #30833, #2654 ) ;
#26437=AXIS2_PLACEMENT_3D ( 'NONE', #22523, #38335, #31765 ) ;
#26440=CARTESIAN_POINT ( 'NONE',  ( 0.5718426945711908571, -1.221126421150759755, 0.7198242229513793777 ) ) ;
#26442=CARTESIAN_POINT ( 'NONE',  ( 0.02571248063816646001, -0.9265510417023297141, 0.5911808037001393679 ) ) ;
#26445=CARTESIAN_POINT ( 'NONE',  ( 0.2817055660618989488, -0.9903619377415766589, 0.7098947161768234260 ) ) ;
#26450=CARTESIAN_POINT ( 'NONE',  ( 0.1371918123484773266, -0.7288778413244972887, 0.5065603813249234255 ) ) ;
#26452=DIRECTION ( 'NONE',  ( 0.000000000000000000, 0.000000000000000000, -1.000000000000000000 ) ) ;
#26454=CARTESIAN_POINT ( 'NONE',  ( 0.2005744727561914464, -1.165451418712258214, 0.7493240844877221418 ) ) ;
#26460=CARTESIAN_POINT ( 'NONE',  ( 0.1861553373212349316, -1.375139781582257914, 0.4202249536440196276 ) ) ;
#26462=AXIS2_PLACEMENT_3D ( 'NONE', #31284, #5330, #27577 ) ;
#26463=CARTESIAN_POINT ( 'NONE',  ( 0.4170199900086061784, -1.169318256293440106, 0.7032566000091412528 ) ) ;
#26465=CARTESIAN_POINT ( 'NONE',  ( 0.5669405059600367558, -1.627145089617755058, 0.5182417262812432091 ) ) ;
#26469=ORIENTED_EDGE ( 'NONE', *, *, #29393, .F. ) ;
#26470=CARTESIAN_POINT ( 'NONE',  ( 0.09463920074833474805, -0.7590106432348279197, 0.6020095118386700195 ) ) ;
#26472=CARTESIAN_POINT ( 'NONE',  ( 0.08929178762115032308, -0.5798774593664931531, 0.08564773658936970790 ) ) ;
#26478=CARTESIAN_POINT ( 'NONE',  ( 0.1239748337567665587, -0.5947780400922306754, 0.3080055205751647263 ) ) ;
#26482=CARTESIAN_POINT ( 'NONE',  ( 0.6238534087474900680, -1.575592206279644136, 0.4182417262808776903 ) ) ;
#26483=CARTESIAN_POINT ( 'NONE',  ( 0.1372954668741161455, -1.287838507416935396, 0.4318400540907381679 ) ) ;
#26488=CARTESIAN_POINT ( 'NONE',  ( 0.2888622377148890585, -0.7373900025806978675, 0.6684008680139050806 ) ) ;
#26498=CARTESIAN_POINT ( 'NONE',  ( 0.4513496650050710657, -1.222212685274413291, 0.4817276195033231567 ) ) ;
#26500=CARTESIAN_POINT ( 'NONE',  ( 0.07958551560962676130, -1.322831287755754648, 0.4682677590956375036 ) ) ;
#26504=CARTESIAN_POINT ( 'NONE',  ( 0.2721752123224986386, -1.596339224327277595, 0.9197038883954219424 ) ) ;
#26507=CARTESIAN_POINT ( 'NONE',  ( 0.5893686083517821750, -1.590946717650547182, 0.4182417262808776903 ) ) ;
#26517=CARTESIAN_POINT ( 'NONE',  ( 0.5433381647791950542, -1.365663563338381570, 0.6765757352007879533 ) ) ;
#26520=CARTESIAN_POINT ( 'NONE',  ( 0.4452807512755668218, -1.047893410216382382, 0.6910429845488149647 ) ) ;
#26525=CARTESIAN_POINT ( 'NONE',  ( 0.2564594514974720130, -1.414529048416510504, 0.9122281602349449070 ) ) ;
#26526=CARTESIAN_POINT ( 'NONE',  ( 0.6602609276941329153, -1.536889406902937072, 0.4273433096175258128 ) ) ;
#26528=CARTESIAN_POINT ( 'NONE',  ( 0.05573493074139709846, -1.335442843293342063, 0.4177417262808780229 ) ) ;
#26539=CARTESIAN_POINT ( 'NONE',  ( 0.3644424172741055346, -1.232111622910960325, 0.6721086862942787787 ) ) ;
#26544=DIRECTION ( 'NONE',  ( 0.8660512985181134660, 0.4999551463232371207, 0.000000000000000000 ) ) ;
#26548=DIRECTION ( 'NONE',  ( -0.4999551463232372317, 0.8660512985181135770, -0.000000000000000000 ) ) ;
#26551=CARTESIAN_POINT ( 'NONE',  ( 0.3831835866196274254, -1.151467227178074593, 0.4237037165649273907 ) ) ;
#26553=CARTESIAN_POINT ( 'NONE',  ( 0.7071069014570956490, -1.521634513519168452, 0.5617257377400114438 ) ) ;
#26555=CIRCLE ( 'NONE', #39661, 0.08249999999977548903 ) ;
#26556=EDGE_CURVE ( 'NONE', #29236, #22989, #15289, .T. ) ;
#26559=CARTESIAN_POINT ( 'NONE',  ( 0.5985082606850495868, -1.473464502187743941, 0.6023744451300401259 ) ) ;
#26560=CARTESIAN_POINT ( 'NONE',  ( 0.3098710801442948748, -1.725017193307739838, 0.7846558205662965690 ) ) ;
#26566=CARTESIAN_POINT ( 'NONE',  ( 0.1731170367617594075, -0.5199985899392068900, 0.1286442151290814462 ) ) ;
#26568=CARTESIAN_POINT ( 'NONE',  ( -0.0004431470427073231017, -0.9367128829938298207, 0.1457185332388704069 ) ) ;
#26569=CARTESIAN_POINT ( 'NONE',  ( 0.6017145574000101194, -1.483072097257081445, 0.5679475895592410728 ) ) ;
#26570=CARTESIAN_POINT ( 'NONE',  ( -0.0002086810045813790077, -0.7085389528372163515, -0.01266920697570707473 ) ) ;
#26572=ORIENTED_EDGE ( 'NONE', *, *, #450, .F. ) ;
#26575=CARTESIAN_POINT ( 'NONE',  ( -0.01345624470603132110, -0.5489092317405479537, 0.2541791200293259112 ) ) ;
#26585=CARTESIAN_POINT ( 'NONE',  ( 0.09998776873723287661, -0.8261931218866173099, 0.3381795186695624733 ) ) ;
#26586=CARTESIAN_POINT ( 'NONE',  ( 0.04211891365776822965, -0.9906088561216523924, 0.6817232344076664674 ) ) ;
#26589=CARTESIAN_POINT ( 'NONE',  ( 0.1472076274870235679, -0.7270890653341587351, 0.5403574314070681561 ) ) ;
#26591=CARTESIAN_POINT ( 'NONE',  ( 0.1246370012518288467, -0.6330505824401759796, 0.3923014813962043545 ) ) ;
#26592=CARTESIAN_POINT ( 'NONE',  ( 0.1790539915098864343, -0.5050269068883876944, 0.2306937646411194032 ) ) ;
#26593=CARTESIAN_POINT ( 'NONE',  ( 0.6069176374591634948, -1.480164522464830990, 0.5706138896049881559 ) ) ;
#26594=CARTESIAN_POINT ( 'NONE',  ( 0.6393295224005999255, -1.564323831884513849, 0.4219358453006255560 ) ) ;
#26595=EDGE_CURVE ( 'NONE', #9524, #16210, #38886, .T. ) ;
#26598=EDGE_CURVE ( 'NONE', #13401, #13556, #6894, .T. ) ;
#26599=AXIS2_PLACEMENT_3D ( 'NONE', #40172, #17371, #8502 ) ;
#26600=CARTESIAN_POINT ( 'NONE',  ( 0.3740960844805631957, -1.108072201694596526, 0.5182417262812423209 ) ) ;
#26601=CARTESIAN_POINT ( 'NONE',  ( 0.07497864282572899719, -1.322056043867073427, 0.4862695133534066794 ) ) ;
#26604=CARTESIAN_POINT ( 'NONE',  ( -8.502430919704473552E-05, -0.7684146918674319426, -0.08995813089792253914 ) ) ;
#26607=CARTESIAN_POINT ( 'NONE',  ( 0.007263304146752605668, -0.7838023699412952627, 0.02006003217016949156 ) ) ;
#26609=CARTESIAN_POINT ( 'NONE',  ( 0.01933088760290150449, -0.9443470376599968352, 0.6102586483404766060 ) ) ;
#26610=CARTESIAN_POINT ( 'NONE',  ( 0.4929039159923706559, -1.082692164550193237, 0.5711674032880966756 ) ) ;
#26612=CARTESIAN_POINT ( 'NONE',  ( 0.6473156011871936677, -1.349322671506162141, 0.8501878200258047302 ) ) ;
#26619=CARTESIAN_POINT ( 'NONE',  ( 0.3084290614922874374, -1.760927762095492843, 0.5681371985488602450 ) ) ;
#26623=ORIENTED_EDGE ( 'NONE', *, *, #22893, .T. ) ;
#26626=CARTESIAN_POINT ( 'NONE',  ( 0.09787890177536405500, -1.020308744753638974, 0.8413265823706557178 ) ) ;
#26627=CARTESIAN_POINT ( 'NONE',  ( 0.1496044234471295975, -1.269186625694784132, 0.4303707757303895098 ) ) ;
#26632=CARTESIAN_POINT ( 'NONE',  ( 0.6761021464639213052, -1.407442781842621171, 0.4761751337611269674 ) ) ;
#26639=CARTESIAN_POINT ( 'NONE',  ( 0.4400409819278914836, -1.228797560110408416, 0.5880944087261866793 ) ) ;
#26642=CARTESIAN_POINT ( 'NONE',  ( 0.08368236660537471672, -1.307117728175614335, 0.5699627548592203219 ) ) ;
#26643=CARTESIAN_POINT ( 'NONE',  ( 0.09173077349526245761, -0.6925701938402700764, 0.2560274467086400274 ) ) ;
#26644=CARTESIAN_POINT ( 'NONE',  ( 0.2705976637934949802, -1.541701018061943484, 0.9966701210605140027 ) ) ;
#26645=CARTESIAN_POINT ( 'NONE',  ( 0.4714652189410261651, -1.557192263116904618, 0.6121692311124370400 ) ) ;
#26646=CARTESIAN_POINT ( 'NONE',  ( 0.1138085506330038799, -0.5805959105637907847, -0.07044495644018930469 ) ) ;
#26648=CARTESIAN_POINT ( 'NONE',  ( 0.09374999999999995837, -0.9316581899787156340, 0.1618212499200845089 ) ) ;
#26649=VERTEX_POINT ( 'NONE', #672 ) ;
#26653=CARTESIAN_POINT ( 'NONE',  ( 0.1434650259794786331, -0.5695106312979485441, 0.4826513458886010910 ) ) ;
#26660=CARTESIAN_POINT ( 'NONE',  ( 0.3778447279644155388, -0.9516834458091659732, 0.7020028943473471950 ) ) ;
#26668=VERTEX_POINT ( 'NONE', #26150 ) ;
#26674=CARTESIAN_POINT ( 'NONE',  ( 0.2330814885300186434, -1.234478371153929555, 0.7248379463662146804 ) ) ;
#26681=CARTESIAN_POINT ( 'NONE',  ( 0.4332292389763821028, -1.186803953203684703, 0.6662783122723310303 ) ) ;
#26684=CARTESIAN_POINT ( 'NONE',  ( 0.1916709472725509622, -0.9174159909098704713, 0.2459055916410233245 ) ) ;
#26687=CARTESIAN_POINT ( 'NONE',  ( 0.5893629127802496592, -1.590949893388290404, 0.4182417262808776903 ) ) ;
#26690=CARTESIAN_POINT ( 'NONE',  ( 0.1845258802888041783, -0.7337134285967986669, 0.05501147976861575639 ) ) ;
#26691=CARTESIAN_POINT ( 'NONE',  ( 0.3649957450613842136, -1.468351375757600996, 0.8486509050985698854 ) ) ;
#26692=CARTESIAN_POINT ( 'NONE',  ( 0.06762866613896016676, -0.6210165958772466688, 0.01354926383832238783 ) ) ;
#26693=CARTESIAN_POINT ( 'NONE',  ( 0.08989780363036058153, -0.5646359461869331353, 0.1460065308160271857 ) ) ;
#26695=ORIENTED_EDGE ( 'NONE', *, *, #14506, .T. ) ;
#26698=CARTESIAN_POINT ( 'NONE',  ( 0.5739388401085829816, -1.499262904232843807, 0.5736237701463445804 ) ) ;
#26702=CARTESIAN_POINT ( 'NONE',  ( 0.6060475248853955943, -1.581096070219540239, 0.4182417262808776903 ) ) ;
#26703=CARTESIAN_POINT ( 'NONE',  ( 0.1896833470237338504, -1.257561668833873103, 0.4318233238025492304 ) ) ;
#26707=CARTESIAN_POINT ( 'NONE',  ( 0.7168528728721502707, -1.464418552067108470, 0.6746166867755808427 ) ) ;
#26714=DIRECTION ( 'NONE',  ( -9.042510699458645841E-13, 1.566396143878659165E-12, -1.000000000000000000 ) ) ;
#26716=CARTESIAN_POINT ( 'NONE',  ( 0.08609895781566062611, -1.325383763084707400, 0.4606884510573937552 ) ) ;
#26717=CARTESIAN_POINT ( 'NONE',  ( 0.1802350563441833808, -0.5022327775090948965, 0.1477559389858786043 ) ) ;
#26720=CARTESIAN_POINT ( 'NONE',  ( 0.6011193747858225578, -1.595581932925099977, 0.4276689662439276396 ) ) ;
#26725=CARTESIAN_POINT ( 'NONE',  ( 0.3211756810167746834, -1.183199798883805887, 0.5707417262808780478 ) ) ;
#26726=ORIENTED_EDGE ( 'NONE', *, *, #32055, .T. ) ;
#26729=CARTESIAN_POINT ( 'NONE',  ( 0.5552614681345688918, -1.388647501241920157, 0.5981693664984994996 ) ) ;
#26730=CARTESIAN_POINT ( 'NONE',  ( 0.2625876981780432828, -0.6796766824346859304, 0.2386862984125060760 ) ) ;
#26732=CARTESIAN_POINT ( 'NONE',  ( 0.4004013247085298488, -1.001184149470538909, 0.6774742858917212063 ) ) ;
#26736=CARTESIAN_POINT ( 'NONE',  ( 0.3272356563838212384, -1.639253224411857390, 0.5768921858655433610 ) ) ;
#26737=CARTESIAN_POINT ( 'NONE',  ( 0.6663393932594230407, -1.528864674313891614, 0.4320056365155769407 ) ) ;
#26738=CARTESIAN_POINT ( 'NONE',  ( 0.1765207216392534473, -0.5289821624952937285, -0.02115802863982717275 ) ) ;
#26739=CARTESIAN_POINT ( 'NONE',  ( 0.4971324743577882899, -1.079965756743124006, 0.4177417262808780229 ) ) ;
#26746=CARTESIAN_POINT ( 'NONE',  ( 0.1484580525513722604, -0.9426921462834582099, 0.6469761069243887830 ) ) ;
#26750=B_SPLINE_CURVE_WITH_KNOTS ( 'NONE', 3,
 ( #13097, #603, #25656, #7303 ),
 .UNSPECIFIED., .F., .F.,
 ( 4, 4 ),
 ( 0.01492582395562414704, 0.01617680779535383279 ),
 .UNSPECIFIED. ) ;
#26751=CARTESIAN_POINT ( 'NONE',  ( 0.1284469837844391393, -0.9382340779789365426, 0.3427534698529470791 ) ) ;
#26754=CARTESIAN_POINT ( 'NONE',  ( 0.6531523644885445234, -1.470371462098315263, 0.4182417262808779124 ) ) ;
#26758=CARTESIAN_POINT ( 'NONE',  ( 0.4120248911441328765, -1.141963342659028102, 0.4320455384514549357 ) ) ;
#26763=CARTESIAN_POINT ( 'NONE',  ( 0.01208707464876302047, -0.4498900264573193475, 0.04206197065121651535 ) ) ;
#26768=EDGE_CURVE ( 'NONE', #20753, #22989, #14795, .T. ) ;
#26770=CARTESIAN_POINT ( 'NONE',  ( 0.1767184732304685202, -0.4886261860184148431, 0.1375861377844761757 ) ) ;
#26773=CARTESIAN_POINT ( 'NONE',  ( 0.1345576988209646330, -0.5547214491096114086, 0.1783673147042096618 ) ) ;
#26776=CARTESIAN_POINT ( 'NONE',  ( -0.0004183621434831840237, -0.7293707673872504849, -0.008477467720215554545 ) ) ;
#26779=B_SPLINE_CURVE_WITH_KNOTS ( 'NONE', 3,
 ( #40556, #20280, #6798, #22462, #37672, #34781 ),
 .UNSPECIFIED., .F., .F.,
 ( 4, 2, 4 ),
 ( 0.000000000000000000, 0.5000000000000000000, 1.000000000000000000 ),
 .UNSPECIFIED. ) ;
#26783=CARTESIAN_POINT ( 'NONE',  ( -0.009205357870253665087, -0.5919609180146404581, 0.3621894606988042553 ) ) ;
#26785=CARTESIAN_POINT ( 'NONE',  ( 0.1428314273233315668, -1.273136066146236312, 0.6057341954371575632 ) ) ;
#26789=ORIENTED_EDGE ( 'NONE', *, *, #24482, .T. ) ;
#26790=ORIENTED_EDGE ( 'NONE', *, *, #15186, .F. ) ;
#26791=CARTESIAN_POINT ( 'NONE',  ( 0.2352121309571624796, -0.9559301127563956113, 0.6564793400487810571 ) ) ;
#26792=CARTESIAN_POINT ( 'NONE',  ( 0.06985341656399968180, -0.5484169138694637846, 0.2034521178982568179 ) ) ;
#26793=CARTESIAN_POINT ( 'NONE',  ( 0.5525824764865431282, -1.511072664810155786, 0.5658631727751453067 ) ) ;
#26794=CARTESIAN_POINT ( 'NONE',  ( 0.02382395405342765254, -1.023441010626642944, 0.5576374536115574765 ) ) ;
#26796=CARTESIAN_POINT ( 'NONE',  ( 0.6544078563150221850, -1.544269123161552626, 0.4241055859090109292 ) ) ;
#26798=CARTESIAN_POINT ( 'NONE',  ( 0.6841302653033145553, -1.411212316466117223, 0.6057417262805112612 ) ) ;
#26799=B_SPLINE_CURVE_WITH_KNOTS ( 'NONE', 3,
 ( #33142, #8856, #8637, #21210, #5148, #27401 ),
 .UNSPECIFIED., .F., .F.,
 ( 4, 2, 4 ),
 ( 0.000000000000000000, 0.2508149426252075376, 0.5016298852504150751 ),
 .UNSPECIFIED. ) ;
#26800=CARTESIAN_POINT ( 'NONE',  ( 0.1876053338355621880, -0.6785855078148245179, 0.1477569985384105666 ) ) ;
#26803=CARTESIAN_POINT ( 'NONE',  ( 6.726208831336936099E-05, -0.6219379412995073020, -0.09511945894820450498 ) ) ;
#26807=CARTESIAN_POINT ( 'NONE',  ( 0.01037466073212112323, -0.7737952308255096057, 0.4846566707863347867 ) ) ;
#26808=CARTESIAN_POINT ( 'NONE',  ( 0.2471460726071840197, -0.9121693139129607442, 0.4829066783201274027 ) ) ;
#26810=CARTESIAN_POINT ( 'NONE',  ( 0.4812359531826634340, -1.078470577594583979, 0.8616913018466071383 ) ) ;
#26812=CARTESIAN_POINT ( 'NONE',  ( 0.3187434959594735995, -1.760361270025436742, 0.5680051819931960511 ) ) ;
#26813=ADVANCED_FACE ( 'NONE', ( #29822 ), #11706, .F. ) ;
#26816=CARTESIAN_POINT ( 'NONE',  ( 0.1487004007006368367, -1.233131608729471695, 0.9291103107006072337 ) ) ;
#26818=CARTESIAN_POINT ( 'NONE',  ( 0.2144290776330740889, -1.231722763067022219, 0.4813240406935799798 ) ) ;
#26819=CARTESIAN_POINT ( 'NONE',  ( 0.4577135909791524848, -1.717961013370186141, 0.5182417262812423209 ) ) ;
#26823=TOROIDAL_SURFACE ( 'NONE', #11719, 0.08249999999977548903, 0.01000000000000000021 ) ;
#26824=CARTESIAN_POINT ( 'NONE',  ( 0.5633629393321837320, -1.208205391268785567, 0.7270432621192387534 ) ) ;
#26825=EDGE_LOOP ( 'NONE', ( #21819, #32784, #31064 ) ) ;
#26834=CARTESIAN_POINT ( 'NONE',  ( -19685.04193433331602, 285.7890798983738136, -1.951739244310253252 ) ) ;
#26835=CARTESIAN_POINT ( 'NONE',  ( 0.2042160338947917320, -0.8611997158126063479, 0.6444930625586713369 ) ) ;
#26836=CARTESIAN_POINT ( 'NONE',  ( 0.2902408836998817687, -1.617250972615089433, 0.9506298565161998004 ) ) ;
#26837=CARTESIAN_POINT ( 'NONE',  ( 0.4886971128151171295, -1.518144040485195800, 0.7197715497223399206 ) ) ;
#26838=CARTESIAN_POINT ( 'NONE',  ( 0.2692931055722388445, -1.652497923304702132, 0.7773017355661825389 ) ) ;
#26840=EDGE_CURVE ( 'NONE', #36726, #19301, #34372, .T. ) ;
#26841=CARTESIAN_POINT ( 'NONE',  ( 0.2325857081196134601, -1.005531832322530184, 0.5832656420552320142 ) ) ;
#26846=CARTESIAN_POINT ( 'NONE',  ( 0.2356700409021097453, -0.6918407148733107803, 0.4984434980982429542 ) ) ;
#26849=CARTESIAN_POINT ( 'NONE',  ( 0.07457743601771446573, -1.318870387072609507, 0.4957195692065117787 ) ) ;
#26852=CARTESIAN_POINT ( 'NONE',  ( 0.4529286794724542986, -1.051290237540063455, 0.7432202178062045084 ) ) ;
#26865=CARTESIAN_POINT ( 'NONE',  ( 0.2557456068137679006, -1.277973818264130479, 0.6877359101403667241 ) ) ;
#26871=CARTESIAN_POINT ( 'NONE',  ( 0.4681644054017271572, -1.238292871408442686, 0.5986446648243279878 ) ) ;
#26876=CARTESIAN_POINT ( 'NONE',  ( 0.3538719729184752749, -1.624715450675502160, 0.4182417262808775238 ) ) ;
#26877=ORIENTED_EDGE ( 'NONE', *, *, #3444, .T. ) ;
#26878=CARTESIAN_POINT ( 'NONE',  ( 0.1915883296772408761, -0.5477411782657776174, 0.1479976049341028554 ) ) ;
#26879=CARTESIAN_POINT ( 'NONE',  ( 0.06043570224876768787, -0.5391841548082976221, 0.1632230437248760602 ) ) ;
#26880=CARTESIAN_POINT ( 'NONE',  ( 0.08926425616020196296, -0.5615075463834332536, 0.07548189203980994189 ) ) ;
#26882=CARTESIAN_POINT ( 'NONE',  ( 0.1176807611043763635, -1.298951677446983588, 0.5132863183563353138 ) ) ;
#26883=EDGE_CURVE ( 'NONE', #12740, #28384, #9815, .T. ) ;
#26888=CARTESIAN_POINT ( 'NONE',  ( 0.1203440671115274391, -0.5719449301461521085, 0.2477259942629035927 ) ) ;
#26895=CARTESIAN_POINT ( 'NONE',  ( 0.2004112705531303495, -1.239815393329114723, 0.4579970032064163976 ) ) ;
#26896=CARTESIAN_POINT ( 'NONE',  ( 0.002290818369124609372, -0.5198888459286679087, 0.1457185332388686583 ) ) ;
#26898=CARTESIAN_POINT ( 'NONE',  ( 0.7185393139234729221, -1.479621239843056157, 0.4933132820244564565 ) ) ;
#26905=CARTESIAN_POINT ( 'NONE',  ( 0.1186969743450562581, -1.297359616540578076, 0.4321288993546299473 ) ) ;
#26906=CARTESIAN_POINT ( 'NONE',  ( 0.3122857990831161556, -1.766572940467653785, 0.5980579735034173838 ) ) ;
#26911=DIRECTION ( 'NONE',  ( -0.4999551463232372317, 0.8660512985181134660, -0.000000000000000000 ) ) ;
#26915=CARTESIAN_POINT ( 'NONE',  ( 0.2318589737339854795, -1.232498520698479982, 0.5197417262808780025 ) ) ;
#26916=CARTESIAN_POINT ( 'NONE',  ( 0.08989780363036058153, -0.5646359461869331353, 0.1460065308160271857 ) ) ;
#26918=CARTESIAN_POINT ( 'NONE',  ( 0.4892141979174440825, -1.277531844236459158, 0.7175028335045045003 ) ) ;
#26921=CARTESIAN_POINT ( 'NONE',  ( 0.4714567382560805875, -1.076664716445512093, 0.6912835816774075548 ) ) ;
#26925=CARTESIAN_POINT ( 'NONE',  ( 0.3271419406413549891, -1.639226515742882917, 0.5756636260908921665 ) ) ;
#26926=CARTESIAN_POINT ( 'NONE',  ( 0.6773337002013100072, -1.513729376107809221, 0.4441964172979790404 ) ) ;
#26927=CARTESIAN_POINT ( 'NONE',  ( 0.1871805636416381813, -0.5848937521155493924, 0.01295504015953219575 ) ) ;
#26928=CARTESIAN_POINT ( 'NONE',  ( 0.4970273525888077026, -1.079783658718535877, 0.3157417262808778213 ) ) ;
#26931=ORIENTED_EDGE ( 'NONE', *, *, #28089, .F. ) ;
#26934=CARTESIAN_POINT ( 'NONE',  ( 0.07907905168990768396, -0.8327024128097890721, 0.1457185332388749033 ) ) ;
#26938=B_SPLINE_CURVE_WITH_KNOTS ( 'NONE', 3,
 ( #4785, #26642, #17360, #17568, #30305, #20256, #1942, #29916, #14667, #39172, #23956, #39363, #5198, #24163, #33392, #1758, #39550, #14270, #20871, #7872 ),
 .UNSPECIFIED., .F., .F.,
 ( 4, 2, 2, 2, 2, 2, 2, 2, 2, 4 ),
 ( 0.000000000000000000, 0.0006013140366011756862, 0.001202628073202351372, 0.001803942109803526950, 0.002104599128104107150, 0.002405256146404686698, 0.003006570183005846664, 0.003607884219607006195, 0.004209198256208165727, 0.004810512292809325692 ),
 .UNSPECIFIED. ) ;
#26939=CARTESIAN_POINT ( 'NONE',  ( 0.1650048525095897667, -0.9588139417348214844, 0.4627461750576811750 ) ) ;
#26940=CARTESIAN_POINT ( 'NONE',  ( 0.6672603290686145439, -1.495344574087576150, 0.4226843776606147851 ) ) ;
#26945=CARTESIAN_POINT ( 'NONE',  ( 0.04703387973542435402, -1.223263004737442428, 0.6745384190568795013 ) ) ;
#26946=CARTESIAN_POINT ( 'NONE',  ( 0.4959366141775247150, -1.219826185980712241, 0.6057417262809806635 ) ) ;
#26947=CYLINDRICAL_SURFACE ( 'NONE', #18585, 0.01000000000000005398 ) ;
#26948=CARTESIAN_POINT ( 'NONE',  ( 2.556504791813307099E-05, -0.4639112435509614718, 0.01040637860906285135 ) ) ;
#26950=CARTESIAN_POINT ( 'NONE',  ( 0.001543112456845291544, -0.4709528296724027063, 0.2942976250601397337 ) ) ;
#26960=CARTESIAN_POINT ( 'NONE',  ( 0.0001947388906042439084, -0.6652226476256291043, -0.02097404292247649973 ) ) ;
#26963=CARTESIAN_POINT ( 'NONE',  ( 0.1272900688827675320, -0.5203071491166968432, 0.3917611924818291680 ) ) ;
#26965=CARTESIAN_POINT ( 'NONE',  ( 0.2710593583788064032, -1.672243337529662810, 0.6600209757948071188 ) ) ;
#26967=CARTESIAN_POINT ( 'NONE',  ( 0.1683750554522408238, -1.244696949452464452, 0.6168817076097603547 ) ) ;
#26968=CYLINDRICAL_SURFACE ( 'NONE', #368, 0.03749999999977545601 ) ;
#26973=CARTESIAN_POINT ( 'NONE',  ( 0.01155593465058764660, -0.8452630998613906987, -0.06009144441515529289 ) ) ;
#26974=CARTESIAN_POINT ( 'NONE',  ( 0.05026878653071940178, -1.025413872748235145, 0.7120682109587219699 ) ) ;
#26975=CARTESIAN_POINT ( 'NONE',  ( 0.09061274716232860238, -0.5518344063121839449, 0.2019960243542438250 ) ) ;
#26976=CARTESIAN_POINT ( 'NONE',  ( 0.1874086131461644433, -0.6929147893325138252, 0.03706785969987234919 ) ) ;
#26977=CARTESIAN_POINT ( 'NONE',  ( 0.4742224691869081354, -1.671175273632494074, 0.5656171320065535024 ) ) ;
#26978=CARTESIAN_POINT ( 'NONE',  ( 0.06485795133942112711, -1.341245217906781528, 0.5684376680647764690 ) ) ;
#26981=CARTESIAN_POINT ( 'NONE',  ( 0.4567198261210261845, -1.219045092035883293, 0.5856983068965102568 ) ) ;
#26989=CARTESIAN_POINT ( 'NONE',  ( 0.01131419357477797018, -0.9464773851093645218, 0.1333178999391497199 ) ) ;
#26992=VECTOR ( 'NONE', #30819, 39.37007874015748854 ) ;
#26993=EDGE_CURVE ( 'NONE', #25669, #32917, #37209, .T. ) ;
#26996=CARTESIAN_POINT ( 'NONE',  ( 0.004299088327612451445, -0.5973376383060815531, 0.3026940496400818970 ) ) ;
#26997=CARTESIAN_POINT ( 'NONE',  ( 0.1863616350354748430, -0.8703638341540448353, 0.1952903930469164218 ) ) ;
#26999=CARTESIAN_POINT ( 'NONE',  ( 0.3900547927747317067, -0.9231895138380423749, 0.8021268779562266138 ) ) ;
#27007=CARTESIAN_POINT ( 'NONE',  ( 0.02616834738919181572, -0.7253350560476993225, 0.5960850904724321886 ) ) ;
#27012=CARTESIAN_POINT ( 'NONE',  ( 0.06356324272688286536, -1.339002332173930832, 0.5682722211006857593 ) ) ;
#27013=CARTESIAN_POINT ( 'NONE',  ( 0.5468032192656866464, -1.183383020191767443, 0.7376474321803302425 ) ) ;
#27015=ORIENTED_EDGE ( 'NONE', *, *, #24487, .T. ) ;
#27018=ORIENTED_EDGE ( 'NONE', *, *, #15483, .F. ) ;
#27020=CARTESIAN_POINT ( 'NONE',  ( 3.466477128667603047, -1.051097370103299733, 0.4182417262808778013 ) ) ;
#27026=CARTESIAN_POINT ( 'NONE',  ( 0.1763646209231259920, -0.8431947878026431198, 0.5885539986222864117 ) ) ;
#27027=CARTESIAN_POINT ( 'NONE',  ( 0.2556018531037459462, -1.498891464106183014, 1.002349236551413281 ) ) ;
#27028=CARTESIAN_POINT ( 'NONE',  ( 0.1828482083265061120, -0.8368919259864775473, 0.6643785663031293032 ) ) ;
#27029=CARTESIAN_POINT ( 'NONE',  ( 0.1142161186253681515, -0.5282243346103802084, -0.03585910532386479832 ) ) ;
#27031=CARTESIAN_POINT ( 'NONE',  ( 0.01562499999999997224, -0.9454337353465638305, 0.1626451679851157184 ) ) ;
#27035=CARTESIAN_POINT ( 'NONE',  ( 0.5937943159907096424, -1.263846424195741891, 0.8742795452994258643 ) ) ;
#27037=EDGE_CURVE ( 'NONE', #40008, #528, #38615, .T. ) ;
#27044=EDGE_CURVE ( 'NONE', #11702, #16451, #10854, .T. ) ;
#27046=CARTESIAN_POINT ( 'NONE',  ( 0.5155751834530871713, -1.137973747986757544, 0.7479765829993398896 ) ) ;
#27052=EDGE_LOOP ( 'NONE', ( #19980, #36380, #30167, #954, #33329, #33072, #6694, #36414 ) ) ;
#27055=CARTESIAN_POINT ( 'NONE',  ( 0.6068013899440870551, -1.480012627510800760, 0.5642015433052736118 ) ) ;
#27057=ORIENTED_EDGE ( 'NONE', *, *, #8109, .F. ) ;
#27060=CARTESIAN_POINT ( 'NONE',  ( 0.1130491610541830005, -1.062706497792865523, 0.7372862091105505389 ) ) ;
#27066=CARTESIAN_POINT ( 'NONE',  ( 0.4688806894441774897, -1.239828276217276759, 0.5901340395503891223 ) ) ;
#27077=CARTESIAN_POINT ( 'NONE',  ( 0.2634339134604823940, -1.167471577589091369, 0.8605345870829919086 ) ) ;
#27078=CARTESIAN_POINT ( 'NONE',  ( 0.6926523052361154287, -1.550981559465477666, 0.5932697689988618572 ) ) ;
#27080=CARTESIAN_POINT ( 'NONE',  ( 0.5006733635628357604, -1.193711096620792889, 0.4198196556967657145 ) ) ;
#27084=CARTESIAN_POINT ( 'NONE',  ( 0.1684271861732587194, -0.7249060024178762829, 0.5310654164351663598 ) ) ;
#27085=ORIENTED_EDGE ( 'NONE', *, *, #11163, .F. ) ;
#27089=CARTESIAN_POINT ( 'NONE',  ( 0.6295207449309501158, -1.563610153985103945, 0.4182417262808776903 ) ) ;
#27090=CARTESIAN_POINT ( 'NONE',  ( 0.1413813297004133662, -1.285503893349357663, 0.4210986513813943510 ) ) ;
#27094=B_SPLINE_CURVE_WITH_KNOTS ( 'NONE', 3,
 ( #21464, #11584, #36667, #15065 ),
 .UNSPECIFIED., .F., .F.,
 ( 4, 4 ),
 ( 0.8392141848601618603, 0.9812523608469967407 ),
 .UNSPECIFIED. ) ;
#27095=CARTESIAN_POINT ( 'NONE',  ( 0.2622253439111549289, -0.6837502657356347990, 0.6133988000875116864 ) ) ;
#27102=CARTESIAN_POINT ( 'NONE',  ( 0.6565669552028456923, -1.566507581639152935, 0.6100543721193861790 ) ) ;
#27107=CARTESIAN_POINT ( 'NONE',  ( 0.002083146443013488870, -0.4777046557262296100, 0.1283381445693447254 ) ) ;
#27112=DIRECTION ( 'NONE',  ( -0.4999551463232347892, 0.8660512985181149093, 0.000000000000000000 ) ) ;
#27119=CARTESIAN_POINT ( 'NONE',  ( 0.3386245021663031318, -1.171855970582244222, 0.5796378340604717572 ) ) ;
#27120=CARTESIAN_POINT ( 'NONE',  ( 0.1915761776375039804, -1.276944146096590016, 0.5182417262812423209 ) ) ;
#27122=CARTESIAN_POINT ( 'NONE',  ( 0.5048881121617861956, -1.301036302150182289, 0.6753596003262275493 ) ) ;
#27125=CARTESIAN_POINT ( 'NONE',  ( 0.3382833150183324755, -0.9396054708716727877, 0.6333258291577809063 ) ) ;
#27131=CARTESIAN_POINT ( 'NONE',  ( 0.3573112754633941401, -1.622562401408601085, 0.5912586822741335846 ) ) ;
#27132=CARTESIAN_POINT ( 'NONE',  ( 0.7000186069066542949, -1.492953544047383563, 0.4955563437734074594 ) ) ;
#27133=CARTESIAN_POINT ( 'NONE',  ( 0.1139707206188099453, -0.5585964955268626353, -0.05809159769505588267 ) ) ;
#27135=VECTOR ( 'NONE', #15193, 39.37007874015748143 ) ;
#27136=B_SPLINE_CURVE_WITH_KNOTS ( 'NONE', 3,
 ( #16971, #13861, #29515, #7703 ),
 .UNSPECIFIED., .F., .F.,
 ( 4, 4 ),
 ( 0.02020468389890235292, 0.1625918618111195091 ),
 .UNSPECIFIED. ) ;
#27139=CARTESIAN_POINT ( 'NONE',  ( 0.1828088565713123503, -1.273079348061378235, 0.4182417262808778013 ) ) ;
#27143=CARTESIAN_POINT ( 'NONE',  ( 0.1316173717439282076, -0.9114899509784721854, 0.5960367549459311132 ) ) ;
#27148=ADVANCED_FACE ( 'NONE', ( #19694 ), #2523, .T. ) ;
#27149=DIRECTION ( 'NONE',  ( -0.4870160029269081092, 0.8733930460526335704, 0.000000000000000000 ) ) ;
#27150=CARTESIAN_POINT ( 'NONE',  ( 0.5708401535611469235, -1.615683077095924736, 0.5197417262808792238 ) ) ;
#27155=CARTESIAN_POINT ( 'NONE',  ( 0.4333926128620538831, -1.140607306138202270, 0.4331035760720922112 ) ) ;
#27156=CARTESIAN_POINT ( 'NONE',  ( 0.4638926575998975621, -1.238161088593346282, 0.6057417262809813296 ) ) ;
#27158=FACE_OUTER_BOUND ( 'NONE', #20438, .T. ) ;
#27159=( BOUNDED_SURFACE ( )  B_SPLINE_SURFACE ( 3, 2, ( 
 ( #13832, #3781, #26018 ),
 ( #7056, #32159, #3968 ),
 ( #17133, #38535, #14045 ),
 ( #38327, #6851, #19431 ),
 ( #939, #35862, #10365 ),
 ( #16335, #22927, #28874 ),
 ( #32567, #7242, #19818 ),
 ( #16940, #29684, #22728 ),
 ( #4383, #7676, #32352 ),
 ( #13236, #25806, #26407 ),
 ( #38937, #16744, #29292 ),
 ( #10159, #7456, #4173 ),
 ( #13639, #26206, #10552 ),
 ( #23127, #35655, #9947 ),
 ( #20034, #10769, #20241 ),
 ( #32761, #4563, #2115 ),
 ( #11368, #14253, #2527 ),
 ( #39954, #33376, #39754 ),
 ( #27218, #36058, #8283 ),
 ( #5594, #17732, #20851 ),
 ( #23541, #11772, #27007 ),
 ( #30706, #4983, #32965 ),
 ( #33562, #30094, #24148 ),
 ( #5179, #14650, #5378 ),
 ( #18152, #39155, #17341 ),
 ( #17552, #20427, #1923 ),
 ( #21039, #36858, #30282 ),
 ( #24332, #36469, #2329 ),
 ( #8068, #33181, #20642 ),
 ( #26626, #11585, #36668 ),
 ( #10981, #21251, #7857 ),
 ( #8673, #30497, #4769 ),
 ( #1742, #23722, #36250 ),
 ( #14440, #29899, #39534 ),
 ( #23937, #26816, #39346 ),
 ( #14869, #8478, #33786 ),
 ( #17941, #27429, #11167 ),
 ( #15266, #86, #37894 ),
 ( #15482, #18774, #9705 ),
 ( #5794, #28036, #12795 ),
 ( #40564, #40146, #30899 ),
 ( #21864, #25358, #22078 ),
 ( #12190, #37072, #25140 ),
 ( #6592, #24750, #2927 ),
 ( #31714, #34180, #9284 ),
 ( #22273, #12383, #34391 ),
 ( #34788, #27617, #2719 ),
 ( #27823, #24938, #40358 ),
 ( #18351, #28423, #6204 ),
 ( #11977, #15672, #24542 ),
 ( #33989, #28219, #37272 ),
 ( #34601, #296, #37466 ),
 ( #9089, #15066, #21655 ),
 ( #31325, #19172, #6403 ),
 ( #5991, #8892, #37681 ),
 ( #21465, #18556, #3132 ),
 ( #31113, #12579, #9499 ),
 ( #18971, #31504, #3313 ),
 ( #15876, #16095, #31923 ),
 ( #3742, #29024, #16295 ),
 ( #34997, #16897, #10326 ),
 ( #38080, #28639, #22683 ),
 ( #22470, #16691, #13185 ),
 ( #29439, #28834, #38496 ),
 ( #7403, #7625, #35217 ),
 ( #1283, #3532, #26356 ),
 ( #1095, #13788, #7017 ),
 ( #9899, #23288, #3923 ),
 ( #29237, #6806, #10111 ),
 ( #13004, #35407, #22887 ) ),
 .UNSPECIFIED., .F., .F., .T. ) 
 B_SPLINE_SURFACE_WITH_KNOTS ( ( 4, 2, 2, 2, 2, 2, 2, 2, 2, 2, 2, 2, 2, 2, 2, 2, 2, 2, 2, 2, 2, 2, 2, 2, 2, 2, 2, 2, 2, 2, 2, 2, 2, 2, 4 ),
 ( 3, 3 ),
 ( 0.006982594028375741814, 0.007169652589743046381, 0.007263181870426699098, 0.007356711151110351815, 0.007730828273844962684, 0.008479062519314182686, 0.009975531010252624425, 0.01147199950119106443, 0.01296846799212950617, 0.01895434195588327139, 0.02045081044682171140, 0.02194727893776015487, 0.02494021591963703488, 0.02793315290151391489, 0.02942962139245235836, 0.03092608988339079837, 0.03391902686526768185, 0.03691196384714456186, 0.03840843233808299839, 0.03990490082902144187, 0.04140136931995988534, 0.04289783781089832881, 0.04364607205636755055, 0.04439430630183677229, 0.04589077479277520882, 0.04663900903824443056, 0.04738724328371364536, 0.04813547752918286710, 0.04888371177465208883, 0.05038018026559053231, 0.05187664875652897578, 0.05337311724746741926, 0.05374723437020202665, 0.05412135149293663405, 0.05486958573840585579 ),
 ( 0.000000000000000000, 1.000000000000000000 ),
 .UNSPECIFIED. ) 
 GEOMETRIC_REPRESENTATION_ITEM ( )  RATIONAL_B_SPLINE_SURFACE ( (
 ( 1.000000000000000000, 0.7687635770067674512, 1.000000000000000000),
 ( 1.000000000000000000, 0.7687635770067674512, 1.000000000000000000),
 ( 1.000000000000000000, 0.7687635770067657859, 1.000000000000000000),
 ( 1.000000000000000000, 0.7687635770067657859, 1.000000000000000000),
 ( 1.000000000000000000, 0.7687635770067644536, 1.000000000000000000),
 ( 1.000000000000000000, 0.7687635770067644536, 1.000000000000000000),
 ( 1.000000000000000000, 0.7687632101434925813, 1.000000000000000000),
 ( 1.000000000000000000, 0.7687598537572957191, 1.000000000000000000),
 ( 1.000000000000000000, 0.7687534107862498134, 1.000000000000000000),
 ( 1.000000000000000000, 0.7687384292891166204, 1.000000000000000000),
 ( 1.000000000000000000, 0.7687365999447838272, 1.000000000000000000),
 ( 1.000000000000000000, 0.7687020167486041666, 1.000000000000000000),
 ( 1.000000000000000000, 0.7686222834918778890, 1.000000000000000000),
 ( 1.000000000000000000, 0.7675492984621066217, 1.000000000000000000),
 ( 1.000000000000000000, 0.7668174832494044635, 1.000000000000000000),
 ( 1.000000000000000000, 0.7652231905048935134, 1.000000000000000000),
 ( 1.000000000000000000, 0.7643808905106918017, 1.000000000000000000),
 ( 1.000000000000000000, 0.7599837323011349177, 1.000000000000000000),
 ( 1.000000000000000000, 0.7555546695031651883, 1.000000000000000000),
 ( 1.000000000000000000, 0.7485199935451233300, 1.000000000000000000),
 ( 1.000000000000000000, 0.7470345500374537817, 1.000000000000000000),
 ( 1.000000000000000000, 0.7439636425267035502, 1.000000000000000000),
 ( 1.000000000000000000, 0.7423870523181574921, 1.000000000000000000),
 ( 1.000000000000000000, 0.7376049540916959080, 1.000000000000000000),
 ( 1.000000000000000000, 0.7343341012102607701, 1.000000000000000000),
 ( 1.000000000000000000, 0.7284347353659686997, 1.000000000000000000),
 ( 1.000000000000000000, 0.7258666192759820612, 1.000000000000000000),
 ( 1.000000000000000000, 0.7233512264919610413, 1.000000000000000000),
 ( 1.000000000000000000, 0.7227328269103746594, 1.000000000000000000),
 ( 1.000000000000000000, 0.7220177958833203791, 1.000000000000000000),
 ( 1.000000000000000000, 0.7219233079132257869, 1.000000000000000000),
 ( 1.000000000000000000, 0.7224401686324471994, 1.000000000000000000),
 ( 1.000000000000000000, 0.7237963925639867568, 1.000000000000000000),
 ( 1.000000000000000000, 0.7277615327345778873, 1.000000000000000000),
 ( 1.000000000000000000, 0.7304068960252722009, 1.000000000000000000),
 ( 1.000000000000000000, 0.7344733377828095433, 1.000000000000000000),
 ( 1.000000000000000000, 0.7358434634388121287, 1.000000000000000000),
 ( 1.000000000000000000, 0.7384753478062177079, 1.000000000000000000),
 ( 1.000000000000000000, 0.7397446418154087766, 1.000000000000000000),
 ( 1.000000000000000000, 0.7420434277178875604, 1.000000000000000000),
 ( 1.000000000000000000, 0.7430738375077751146, 1.000000000000000000),
 ( 1.000000000000000000, 0.7446479001369198381, 1.000000000000000000),
 ( 1.000000000000000000, 0.7451730098702049609, 1.000000000000000000),
 ( 1.000000000000000000, 0.7453954219144471871, 1.000000000000000000),
 ( 1.000000000000000000, 0.7453712964557482890, 1.000000000000000000),
 ( 1.000000000000000000, 0.7450704390704340208, 1.000000000000000000),
 ( 1.000000000000000000, 0.7447959842850340184, 1.000000000000000000),
 ( 1.000000000000000000, 0.7435913020326400114, 1.000000000000000000),
 ( 1.000000000000000000, 0.7422580051630394138, 1.000000000000000000),
 ( 1.000000000000000000, 0.7395387433289906109, 1.000000000000000000),
 ( 1.000000000000000000, 0.7385151462303933823, 1.000000000000000000),
 ( 1.000000000000000000, 0.7363255657919565156, 1.000000000000000000),
 ( 1.000000000000000000, 0.7351593361101353974, 1.000000000000000000),
 ( 1.000000000000000000, 0.7327799655195763595, 1.000000000000000000),
 ( 1.000000000000000000, 0.7315669817046001056, 1.000000000000000000),
 ( 1.000000000000000000, 0.7291668309240953993, 1.000000000000000000),
 ( 1.000000000000000000, 0.7279734049794366335, 1.000000000000000000),
 ( 1.000000000000000000, 0.7245550934509018548, 1.000000000000000000),
 ( 1.000000000000000000, 0.7225262869826848400, 1.000000000000000000),
 ( 1.000000000000000000, 0.7191733065149791271, 1.000000000000000000),
 ( 1.000000000000000000, 0.7178371072958583676, 1.000000000000000000),
 ( 1.000000000000000000, 0.7159520326050418104, 1.000000000000000000),
 ( 1.000000000000000000, 0.7154250687472349934, 1.000000000000000000),
 ( 1.000000000000000000, 0.7152986269598831104, 1.000000000000000000),
 ( 1.000000000000000000, 0.7153184165285554341, 1.000000000000000000),
 ( 1.000000000000000000, 0.7151210821975008125, 1.000000000000000000),
 ( 1.000000000000000000, 0.7151025729118313246, 1.000000000000000000),
 ( 1.000000000000000000, 0.7149568612536305601, 1.000000000000000000),
 ( 1.000000000000000000, 0.7148599564469685363, 1.000000000000000000),
 ( 1.000000000000000000, 0.7147632890095302338, 1.000000000000000000) ) ) 
 REPRESENTATION_ITEM ( '' )  SURFACE ( )  );
#27160=CARTESIAN_POINT ( 'NONE',  ( 2.612502379249534283E-05, -0.4595599869189778697, 0.01785893867001119018 ) ) ;
#27169=CARTESIAN_POINT ( 'NONE',  ( 0.4166104074968063342, -1.713279937176168888, 0.4265607484113185244 ) ) ;
#27173=CARTESIAN_POINT ( 'NONE',  ( 0.0005173413194128835589, -0.6356009618386162519, -0.005393434144287580050 ) ) ;
#27180=CARTESIAN_POINT ( 'NONE',  ( 0.2675213926922588303, -1.675618524670827725, 0.5885039628761479236 ) ) ;
#27181=CARTESIAN_POINT ( 'NONE',  ( 0.5960624699613672473, -1.598417375062506807, 0.4241902398403092911 ) ) ;
#27182=CARTESIAN_POINT ( 'NONE',  ( 0.1219191204388515443, -1.265695392162811128, 0.6214586437892982707 ) ) ;
#27185=CARTESIAN_POINT ( 'NONE',  ( 0.5128645028602584199, -1.648320493942843079, 0.5682417262808785452 ) ) ;
#27188=CARTESIAN_POINT ( 'NONE',  ( 0.01158602179187158757, -0.8240205477835698122, -0.07428298264304349086 ) ) ;
#27189=CARTESIAN_POINT ( 'NONE',  ( 0.2209956536232957902, -1.227897296991992793, 0.5182417262820130377 ) ) ;
#27190=CARTESIAN_POINT ( 'NONE',  ( 0.1327909607021672822, -0.7181627890942366976, 0.4916566485045106294 ) ) ;
#27191=CARTESIAN_POINT ( 'NONE',  ( 0.1873172703549026430, -0.6992301746806637297, 0.03180769156107667722 ) ) ;
#27192=CARTESIAN_POINT ( 'NONE',  ( 0.4732241761476873032, -1.676040907666597635, 0.5636287125706156420 ) ) ;
#27193=CARTESIAN_POINT ( 'NONE',  ( 0.05990452446249143470, -1.332664632394616522, 0.5684199413688966196 ) ) ;
#27201=CARTESIAN_POINT ( 'NONE',  ( 0.6451746001002063302, -1.456551915967818189, 0.4182417262808775238 ) ) ;
#27203=CARTESIAN_POINT ( 'NONE',  ( 0.4438612498438265774, -1.115686201973224989, 0.5854483341245866335 ) ) ;
#27206=CARTESIAN_POINT ( 'NONE',  ( 0.1287314663193102893, -1.150224043500909454, 0.9169127589950010204 ) ) ;
#27208=CARTESIAN_POINT ( 'NONE',  ( 0.4871018846440973715, -1.079508789421436799, 0.5988988590622403851 ) ) ;
#27209=CARTESIAN_POINT ( 'NONE',  ( 0.03517919600029659893, -0.9626726882664039531, 0.6501402935033664399 ) ) ;
#27211=CARTESIAN_POINT ( 'NONE',  ( 0.1893427799090355301, -0.4853919354581605061, 0.2707563002020392240 ) ) ;
#27218=CARTESIAN_POINT ( 'NONE',  ( 0.02214534912214586454, -0.6642453835387356342, 0.4942379723847386552 ) ) ;
#27220=CARTESIAN_POINT ( 'NONE',  ( 0.5878316020795693042, -1.491211184378168131, 0.5715274954139647479 ) ) ;
#27221=CARTESIAN_POINT ( 'NONE',  ( 0.2904739219323096422, -1.661323359162851787, 0.4499284763591545055 ) ) ;
#27222=DIRECTION ( 'NONE',  ( 0.01254811300245564816, 0.8659344938869285579, 0.4999999971568664936 ) ) ;
#27225=CARTESIAN_POINT ( 'NONE',  ( 0.5974340449968663647, -1.261189741147681787, 0.6853727476855657752 ) ) ;
#27230=ORIENTED_EDGE ( 'NONE', *, *, #23573, .F. ) ;
#27240=CARTESIAN_POINT ( 'NONE',  ( 0.09432152222331363634, -0.7171591389413056739, 0.2904309725956230603 ) ) ;
#27242=CARTESIAN_POINT ( 'NONE',  ( 0.3074989459046198470, -1.644816290331682085, 0.9179228641454580950 ) ) ;
#27243=CARTESIAN_POINT ( 'NONE',  ( 0.4966101132311644406, -1.532727327792678951, 0.6782467145029912325 ) ) ;
#27244=VECTOR ( 'NONE', #28204, 39.37007874015748143 ) ;
#27246=CARTESIAN_POINT ( 'NONE',  ( 0.1876053338355621880, -0.6785855078148245179, 0.1477569985384105666 ) ) ;
#27247=CARTESIAN_POINT ( 'NONE',  ( 0.07484086907908865660, -1.207164791911022217, 0.6604330453735346440 ) ) ;
#27250=CARTESIAN_POINT ( 'NONE',  ( 0.3187641638634987618, -1.760284878867080183, 0.5597302103697527897 ) ) ;
#27251=CARTESIAN_POINT ( 'NONE',  ( 0.5539872852267673231, -1.198627223726707491, 0.8202900059160223023 ) ) ;
#27257=CARTESIAN_POINT ( 'NONE',  ( 0.06837834821047945877, -1.326772567953161897, 0.5201612180504711080 ) ) ;
#27260=CARTESIAN_POINT ( 'NONE',  ( 0.3283134639458292758, -1.178171897100129151, 0.5638118889048701066 ) ) ;
#27261=CARTESIAN_POINT ( 'NONE',  ( 0.5555567715531690709, -1.190973094708358992, 0.5709149340790615756 ) ) ;
#27270=AXIS2_PLACEMENT_3D ( 'NONE', #17865, #30430, #20781 ) ;
#27273=CARTESIAN_POINT ( 'NONE',  ( 0.5318682467102796574, -1.150266585189366531, 0.6291131035211885436 ) ) ;
#27275=CARTESIAN_POINT ( 'NONE',  ( 0.1756863999069679660, -1.240364938524567862, 0.7368202461708308615 ) ) ;
#27284=CARTESIAN_POINT ( 'NONE',  ( 0.3957667564970019369, -1.142477732822457126, 0.6888951601802728586 ) ) ;
#27286=CARTESIAN_POINT ( 'NONE',  ( 0.4751248519516730884, -1.681100737592190031, 0.5628962907142390781 ) ) ;
#27291=EDGE_CURVE ( 'NONE', #34692, #39668, #12456, .T. ) ;
#27295=CARTESIAN_POINT ( 'NONE',  ( 0.1868687334809603917, -0.4547550531002670371, 0.05501147976861575639 ) ) ;
#27296=CARTESIAN_POINT ( 'NONE',  ( 0.3705980884814369936, -1.414600388509865914, 0.8578092172935054549 ) ) ;
#27299=CARTESIAN_POINT ( 'NONE',  ( 0.4974456442574050619, -1.184401136727558868, 0.4224083929475309640 ) ) ;
#27304=CARTESIAN_POINT ( 'NONE',  ( 0.5800985813862742368, -1.490016391247783734, 0.6431135307928460554 ) ) ;
#27306=CARTESIAN_POINT ( 'NONE',  ( 0.6699292074404794572, -1.569526485364059143, 0.6071573546319902759 ) ) ;
#27313=CARTESIAN_POINT ( 'NONE',  ( 0.4717011137366580176, -1.062550488221034151, 0.8575416557712804977 ) ) ;
#27320=CARTESIAN_POINT ( 'NONE',  ( 0.5862859414779472145, -1.607631461875910217, 0.5832712881534547478 ) ) ;
#27321=DIRECTION ( 'NONE',  ( 0.8660512985181139101, 0.4999551463232366766, 0.000000000000000000 ) ) ;
#27324=CARTESIAN_POINT ( 'NONE',  ( 0.001298983775798597754, -0.4632363948272406606, 0.3098607539948510792 ) ) ;
#27325=CARTESIAN_POINT ( 'NONE',  ( 0.1316017208954911033, -1.248059642665102942, 0.5182417262812423209 ) ) ;
#27332=CARTESIAN_POINT ( 'NONE',  ( 0.3571916633338231839, -1.156198450587171189, 0.5973401585408657510 ) ) ;
#27336=CARTESIAN_POINT ( 'NONE',  ( 0.5229710184148730345, -1.333122656980544773, 0.5928855954934411088 ) ) ;
#27338=VERTEX_POINT ( 'NONE', #3016 ) ;
#27339=CARTESIAN_POINT ( 'NONE',  ( 0.5130887424854349010, -1.117175276521638505, 0.5842416974757255188 ) ) ;
#27340=VERTEX_POINT ( 'NONE', #24828 ) ;
#27344=CARTESIAN_POINT ( 'NONE',  ( 0.08222542156927918622, -1.327483614382551913, 0.4683366274853996702 ) ) ;
#27345=CARTESIAN_POINT ( 'NONE',  ( 0.3593153017356163215, -1.620878803526070389, 0.6356398769032042262 ) ) ;
#27346=CARTESIAN_POINT ( 'NONE',  ( 0.7068366539029264928, -1.522610279710209680, 0.5630547890730004390 ) ) ;
#27347=CARTESIAN_POINT ( 'NONE',  ( 0.1880119672192303582, -0.5274192702082527440, 0.09355512109399032050 ) ) ;
#27349=EDGE_LOOP ( 'NONE', ( #25178, #11929, #25401, #17244 ) ) ;
#27351=CIRCLE ( 'NONE', #25384, 0.03749999999977551152 ) ;
#27352=CARTESIAN_POINT ( 'NONE',  ( 0.4162193950359272532, -1.008383645579083554, 0.7108382935901826905 ) ) ;
#27355=CARTESIAN_POINT ( 'NONE',  ( 0.4015936175283410514, -1.155705023113092533, 0.5182417262812423209 ) ) ;
#27358=CARTESIAN_POINT ( 'NONE',  ( 0.3072783065116599377, -1.250270042923148583, 0.6870471857482981504 ) ) ;
#27362=CARTESIAN_POINT ( 'NONE',  ( 0.3933867764525452726, -1.106167708152965723, 0.6141292311898844947 ) ) ;
#27365=CARTESIAN_POINT ( 'NONE',  ( 0.2197066928929958252, -0.9902086090378329208, 0.5562769007654783104 ) ) ;
#27368=CARTESIAN_POINT ( 'NONE',  ( 0.3924513946351673721, -1.141110873382124913, 0.4807468720547258823 ) ) ;
#27369=CARTESIAN_POINT ( 'NONE',  ( 0.002346242718065488699, -0.9632443647534850717, 0.3631189922238501344 ) ) ;
#27371=CARTESIAN_POINT ( 'NONE',  ( 0.4844264163852358696, -1.123939254815026878, 0.5158946235675032632 ) ) ;
#27372=CARTESIAN_POINT ( 'NONE',  ( 0.5566683473865443599, -1.184766897212384151, 0.6057417262809812186 ) ) ;
#27375=CARTESIAN_POINT ( 'NONE',  ( 0.01194366878076004966, -0.5146706732448569355, -0.04802372811395377861 ) ) ;
#27377=CARTESIAN_POINT ( 'NONE',  ( 0.0004843130070887482585, -0.4400213179164120803, 0.1732464827935638330 ) ) ;
#27388=ORIENTED_EDGE ( 'NONE', *, *, #36301, .F. ) ;
#27389=CARTESIAN_POINT ( 'NONE',  ( -0.001014514837871428703, -0.7910287684333593416, 0.01309347023044784945 ) ) ;
#27395=ORIENTED_EDGE ( 'NONE', *, *, #8667, .T. ) ;
#27396=CARTESIAN_POINT ( 'NONE',  ( 0.2694109831733587646, -1.541367803212651655, 0.8730078803289684775 ) ) ;
#27398=CARTESIAN_POINT ( 'NONE',  ( 0.2225804103835565539, -1.238343994408460214, 0.5682417262808779901 ) ) ;
#27401=CARTESIAN_POINT ( 'NONE',  ( 0.7053410326410682885, -1.513865973459305625, 0.5669051209305092653 ) ) ;
#27406=CARTESIAN_POINT ( 'NONE',  ( 0.3373193197188696923, -1.055824305789904161, 0.7619749169485852125 ) ) ;
#27407=CARTESIAN_POINT ( 'NONE',  ( 0.1855569663413472736, -0.8197182691652543651, 0.09662382917702272422 ) ) ;
#27411=CARTESIAN_POINT ( 'NONE',  ( 0.3935425020819560138, -1.717736786839809682, 0.4220810518247123388 ) ) ;
#27413=EDGE_CURVE ( 'NONE', #17214, #38375, #4754, .T. ) ;
#27415=CARTESIAN_POINT ( 'NONE',  ( 0.4904112910084876820, -1.188461936721588508, 0.4282417262808777547 ) ) ;
#27420=CARTESIAN_POINT ( 'NONE',  ( 0.2844183530474730937, -1.648412185216814541, 0.8663902821515296893 ) ) ;
#27421=CARTESIAN_POINT ( 'NONE',  ( 0.01946601547008546679, -0.9333846633216874578, 0.6017762147510251625 ) ) ;
#27423=CARTESIAN_POINT ( 'NONE',  ( 0.3136609249452982917, -0.7980415872784507592, 0.6920156437578004471 ) ) ;
#27424=DIRECTION ( 'NONE',  ( 0.4999551463232372317, -0.8660512985181135770, 0.000000000000000000 ) ) ;
#27426=CYLINDRICAL_SURFACE ( 'NONE', #33607, 0.1500000000000000500 ) ;
#27428=CARTESIAN_POINT ( 'NONE',  ( 0.6479348668002676837, -1.454958465852009830, 0.4182417262808776348 ) ) ;
#27429=CARTESIAN_POINT ( 'NONE',  ( 0.1712457320379880688, -1.308359377140657198, 0.9395131347236835850 ) ) ;
#27431=CARTESIAN_POINT ( 'NONE',  ( 0.5869881002782089130, -1.486012224770534740, 0.6423071506457943558 ) ) ;
#27435=CARTESIAN_POINT ( 'NONE',  ( 0.4936113061342744524, -1.107001320208115036, 0.7496827700887727097 ) ) ;
#27436=EDGE_LOOP ( 'NONE', ( #22895, #9679, #35598, #29436 ) ) ;
#27438=CARTESIAN_POINT ( 'NONE',  ( 0.2310704385326068921, -0.6810227473006470467, 0.4838669985239971161 ) ) ;
#27440=CARTESIAN_POINT ( 'NONE',  ( 0.3187641638634987618, -1.760284878867080183, 0.5597302103697527897 ) ) ;
#27443=CARTESIAN_POINT ( 'NONE',  ( 0.09148389223799407999, -0.7122299647079209928, 0.2589910736622687559 ) ) ;
#27445=CARTESIAN_POINT ( 'NONE',  ( 0.4980715694105531388, -1.542567323246221145, 0.5836530299116245990 ) ) ;
#27446=CARTESIAN_POINT ( 'NONE',  ( 0.3335735135025916787, -1.761544825112107526, 0.4744483505433231829 ) ) ;
#27447=CARTESIAN_POINT ( 'NONE',  ( -0.001314104238682122210, -0.8140392535364435744, 0.03481557541610642154 ) ) ;
#27448=CARTESIAN_POINT ( 'NONE',  ( 0.01358515540082348184, -1.035362938470157701, 0.5742360950302952682 ) ) ;
#27452=CARTESIAN_POINT ( 'NONE',  ( 0.3426364375912121507, -0.9538486569171759077, 0.8392164456209516565 ) ) ;
#27455=SHAPE_REPRESENTATION_RELATIONSHIP ( 'NONE' , 'NONE' ,  #25967, #39278 ) ;
#27457=CARTESIAN_POINT ( 'NONE',  ( 0.5755305386461456729, -1.223609111988087861, 0.6057417262809032810 ) ) ;
#27459=CARTESIAN_POINT ( 'NONE',  ( 0.3223562399630707787, -1.181388948535295969, 0.4642260976938263894 ) ) ;
#27460=CARTESIAN_POINT ( 'NONE',  ( 0.2003179398552689949, -0.7109237300142917659, 0.3290305662194804026 ) ) ;
#27461=B_SPLINE_SURFACE_WITH_KNOTS ( 'NONE', 3, 1, ( 
 ( #35350, #29174 ),
 ( #20134, #20329 ),
 ( #16843, #38221 ),
 ( #22621, #32451 ),
 ( #32060, #23014 ),
 ( #38427, #29574 ) ),
 .UNSPECIFIED., .F., .F., .F.,
 ( 4, 2, 4 ),
 ( 2, 2 ),
 ( 1.913048296048411236E-15, 0.5000000000000000000, 1.228824370872419358 ),
 ( 0.000000000000000000, 1.000000000000000000 ),
 .UNSPECIFIED. ) ;
#27465=CARTESIAN_POINT ( 'NONE',  ( 0.4434045676814238890, -1.200249727390046095, 0.6565421829911162188 ) ) ;
#27467=ORIENTED_EDGE ( 'NONE', *, *, #13749, .F. ) ;
#27468=CARTESIAN_POINT ( 'NONE',  ( 0.4625870132446883165, -1.136566534039517018, 0.4526360456727940296 ) ) ;
#27469=CARTESIAN_POINT ( 'NONE',  ( 0.08989780363036058153, -0.5646359461869331353, 0.1460065308160271857 ) ) ;
#27472=CARTESIAN_POINT ( 'NONE',  ( 0.02505718529252235621, -0.8981064542781922455, 0.5277094094783241207 ) ) ;
#27473=ORIENTED_EDGE ( 'NONE', *, *, #9314, .T. ) ;
#27477=CARTESIAN_POINT ( 'NONE',  ( 0.7370562124357561418, -1.515684240363464941, 0.4449423861150900716 ) ) ;
#27479=CARTESIAN_POINT ( 'NONE',  ( 0.4592765119208255808, -1.225248709697466909, 0.6570367264342110714 ) ) ;
#27482=DIRECTION ( 'NONE',  ( 0.4999551463232372317, -0.8660512985181134660, 0.000000000000000000 ) ) ;
#27483=ORIENTED_EDGE ( 'NONE', *, *, #34617, .T. ) ;
#27485=CARTESIAN_POINT ( 'NONE',  ( 0.07797173117127408071, -1.322015870089231493, 0.5685938977595220711 ) ) ;
#27489=CARTESIAN_POINT ( 'NONE',  ( 0.4418185801296429238, -1.573801657680888866, 0.5756389504404278989 ) ) ;
#27495=CARTESIAN_POINT ( 'NONE',  ( 0.2128900943681608926, -0.8312134757594041856, 0.6484179518193018410 ) ) ;
#27496=CARTESIAN_POINT ( 'NONE',  ( 0.4849335853385449147, -1.661118561410368732, 0.4921452663170099995 ) ) ;
#27497=DIRECTION ( 'NONE',  ( -0.5608954083811059643, 0.8278866715058241788, 0.000000000000000000 ) ) ;
#27499=CARTESIAN_POINT ( 'NONE',  ( 0.4420022301528205300, -1.686445855772613855, 0.4182417262808775793 ) ) ;
#27503=CARTESIAN_POINT ( 'NONE',  ( 0.1998706582382908103, -0.5568697517490295290, 0.3524876158099713441 ) ) ;
#27506=FACE_OUTER_BOUND ( 'NONE', #3170, .T. ) ;
#27510=CARTESIAN_POINT ( 'NONE',  ( 0.6574645389592653766, -1.565081392064861410, 0.6191400650029853514 ) ) ;
#27512=CARTESIAN_POINT ( 'NONE',  ( 0.6635030265783503634, -1.456878713983702056, 0.4329734231317256543 ) ) ;
#27515=EDGE_LOOP ( 'NONE', ( #18174, #28374, #7162, #24391, #32573, #9847 ) ) ;
#27516=CARTESIAN_POINT ( 'NONE',  ( 3.414809992080329023E-17, -0.4262518876079541830, 0.1639910581422319991 ) ) ;
#27517=CARTESIAN_POINT ( 'NONE',  ( 0.5325131901480560925, -1.521657566433719300, 0.5503197480263272157 ) ) ;
#27518=CARTESIAN_POINT ( 'NONE',  ( 0.1176733790823393522, -1.298938889880303371, 0.5182417262812425429 ) ) ;
#27522=ADVANCED_FACE ( 'NONE', ( #15956 ), #377, .T. ) ;
#27527=CARTESIAN_POINT ( 'NONE',  ( 0.4728208306174679354, -1.251385747785768610, 0.7149255309087257926 ) ) ;
#27530=CARTESIAN_POINT ( 'NONE',  ( 0.3960970180006803121, -1.016137033769514808, 0.6457357589753065508 ) ) ;
#27537=CARTESIAN_POINT ( 'NONE',  ( 0.03562661732870475717, -0.5340764826629550432, 0.1545348805129083680 ) ) ;
#27538=CARTESIAN_POINT ( 'NONE',  ( 0.3511079287476752686, -1.164805985122749687, 0.4335040596137051394 ) ) ;
#27539=CARTESIAN_POINT ( 'NONE',  ( 0.1858368116309794815, -0.7426394543890098010, -0.01208864215565694927 ) ) ;
#27542=ORIENTED_EDGE ( 'NONE', *, *, #27788, .T. ) ;
#27543=CARTESIAN_POINT ( 'NONE',  ( 0.3607641608100094488, -0.9525365098903693095, 0.6616485578905302312 ) ) ;
#27544=CARTESIAN_POINT ( 'NONE',  ( 0.4652240812381422952, -1.367871865765116990, 0.8203737607537802123 ) ) ;
#27545=ORIENTED_EDGE ( 'NONE', *, *, #13943, .T. ) ;
#27548=CARTESIAN_POINT ( 'NONE',  ( 0.1954707032480469397, -1.039694013094895508, 0.7297344613678689029 ) ) ;
#27551=CARTESIAN_POINT ( 'NONE',  ( 0.4368279861777732975, -1.677667223885756398, 0.4182417262808776903 ) ) ;
#27553=CARTESIAN_POINT ( 'NONE',  ( 0.6522089892707538805, -1.452491178199303956, 0.4224083929475448973 ) ) ;
#27558=EDGE_CURVE ( 'NONE', #34759, #17214, #30443, .T. ) ;
#27559=CARTESIAN_POINT ( 'NONE',  ( 0.4846870251237639371, -1.126101711201861644, 0.5058349955967992306 ) ) ;
#27560=EDGE_CURVE ( 'NONE', #26649, #24616, #33013, .T. ) ;
#27561=CARTESIAN_POINT ( 'NONE',  ( 0.3605448558321485697, -1.159604706203796631, 0.5182417262812284431 ) ) ;
#27563=CARTESIAN_POINT ( 'NONE',  ( 0.0001246750752516694331, -0.5758935607867365913, -0.07708628032613852599 ) ) ;
#27566=CARTESIAN_POINT ( 'NONE',  ( 0.7341807115343071954, -1.546815077829952978, 0.5182417262812423209 ) ) ;
#27567=EDGE_LOOP ( 'NONE', ( #34026, #6409, #25405 ) ) ;
#27571=ORIENTED_EDGE ( 'NONE', *, *, #22252, .F. ) ;
#27574=CARTESIAN_POINT ( 'NONE',  ( 0.002311469189254836219, -0.5280309338796042029, 0.1382921204161675355 ) ) ;
#27575=ORIENTED_EDGE ( 'NONE', *, *, #35525, .F. ) ;
#27577=DIRECTION ( 'NONE',  ( -0.8660512985181133550, -0.4999551463232372317, 0.000000000000000000 ) ) ;
#27579=CARTESIAN_POINT ( 'NONE',  ( 0.2656334329314738452, -1.675010518447552776, 0.5636784135978708532 ) ) ;
#27580=CARTESIAN_POINT ( 'NONE',  ( 0.3045945486428198734, -1.056159242937262821, 0.7373969915095198724 ) ) ;
#27581=CARTESIAN_POINT ( 'NONE',  ( 0.1765456504409605443, -1.243775442361034544, 0.6134035678024805094 ) ) ;
#27582=CARTESIAN_POINT ( 'NONE',  ( 0.3613652144640472352, -1.159105058189230597, 0.5085157022477851951 ) ) ;
#27588=CARTESIAN_POINT ( 'NONE',  ( 0.3793181961222715226, -1.724015678557569320, 0.4221277619539407500 ) ) ;
#27589=CARTESIAN_POINT ( 'NONE',  ( 0.6465835049539362389, -1.539613817736340318, 0.4182417262808776903 ) ) ;
#27590=CARTESIAN_POINT ( 'NONE',  ( 0.3759499381784230376, -1.134508656596316944, 0.8084154480762882899 ) ) ;
#27591=CARTESIAN_POINT ( 'NONE',  ( 0.01202655180096142383, -0.9511917420203161999, 0.2808540945044247228 ) ) ;
#27594=CARTESIAN_POINT ( 'NONE',  ( 0.3003069805930505543, -1.615165612650612426, 0.9446834537455470748 ) ) ;
#27600=CARTESIAN_POINT ( 'NONE',  ( -0.0004530311258370896157, -0.9366683044365211597, 0.1504526319320767802 ) ) ;
#27606=CARTESIAN_POINT ( 'NONE',  ( 0.003124719664520401140, -0.5686731593868927792, 0.1286173008190011902 ) ) ;
#27607=CARTESIAN_POINT ( 'NONE',  ( 0.06466273788562305891, -1.136606943108019463, 0.7597147705880777924 ) ) ;
#27609=CARTESIAN_POINT ( 'NONE',  ( 0.3805742881279173817, -0.9147748976205605231, 0.7744170315737640697 ) ) ;
#27616=CARTESIAN_POINT ( 'NONE',  ( 0.6451746001002063302, -1.456551915967818189, 0.4182417262808775238 ) ) ;
#27617=CARTESIAN_POINT ( 'NONE',  ( 0.2388294604317064973, -1.536022005946620528, 0.8953658808002388225 ) ) ;
#27619=CARTESIAN_POINT ( 'NONE',  ( 0.5887768677989536625, -1.490289241820755617, 0.6055812475267198236 ) ) ;
#27620=CARTESIAN_POINT ( 'NONE',  ( 0.3600571967235919879, -1.747985310352905719, 0.4400630855740547132 ) ) ;
#27621=ORIENTED_EDGE ( 'NONE', *, *, #15483, .T. ) ;
#27623=CARTESIAN_POINT ( 'NONE',  ( 0.3225930820597290305, -0.8396780885765841029, 0.6764912411861826458 ) ) ;
#27633=CARTESIAN_POINT ( 'NONE',  ( 0.09278646505816903756, -0.7145150594772067265, 0.2750910907217022361 ) ) ;
#27635=CARTESIAN_POINT ( 'NONE',  ( 0.4972415774783536802, -1.542437756487440303, 0.5698391771344212264 ) ) ;
#27636=CARTESIAN_POINT ( 'NONE',  ( 0.3226000049158921912, -1.763919894439656133, 0.5248175239680957782 ) ) ;
#27637=CARTESIAN_POINT ( 'NONE',  ( -0.0001015365960684644825, -0.6986948758057686115, -0.02208683258971757754 ) ) ;
#27638=CARTESIAN_POINT ( 'NONE',  ( 7.048302186126095272E-05, -0.9486411243827373996, 0.1970497354082177133 ) ) ;
#27643=CARTESIAN_POINT ( 'NONE',  ( 0.6033864073621231228, -1.403448924263456021, 0.8611617019206015966 ) ) ;
#27648=CARTESIAN_POINT ( 'NONE',  ( 0.2614959211572117637, -1.678097089283488330, 0.5385591481521548873 ) ) ;
#27649=EDGE_CURVE ( 'NONE', #8445, #11170, #36450, .T. ) ;
#27651=CARTESIAN_POINT ( 'NONE',  ( 0.5530797604979859061, -1.185210387710321944, 0.6074893116751658440 ) ) ;
#27656=CARTESIAN_POINT ( 'NONE',  ( 0.4905717239428445953, -1.546361816834758152, 0.5738993346725939082 ) ) ;
#27661=TOROIDAL_SURFACE ( 'NONE', #9919, 0.08249999999977548903, 0.01000000000000000021 ) ;
#27666=CARTESIAN_POINT ( 'NONE',  ( 0.04094777560533426064, -0.9548371111386207977, 0.6396399729219502950 ) ) ;
#27667=ORIENTED_EDGE ( 'NONE', *, *, #8785, .T. ) ;
#27669=CARTESIAN_POINT ( 'NONE',  ( 0.3083966533127217580, -1.760901789209341262, 0.5682271305178940857 ) ) ;
#27678=CARTESIAN_POINT ( 'NONE',  ( 0.3824648761862433632, -1.161281635269272305, 0.4182417262808778013 ) ) ;
#27681=CARTESIAN_POINT ( 'NONE',  ( 0.3805693354401638029, -1.436365483031340595, 0.8498359687909504689 ) ) ;
#27684=CARTESIAN_POINT ( 'NONE',  ( 0.3047936848243344432, -1.756875962071034580, 0.5682417262361116883 ) ) ;
#27686=B_SPLINE_CURVE_WITH_KNOTS ( 'NONE', 3,
 ( #4521, #17086, #33126, #29634, #27169, #17500 ),
 .UNSPECIFIED., .F., .F.,
 ( 4, 2, 4 ),
 ( 0.000000000000000000, 0.0005458736207840705207, 0.001091747241568141041 ),
 .UNSPECIFIED. ) ;
#27687=ORIENTED_EDGE ( 'NONE', *, *, #38043, .T. ) ;
#27691=CIRCLE ( 'NONE', #3356, 0.03749999999977551152 ) ;
#27692=CARTESIAN_POINT ( 'NONE',  ( 0.1232466757695174497, -0.5723387072628065564, 0.2472162040730083721 ) ) ;
#27693=CARTESIAN_POINT ( 'NONE',  ( 0.4839100550601997952, -1.674307978549753440, 0.5301044316523388922 ) ) ;
#27701=CARTESIAN_POINT ( 'NONE',  ( 0.2347838743403539985, -1.231490626770528563, 0.5148488905547541350 ) ) ;
#27702=CARTESIAN_POINT ( 'NONE',  ( 0.6789872039812443472, -1.407470790535994221, 0.5375528621076278712 ) ) ;
#27704=CARTESIAN_POINT ( 'NONE',  ( 0.01018801482832277540, -1.013890353644918862, 0.5362285315871677671 ) ) ;
#27708=CARTESIAN_POINT ( 'NONE',  ( 0.3925833169928708566, -1.148390097986053293, 0.4243636716995100588 ) ) ;
#27710=VERTEX_POINT ( 'NONE', #33355 ) ;
#27715=ORIENTED_EDGE ( 'NONE', *, *, #4254, .F. ) ;
#27719=CARTESIAN_POINT ( 'NONE',  ( 0.3816469784432204304, -1.141973345686314811, 0.6053139149380659667 ) ) ;
#27723=CARTESIAN_POINT ( 'NONE',  ( 0.5337345016547716536, -1.351630938401003235, 0.5946468524951272761 ) ) ;
#27726=CARTESIAN_POINT ( 'NONE',  ( 0.3630793090018165636, -0.9924503543686107321, 0.6290125294248597454 ) ) ;
#27730=VERTEX_POINT ( 'NONE', #36235 ) ;
#27731=CARTESIAN_POINT ( 'NONE',  ( 0.009367919695839343336, -0.5831258035308336529, 0.02670069209610665198 ) ) ;
#27732=CARTESIAN_POINT ( 'NONE',  ( 0.03562661732870521514, -0.5340764826629550432, 0.1457185332388687693 ) ) ;
#27734=CARTESIAN_POINT ( 'NONE',  ( 0.1762014475043635342, -0.5919070258151631903, -0.06363282137695237817 ) ) ;
#27736=VERTEX_POINT ( 'NONE', #39734 ) ;
#27738=CARTESIAN_POINT ( 'NONE',  ( 0.3375401459729027720, -0.9900294755946262848, 0.5931500777746694375 ) ) ;
#27740=CARTESIAN_POINT ( 'NONE',  ( 0.5154828406948165354, -1.449888099294595500, 0.7698194787142327300 ) ) ;
#27745=VECTOR ( 'NONE', #40638, 39.37007874015748143 ) ;
#27749=CARTESIAN_POINT ( 'NONE',  ( 0.07556315841227354002, -1.331191507351498160, 0.4849083929475443422 ) ) ;
#27751=AXIS2_PLACEMENT_3D ( 'NONE', #3729, #13169, #18540 ) ;
#27752=CARTESIAN_POINT ( 'NONE',  ( 0.08546473275284281745, -1.263146999130163373, 0.5182417262812423209 ) ) ;
#27755=CARTESIAN_POINT ( 'NONE',  ( 0.08097120591835743619, -1.368856899881548683, 0.5761801428003342496 ) ) ;
#27759=CARTESIAN_POINT ( 'NONE',  ( 0.4532329859814145934, -1.135673831482812979, 0.4497956394000192093 ) ) ;
#27760=CARTESIAN_POINT ( 'NONE',  ( 0.5535089670275162854, -1.186427276555303001, 0.6057417262809813296 ) ) ;
#27762=CARTESIAN_POINT ( 'NONE',  ( -0.002083146443013336215, -0.8967360763018585867, 0.1624439089914547774 ) ) ;
#27766=ORIENTED_EDGE ( 'NONE', *, *, #22252, .T. ) ;
#27782=CARTESIAN_POINT ( 'NONE',  ( 0.003557204563558416955, -0.5929878893131403927, 0.3587067422883609691 ) ) ;
#27784=CARTESIAN_POINT ( 'NONE',  ( 0.08667892099931116812, -1.311828707399254279, 0.5891665326009013492 ) ) ;
#27785=DIRECTION ( 'NONE',  ( 0.8660512985181133550, 0.4999551463232372317, 0.000000000000000000 ) ) ;
#27788=EDGE_CURVE ( 'NONE', #24651, #37794, #19228, .T. ) ;
#27792=EDGE_CURVE ( 'NONE', #2643, #4246, #25132, .T. ) ;
#27793=CARTESIAN_POINT ( 'NONE',  ( 0.01128677947712186484, -0.9461986806730106059, 0.1457185332388702959 ) ) ;
#27796=CARTESIAN_POINT ( 'NONE',  ( 0.4923102438893445232, -1.287854413602990133, 0.8084835653369039088 ) ) ;
#27800=CARTESIAN_POINT ( 'NONE',  ( 0.3241018648587293272, -1.757744033614132118, 0.6567149589598120230 ) ) ;
#27801=FACE_OUTER_BOUND ( 'NONE', #7058, .T. ) ;
#27802=CARTESIAN_POINT ( 'NONE',  ( 0.4144363316557380661, -1.243523414473156397, 0.5370935844994736419 ) ) ;
#27803=CARTESIAN_POINT ( 'NONE',  ( 0.5694934407712974878, -1.613350223101006620, 0.4177417262808785781 ) ) ;
#27810=CARTESIAN_POINT ( 'NONE',  ( 0.002089204316143729572, -0.4812299151504488837, 0.2002484561318531031 ) ) ;
#27811=CARTESIAN_POINT ( 'NONE',  ( 0.03947150132052767296, -1.011495197293007076, 0.7004091584170603069 ) ) ;
#27814=CARTESIAN_POINT ( 'NONE',  ( 0.7227036224969136669, -1.477504586156484612, 0.6121051687398550989 ) ) ;
#27816=CARTESIAN_POINT ( 'NONE',  ( 0.6776375915179856380, -1.553024467591962665, 0.6114064090131621221 ) ) ;
#27819=AXIS2_PLACEMENT_3D ( 'NONE', #8920, #2961, #8315 ) ;
#27823=CARTESIAN_POINT ( 'NONE',  ( 0.2529494766129096739, -1.556025590441917128, 0.8771849030697340677 ) ) ;
#27824=CARTESIAN_POINT ( 'NONE',  ( 0.1283662278338046081, -0.5536758349069195173, 0.1788647258318563915 ) ) ;
#27827=CARTESIAN_POINT ( 'NONE',  ( 0.4660228360541302517, -1.069033551699853479, 0.7465831672886248382 ) ) ;
#27829=ORIENTED_EDGE ( 'NONE', *, *, #30152, .F. ) ;
#27830=CARTESIAN_POINT ( 'NONE',  ( 0.4100237506442933610, -0.9802720315809884122, 0.7587508493699357537 ) ) ;
#27839=CARTESIAN_POINT ( 'NONE',  ( 0.08779053797915296886, -0.7269445601652628763, 0.2094401179698018867 ) ) ;
#27841=CARTESIAN_POINT ( 'NONE',  ( 0.3106403372944860908, -1.755530900668034189, 0.6572509151387877502 ) ) ;
#27843=CARTESIAN_POINT ( 'NONE',  ( 0.1312703668873084484, -0.6769293281215125191, 0.4711565125189325354 ) ) ;
#27844=CARTESIAN_POINT ( 'NONE',  ( 0.3290154599841292327, -1.759929421022380369, 0.4808583447391158727 ) ) ;
#27847=ORIENTED_EDGE ( 'NONE', *, *, #2997, .T. ) ;
#27848=CARTESIAN_POINT ( 'NONE',  ( 0.4266995953040617628, -1.696353446692786981, 0.4244815370374785402 ) ) ;
#27849=CARTESIAN_POINT ( 'NONE',  ( 0.3413008603379567019, -0.8270678360722266698, 0.7412715964732541352 ) ) ;
#27856=CARTESIAN_POINT ( 'NONE',  ( 0.4012095065101706770, -1.155916531200418484, 0.4182417262808778013 ) ) ;
#27860=CARTESIAN_POINT ( 'NONE',  ( 0.5031347454681565079, -1.114267567382387414, 0.6816460158534795033 ) ) ;
#27873=CARTESIAN_POINT ( 'NONE',  ( 0.08984346464585953040, -0.5645865489369916723, 0.1381676437203310515 ) ) ;
#27874=ORIENTED_EDGE ( 'NONE', *, *, #382, .T. ) ;
#27877=CARTESIAN_POINT ( 'NONE',  ( 0.1685152595565323486, -1.372181050131067614, 0.6250859892303964882 ) ) ;
#27882=CARTESIAN_POINT ( 'NONE',  ( 0.7437969124434082868, -1.515212563166708604, 0.5942788597236812187 ) ) ;
#27890=EDGE_CURVE ( 'NONE', #24566, #30626, #30878, .T. ) ;
#27891=CARTESIAN_POINT ( 'NONE',  ( 0.1321480585992808876, -0.6771580847970606332, 0.5036894915659911875 ) ) ;
#27893=CARTESIAN_POINT ( 'NONE',  ( 0.7043549991621405049, -1.517507936983845562, 0.5724489891249867624 ) ) ;
#27894=CARTESIAN_POINT ( 'NONE',  ( 0.08644374222443337863, -0.6311465605765145259, 0.4038393922213947551 ) ) ;
#27896=CARTESIAN_POINT ( 'NONE',  ( 0.5743547643448889684, -1.610790646010106686, 0.4680204833954097476 ) ) ;
#27903=CARTESIAN_POINT ( 'NONE',  ( 0.1289834210817078219, -0.6043023202742757727, 0.3280125156933150210 ) ) ;
#27904=CARTESIAN_POINT ( 'NONE',  ( 0.4773291537012285812, -1.665277132842807539, 0.4700098364638956583 ) ) ;
#27909=CARTESIAN_POINT ( 'NONE',  ( 0.5909188805876135486, -1.601585752074797142, 0.4182417262808776348 ) ) ;
#27911=CARTESIAN_POINT ( 'NONE',  ( 0.1840556061914042918, -0.8547754003400971357, 0.1463983740523600863 ) ) ;
#27913=CARTESIAN_POINT ( 'NONE',  ( 0.2575330336140166931, -0.6922558787343077169, 0.5832620184353838333 ) ) ;
#27918=CARTESIAN_POINT ( 'NONE',  ( 0.08736999187406781220, -0.8328363605256602353, 0.2358003664843119906 ) ) ;
#27926=CARTESIAN_POINT ( 'NONE',  ( 0.6498387395261642219, -1.464631408770378895, 0.4182417262808778013 ) ) ;
#27927=CARTESIAN_POINT ( 'NONE',  ( 0.3912779971226761355, -1.730232005297420717, 0.6096916113967504325 ) ) ;
#27928=AXIS2_PLACEMENT_3D ( 'NONE', #18821, #34027, #24373 ) ;
#27929=ORIENTED_EDGE ( 'NONE', *, *, #15292, .T. ) ;
#27931=CARTESIAN_POINT ( 'NONE',  ( 0.4265404446467185307, -1.123912635142109817, 0.5182417262812248904 ) ) ;
#27935=CARTESIAN_POINT ( 'NONE',  ( 0.3927094301483936567, -1.138811079655472902, 0.7324022214491040517 ) ) ;
#27937=ORIENTED_EDGE ( 'NONE', *, *, #35065, .F. ) ;
#27938=CARTESIAN_POINT ( 'NONE',  ( 0.2554252512568409572, -0.9178124959013912454, 0.5002157811656953168 ) ) ;
#27943=CARTESIAN_POINT ( 'NONE',  ( 0.1047008573566304973, -1.402533878584439453, 0.6140111174542888239 ) ) ;
#27946=CARTESIAN_POINT ( 'NONE',  ( 0.3775997949916232166, -1.569494078844261731, 0.7643415720515360778 ) ) ;
#27948=CARTESIAN_POINT ( 'NONE',  ( 0.1135149208409055033, -0.6240967447601386553, -0.08736365982372026884 ) ) ;
#27951=VERTEX_POINT ( 'NONE', #18336 ) ;
#27952=CARTESIAN_POINT ( 'NONE',  ( 0.4610375578740096847, -1.058108534101625198, 0.6327206492055766907 ) ) ;
#27953=CARTESIAN_POINT ( 'NONE',  ( 0.5534818102155456554, -1.511209893663564952, 0.5824172004013893345 ) ) ;
#27964=CARTESIAN_POINT ( 'NONE',  ( 0.4263817149093077630, -1.123637674285695276, 0.5237040708327734828 ) ) ;
#27965=CARTESIAN_POINT ( 'NONE',  ( 0.07801557919154505916, -1.344960384177054546, 0.6336995499099050688 ) ) ;
#27968=CARTESIAN_POINT ( 'NONE',  ( 0.2225775331702970761, -0.9343733720331020010, 0.4090965549137709489 ) ) ;
#27969=CARTESIAN_POINT ( 'NONE',  ( 0.4676908246382645018, -1.116468242743651418, 0.5700470834645430251 ) ) ;
#27970=CARTESIAN_POINT ( 'NONE',  ( 0.4567988949776999319, -1.218949203222925659, 0.6057417262810179670 ) ) ;
#27973=CARTESIAN_POINT ( 'NONE',  ( 0.0006292437964357017102, -0.9180166443092167006, 0.3683461522897012452 ) ) ;
#27983=CARTESIAN_POINT ( 'NONE',  ( 0.5185199569154549382, -1.918301849770578604, 0.5182417262812423209 ) ) ;
#27989=FACE_OUTER_BOUND ( 'NONE', #24936, .T. ) ;
#27991=CARTESIAN_POINT ( 'NONE',  ( -0.001323340259884761604, -0.5441669509461014576, 0.2330429837679495741 ) ) ;
#27993=CARTESIAN_POINT ( 'NONE',  ( 0.09320273485841774896, -1.292715317639649308, 0.5862264040831728362 ) ) ;
#28000=LINE ( 'NONE', #12552, #3392 ) ;
#28005=CARTESIAN_POINT ( 'NONE',  ( 0.4107868727942790010, -1.187545294887579095, 0.8166605323444690034 ) ) ;
#28006=( BOUNDED_SURFACE ( )  B_SPLINE_SURFACE ( 3, 2, ( 
 ( #10526, #16116, #6607 ),
 ( #25776, #25989, #38295 ),
 ( #28655, #29044, #9914 ),
 ( #38513, #13019, #19406 ),
 ( #38096, #3330, #10126 ),
 ( #912, #22702, #25568 ),
 ( #16313, #22486, #35233 ),
 ( #35011, #4142, #6823 ),
 ( #31940, #7034, #10343 ),
 ( #19603, #22905, #32325 ),
 ( #16711, #36029, #14621 ),
 ( #17108, #13808, #26377 ),
 ( #38907, #16914, #11559 ),
 ( #26792, #26975, #20404 ),
 ( #39724, #7647, #4742 ),
 ( #23698, #4542, #20211 ),
 ( #10735, #24122, #36439 ),
 ( #32736, #36644, #32535 ),
 ( #20002, #39509, #4353 ),
 ( #23514, #1501, #20615 ),
 ( #1900, #23910, #36225 ),
 ( #14413, #14015, #7833 ),
 ( #29869, #11341, #17313 ),
 ( #29459, #39128, #1303 ),
 ( #39319, #1708, #27190 ),
 ( #23309, #8253, #29656 ),
 ( #35834, #26589, #10952 ),
 ( #32936, #14227, #11139 ),
 ( #8040, #33150, #20825 ),
 ( #4957, #17522, #30072 ),
 ( #33345, #5155, #17706 ),
 ( #30252, #2082, #12362 ),
 ( #33970, #25112, #2302 ),
 ( #40540, #8643, #40330 ),
 ( #17908, #8449, #5774 ),
 ( #15650, #39932, #2500 ),
 ( #33752, #2902, #21016 ),
 ( #28199, #63, #12555 ),
 ( #30473, #11748, #24306 ),
 ( #14843, #37042, #24918 ),
 ( #18328, #33534, #27406 ),
 ( #34155, #5344, #8864 ),
 ( #27590, #36830, #37445 ),
 ( #28005, #15042, #21217 ),
 ( #18128, #18525, #15237 ),
 ( #5566, #24511, #30874 ),
 ( #21443, #30683, #9256 ),
 ( #2692, #27796, #9070 ),
 ( #21834, #12161, #24724 ),
 ( #37253, #21633, #34362 ),
 ( #5966, #40117, #11947 ),
 ( #31081, #15453, #6176 ),
 ( #18745, #31297, #3107 ),
 ( #25329, #22444, #31486 ),
 ( #37654, #31897, #9685 ),
 ( #28998, #3717, #25530 ),
 ( #25723, #22250, #38254 ),
 ( #32279, #29211, #16457 ),
 ( #6571, #483, #19149 ),
 ( #12979, #1073, #22052 ),
 ( #19360, #32093, #31686 ),
 ( #37869, #16269, #9871 ),
 ( #28808, #34764, #9470 ),
 ( #38470, #16663, #13371 ),
 ( #862, #10084, #34972 ),
 ( #3293, #670, #22657 ) ),
 .UNSPECIFIED., .F., .F., .T. ) 
 B_SPLINE_SURFACE_WITH_KNOTS ( ( 4, 2, 2, 2, 2, 2, 2, 2, 2, 2, 2, 2, 2, 2, 2, 2, 2, 2, 2, 2, 2, 2, 2, 2, 2, 2, 2, 2, 2, 2, 2, 2, 4 ),
 ( 3, 3 ),
 ( 0.003862184171445387244, 0.004005911543370605475, 0.004077775229333214374, 0.004113707072314519257, 0.004149638915295824140, 0.004437093659146261471, 0.005012003146847136131, 0.006161822122248884585, 0.006736731609949758379, 0.007311641097650633039, 0.008461460073052382361, 0.01306073597465937618, 0.01421055495006112376, 0.01536037392546287308, 0.01651019290086462241, 0.01766001187626637173, 0.01995964982706986690, 0.02225928777787336554, 0.02340910675327511486, 0.02455892572867686419, 0.02685856367948035936, 0.02915820163028385453, 0.03145783958108735318, 0.03260765855648910250, 0.03375747753189084488, 0.03490729650729259420, 0.03605711548269434352, 0.03663202497039522165, 0.03720693445809609284, 0.03778184394579696403, 0.03835675343349784217, 0.03950657240889959149, 0.04065639138430134081 ),
 ( 0.000000000000000000, 1.000000000000000000 ),
 .UNSPECIFIED. ) 
 GEOMETRIC_REPRESENTATION_ITEM ( )  RATIONAL_B_SPLINE_SURFACE ( (
 ( 1.000000000000000000, 0.7659831817177167324, 1.000000000000000000),
 ( 1.000000000000000000, 0.7659831817177167324, 1.000000000000000000),
 ( 1.000000000000000000, 0.7659831817177171764, 1.000000000000000000),
 ( 1.000000000000000000, 0.7659831817177171764, 1.000000000000000000),
 ( 1.000000000000000000, 0.7659831817177167324, 1.000000000000000000),
 ( 1.000000000000000000, 0.7659831817177167324, 1.000000000000000000),
 ( 1.000000000000000000, 0.7659823156457327142, 1.000000000000000000),
 ( 1.000000000000000000, 0.7659781499614458644, 1.000000000000000000),
 ( 1.000000000000000000, 0.7659750002451379824, 1.000000000000000000),
 ( 1.000000000000000000, 0.7659380538139435313, 1.000000000000000000),
 ( 1.000000000000000000, 0.7658458401200891608, 1.000000000000000000),
 ( 1.000000000000000000, 0.7655236400952580844, 1.000000000000000000),
 ( 1.000000000000000000, 0.7652407285018256733, 1.000000000000000000),
 ( 1.000000000000000000, 0.7644032511843058542, 1.000000000000000000),
 ( 1.000000000000000000, 0.7639223851950867061, 1.000000000000000000),
 ( 1.000000000000000000, 0.7630220264715582568, 1.000000000000000000),
 ( 1.000000000000000000, 0.7627024615980096955, 1.000000000000000000),
 ( 1.000000000000000000, 0.7620247162771555116, 1.000000000000000000),
 ( 1.000000000000000000, 0.7616570060786606033, 1.000000000000000000),
 ( 1.000000000000000000, 0.7604379540530756820, 1.000000000000000000),
 ( 1.000000000000000000, 0.7595531301201857710, 1.000000000000000000),
 ( 1.000000000000000000, 0.7545224428441196229, 1.000000000000000000),
 ( 1.000000000000000000, 0.7493009569406670067, 1.000000000000000000),
 ( 1.000000000000000000, 0.7423160112036807368, 1.000000000000000000),
 ( 1.000000000000000000, 0.7409110957858757729, 1.000000000000000000),
 ( 1.000000000000000000, 0.7381237456055174118, 1.000000000000000000),
 ( 1.000000000000000000, 0.7367470398672157916, 1.000000000000000000),
 ( 1.000000000000000000, 0.7341806964246635481, 1.000000000000000000),
 ( 1.000000000000000000, 0.7329567133465884066, 1.000000000000000000),
 ( 1.000000000000000000, 0.7308089355666729237, 1.000000000000000000),
 ( 1.000000000000000000, 0.7298844137523633480, 1.000000000000000000),
 ( 1.000000000000000000, 0.7279463615642568497, 1.000000000000000000),
 ( 1.000000000000000000, 0.7277005349271021828, 1.000000000000000000),
 ( 1.000000000000000000, 0.7325814144033533371, 1.000000000000000000),
 ( 1.000000000000000000, 0.7379337678855741878, 1.000000000000000000),
 ( 1.000000000000000000, 0.7540011851016407141, 1.000000000000000000),
 ( 1.000000000000000000, 0.7607161262302054583, 1.000000000000000000),
 ( 1.000000000000000000, 0.7755360273599477550, 1.000000000000000000),
 ( 1.000000000000000000, 0.7835406870239474131, 1.000000000000000000),
 ( 1.000000000000000000, 0.8061417792357221668, 1.000000000000000000),
 ( 1.000000000000000000, 0.8187798214764351323, 1.000000000000000000),
 ( 1.000000000000000000, 0.8359312486381417218, 1.000000000000000000),
 ( 1.000000000000000000, 0.8408816577689636196, 1.000000000000000000),
 ( 1.000000000000000000, 0.8450128811913334426, 1.000000000000000000),
 ( 1.000000000000000000, 0.8442046636671193260, 1.000000000000000000),
 ( 1.000000000000000000, 0.8395230928915869972, 1.000000000000000000),
 ( 1.000000000000000000, 0.8373721201386176149, 1.000000000000000000),
 ( 1.000000000000000000, 0.8317843866040760537, 1.000000000000000000),
 ( 1.000000000000000000, 0.8283573055353494752, 1.000000000000000000),
 ( 1.000000000000000000, 0.8200239860571119088, 1.000000000000000000),
 ( 1.000000000000000000, 0.8150997353630367037, 1.000000000000000000),
 ( 1.000000000000000000, 0.8031390929375081811, 1.000000000000000000),
 ( 1.000000000000000000, 0.7961772277509610030, 1.000000000000000000),
 ( 1.000000000000000000, 0.7836509786413579093, 1.000000000000000000),
 ( 1.000000000000000000, 0.7791219561609438182, 1.000000000000000000),
 ( 1.000000000000000000, 0.7693659621982237296, 1.000000000000000000),
 ( 1.000000000000000000, 0.7641340825345092069, 1.000000000000000000),
 ( 1.000000000000000000, 0.7536989215030908129, 1.000000000000000000),
 ( 1.000000000000000000, 0.7484621702622018535, 1.000000000000000000),
 ( 1.000000000000000000, 0.7385966617950382451, 1.000000000000000000),
 ( 1.000000000000000000, 0.7339569418095627240, 1.000000000000000000),
 ( 1.000000000000000000, 0.7219887718280880717, 1.000000000000000000),
 ( 1.000000000000000000, 0.7165447210591409100, 1.000000000000000000),
 ( 1.000000000000000000, 0.7095247715316972403, 1.000000000000000000),
 ( 1.000000000000000000, 0.7079216154009045914, 1.000000000000000000),
 ( 1.000000000000000000, 0.7071730258920838619, 1.000000000000000000) ) ) 
 REPRESENTATION_ITEM ( '' )  SURFACE ( )  );
#28007=CARTESIAN_POINT ( 'NONE',  ( 0.1633339118204678586, -0.8580491329167432291, 0.4791465288558531821 ) ) ;
#28009=CARTESIAN_POINT ( 'NONE',  ( 0.1032247015330990531, -0.8975257853914290207, 0.8793098326616880511 ) ) ;
#28011=CARTESIAN_POINT ( 'NONE',  ( 0.7472019744968698696, -1.513150647243692637, 0.5707417262808793801 ) ) ;
#28012=EDGE_CURVE ( 'NONE', #33041, #40153, #8790, .T. ) ;
#28019=CARTESIAN_POINT ( 'NONE',  ( 0.002083146443013504916, -0.4777046557262296100, 0.1457185332388684640 ) ) ;
#28020=CARTESIAN_POINT ( 'NONE',  ( 0.09334160340306593695, -1.332730469180070765, 0.7045675880059063534 ) ) ;
#28023=CARTESIAN_POINT ( 'NONE',  ( 0.4627885704097156050, -1.051432690887019072, 0.8329284434066291931 ) ) ;
#28025=EDGE_CURVE ( 'NONE', #38731, #27338, #28900, .T. ) ;
#28036=CARTESIAN_POINT ( 'NONE',  ( 0.1995336070936418182, -1.402089414342744700, 0.9384260727155151471 ) ) ;
#28037=CARTESIAN_POINT ( 'NONE',  ( 0.5877737341208254529, -1.491194589871079001, 0.5703655673359632194 ) ) ;
#28040=CARTESIAN_POINT ( 'NONE',  ( 0.4795791402848185725, -1.087578995800233095, 0.7487995513514865698 ) ) ;
#28043=CARTESIAN_POINT ( 'NONE',  ( 0.6988918244707941207, -1.438898845315309094, 0.5752146833678662974 ) ) ;
#28052=CARTESIAN_POINT ( 'NONE',  ( 0.1357061440364132343, -0.8234802076881400090, 0.4864660559418247376 ) ) ;
#28054=CARTESIAN_POINT ( 'NONE',  ( 0.4899971463290487828, -1.463357359739534846, 0.7777802213075096782 ) ) ;
#28055=CARTESIAN_POINT ( 'NONE',  ( 0.3320566521985225950, -1.758475802836519941, 0.4740614269747379095 ) ) ;
#28056=CARTESIAN_POINT ( 'NONE',  ( 0.0007905216470313744179, -0.6035600366138994533, 4.286223126101739974E-05 ) ) ;
#28060=CARTESIAN_POINT ( 'NONE',  ( 0.4175465041423866430, -1.703516643873120184, 0.6086626662040888203 ) ) ;
#28061=CARTESIAN_POINT ( 'NONE',  ( 0.6811486575909255770, -1.402667997544871037, 0.7201154234290257916 ) ) ;
#28065=CARTESIAN_POINT ( 'NONE',  ( 0.4000062018654670370, -1.149314450333016380, 0.4182417262808721947 ) ) ;
#28067=CARTESIAN_POINT ( 'NONE',  ( 0.3466030059118228035, -1.167433418478718510, 0.4480105783002163444 ) ) ;
#28068=CARTESIAN_POINT ( 'NONE',  ( 0.4384178598954188155, -1.040563892421024983, 0.6900182345289431751 ) ) ;
#28072=EDGE_CURVE ( 'NONE', #35465, #4497, #13235, .T. ) ;
#28074=CARTESIAN_POINT ( 'NONE',  ( 0.4901745208690559408, -1.545214605713521205, 0.5488368183266709721 ) ) ;
#28078=CARTESIAN_POINT ( 'NONE',  ( 0.4676597105902504659, -1.237282431096226043, 0.6057417262810000924 ) ) ;
#28084=CARTESIAN_POINT ( 'NONE',  ( 0.08250975870084176211, -1.108734649457161270, 0.7537977879433896966 ) ) ;
#28087=CARTESIAN_POINT ( 'NONE',  ( 0.3135347772105874231, -1.762222029724279881, 0.5682242226546108110 ) ) ;
#28089=EDGE_CURVE ( 'NONE', #26082, #38131, #37628, .T. ) ;
#28093=CARTESIAN_POINT ( 'NONE',  ( 0.5073704149278759346, -1.163922025721008557, 0.5182417262812423209 ) ) ;
#28096=CARTESIAN_POINT ( 'NONE',  ( 0.1174566253694137585, -0.6744780707208714032, 0.4348850488351332921 ) ) ;
#28099=CARTESIAN_POINT ( 'NONE',  ( 0.4717667268771776334, -1.556274250605339082, 0.6275438343556190013 ) ) ;
#28100=CARTESIAN_POINT ( 'NONE',  ( 0.6699292074404794572, -1.569526485364059143, 0.6071573546319902759 ) ) ;
#28101=CARTESIAN_POINT ( 'NONE',  ( 0.5730681724893124107, -1.614269927704049978, 0.5633518820464606947 ) ) ;
#28106=CARTESIAN_POINT ( 'NONE',  ( 0.1252372108451314248, -0.5576925373213490467, 0.1984031368276146234 ) ) ;
#28107=CARTESIAN_POINT ( 'NONE',  ( 0.4503334983497291888, -1.681198024010658543, 0.4342754154380044640 ) ) ;
#28110=CARTESIAN_POINT ( 'NONE',  ( 0.6672263256168233791, -1.559577713309469038, 0.6159734170043378310 ) ) ;
#28113=CARTESIAN_POINT ( 'NONE',  ( 0.1896879205916190136, -0.5058468364965200692, 0.1731371019803292222 ) ) ;
#28115=CARTESIAN_POINT ( 'NONE',  ( 0.01511362640256554493, -1.029621820521785525, 0.5875183992405329514 ) ) ;
#28121=B_SPLINE_CURVE_WITH_KNOTS ( 'NONE', 3,
 ( #9583, #19049, #31584, #32950, #34674, #16726, #32747, #1314, #13629, #4753, #22160, #25438, #9779, #7844, #6481, #6681, #23325, #3403, #22350, #29272, #19256, #31798, #28295, #26194, #4159, #38918, #35636, #15959, #165, #1124, #38718, #20018, #28504, #380, #20416, #10750, #23525, #12655, #29669, #10540, #23111, #32547, #4367, #12880, #16926, #29470, #10965, #14029, #13821, #26391, #35846, #7658, #20226, #4552 ),
 .UNSPECIFIED., .F., .F.,
 ( 4, 2, 2, 2, 2, 2, 2, 2, 2, 2, 2, 2, 2, 2, 2, 2, 2, 2, 2, 2, 2, 2, 2, 2, 2, 2, 4 ),
 ( -5.999999999642378183E-08, 0.0001480793356628742755, 0.0002962186713257449421, 0.0005924973426514890942, 0.001185054685302977615, 0.002370169370605954440, 0.003555284055908931699, 0.004740398741211909392, 0.009480857482423813223, 0.01185108685302976687, 0.01303620153833274717, 0.01422131622363572399, 0.01896177496484765038, 0.02133200433545361097, 0.02370223370605956809, 0.02607246307666552174, 0.02844269244727147886, 0.02962780713257446782, 0.03081292181787745679, 0.03199803650318044229, 0.03318315118848343126, 0.03436826587378641329, 0.03496082321643790430, 0.03555338055908939532, 0.03614593790174088633, 0.03673849524439237735, 0.03792360992969536632 ),
 .UNSPECIFIED. ) ;
#28126=CARTESIAN_POINT ( 'NONE',  ( 0.4813244371982610681, -1.269896034304244248, 0.7940112196239507147 ) ) ;
#28129=CARTESIAN_POINT ( 'NONE',  ( 0.4195420834447322611, -1.713617687370894593, 0.6096044365181384483 ) ) ;
#28130=ORIENTED_EDGE ( 'NONE', *, *, #9139, .T. ) ;
#28132=CARTESIAN_POINT ( 'NONE',  ( 0.2952349374191504672, -1.312115508766679817, 0.5179655188836596036 ) ) ;
#28133=CARTESIAN_POINT ( 'NONE',  ( 0.07779920321647403048, -1.322114474344633583, 0.5682417262808776570 ) ) ;
#28134=EDGE_CURVE ( 'NONE', #25255, #3822, #12730, .T. ) ;
#28136=CARTESIAN_POINT ( 'NONE',  ( 0.5003935287345969707, -1.293448292103240638, 0.6068886689937365020 ) ) ;
#28137=LINE ( 'NONE', #2, #35121 ) ;
#28139=CARTESIAN_POINT ( 'NONE',  ( 0.5099336548069899333, -1.112575729146672243, 0.5993070616419141627 ) ) ;
#28143=CARTESIAN_POINT ( 'NONE',  ( -0.01736481776669303659, -0.6872203660140440151, 0.1457185332388702681 ) ) ;
#28145=CARTESIAN_POINT ( 'NONE',  ( 0.3853064297010572736, -1.605638540110655210, 0.5751012791866177976 ) ) ;
#28147=CARTESIAN_POINT ( 'NONE',  ( 0.1867164799886507631, -0.6336341480852951680, -0.01319825145230188283 ) ) ;
#28152=CARTESIAN_POINT ( 'NONE',  ( 0.4367293978554446787, -1.042335339574861131, 0.6370487242724790500 ) ) ;
#28153=CARTESIAN_POINT ( 'NONE',  ( 0.1178863413097692436, -0.5755085003802594690, 0.2594340787492229183 ) ) ;
#28158=CARTESIAN_POINT ( 'NONE',  ( 0.1176733790823393522, -1.298938889880303371, 0.5182417262812425429 ) ) ;
#28159=CARTESIAN_POINT ( 'NONE',  ( 0.4419048264407517412, -1.686280600454952205, 0.4284299735157269251 ) ) ;
#28160=CARTESIAN_POINT ( 'NONE',  ( 0.4000099798367660608, -1.704638381955401183, 0.4182417262808776903 ) ) ;
#28161=CARTESIAN_POINT ( 'NONE',  ( 0.2208526919740124717, -1.239328936468657272, 0.5723503595998229443 ) ) ;
#28167=CARTESIAN_POINT ( 'NONE',  ( 0.2159838750730762591, -0.9307556585230835067, 0.3864363914520806964 ) ) ;
#28169=CARTESIAN_POINT ( 'NONE',  ( 0.4538010422723244286, -1.220679807276677575, 0.6057417262810179670 ) ) ;
#28170=CARTESIAN_POINT ( 'NONE',  ( 0.3167162826948920484, -1.173191636801490745, 0.5491094731419751129 ) ) ;
#28171=CARTESIAN_POINT ( 'NONE',  ( 0.1224152969000399382, -1.440949543414774547, 0.5682417262808782121 ) ) ;
#28172=CARTESIAN_POINT ( 'NONE',  ( 0.2615594559960963683, -1.678060962790617783, 0.5376464678218270121 ) ) ;
#28174=CARTESIAN_POINT ( 'NONE',  ( 0.3508778134978967067, -1.164926840218082127, 0.4278213320778186390 ) ) ;
#28177=FACE_OUTER_BOUND ( 'NONE', #11128, .T. ) ;
#28179=CARTESIAN_POINT ( 'NONE',  ( 0.2616322387702281205, -1.678013124025769187, 0.5382687897764735219 ) ) ;
#28181=CARTESIAN_POINT ( 'NONE',  ( 0.5767892224792289246, -1.425666411081258467, 0.6016736859548048599 ) ) ;
#28183=ORIENTED_EDGE ( 'NONE', *, *, #16729, .T. ) ;
#28186=ORIENTED_EDGE ( 'NONE', *, *, #447, .T. ) ;
#28187=CARTESIAN_POINT ( 'NONE',  ( 0.2974677162926867013, -1.656770836169560335, 0.5772130710687483068 ) ) ;
#28189=CARTESIAN_POINT ( 'NONE',  ( 0.4440535265307390955, -1.714300051848237638, 0.5182417262812423209 ) ) ;
#28191=EDGE_CURVE ( 'NONE', #12748, #13839, #13349, .T. ) ;
#28196=DIRECTION ( 'NONE',  ( -0.7173209392562553965, -0.6967428969270202943, -7.540734276611761816E-05 ) ) ;
#28199=CARTESIAN_POINT ( 'NONE',  ( 0.2721784717217399230, -0.9829408826315968462, 0.7561764537945854237 ) ) ;
#28200=CARTESIAN_POINT ( 'NONE',  ( 0.3444280284632370015, -1.101336781896232075, 0.7393691862850351182 ) ) ;
#28201=CARTESIAN_POINT ( 'NONE',  ( 0.2734857512113577083, -1.671572137726918816, 0.6513199796913040629 ) ) ;
#28202=CARTESIAN_POINT ( 'NONE',  ( 0.3202835734604576046, -1.704999925949175710, 0.8356439209704767945 ) ) ;
#28204=DIRECTION ( 'NONE',  ( -0.6967428928481391726, 0.7173209432181241185, -7.540734276603101752E-05 ) ) ;
#28210=CARTESIAN_POINT ( 'NONE',  ( 0.1019768089910752101, -1.315145345007704192, 0.7228722810749433902 ) ) ;
#28212=CARTESIAN_POINT ( 'NONE',  ( 0.6347819612394876021, -1.328236395719069263, 0.8269854195084552773 ) ) ;
#28214=CARTESIAN_POINT ( 'NONE',  ( 0.6727416549544570357, -1.556482965640024974, 0.6140251777818144241 ) ) ;
#28219=CARTESIAN_POINT ( 'NONE',  ( 0.2559586117443874986, -1.601769494230190327, 0.8408691708661252262 ) ) ;
#28220=CARTESIAN_POINT ( 'NONE',  ( 0.5875213160827347236, -1.472591613620396922, 0.6829739459387013101 ) ) ;
#28223=CARTESIAN_POINT ( 'NONE',  ( 0.2139922239084591227, -0.7322259512090013578, 0.4012976140435131622 ) ) ;
#28235=EDGE_CURVE ( 'NONE', #17780, #23287, #38952, .T. ) ;
#28236=CARTESIAN_POINT ( 'NONE',  ( 0.2404999449471016959, -0.9448023322974971050, 0.6708547505071026373 ) ) ;
#28238=CARTESIAN_POINT ( 'NONE',  ( 0.4304258907306922621, -1.358867810424106315, 0.8370822606288357282 ) ) ;
#28242=CARTESIAN_POINT ( 'NONE',  ( 0.4778061690595215572, -1.668017292664590645, 0.5682417262808788783 ) ) ;
#28243=CARTESIAN_POINT ( 'NONE',  ( 0.6659438668093399238, -1.561559416909786613, 0.5697186424223757983 ) ) ;
#28249=CARTESIAN_POINT ( 'NONE',  ( 0.07539036843641495900, -1.329185100875404313, 0.6514330093269139477 ) ) ;
#28250=CARTESIAN_POINT ( 'NONE',  ( 0.1874843899254543811, -0.7932266022496337055, 0.2338244398510780642 ) ) ;
#28255=CARTESIAN_POINT ( 'NONE',  ( 0.5845704849289827809, -1.492672057029025279, 0.5599513125418986714 ) ) ;
#28257=B_SPLINE_CURVE_WITH_KNOTS ( 'NONE', 3,
 ( #26559, #23486, #36003, #7809 ),
 .UNSPECIFIED., .F., .F.,
 ( 4, 4 ),
 ( 0.000000000000000000, 0.0003243177824960875302 ),
 .UNSPECIFIED. ) ;
#28260=LINE ( 'NONE', #9550, #1342 ) ;
#28262=CARTESIAN_POINT ( 'NONE',  ( 0.08828290717378418917, -0.6324995549925619409, 0.03536146464536887857 ) ) ;
#28263=ORIENTED_EDGE ( 'NONE', *, *, #1224, .T. ) ;
#28264=CARTESIAN_POINT ( 'NONE',  ( 0.3405242896115078244, -1.744906522954274175, 0.4484829386636804971 ) ) ;
#28265=CARTESIAN_POINT ( 'NONE',  ( 0.1251005810423869713, -1.257534650344321880, 0.7423098211221518250 ) ) ;
#28270=ORIENTED_EDGE ( 'NONE', *, *, #39452, .T. ) ;
#28277=CARTESIAN_POINT ( 'NONE',  ( 0.09797155024083728514, -0.5964682206075406778, 0.3201474151171130322 ) ) ;
#28281=CARTESIAN_POINT ( 'NONE',  ( 0.07414319037446265304, -0.5634787072276313813, 0.2482676990552415974 ) ) ;
#28285=CARTESIAN_POINT ( 'NONE',  ( 0.4122350904075519074, -1.076876625835822887, 0.6345610635168674740 ) ) ;
#28286=EDGE_CURVE ( 'NONE', #33071, #25669, #34725, .T. ) ;
#28287=CARTESIAN_POINT ( 'NONE',  ( 0.1266223302490341873, -1.314440782070608327, 0.5182417262812423209 ) ) ;
#28288=CARTESIAN_POINT ( 'NONE',  ( 0.1897113924121462125, -0.5340544967971894152, 0.1465862501021127640 ) ) ;
#28290=CARTESIAN_POINT ( 'NONE',  ( 0.5807000928386124583, -1.495207826712593890, 0.5692575695771724398 ) ) ;
#28295=CARTESIAN_POINT ( 'NONE',  ( 0.1531253909584859019, -0.7850955375911295997, 0.6127314896756340667 ) ) ;
#28297=CARTESIAN_POINT ( 'NONE',  ( 0.4514527476588715560, -1.032880248282614266, 0.8272311760340308462 ) ) ;
#28301=CARTESIAN_POINT ( 'NONE',  ( 0.03387208585097720159, -1.140508953265759962, 0.6721967346510711039 ) ) ;
#28304=CARTESIAN_POINT ( 'NONE',  ( 0.1934354357533958624, -0.7450421482614953961, 0.3186346416980788132 ) ) ;
#28306=CARTESIAN_POINT ( 'NONE',  ( 0.06443582815874859815, -0.8352844082028778594, 0.1457185332388699350 ) ) ;
#28308=FACE_OUTER_BOUND ( 'NONE', #4784, .T. ) ;
#28312=CARTESIAN_POINT ( 'NONE',  ( 0.6642913206916110092, -1.495764917729122123, 0.4182417262808777458 ) ) ;
#28313=CARTESIAN_POINT ( 'NONE',  ( 0.6985364634159124675, -1.438850461896725275, 0.5682400285031795617 ) ) ;
#28317=CARTESIAN_POINT ( 'NONE',  ( 0.2232773634713763056, -1.353530203713960045, 0.4677345876144705095 ) ) ;
#28318=CARTESIAN_POINT ( 'NONE',  ( 0.1856533569311497323, -0.7573055082216308964, 0.1457185332388697685 ) ) ;
#28320=CARTESIAN_POINT ( 'NONE',  ( 0.5120345133055148601, -1.314022687763800157, 0.5963220732961661552 ) ) ;
#28321=VECTOR ( 'NONE', #34508, 39.37007874015748143 ) ;
#28324=CARTESIAN_POINT ( 'NONE',  ( 0.4709147388527493705, -1.070627459034787954, 0.6206731519243955386 ) ) ;
#28328=CARTESIAN_POINT ( 'NONE',  ( 0.05267389698015547544, -1.086150594168910466, 0.7379831432407867320 ) ) ;
#28329=ORIENTED_EDGE ( 'NONE', *, *, #5102, .F. ) ;
#28330=EDGE_CURVE ( 'NONE', #7024, #19095, #12028, .T. ) ;
#28331=ORIENTED_EDGE ( 'NONE', *, *, #15969, .F. ) ;
#28333=CARTESIAN_POINT ( 'NONE',  ( 0.3852216438992382419, -1.605616193201484965, 0.5739667088636910552 ) ) ;
#28335=CARTESIAN_POINT ( 'NONE',  ( 0.1114066244466402900, -0.9052510818166191742, 0.04196736182216751626 ) ) ;
#28338=AXIS2_PLACEMENT_3D ( 'NONE', #4771, #8071, #36472 ) ;
#28342=EDGE_CURVE ( 'NONE', #12586, #38403, #8082, .T. ) ;
#28343=CARTESIAN_POINT ( 'NONE',  ( 0.5663790608840560958, -1.497944059049526988, 0.6446960571708316712 ) ) ;
#28345=CARTESIAN_POINT ( 'NONE',  ( 0.01405263366207808347, -0.9640798247225310647, 0.3811368675598582612 ) ) ;
#28349=ADVANCED_FACE ( 'NONE', ( #12323 ), #28353, .F. ) ;
#28350=CARTESIAN_POINT ( 'NONE',  ( 0.2983165958604226398, -1.151818276997767621, 0.5182417262812423209 ) ) ;
#28353=PLANE ( 'NONE',  #5425 ) ;
#28355=CARTESIAN_POINT ( 'NONE',  ( 0.1210494546010137118, -1.266445924951928204, 0.6212394332447065404 ) ) ;
#28358=CARTESIAN_POINT ( 'NONE',  ( 0.1166065821415037673, -1.415338206367125817, 0.5822564622277803803 ) ) ;
#28360=ADVANCED_FACE ( 'NONE', ( #37823 ), #37714, .T. ) ;
#28362=CARTESIAN_POINT ( 'NONE',  ( 0.3689192748036780878, -1.014666054483551294, 0.6186952232919745720 ) ) ;
#28364=CARTESIAN_POINT ( 'NONE',  ( 0.1916453137239563509, -1.371753268179084717, 0.4817276165294532841 ) ) ;
#28365=CARTESIAN_POINT ( 'NONE',  ( 0.5523000078138265989, -1.163818204720048266, 0.6057417262810179670 ) ) ;
#28369=CARTESIAN_POINT ( 'NONE',  ( 0.0002700364102348538193, -0.8386493658592084621, 0.3780876778669690075 ) ) ;
#28370=CARTESIAN_POINT ( 'NONE',  ( 0.0001126841386759542179, -0.5849248619627643864, -0.08138210067616551135 ) ) ;
#28372=CARTESIAN_POINT ( 'NONE',  ( 0.6929208297549553919, -1.429122597532291650, 0.5682417262808779901 ) ) ;
#28374=ORIENTED_EDGE ( 'NONE', *, *, #440, .T. ) ;
#28380=CARTESIAN_POINT ( 'NONE',  ( 0.6113557282315684738, -1.476144099735155368, 0.5498370725323885599 ) ) ;
#28381=CARTESIAN_POINT ( 'NONE',  ( 0.3690965330173307524, -1.099411688709415413, 0.5182417262812423209 ) ) ;
#28384=VERTEX_POINT ( 'NONE', #34117 ) ;
#28385=CARTESIAN_POINT ( 'NONE',  ( 0.2024457102403973141, -0.7198351356486335506, 0.3420682486339518547 ) ) ;
#28387=CARTESIAN_POINT ( 'NONE',  ( 0.2974186907859220352, -1.656756618909332124, 0.5765815979583946982 ) ) ;
#28389=CARTESIAN_POINT ( 'NONE',  ( 0.1190963382269523835, -1.288349449013993508, 0.6004008909010771777 ) ) ;
#28394=EDGE_CURVE ( 'NONE', #36916, #11923, #17923, .T. ) ;
#28398=EDGE_CURVE ( 'NONE', #11030, #33002, #19594, .T. ) ;
#28400=CARTESIAN_POINT ( 'NONE',  ( 0.3817504269947164519, -1.726033828776057266, 0.4251703030630530900 ) ) ;
#28403=AXIS2_PLACEMENT_3D ( 'NONE', #6390, #38065, #15656 ) ;
#28404=CARTESIAN_POINT ( 'NONE',  ( 0.1261292094506294148, -0.8244062005499848134, 0.1786220713650574499 ) ) ;
#28406=CARTESIAN_POINT ( 'NONE',  ( 0.1822227791794524265, -1.186887416757892888, 1.012788992251323350 ) ) ;
#28413=CARTESIAN_POINT ( 'NONE',  ( 0.1249840844849290228, -1.018512954913863844, 0.9570223520903572423 ) ) ;
#28414=CARTESIAN_POINT ( 'NONE',  ( 0.1017718266971927438, -1.363853815782150924, 0.6879803626369204173 ) ) ;
#28418=CARTESIAN_POINT ( 'NONE',  ( 0.6965523178711373609, -1.533409646290749828, 0.5827623954312006749 ) ) ;
#28419=AXIS2_PLACEMENT_3D ( 'NONE', #30381, #40236, #36952 ) ;
#28422=CARTESIAN_POINT ( 'NONE',  ( 0.1055042220909814948, -1.411635777700159800, 0.5659469840222108861 ) ) ;
#28423=CARTESIAN_POINT ( 'NONE',  ( 0.2493882130568067512, -1.574984837766822965, 0.8682191111569700359 ) ) ;
#28425=CARTESIAN_POINT ( 'NONE',  ( 0.1320129719769623233, -0.5716393116954411324, 0.2400138632674352901 ) ) ;
#28436=ORIENTED_EDGE ( 'NONE', *, *, #6993, .T. ) ;
#28437=CARTESIAN_POINT ( 'NONE',  ( 0.1005327108732830682, -0.7654220390130497265, 0.3417061460467297751 ) ) ;
#28439=CARTESIAN_POINT ( 'NONE',  ( 0.5245207932248472371, -1.526647649442574473, 0.5610456953807425595 ) ) ;
#28444=CARTESIAN_POINT ( 'NONE',  ( 0.4486004395777776210, -1.685563693236277416, 0.6043086445225501757 ) ) ;
#28445=CARTESIAN_POINT ( 'NONE',  ( 0.6990254338941188639, -1.438807163059433458, 0.5794947641723904308 ) ) ;
#28448=CARTESIAN_POINT ( 'NONE',  ( 0.6097404743490668633, -1.478808349948183443, 0.5913594100522746588 ) ) ;
#28450=CARTESIAN_POINT ( 'NONE',  ( 0.1852718761952666104, -0.8389489029336036907, 0.1457185345930598341 ) ) ;
#28452=CARTESIAN_POINT ( 'NONE',  ( 0.04329528483221436325, -1.226008797194266586, 0.6628706426414217034 ) ) ;
#28454=CARTESIAN_POINT ( 'NONE',  ( 0.5138235575674273692, -1.118575097671381080, 0.5744212141803229921 ) ) ;
#28456=DIRECTION ( 'NONE',  ( 0.8660512985181135770, 0.4999551463232372317, 0.000000000000000000 ) ) ;
#28457=B_SPLINE_CURVE_WITH_KNOTS ( 'NONE', 3,
 ( #34234, #24597, #28087, #27669, #12243, #21520 ),
 .UNSPECIFIED., .F., .F.,
 ( 4, 2, 4 ),
 ( 0.000000000000000000, 0.5000000000000000000, 1.000000000000000000 ),
 .UNSPECIFIED. ) ;
#28458=CARTESIAN_POINT ( 'NONE',  ( 0.4662642109249354738, -1.558585770123256387, 0.5489026516414302614 ) ) ;
#28461=( BOUNDED_SURFACE ( )  B_SPLINE_SURFACE ( 3, 2, ( 
 ( #7953, #23826, #11670 ),
 ( #20938, #36348, #12076 ),
 ( #8774, #2217, #8561 ),
 ( #36750, #4867, #17827 ),
 ( #15147, #27320, #30386 ),
 ( #21351, #8165, #14757 ),
 ( #40034, #40240, #14538 ),
 ( #33890, #36141, #30791 ),
 ( #8369, #39849, #24226 ),
 ( #20525, #17436, #29991 ),
 ( #27510, #27102, #14340 ),
 ( #21134, #33661, #5474 ) ),
 .UNSPECIFIED., .F., .F., .F. ) 
 B_SPLINE_SURFACE_WITH_KNOTS ( ( 4, 2, 2, 2, 2, 4 ),
 ( 3, 3 ),
 ( -2.194247311574145322E-05, 0.0004166382859409436027, 0.0008552190449976286146, 0.001732380563110998747, 0.002609542081224368662, 0.003486703599337739011 ),
 ( 0.000000000000000000, 1.000000000000000000 ),
 .UNSPECIFIED. ) 
 GEOMETRIC_REPRESENTATION_ITEM ( )  RATIONAL_B_SPLINE_SURFACE ( (
 ( 1.000000000000000000, 0.7032244542329121328, 1.000000000000000000),
 ( 1.000000000000000000, 0.7033233483186307478, 1.000000000000000000),
 ( 1.000000000000000000, 0.7045246448745312584, 1.000000000000000000),
 ( 1.000000000000000000, 0.7073062858921952412, 1.000000000000000000),
 ( 1.000000000000000000, 0.7090759679026412687, 1.000000000000000000),
 ( 1.000000000000000000, 0.7151776825359495993, 1.000000000000000000),
 ( 1.000000000000000000, 0.7200725892538363260, 1.000000000000000000),
 ( 1.000000000000000000, 0.7289630251952065043, 1.000000000000000000),
 ( 1.000000000000000000, 0.7326908029506756792, 1.000000000000000000),
 ( 1.000000000000000000, 0.7366628156064797261, 1.000000000000000000),
 ( 1.000000000000000000, 0.7367803224921714023, 1.000000000000000000),
 ( 1.000000000000000000, 0.7348357107204075422, 1.000000000000000000) ) ) 
 REPRESENTATION_ITEM ( '' )  SURFACE ( )  );
#28462=VERTEX_POINT ( 'NONE', #20126 ) ;
#28463=CARTESIAN_POINT ( 'NONE',  ( 0.4390406754936738154, -1.575939765669403192, 0.6014929107880048198 ) ) ;
#28466=CARTESIAN_POINT ( 'NONE',  ( 0.08592534930546107119, -0.7849569399949006820, 0.07020894479808938160 ) ) ;
#28469=CARTESIAN_POINT ( 'NONE',  ( 0.1700065278191711104, -1.375428071273553376, 0.6154404651844289642 ) ) ;
#28483=CARTESIAN_POINT ( 'NONE',  ( 0.09014882583140459982, -0.6063924461725455073, 0.1729119204149524025 ) ) ;
#28488=CARTESIAN_POINT ( 'NONE',  ( 0.3101835799050875475, -1.221649658806551297, 0.8662723704748881426 ) ) ;
#28492=CARTESIAN_POINT ( 'NONE',  ( 0.06843411546424661707, -1.327640554429453168, 0.5682417262808774350 ) ) ;
#28493=CARTESIAN_POINT ( 'NONE',  ( 0.3347563140814358018, -1.025429894978651779, 0.6211877635660684183 ) ) ;
#28497=CARTESIAN_POINT ( 'NONE',  ( 0.1887412855916241194, -0.4595320686313542624, 0.1446142472693910663 ) ) ;
#28498=CARTESIAN_POINT ( 'NONE',  ( 0.1458595596271754224, -0.6542043499068329604, 0.4259781829602066194 ) ) ;
#28501=CARTESIAN_POINT ( 'NONE',  ( 0.08372836835944071077, -1.326477885028105375, 0.4882417262808781966 ) ) ;
#28504=CARTESIAN_POINT ( 'NONE',  ( 0.4196576349101079351, -1.201297826476563024, 0.8179721269271881257 ) ) ;
#28506=CARTESIAN_POINT ( 'NONE',  ( 0.2318926187578342901, -0.6847811903715324000, 0.4821206442548801596 ) ) ;
#28510=CARTESIAN_POINT ( 'NONE',  ( 0.05981300713595071039, -1.256039768099636689, 0.6499504827381740180 ) ) ;
#28513=EDGE_CURVE ( 'NONE', #26063, #38731, #814, .T. ) ;
#28525=EDGE_CURVE ( 'NONE', #20299, #20709, #6945, .T. ) ;
#28526=CARTESIAN_POINT ( 'NONE',  ( 0.3249891007434509982, -1.168521056691680382, 0.5670768804972423638 ) ) ;
#28527=ADVANCED_FACE ( 'NONE', ( #35526 ), #2499, .T. ) ;
#28528=ORIENTED_EDGE ( 'NONE', *, *, #8618, .T. ) ;
#28530=FACE_OUTER_BOUND ( 'NONE', #11920, .T. ) ;
#28531=CARTESIAN_POINT ( 'NONE',  ( 0.4717517922261478813, -1.668493369395022796, 0.4596108401464155668 ) ) ;
#28534=CARTESIAN_POINT ( 'NONE',  ( 0.4964455468594098919, -1.286167783046271440, 0.6305352476659182859 ) ) ;
#28537=CARTESIAN_POINT ( 'NONE',  ( 0.4162441775219429263, -1.040631601589554034, 0.6343403631529308528 ) ) ;
#28540=CARTESIAN_POINT ( 'NONE',  ( -0.002288348195190195115, -0.8555288688122634211, 0.1914435222285272298 ) ) ;
#28542=CONICAL_SURFACE ( 'NONE', #16037, 0.1762268159172233339, 0.7853981633974500554 ) ;
#28544=CARTESIAN_POINT ( 'NONE',  ( 0.04803016009707770928, -0.5362635619093905071, 0.1543674294428551697 ) ) ;
#28545=EDGE_CURVE ( 'NONE', #16949, #17350, #230, .T. ) ;
#28546=CARTESIAN_POINT ( 'NONE',  ( 0.08672709535528307090, -0.7521132484280468322, 0.01666405986956852672 ) ) ;
#28547=CARTESIAN_POINT ( 'NONE',  ( 0.1842062797954040487, -0.8537295084795349931, 0.1492890682281529657 ) ) ;
#28551=B_SPLINE_CURVE_WITH_KNOTS ( 'NONE', 3,
 ( #32804, #29727, #13874, #27273, #30142, #1367, #14096, #39391, #38987, #4816, #20284, #1573, #39204, #11631, #11025, #7905, #23583, #29948, #20477, #33010, #17390, #1787, #1970, #23990, #14301, #11212, #8522, #23778, #36295, #8118, #20695, #33226, #5035, #2169, #14489, #39801 ),
 .UNSPECIFIED., .F., .F.,
 ( 4, 2, 2, 2, 2, 2, 2, 2, 2, 2, 2, 2, 2, 2, 2, 2, 2, 4 ),
 ( -6.000000000055645558E-08, 0.001367160778072117446, 0.002050771167108184339, 0.002734381556144251449, 0.003417991945180318125, 0.004101602334216384801, 0.004785212723252451478, 0.005468823112288519021, 0.006152433501324586565, 0.006836043890360653241, 0.008203264668432784859, 0.008886875057468849801, 0.009570485446504914742, 0.01093770622457703942, 0.01230492700264916410, 0.01367214778072128704, 0.01640658933686554161, 0.02187547244915405420 ),
 .UNSPECIFIED. ) ;
#28552=CARTESIAN_POINT ( 'NONE',  ( 0.3348264461528376867, -1.289438405178311209, 0.5735458425336941168 ) ) ;
#28553=CARTESIAN_POINT ( 'NONE',  ( 0.3508289865554531928, -1.132338794321712916, 0.8154384950216992944 ) ) ;
#28556=CARTESIAN_POINT ( 'NONE',  ( 0.1874490856083247670, -0.6900333170255394943, 0.05073663252241766841 ) ) ;
#28562=DIRECTION ( 'NONE',  ( 0.9998941247116546194, -0.01455087607601020412, 0.0001066420868422379362 ) ) ;
#28563=CARTESIAN_POINT ( 'NONE',  ( 0.08534891775908995393, -0.7691016309398805983, 0.1031615689448583950 ) ) ;
#28564=CARTESIAN_POINT ( 'NONE',  ( 0.2637382839637063547, -0.6009449316864781121, 0.1932256475537140750 ) ) ;
#28565=DIRECTION ( 'NONE',  ( 0.0001066307966868756642, -1.551735798904719862E-06, -0.9999999943137325431 ) ) ;
#28566=CARTESIAN_POINT ( 'NONE',  ( 0.1281055102147601044, -1.260775204155497375, 0.6226496396147861434 ) ) ;
#28568=CARTESIAN_POINT ( 'NONE',  ( 0.1316017208954911033, -1.248059642665102942, 0.5182417262812423209 ) ) ;
#28571=CARTESIAN_POINT ( 'NONE',  ( 0.4434061351937851336, -1.055534433944394390, 0.6333734109485414931 ) ) ;
#28572=AXIS2_PLACEMENT_3D ( 'NONE', #26800, #20411, #39326 ) ;
#28574=CARTESIAN_POINT ( 'NONE',  ( 0.5534381859858074071, -1.186304665530027558, 0.6057417262809816627 ) ) ;
#28576=AXIS2_PLACEMENT_3D ( 'NONE', #35957, #7766, #20332 ) ;
#28577=EDGE_CURVE ( 'NONE', #24913, #20299, #6743, .T. ) ;
#28580=CARTESIAN_POINT ( 'NONE',  ( 0.06399702207960011879, -1.267566535398010563, 0.6886354586937382116 ) ) ;
#28583=DIRECTION ( 'NONE',  ( 0.8660512985181134660, 0.4999551463232371762, 0.000000000000000000 ) ) ;
#28586=ORIENTED_EDGE ( 'NONE', *, *, #33508, .T. ) ;
#28592=CARTESIAN_POINT ( 'NONE',  ( 0.5755900408509843080, -1.422326445372266379, 0.6246236810960820174 ) ) ;
#28596=CARTESIAN_POINT ( 'NONE',  ( 0.5859306440460040344, -1.604270562037251713, 0.4385162621962425678 ) ) ;
#28597=EDGE_LOOP ( 'NONE', ( #38285, #25879, #37088, #9182 ) ) ;
#28598=CARTESIAN_POINT ( 'NONE',  ( 0.2992444779679390154, -1.656912578960057170, 0.6025679435408887175 ) ) ;
#28600=CARTESIAN_POINT ( 'NONE',  ( 0.5953197980378828191, -1.599064723402610300, 0.4311035055375505576 ) ) ;
#28603=CARTESIAN_POINT ( 'NONE',  ( 0.1844975769085782369, -0.8266995537623093027, 0.05501147976861575639 ) ) ;
#28611=CARTESIAN_POINT ( 'NONE',  ( 0.1862785929144180619, -0.9153889657460283491, 0.1591853427980846336 ) ) ;
#28614=CARTESIAN_POINT ( 'NONE',  ( 0.2149313114772367361, -0.9162195584033384632, 0.6271167533926740312 ) ) ;
#28616=CARTESIAN_POINT ( 'NONE',  ( 0.03315096893860772914, -0.7291808658770100315, 0.5842526001130612379 ) ) ;
#28625=CARTESIAN_POINT ( 'NONE',  ( -9.828236692375560680E-17, -0.4262518876079541830, 0.09312799375524088985 ) ) ;
#28626=CARTESIAN_POINT ( 'NONE',  ( 0.1188901005336925887, -1.412173384746612470, 0.5925880645485681608 ) ) ;
#28631=B_SPLINE_CURVE_WITH_KNOTS ( 'NONE', 3,
 ( #16867, #13362, #7365, #7167, #29204, #26139, #13756, #22434, #29602, #34962, #658, #26322, #28988, #16261, #25937, #19735, #38847, #32689, #38458, #16445, #19553, #13148 ),
 .UNSPECIFIED., .F., .F.,
 ( 4, 2, 2, 2, 2, 2, 2, 2, 2, 2, 4 ),
 ( 0.009671489109998996150, 0.01088255487380758793, 0.01209362063761617798, 0.01269915351952047300, 0.01330468640142476802, 0.01451575216523336154, 0.01572681792904195158, 0.01633235081094624661, 0.01693788369285054163, 0.01814894945665913167, 0.01936001522046771825 ),
 .UNSPECIFIED. ) ;
#28633=CARTESIAN_POINT ( 'NONE',  ( 0.4688079631758284016, -1.116561345930851656, 0.5688791344137259509 ) ) ;
#28635=CARTESIAN_POINT ( 'NONE',  ( 0.1879136253127565159, -0.5789011793442228049, 0.2920474488862616069 ) ) ;
#28639=CARTESIAN_POINT ( 'NONE',  ( 0.2638696491212411122, -1.678849922788173910, 0.6249181099526833760 ) ) ;
#28640=CARTESIAN_POINT ( 'NONE',  ( 0.5947882614772961318, -1.487164117345723735, 0.5703039760230342869 ) ) ;
#28644=ORIENTED_EDGE ( 'NONE', *, *, #18790, .T. ) ;
#28651=DIRECTION ( 'NONE',  ( -0.4999551463232372317, 0.8660512985181135770, -0.000000000000000000 ) ) ;
#28654=CARTESIAN_POINT ( 'NONE',  ( 0.2038982337730780858, -0.9000317451160128046, 0.6260891870533979997 ) ) ;
#28655=CARTESIAN_POINT ( 'NONE',  ( 0.06924657340765605351, -0.5400045880099076934, 0.1408780685345814021 ) ) ;
#28656=CARTESIAN_POINT ( 'NONE',  ( 0.5384178852093373102, -1.518839747657279693, 0.5610560271465162563 ) ) ;
#28657=EDGE_CURVE ( 'NONE', #12308, #37890, #13380, .T. ) ;
#28661=CARTESIAN_POINT ( 'NONE',  ( 0.6670706299876395518, -1.560988262821363159, 0.5986134368056421629 ) ) ;
#28665=CARTESIAN_POINT ( 'NONE',  ( 0.1351500142932794135, -0.5720763397125275818, 0.2394465910792453189 ) ) ;
#28666=CARTESIAN_POINT ( 'NONE',  ( -0.002366742664566666259, -0.8470346775007634443, 0.1487544527304272002 ) ) ;
#28670=CARTESIAN_POINT ( 'NONE',  ( 0.01926973937230214845, -1.027504089262102349, 0.6199911605063174180 ) ) ;
#28671=CARTESIAN_POINT ( 'NONE',  ( 0.3725907112986628911, -0.9732892004818366471, 0.6614114956809742374 ) ) ;
#28683=AXIS2_PLACEMENT_3D ( 'NONE', #13958, #26323, #23251 ) ;
#28685=CARTESIAN_POINT ( 'NONE',  ( 0.06831029412767206099, -1.252103505662720773, 0.7560490987658511353 ) ) ;
#28688=CARTESIAN_POINT ( 'NONE',  ( 0.5185199569154549382, -1.918301849770578604, 0.5182417262812423209 ) ) ;
#28691=DIRECTION ( 'NONE',  ( 0.4999551463232371762, -0.8660512985181134660, 0.000000000000000000 ) ) ;
#28696=CARTESIAN_POINT ( 'NONE',  ( 0.01562500000000001041, -0.4734555301001455718, 0.3484897634354066631 ) ) ;
#28700=CARTESIAN_POINT ( 'NONE',  ( 0.2111055010124828490, -0.8551966691801877740, 0.6642139276148122384 ) ) ;
#28702=ORIENTED_EDGE ( 'NONE', *, *, #28394, .F. ) ;
#28703=CARTESIAN_POINT ( 'NONE',  ( 0.007612700501528337112, -0.5283205944668291076, 0.4322922080670053013 ) ) ;
#28704=CARTESIAN_POINT ( 'NONE',  ( 0.4664867455706405153, -1.541371222339207980, 0.7051371147911057458 ) ) ;
#28705=CARTESIAN_POINT ( 'NONE',  ( 0.04040949304222755945, -0.7990836459010076664, 0.6824493494041665720 ) ) ;
#28708=CARTESIAN_POINT ( 'NONE',  ( 0.4271525060574433152, -1.046616626432022024, 0.6356164445927319218 ) ) ;
#28712=FACE_OUTER_BOUND ( 'NONE', #29032, .T. ) ;
#28713=CARTESIAN_POINT ( 'NONE',  ( 0.3964953586213888492, -1.184310263668996388, 0.8231536074751556464 ) ) ;
#28714=B_SPLINE_CURVE_WITH_KNOTS ( 'NONE', 3,
 ( #3196, #6280, #25002, #37535 ),
 .UNSPECIFIED., .F., .F.,
 ( 4, 4 ),
 ( 0.000000000000000000, 0.001608604910876098313 ),
 .UNSPECIFIED. ) ;
#28717=B_SPLINE_CURVE_WITH_KNOTS ( 'NONE', 3,
 ( #7649, #17316, #20213, #32738, #35425, #29659, #14017, #23700, #4959, #26592, #20005, #19788, #32328, #1113, #4145, #22908 ),
 .UNSPECIFIED., .F., .F.,
 ( 4, 2, 2, 2, 2, 2, 2, 4 ),
 ( 0.000000000000000000, 0.0006596505163732249016, 0.001319301032746449803, 0.001978951549119674705, 0.002638602065492899607, 0.003957903098239352012, 0.004617553614612577781, 0.005277204130985802683 ),
 .UNSPECIFIED. ) ;
#28720=CARTESIAN_POINT ( 'NONE',  ( 0.2055745749294108637, -0.6303510842867390274, 0.3631342511460070033 ) ) ;
#28722=CARTESIAN_POINT ( 'NONE',  ( 0.4338848837222285537, -1.129391978085439341, 0.4668060154234752179 ) ) ;
#28723=CARTESIAN_POINT ( 'NONE',  ( 0.03165525491262633634, -1.070880979729221805, 0.6191223686483765531 ) ) ;
#28724=B_SPLINE_CURVE_WITH_KNOTS ( 'NONE', 3,
 ( #37446, #28809, #6177, #25116 ),
 .UNSPECIFIED., .F., .F.,
 ( 4, 4 ),
 ( 0.000000000000000000, 2.831411885517509102E-06 ),
 .UNSPECIFIED. ) ;
#28726=CARTESIAN_POINT ( 'NONE',  ( 0.1947422056511775024, -0.6388409797470162577, 0.3264359486978148928 ) ) ;
#28727=CARTESIAN_POINT ( 'NONE',  ( 0.1477639946820497596, -0.8713623285363897297, 0.5125172420040071675 ) ) ;
#28728=LINE ( 'NONE', #16371, #10040 ) ;
#28736=CARTESIAN_POINT ( 'NONE',  ( 0.1157895654112029854, -1.415802608199387524, 0.5684094141069466755 ) ) ;
#28737=CARTESIAN_POINT ( 'NONE',  ( 0.4880577024640926909, -1.660084872155127789, 0.5232815315491193831 ) ) ;
#28739=CARTESIAN_POINT ( 'NONE',  ( 0.4831561709721949871, -1.265801553224180420, 0.6869631041800865479 ) ) ;
#28742=CARTESIAN_POINT ( 'NONE',  ( 0.4924424051965485827, -1.082438949443123688, 0.5780025781777323735 ) ) ;
#28745=CARTESIAN_POINT ( 'NONE',  ( 0.01894369509073403832, -0.9414322060572338779, 0.6002815649858233016 ) ) ;
#28747=CARTESIAN_POINT ( 'NONE',  ( 0.04522317044199464925, -0.6176467172810933270, 0.3942814645560069331 ) ) ;
#28748=CARTESIAN_POINT ( 'NONE',  ( 0.08508713924366427539, -0.8316154493940929315, 0.1485430111225241878 ) ) ;
#28749=CARTESIAN_POINT ( 'NONE',  ( 0.1110068091790888528, -0.9275713612966570709, 0.1181997008846571301 ) ) ;
#28756=CARTESIAN_POINT ( 'NONE',  ( 0.5669386463960099931, -1.503236241879966739, 0.5732355569184157673 ) ) ;
#28763=CARTESIAN_POINT ( 'NONE',  ( 0.07824279859864782805, -1.322120931084001416, 0.4675977987765131960 ) ) ;
#28765=DIRECTION ( 'NONE',  ( -1.000000000000000000, 0.000000000000000000, 0.000000000000000000 ) ) ;
#28768=CARTESIAN_POINT ( 'NONE',  ( 0.5117021325268811260, -1.128961434293810129, 0.8718124831259003171 ) ) ;
#28769=CARTESIAN_POINT ( 'NONE',  ( 0.1864595955553456363, -0.7573173291059521750, 0.1477569985384105666 ) ) ;
#28775=CARTESIAN_POINT ( 'NONE',  ( 0.4544922177887179005, -1.243424314323010593, 0.6057417262809816627 ) ) ;
#28776=CARTESIAN_POINT ( 'NONE',  ( 0.1864550573006002465, -0.7573172630633775437, 0.1903174488078394899 ) ) ;
#28779=CARTESIAN_POINT ( 'NONE',  ( 0.2936473109780965429, -1.729059834919730809, 0.6366410771178455663 ) ) ;
#28780=CARTESIAN_POINT ( 'NONE',  ( -0.0002002802745677785610, -0.8521680098439298190, -0.04184250874055703978 ) ) ;
#28786=DIRECTION ( 'NONE',  ( 1.060606950627616897E-16, 6.122684696619992497E-17, 1.000000000000000000 ) ) ;
#28790=CARTESIAN_POINT ( 'NONE',  ( 0.6233463770837441853, -1.469195350882636975, 0.5327916358142242848 ) ) ;
#28791=DIRECTION ( 'NONE',  ( 0.4999551463232372317, -0.8660512985181135770, 0.000000000000000000 ) ) ;
#28792=ORIENTED_EDGE ( 'NONE', *, *, #24256, .T. ) ;
#28793=ORIENTED_EDGE ( 'NONE', *, *, #27558, .F. ) ;
#28795=ORIENTED_EDGE ( 'NONE', *, *, #16453, .T. ) ;
#28796=CARTESIAN_POINT ( 'NONE',  ( 0.2973691820713019185, -1.656741485100140521, 0.5759490276894616567 ) ) ;
#28800=CARTESIAN_POINT ( 'NONE',  ( 0.1903632525096057571, -0.9196856789278203825, -0.08446770797961487831 ) ) ;
#28805=CARTESIAN_POINT ( 'NONE',  ( 0.2125266968579154203, -0.8550337035768073024, 0.3872327398333365589 ) ) ;
#28808=CARTESIAN_POINT ( 'NONE',  ( 0.5837773615624999302, -1.483316297997810729, 0.6618257327465461026 ) ) ;
#28809=CARTESIAN_POINT ( 'NONE',  ( 0.6985179347537009420, -1.438818273427901584, 0.5682411603540067357 ) ) ;
#28812=CARTESIAN_POINT ( 'NONE',  ( 0.4582099881933914820, -1.160100326466038112, 0.4182417262808778013 ) ) ;
#28814=AXIS2_PLACEMENT_3D ( 'NONE', #27246, #20451, #35884 ) ;
#28815=CARTESIAN_POINT ( 'NONE',  ( -0.002282498291095993656, -0.8555267327002353817, 0.1457185332388701293 ) ) ;
#28821=CARTESIAN_POINT ( 'NONE',  ( -3.276078897458520021E-17, -0.4262518876079541830, 0.1281883534109924672 ) ) ;
#28822=CARTESIAN_POINT ( 'NONE',  ( 0.1032092726473410188, -1.372029763476367403, 0.6793900317012312451 ) ) ;
#28825=CARTESIAN_POINT ( 'NONE',  ( 0.3817504269947160078, -1.726033828776056378, 0.4251703030630522018 ) ) ;
#28834=CARTESIAN_POINT ( 'NONE',  ( 0.2607738564055140928, -1.679248230842525169, 0.5808287157383641430 ) ) ;
#28835=CARTESIAN_POINT ( 'NONE',  ( 0.5448905143716247235, -1.417074983688033640, 0.7694088827245902928 ) ) ;
#28838=ORIENTED_EDGE ( 'NONE', *, *, #6175, .F. ) ;
#28846=CARTESIAN_POINT ( 'NONE',  ( 0.09262226466725992369, -0.7756921188983920690, 0.2845593417137921577 ) ) ;
#28849=CARTESIAN_POINT ( 'NONE',  ( 0.5400961048456246472, -1.518900631274988866, 0.5940360734052072544 ) ) ;
#28856=CARTESIAN_POINT ( 'NONE',  ( 0.6587214591109057382, -1.529505462609035193, 0.7312054128241273210 ) ) ;
#28857=FACE_OUTER_BOUND ( 'NONE', #17947, .T. ) ;
#28858=CARTESIAN_POINT ( 'NONE',  ( 0.3799940994133568228, -1.120217080746673588, 0.7999332164991961314 ) ) ;
#28863=CARTESIAN_POINT ( 'NONE',  ( 0.05963972588713747913, -1.330888851906829595, 0.5826259623951950406 ) ) ;
#28864=CARTESIAN_POINT ( 'NONE',  ( 0.4989999315605664343, -1.099494619349625113, 0.6223919996226902063 ) ) ;
#28873=CARTESIAN_POINT ( 'NONE',  ( 0.4330280987197626663, -1.579361639735390010, 0.5968389982114721271 ) ) ;
#28874=CARTESIAN_POINT ( 'NONE',  ( 0.002296835029420926742, -0.5198933010532099663, 0.1467999231854336672 ) ) ;
#28875=CARTESIAN_POINT ( 'NONE',  ( 0.1852083516168847588, -0.8428145337524144409, 0.2138870730384467567 ) ) ;
#28877=CARTESIAN_POINT ( 'NONE',  ( 0.05567535398968421340, -1.335339640988971288, 0.4687417262808780127 ) ) ;
#28878=CARTESIAN_POINT ( 'NONE',  ( 0.6802496923668470696, -1.403733334520502973, 0.6188728273484885856 ) ) ;
#28879=EDGE_LOOP ( 'NONE', ( #32921, #23966, #4426, #17593 ) ) ;
#28880=EDGE_LOOP ( 'NONE', ( #29596, #33689, #13741, #23277, #29974, #24070 ) ) ;
#28885=EDGE_LOOP ( 'NONE', ( #14074, #1299, #30056, #16854 ) ) ;
#28886=CARTESIAN_POINT ( 'NONE',  ( 0.4212239597017563009, -1.699686401043103867, 0.5682417262808792113 ) ) ;
#28887=CARTESIAN_POINT ( 'NONE',  ( 0.2513281675165960349, -0.9200942028859548927, 0.7135546038586990658 ) ) ;
#28888=CARTESIAN_POINT ( 'NONE',  ( 0.03721266748343820402, -0.6194934239485735405, 0.6037397677565615739 ) ) ;
#28889=CARTESIAN_POINT ( 'NONE',  ( 0.08524078840219724562, -0.5428247996486972315, 0.1539524137301193363 ) ) ;
#28892=CARTESIAN_POINT ( 'NONE',  ( 0.6091039633998347469, -1.477405756664260439, 0.4854686549615686575 ) ) ;
#28893=CARTESIAN_POINT ( 'NONE',  ( 0.4531532885747490691, -1.103993380834564775, 0.5911741900463310939 ) ) ;
#28895=ADVANCED_FACE ( 'NONE', ( #10132 ), #32424, .T. ) ;
#28897=CARTESIAN_POINT ( 'NONE',  ( 0.1887417687075507722, -0.4595378961884863389, 0.1473935149025172031 ) ) ;
#28900=B_SPLINE_CURVE_WITH_KNOTS ( 'NONE', 3,
 ( #5779, #15461, #15247, #27802, #40546, #12366, #29615, #22450, #1078, #19749, #32491, #32097, #25952, #31906, #7179, #29420 ),
 .UNSPECIFIED., .F., .F.,
 ( 4, 2, 2, 2, 2, 2, 2, 4 ),
 ( 0.002977950600791165556, 0.003350110441325639555, 0.003722270281860113553, 0.004094430122394587986, 0.004466589962929061984, 0.004838749803463535983, 0.005210909643998009981, 0.005955229325066958845 ),
 .UNSPECIFIED. ) ;
#28903=CARTESIAN_POINT ( 'NONE',  ( 0.3225930820597290305, -0.8396780885765841029, 0.6764912411861826458 ) ) ;
#28904=CARTESIAN_POINT ( 'NONE',  ( 0.4572296806421124460, -1.116135140744203502, 0.5564961385877081890 ) ) ;
#28905=CARTESIAN_POINT ( 'NONE',  ( 0.03592955808354850872, -1.097415845682047753, 0.6391787347605660807 ) ) ;
#28906=CIRCLE ( 'NONE', #23673, 0.009999999999999995004 ) ;
#28908=CARTESIAN_POINT ( 'NONE',  ( 0.1925648626342071068, -0.7537655587791137757, 0.3141518395702517785 ) ) ;
#28909=CARTESIAN_POINT ( 'NONE',  ( 0.3182721343743615816, -1.037109716264222659, 0.7330233950017801536 ) ) ;
#28915=CARTESIAN_POINT ( 'NONE',  ( 0.5561777791303107454, -1.388654548445044323, 0.7524667234028521445 ) ) ;
#28916=CARTESIAN_POINT ( 'NONE',  ( 0.07550739411094989362, -0.8311898289549712882, 0.1457185332388705179 ) ) ;
#28917=CARTESIAN_POINT ( 'NONE',  ( 0.3704697912810962501, -1.166474544107111377, 0.4182417262808778013 ) ) ;
#28921=CARTESIAN_POINT ( 'NONE',  ( 0.1882419910544414765, -0.5601865779007185742, 0.2791098525572430766 ) ) ;
#28924=CARTESIAN_POINT ( 'NONE',  ( 0.3363348836112549645, -1.066364408820902998, 0.7268484058858328822 ) ) ;
#28927=CARTESIAN_POINT ( 'NONE',  ( 0.3459602365858145401, -1.002069219538038736, 0.6041729112776661470 ) ) ;
#28930=CARTESIAN_POINT ( 'NONE',  ( 0.5509968806096897653, -1.899553531783569449, 0.5182417262812423209 ) ) ;
#28933=CARTESIAN_POINT ( 'NONE',  ( 0.4136565266000814534, -1.589555752243668962, 0.5742607991556297753 ) ) ;
#28934=CARTESIAN_POINT ( 'NONE',  ( 0.08600443180144776156, -0.7812038045049116697, 0.06558878796052790283 ) ) ;
#28935=FACE_OUTER_BOUND ( 'NONE', #5320, .T. ) ;
#28936=CARTESIAN_POINT ( 'NONE',  ( 0.06911925242283332993, -0.5409396888079850418, 0.1263946519415101166 ) ) ;
#28937=EDGE_LOOP ( 'NONE', ( #10673, #23347 ) ) ;
#28939=EDGE_LOOP ( 'NONE', ( #37724, #35663, #7578, #5752 ) ) ;
#28940=CARTESIAN_POINT ( 'NONE',  ( 0.4898967846823991668, -1.079624215837351242, 0.5968486766476291949 ) ) ;
#28941=CARTESIAN_POINT ( 'NONE',  ( 0.5664215386550598419, -1.503089260598527321, 0.5634370993589044030 ) ) ;
#28943=CARTESIAN_POINT ( 'NONE',  ( 0.07172784347629639068, -1.333591952913690593, 0.4986392271462748438 ) ) ;
#28947=ORIENTED_EDGE ( 'NONE', *, *, #39069, .F. ) ;
#28950=CARTESIAN_POINT ( 'NONE',  ( 0.3262646141370696418, -1.756421352762273846, 0.5762462443359027686 ) ) ;
#28951=CARTESIAN_POINT ( 'NONE',  ( 0.08657376948451865617, -0.8126112693459484060, 0.01976600836222000904 ) ) ;
#28952=CARTESIAN_POINT ( 'NONE',  ( 0.5598795747092503161, -1.507486333647360510, 0.5722829373276135945 ) ) ;
#28955=CARTESIAN_POINT ( 'NONE',  ( 0.1102224200671288595, -1.400663116118479490, 0.6358304045325068321 ) ) ;
#28958=CARTESIAN_POINT ( 'NONE',  ( 0.5965761245944036784, -1.493465029535157029, 0.5182417262812423209 ) ) ;
#28960=CARTESIAN_POINT ( 'NONE',  ( 0.4744622997635568606, -1.208877113836489547, 0.5084237165177825091 ) ) ;
#28962=CARTESIAN_POINT ( 'NONE',  ( 0.2426062050407847281, -1.584949062848913348, 0.8214247301831154591 ) ) ;
#28965=AXIS2_PLACEMENT_3D ( 'NONE', #28143, #5284, #33686 ) ;
#28977=CARTESIAN_POINT ( 'NONE',  ( 0.4451373613274108854, -1.213283134829647114, 0.7682095407564263345 ) ) ;
#28981=CARTESIAN_POINT ( 'NONE',  ( 0.4865355734717750624, -1.097175741254786452, 0.7494200075675998551 ) ) ;
#28986=CARTESIAN_POINT ( 'NONE',  ( 0.2904216923373793002, -1.605717452676975077, 0.8056108489146471818 ) ) ;
#28988=CARTESIAN_POINT ( 'NONE',  ( 0.1117172404438186717, -0.8790865271448059515, -0.001403887437530376659 ) ) ;
#28992=ORIENTED_EDGE ( 'NONE', *, *, #18311, .F. ) ;
#28996=CARTESIAN_POINT ( 'NONE',  ( 0.1109049718728861156, -0.9286333055842311834, 0.1443021394692906578 ) ) ;
#28998=CARTESIAN_POINT ( 'NONE',  ( 0.5582418957589161401, -1.431870684052794385, 0.7524718376146050103 ) ) ;
#29000=CARTESIAN_POINT ( 'NONE',  ( 0.3828917794701993671, -1.259344239476607452, 0.5976400823309563348 ) ) ;
#29013=CARTESIAN_POINT ( 'NONE',  ( 0.1808332695554492053, -0.4986102965419587085, 0.1174482592749270665 ) ) ;
#29023=CARTESIAN_POINT ( 'NONE',  ( 0.4688079631758284016, -1.116561345930851656, 0.5688791344137259509 ) ) ;
#29024=CARTESIAN_POINT ( 'NONE',  ( 0.2662821865085873707, -1.672322712245089882, 0.6834728152926629052 ) ) ;
#29025=ADVANCED_FACE ( 'NONE', ( #35839 ), #23914, .T. ) ;
#29027=CARTESIAN_POINT ( 'NONE',  ( 0.1313240903384290670, -0.5586677835130641201, 0.1977070789115515925 ) ) ;
#29032=EDGE_LOOP ( 'NONE', ( #28331, #12814, #5341, #7780, #34339, #18194 ) ) ;
#29033=ORIENTED_EDGE ( 'NONE', *, *, #32055, .F. ) ;
#29042=ORIENTED_EDGE ( 'NONE', *, *, #13025, .F. ) ;
#29043=CARTESIAN_POINT ( 'NONE',  ( 0.08560004179328287166, -0.7895966635341131745, 0.1829049723430900276 ) ) ;
#29044=CARTESIAN_POINT ( 'NONE',  ( 0.08990936761269285871, -0.5436479961250832993, 0.1408780685345787931 ) ) ;
#29045=CARTESIAN_POINT ( 'NONE',  ( 0.5285810829098267494, -1.495792263264798860, 0.7113523899947146178 ) ) ;
#29047=ADVANCED_FACE ( 'NONE', ( #26021 ), #5082, .T. ) ;
#29053=CARTESIAN_POINT ( 'NONE',  ( 0.2279584765017062808, -0.8282534240391157265, 0.6402501348084159716 ) ) ;
#29054=CARTESIAN_POINT ( 'NONE',  ( -1.627503956099404352E-05, -0.7038055984667742626, -0.1033392639723096362 ) ) ;
#29055=B_SPLINE_CURVE_WITH_KNOTS ( 'NONE', 3,
 ( #33031, #23794, #26687, #36316 ),
 .UNSPECIFIED., .F., .F.,
 ( 4, 4 ),
 ( 0.003768912384866303020, 0.004058730305933713235 ),
 .UNSPECIFIED. ) ;
#29059=CARTESIAN_POINT ( 'NONE',  ( 0.1362517741244128056, -1.308408735431443093, 0.8505046261270597929 ) ) ;
#29060=CARTESIAN_POINT ( 'NONE',  ( 0.4898164652207312453, -1.090206986453526872, 0.6335228833721541220 ) ) ;
#29073=CARTESIAN_POINT ( 'NONE',  ( 0.08544226047625283482, -0.8041154030964468014, 0.1055056433848701458 ) ) ;
#29074=VERTEX_POINT ( 'NONE', #22731 ) ;
#29075=CARTESIAN_POINT ( 'NONE',  ( 0.4970273525888077026, -1.079783658718535877, 0.3157417262808778213 ) ) ;
#29076=ADVANCED_FACE ( 'NONE', ( #38539 ), #15121, .T. ) ;
#29077=CARTESIAN_POINT ( 'NONE',  ( 0.6145270684574122289, -1.293427813764720824, 0.7790094959668801833 ) ) ;
#29084=CARTESIAN_POINT ( 'NONE',  ( 0.6835481475269494789, -1.411548362123641098, 0.6057417262805111502 ) ) ;
#29088=CARTESIAN_POINT ( 'NONE',  ( 0.008360580759598704517, -0.6769370512592758349, -0.01223308801627121661 ) ) ;
#29089=CARTESIAN_POINT ( 'NONE',  ( 0.1843596291497116846, -0.8425532430273316997, 0.6072516196132035082 ) ) ;
#29091=CARTESIAN_POINT ( 'NONE',  ( 0.0004836969055040355077, -0.4494541051812985799, 0.2297460066914376320 ) ) ;
#29093=CARTESIAN_POINT ( 'NONE',  ( 0.1472789844204966947, -0.7831370643385257013, 0.6122178998912563008 ) ) ;
#29095=CARTESIAN_POINT ( 'NONE',  ( 0.07642826425048794559, -0.9569100421164248305, 0.8158992369460693617 ) ) ;
#29104=CARTESIAN_POINT ( 'NONE',  ( 0.1153471661800037629, -0.4465907051537517658, 0.1365881794216603218 ) ) ;
#29110=CARTESIAN_POINT ( 'NONE',  ( 0.1943341254738605584, -0.5992045414336306663, 0.2618067726929366734 ) ) ;
#29112=CARTESIAN_POINT ( 'NONE',  ( 0.06493940447479917832, -1.341270385318114045, 0.5780714437177661980 ) ) ;
#29113=AXIS2_PLACEMENT_3D ( 'NONE', #39890, #8209, #26544 ) ;
#29117=CARTESIAN_POINT ( 'NONE',  ( 0.2101388107736075483, -0.9193160678141170106, 0.6295685468235113769 ) ) ;
#29119=CARTESIAN_POINT ( 'NONE',  ( 0.7066109249242027435, -1.499057094600571238, 0.5182417262806440217 ) ) ;
#29124=CARTESIAN_POINT ( 'NONE',  ( 0.09027510456495055347, -0.5695500423695799563, 0.1845836558560018104 ) ) ;
#29128=B_SPLINE_CURVE_WITH_KNOTS ( 'NONE', 3,
 ( #20716, #33247, #30162, #1989, #14512, #27078, #39611, #11446, #24013, #28100 ),
 .UNSPECIFIED., .F., .F.,
 ( 4, 2, 2, 2, 4 ),
 ( 0.000000000000000000, 0.0004980634626862015047, 0.0009961269253724030093, 0.001494190388058604622, 0.001992253850744806019 ),
 .UNSPECIFIED. ) ;
#29130=CARTESIAN_POINT ( 'NONE',  ( 0.1050700346926137646, -0.9324735298191096922, 0.6219226790663787696 ) ) ;
#29134=CARTESIAN_POINT ( 'NONE',  ( 0.5959315179729184342, -1.587052097778459236, 0.4182417262808776903 ) ) ;
#29135=CARTESIAN_POINT ( 'NONE',  ( 0.1856533569311497323, -0.7573055082216308964, 0.1457185332388697685 ) ) ;
#29136=CARTESIAN_POINT ( 'NONE',  ( 0.4466969641109395095, -1.208888639451673130, 0.6872926701319916898 ) ) ;
#29138=CARTESIAN_POINT ( 'NONE',  ( 0.3088664963667265839, -1.757905065063136263, 0.5295467280985149960 ) ) ;
#29143=ORIENTED_EDGE ( 'NONE', *, *, #28134, .T. ) ;
#29144=CARTESIAN_POINT ( 'NONE',  ( 0.3372045214619368569, -1.404289603606768022, 0.8754725392422132435 ) ) ;
#29145=CARTESIAN_POINT ( 'NONE',  ( 0.08513964112126702621, -0.8107931711784008844, 0.1400984422957800846 ) ) ;
#29146=CARTESIAN_POINT ( 'NONE',  ( 0.1978587402095110526, -0.5849795632144990654, 0.3178455878192493200 ) ) ;
#29148=ORIENTED_EDGE ( 'NONE', *, *, #18835, .F. ) ;
#29152=CARTESIAN_POINT ( 'NONE',  ( 0.06936654275873489761, -1.327133429011184917, 0.5458395137742713121 ) ) ;
#29153=CARTESIAN_POINT ( 'NONE',  ( 0.1194264420602569737, -0.5625551924984868446, 0.2197023614733592256 ) ) ;
#29155=CARTESIAN_POINT ( 'NONE',  ( 0.1874546992375723808, -0.6895993665818519469, 0.05733668763868348534 ) ) ;
#29159=CARTESIAN_POINT ( 'NONE',  ( 0.1859644761936219692, -0.7910310107535581947, 0.1899855147966034163 ) ) ;
#29160=CARTESIAN_POINT ( 'NONE',  ( 0.4062230848227149638, -1.145582794160931117, 0.4248905050063955802 ) ) ;
#29162=CARTESIAN_POINT ( 'NONE',  ( 0.08630618708051779331, -0.7262393365227618469, 0.1454069901622962735 ) ) ;
#29164=B_SPLINE_CURVE_WITH_KNOTS ( 'NONE', 3,
 ( #35170, #13564, #19932, #25926, #34747, #19132, #38449, #10464, #12962, #31670 ),
 .UNSPECIFIED., .F., .F.,
 ( 4, 2, 2, 2, 4 ),
 ( 0.001190081892692469809, 0.001790126153740256160, 0.002390170414788042510, 0.002990214675835828860, 0.003590258936883615210 ),
 .UNSPECIFIED. ) ;
#29165=CARTESIAN_POINT ( 'NONE',  ( 0.7032651991748780640, -1.440401145529036642, 0.7869155231269625572 ) ) ;
#29169=CARTESIAN_POINT ( 'NONE',  ( 0.07779920321647403048, -1.322114474344633583, 0.5682417262808776570 ) ) ;
#29174=CARTESIAN_POINT ( 'NONE',  ( 0.6960334162051958762, -1.427192076786115926, 0.4182417262808776348 ) ) ;
#29176=CARTESIAN_POINT ( 'NONE',  ( 0.2493678129588278725, -1.619726033520551667, 0.7664167198318853069 ) ) ;
#29177=CARTESIAN_POINT ( 'NONE',  ( -0.0004140221094746326480, -0.9366944287225720256, 0.1292664348825115495 ) ) ;
#29182=CARTESIAN_POINT ( 'NONE',  ( 0.3584893225414327311, -1.160935888217208944, 0.4273648005544712358 ) ) ;
#29184=AXIS2_PLACEMENT_3D ( 'NONE', #35704, #20089, #23992 ) ;
#29192=CARTESIAN_POINT ( 'NONE',  ( 0.5056812288904104502, -1.307114837766834903, 0.7688671359748000533 ) ) ;
#29195=CARTESIAN_POINT ( 'NONE',  ( 0.5342447626335863342, -1.156090923338821463, 0.6541422520001994867 ) ) ;
#29196=CIRCLE ( 'NONE', #26599, 0.009999999999999991535 ) ;
#29199=CARTESIAN_POINT ( 'NONE',  ( 0.5776223404472408118, -1.608891578473971462, 0.4473154535768434914 ) ) ;
#29202=CARTESIAN_POINT ( 'NONE',  ( 0.2958245360769962695, -1.526781842427403779, 0.8634596908947912430 ) ) ;
#29204=CARTESIAN_POINT ( 'NONE',  ( 0.1126380441730984588, -0.7649468025915582281, -0.08306241175244397090 ) ) ;
#29207=ORIENTED_EDGE ( 'NONE', *, *, #25749, .T. ) ;
#29208=CARTESIAN_POINT ( 'NONE',  ( 0.5446892099791311725, -1.168309311726712929, 0.5668322337678470824 ) ) ;
#29209=CARTESIAN_POINT ( 'NONE',  ( 0.1862143093560918450, -0.9153542374866598941, 0.1449575636331434381 ) ) ;
#29211=CARTESIAN_POINT ( 'NONE',  ( 0.5846648009247458200, -1.436025231029266491, 0.7313505297771951685 ) ) ;
#29212=CARTESIAN_POINT ( 'NONE',  ( 0.1431253995614544250, -0.8748228831234901026, 0.5195852956218338647 ) ) ;
#29215=EDGE_CURVE ( 'NONE', #33041, #25042, #33785, .T. ) ;
#29221=CARTESIAN_POINT ( 'NONE',  ( 0.6580168967375891187, -1.537959750076741905, 0.4238314998512365261 ) ) ;
#29222=CARTESIAN_POINT ( 'NONE',  ( 0.5959315179729184342, -1.587052097778459236, 0.4182417262808776903 ) ) ;
#29223=CARTESIAN_POINT ( 'NONE',  ( 0.3223881462519361807, -1.760756727098002905, 0.4929000792678752130 ) ) ;
#29231=CARTESIAN_POINT ( 'NONE',  ( 0.4542745521636228356, -1.690364615762230072, 0.4457110224561552925 ) ) ;
#29236=VERTEX_POINT ( 'NONE', #13642 ) ;
#29237=CARTESIAN_POINT ( 'NONE',  ( 0.2656489473450271976, -1.672876873347360460, 0.5357873754474390404 ) ) ;
#29239=CARTESIAN_POINT ( 'NONE',  ( 0.4665068745543000661, -1.281967417980122592, 0.8176874307884230975 ) ) ;
#29240=CARTESIAN_POINT ( 'NONE',  ( 0.5454073695792218679, -1.172337910823015861, 0.5979107612308603992 ) ) ;
#29246=CARTESIAN_POINT ( 'NONE',  ( 0.5981247542016078222, -1.393184347378918719, 0.8655563894600949437 ) ) ;
#29249=CARTESIAN_POINT ( 'NONE',  ( -0.01381286397089885078, -0.5423028182772705597, 0.2346020896048880977 ) ) ;
#29255=CARTESIAN_POINT ( 'NONE',  ( 0.1053302763654986457, -0.8311093529158266602, 0.3669983993270940492 ) ) ;
#29259=CARTESIAN_POINT ( 'NONE',  ( 0.5403123773656385298, -1.518157346897373472, 0.6083719484155812873 ) ) ;
#29260=ORIENTED_EDGE ( 'NONE', *, *, #19478, .F. ) ;
#29263=CARTESIAN_POINT ( 'NONE',  ( 0.7154111682914670034, -1.479334727086170531, 0.5070875326645477577 ) ) ;
#29265=DIRECTION ( 'NONE',  ( 0.9998941247116546194, -0.01455087607601020412, 0.0001066420868422379633 ) ) ;
#29267=FACE_OUTER_BOUND ( 'NONE', #5509, .T. ) ;
#29270=CARTESIAN_POINT ( 'NONE',  ( 0.6077303093371694276, -1.473904537801408399, 0.6398553165839666601 ) ) ;
#29271=CARTESIAN_POINT ( 'NONE',  ( 0.01162314945304296701, -0.7953763623839829044, -0.08968356552621570277 ) ) ;
#29272=CARTESIAN_POINT ( 'NONE',  ( 0.1335939600180593712, -0.7447735389487355473, 0.5690569422650127995 ) ) ;
#29273=B_SPLINE_CURVE_WITH_KNOTS ( 'NONE', 3,
 ( #31072, #2492, #27582, #39713, #2685, #8853, #15443, #37435, #15227, #11741 ),
 .UNSPECIFIED., .F., .F.,
 ( 4, 2, 2, 2, 4 ),
 ( 0.002284120846990289264, 0.002652607256290875643, 0.003021093665591462023, 0.003389580074892048402, 0.003758066484192634782 ),
 .UNSPECIFIED. ) ;
#29277=CARTESIAN_POINT ( 'NONE',  ( 0.4089992519647981384, -1.131314579718122992, 0.3157417262808777658 ) ) ;
#29281=CARTESIAN_POINT ( 'NONE',  ( -0.002783323111321702164, -0.8122190247268278318, 0.2436509486217987297 ) ) ;
#29282=CARTESIAN_POINT ( 'NONE',  ( 0.3243638931714790674, -0.9652511992726795498, 0.5977393664509621507 ) ) ;
#29285=CARTESIAN_POINT ( 'NONE',  ( 0.3817504269947758488, -1.726033828776070367, 0.4251703030630866742 ) ) ;
#29287=FACE_OUTER_BOUND ( 'NONE', #35445, .T. ) ;
#29292=CARTESIAN_POINT ( 'NONE',  ( 0.002326877264082053299, -0.5233753183007167076, 0.1831555727087032792 ) ) ;
#29293=CARTESIAN_POINT ( 'NONE',  ( 0.1840595033465176056, -0.8547675690073376353, 0.1457166466292989515 ) ) ;
#29296=CARTESIAN_POINT ( 'NONE',  ( 0.6622529324379804461, -1.370658042826599310, 0.7087354899337895420 ) ) ;
#29301=FACE_OUTER_BOUND ( 'NONE', #16048, .T. ) ;
#29302=CARTESIAN_POINT ( 'NONE',  ( 0.6059691746655119227, -1.480133143157562170, 0.5526975506195443977 ) ) ;
#29305=ORIENTED_EDGE ( 'NONE', *, *, #5635, .F. ) ;
#29306=CARTESIAN_POINT ( 'NONE',  ( 0.5118594077320766100, -1.202344868804445133, 1.007689851825548599 ) ) ;
#29307=AXIS2_PLACEMENT_3D ( 'NONE', #15513, #17767, #36504 ) ;
#29308=CARTESIAN_POINT ( 'NONE',  ( 0.09436846326521548811, -0.6977451578140484445, 0.2870226784748305393 ) ) ;
#29309=CARTESIAN_POINT ( 'NONE',  ( 0.001484853620285140697, -0.4699967301967150068, 0.2916140860605750951 ) ) ;
#29310=CARTESIAN_POINT ( 'NONE',  ( 0.4566189328666658831, -1.463090425276903250, 0.7988651862389967162 ) ) ;
#29311=CARTESIAN_POINT ( 'NONE',  ( 0.1136081630506033391, -0.6096919713534713070, -0.08294989974448961634 ) ) ;
#29313=CARTESIAN_POINT ( 'NONE',  ( 0.3801146823547868481, -1.145807599758760897, 0.5916166056748334290 ) ) ;
#29315=ORIENTED_EDGE ( 'NONE', *, *, #33368, .T. ) ;
#29317=CARTESIAN_POINT ( 'NONE',  ( 0.3218915951663034458, -1.643224469256787446, 0.5371356550339121405 ) ) ;
#29318=CARTESIAN_POINT ( 'NONE',  ( 0.1271493835291065966, -0.5197209161013818246, 0.3904091046342937910 ) ) ;
#29322=( BOUNDED_SURFACE ( )  B_SPLINE_SURFACE ( 3, 2, ( 
 ( #29104, #37536, #22155 ),
 ( #12451, #19044, #6672 ),
 ( #31791, #575, #25433 ),
 ( #13070, #25622, #38155 ),
 ( #22547, #28497, #35077 ),
 ( #6880, #18852, #19458 ),
 ( #35284, #38353, #31993 ),
 ( #31395, #15739, #28288 ),
 ( #10191, #28897, #759 ),
 ( #25834, #12875, #7079 ),
 ( #31576, #25003, #12649 ),
 ( #9578, #3395, #15951 ),
 ( #7269, #26431, #35684 ),
 ( #29711, #32990, #36275 ),
 ( #20457, #33208, #10579 ),
 ( #23153, #1556, #38968 ),
 ( #26045, #4588, #23370 ),
 ( #7484, #29510, #35468 ),
 ( #17372, #5013, #39184 ),
 ( #20064, #22951, #32788 ),
 ( #10797, #8097, #17160 ),
 ( #1770, #10387, #20674 ),
 ( #14076, #17580, #966 ),
 ( #29318, #20266, #36084 ),
 ( #7700, #35892, #11193 ),
 ( #39373, #19847, #14281 ),
 ( #26653, #11010, #32379 ),
 ( #26231, #1349, #38752 ),
 ( #4797, #13476, #23566 ),
 ( #7886, #29928, #26846 ),
 ( #4206, #32595, #13857 ),
 ( #4408, #38564, #23756 ),
 ( #13665, #16967, #16770 ),
 ( #1165, #34206, #30122 ),
 ( #14894, #6017, #23968 ),
 ( #2745, #2144, #30922 ),
 ( #24569, #20881, #24173 ),
 ( #21068, #36497, #33403 ),
 ( #21277, #27849, #5210 ),
 ( #5620, #1953, #24357 ),
 ( #18176, #2352, #39781 ),
 ( #24774, #14468, #15294 ),
 ( #27452, #39977, #8311 ),
 ( #33814, #8701, #12214 ),
 ( #30729, #2550, #17764 ),
 ( #30316, #14682, #40389 ),
 ( #36890, #39564, #37099 ),
 ( #15087, #9110, #11612 ),
 ( #18374, #8914, #27251 ),
 ( #5404, #21492, #36697 ),
 ( #5815, #27035, #11396 ),
 ( #37297, #21676, #34011 ),
 ( #8504, #33595, #17967 ),
 ( #11798, #12004, #30528 ),
 ( #27643, #40173, #3554 ),
 ( #19195, #34416, #37917 ),
 ( #22493, #318, #6232 ),
 ( #9727, #22296, #3340 ),
 ( #34811, #40585, #9924 ),
 ( #6616, #9310, #28061 ),
 ( #15900, #15508, #25783 ),
 ( #13027, #3766, #25383 ),
 ( #28856, #12823, #16319 ),
 ( #19412, #35018, #31735 ),
 ( #3153, #24959, #22709 ),
 ( #34624, #10135, #2956 ),
 ( #16123, #25575, #12604 ),
 ( #12407, #15693, #6830 ),
 ( #28661, #37489, #37703 ),
 ( #530, #38105, #28445 ),
 ( #31946, #21889, #715 ),
 ( #18800, #31351, #35240 ),
 ( #28243, #38303, #108 ),
 ( #13216, #18582, #31140 ),
 ( #6425, #25164, #9526 ),
 ( #22104, #18993, #31526 ),
 ( #32332, #13815, #11145 ),
 ( #20217, #32542, #23704 ),
 ( #17115, #20410, #19795 ),
 ( #26189, #1507, #38519 ) ),
 .UNSPECIFIED., .F., .F., .T. ) 
 B_SPLINE_SURFACE_WITH_KNOTS ( ( 4, 2, 2, 2, 2, 2, 2, 2, 2, 2, 2, 2, 2, 2, 2, 2, 2, 2, 2, 2, 2, 2, 2, 2, 2, 2, 2, 2, 2, 2, 2, 2, 2, 2, 2, 2, 2, 2, 2, 4 ),
 ( 3, 3 ),
 ( 0.006927710299821351891, 0.007080480144256291047, 0.007156865066473760625, 0.007175961297028127586, 0.007195057527582495414, 0.007233249988691230203, 0.007538789677561109383, 0.008149869055300866874, 0.009372027810780381857, 0.009983107188520138481, 0.01059418656625989684, 0.01181634532173941182, 0.01426066283269844179, 0.01548282158817795677, 0.01670498034365747175, 0.01914929785461650172, 0.02037145661009601844, 0.02159361536557553168, 0.02403793287653456165, 0.02526009163201407837, 0.02648225038749359161, 0.02892656789845262158, 0.03137088540941165155, 0.03381520292037068498, 0.03625952043132971148, 0.03748167918680922472, 0.03870383794228873797, 0.03992599669776825122, 0.04114815545324777141, 0.04175923483098753497, 0.04237031420872729159, 0.04298139358646704822, 0.04359247296420680484, 0.04481463171968631809, 0.04542571109742607471, 0.04573125078629595303, 0.04580763570851342781, 0.04584582816962216173, 0.04588402063073089565, 0.04603679047516583134 ),
 ( 0.000000000000000000, 1.000000000000000000 ),
 .UNSPECIFIED. ) 
 GEOMETRIC_REPRESENTATION_ITEM ( )  RATIONAL_B_SPLINE_SURFACE ( (
 ( 1.000000000000000000, 0.7702110884164732330, 1.000000000000000000),
 ( 1.000000000000000000, 0.7702110884164732330, 1.000000000000000000),
 ( 1.000000000000000000, 0.7702110884164714566, 1.000000000000000000),
 ( 1.000000000000000000, 0.7702110884164714566, 1.000000000000000000),
 ( 1.000000000000000000, 0.7702110884164720117, 1.000000000000000000),
 ( 1.000000000000000000, 0.7702110884164720117, 1.000000000000000000),
 ( 1.000000000000000000, 0.7702110011759223385, 1.000000000000000000),
 ( 1.000000000000000000, 0.7702104367782812711, 1.000000000000000000),
 ( 1.000000000000000000, 0.7702099955263094211, 1.000000000000000000),
 ( 1.000000000000000000, 0.7702082218146070192, 1.000000000000000000),
 ( 1.000000000000000000, 0.7702064393915036833, 1.000000000000000000),
 ( 1.000000000000000000, 0.7701856336384715895, 1.000000000000000000),
 ( 1.000000000000000000, 0.7701341339086081872, 1.000000000000000000),
 ( 1.000000000000000000, 0.7699716772124094444, 1.000000000000000000),
 ( 1.000000000000000000, 0.7698275467342896583, 1.000000000000000000),
 ( 1.000000000000000000, 0.7695145108938888923, 1.000000000000000000),
 ( 1.000000000000000000, 0.7694543563866118596, 1.000000000000000000),
 ( 1.000000000000000000, 0.7690885663133745220, 1.000000000000000000),
 ( 1.000000000000000000, 0.7689098704262390394, 1.000000000000000000),
 ( 1.000000000000000000, 0.7684714123184787082, 1.000000000000000000),
 ( 1.000000000000000000, 0.7682081441206239925, 1.000000000000000000),
 ( 1.000000000000000000, 0.7673848213495205739, 1.000000000000000000),
 ( 1.000000000000000000, 0.7667110773309444571, 1.000000000000000000),
 ( 1.000000000000000000, 0.7644349880097887073, 1.000000000000000000),
 ( 1.000000000000000000, 0.7629103163539596721, 1.000000000000000000),
 ( 1.000000000000000000, 0.7602566924737247378, 1.000000000000000000),
 ( 1.000000000000000000, 0.7593162002605474692, 1.000000000000000000),
 ( 1.000000000000000000, 0.7573931270347130651, 1.000000000000000000),
 ( 1.000000000000000000, 0.7564157440002493571, 1.000000000000000000),
 ( 1.000000000000000000, 0.7534999497245773448, 1.000000000000000000),
 ( 1.000000000000000000, 0.7515885138869485838, 1.000000000000000000),
 ( 1.000000000000000000, 0.7495871733758280309, 1.000000000000000000),
 ( 1.000000000000000000, 0.7490774071070243068, 1.000000000000000000),
 ( 1.000000000000000000, 0.7486382088202092611, 1.000000000000000000),
 ( 1.000000000000000000, 0.7486976975356955943, 1.000000000000000000),
 ( 1.000000000000000000, 0.7501897554486547381, 1.000000000000000000),
 ( 1.000000000000000000, 0.7529466885742388538, 1.000000000000000000),
 ( 1.000000000000000000, 0.7614317847769825898, 1.000000000000000000),
 ( 1.000000000000000000, 0.7649793793770901518, 1.000000000000000000),
 ( 1.000000000000000000, 0.7733644470982655728, 1.000000000000000000),
 ( 1.000000000000000000, 0.7782111082216958131, 1.000000000000000000),
 ( 1.000000000000000000, 0.7935801609140271662, 1.000000000000000000),
 ( 1.000000000000000000, 0.8047319212507089148, 1.000000000000000000),
 ( 1.000000000000000000, 0.8229932177232615054, 1.000000000000000000),
 ( 1.000000000000000000, 0.8301201759576161132, 1.000000000000000000),
 ( 1.000000000000000000, 0.8391316605326407663, 1.000000000000000000),
 ( 1.000000000000000000, 0.8411418536465049556, 1.000000000000000000),
 ( 1.000000000000000000, 0.8403510782710301719, 1.000000000000000000),
 ( 1.000000000000000000, 0.8376700127300911181, 1.000000000000000000),
 ( 1.000000000000000000, 0.8302417975051545884, 1.000000000000000000),
 ( 1.000000000000000000, 0.8271837635025202085, 1.000000000000000000),
 ( 1.000000000000000000, 0.8196313788825587698, 1.000000000000000000),
 ( 1.000000000000000000, 0.8151231434854736557, 1.000000000000000000),
 ( 1.000000000000000000, 0.8044346982436086924, 1.000000000000000000),
 ( 1.000000000000000000, 0.7981958681030024705, 1.000000000000000000),
 ( 1.000000000000000000, 0.7834537592509257520, 1.000000000000000000),
 ( 1.000000000000000000, 0.7750610009823194479, 1.000000000000000000),
 ( 1.000000000000000000, 0.7615137475724482741, 1.000000000000000000),
 ( 1.000000000000000000, 0.7568191938289150489, 1.000000000000000000),
 ( 1.000000000000000000, 0.7477386341990411855, 1.000000000000000000),
 ( 1.000000000000000000, 0.7433521509119807025, 1.000000000000000000),
 ( 1.000000000000000000, 0.7352470023408808064, 1.000000000000000000),
 ( 1.000000000000000000, 0.7315263130049088902, 1.000000000000000000),
 ( 1.000000000000000000, 0.7249624713081709304, 1.000000000000000000),
 ( 1.000000000000000000, 0.7221161546641846618, 1.000000000000000000),
 ( 1.000000000000000000, 0.7150846530265827505, 1.000000000000000000),
 ( 1.000000000000000000, 0.7122753070958832700, 1.000000000000000000),
 ( 1.000000000000000000, 0.7098586832190030282, 1.000000000000000000),
 ( 1.000000000000000000, 0.7093529624755150476, 1.000000000000000000),
 ( 1.000000000000000000, 0.7089420370521081205, 1.000000000000000000),
 ( 1.000000000000000000, 0.7088634414763608227, 1.000000000000000000),
 ( 1.000000000000000000, 0.7088270497185857888, 1.000000000000000000),
 ( 1.000000000000000000, 0.7088245591381706623, 1.000000000000000000),
 ( 1.000000000000000000, 0.7088184571567831549, 1.000000000000000000),
 ( 1.000000000000000000, 0.7087890813305628424, 1.000000000000000000),
 ( 1.000000000000000000, 0.7087532025278564518, 1.000000000000000000),
 ( 1.000000000000000000, 0.7087352638298917151, 1.000000000000000000),
 ( 1.000000000000000000, 0.7086455738595582865, 1.000000000000000000),
 ( 1.000000000000000000, 0.7085738331447311023, 1.000000000000000000),
 ( 1.000000000000000000, 0.7085021037179024539, 1.000000000000000000) ) ) 
 REPRESENTATION_ITEM ( '' )  SURFACE ( )  );
#29327=CYLINDRICAL_SURFACE ( 'NONE', #13271, 0.03749999999977557397 ) ;
#29328=CARTESIAN_POINT ( 'NONE',  ( 0.4763737863547038431, -1.078928959615589100, 0.8012595312036666639 ) ) ;
#29329=CARTESIAN_POINT ( 'NONE',  ( 0.5161351604351521738, -1.173682792831946653, 0.4572090867639507783 ) ) ;
#29333=CARTESIAN_POINT ( 'NONE',  ( 0.3303154085096511317, -1.292090888104762136, 0.5056921649335895941 ) ) ;
#29334=CARTESIAN_POINT ( 'NONE',  ( 0.3836975776547298378, -1.127091824346511784, 0.7305314326323552043 ) ) ;
#29339=ORIENTED_EDGE ( 'NONE', *, *, #32903, .F. ) ;
#29341=CARTESIAN_POINT ( 'NONE',  ( 0.5382307432915078849, -1.161159458769174257, 0.5682417262808779901 ) ) ;
#29345=CARTESIAN_POINT ( 'NONE',  ( 0.05555397280954740835, -0.8368505189396914234, 0.1457185332388726828 ) ) ;
#29352=CARTESIAN_POINT ( 'NONE',  ( 0.4906695346912424704, -1.277893297672507034, 0.5826988468483825789 ) ) ;
#29353=CARTESIAN_POINT ( 'NONE',  ( 0.01173648626945268322, -0.6872203660140956405, -0.1131804859792006068 ) ) ;
#29356=EDGE_LOOP ( 'NONE', ( #8124, #27467, #20263, #31128 ) ) ;
#29358=EDGE_LOOP ( 'NONE', ( #33874, #35414, #30227, #4043, #1965, #3895 ) ) ;
#29359=CARTESIAN_POINT ( 'NONE',  ( 0.4129595026082335529, -1.589300418172787666, 0.5636185827902593370 ) ) ;
#29360=CARTESIAN_POINT ( 'NONE',  ( 0.08589675992784878700, -0.7862823833295263798, 0.07193548024800379415 ) ) ;
#29362=CARTESIAN_POINT ( 'NONE',  ( 0.1242151342619402660, -1.295214500222888532, 0.4951799652504541571 ) ) ;
#29367=CARTESIAN_POINT ( 'NONE',  ( 0.5619293104143906481, -1.477014897282695527, 0.7041609149778610410 ) ) ;
#29372=CARTESIAN_POINT ( 'NONE',  ( 0.1852724517579373009, -0.8388905295248703098, 0.1482875376949696067 ) ) ;
#29375=CARTESIAN_POINT ( 'NONE',  ( 0.4520951681308373327, -1.683581237827290522, 0.6019770548139172783 ) ) ;
#29377=CARTESIAN_POINT ( 'NONE',  ( 0.7308477326836637644, -1.487300591783543124, 0.7156276807793737760 ) ) ;
#29383=CARTESIAN_POINT ( 'NONE',  ( 0.1849973320602424365, -0.7741433581987759993, -0.0006474567843166786907 ) ) ;
#29385=CARTESIAN_POINT ( 'NONE',  ( 0.08222542156928025481, -1.327483614382551247, 0.4683366274853974498 ) ) ;
#29386=CARTESIAN_POINT ( 'NONE',  ( 0.1287314663193102893, -1.150224043500909454, 0.9169127589950010204 ) ) ;
#29393=EDGE_CURVE ( 'NONE', #37794, #23886, #32455, .T. ) ;
#29396=CARTESIAN_POINT ( 'NONE',  ( 0.2316917763911649497, -1.232208891764917880, 0.5707417262808780478 ) ) ;
#29399=DIRECTION ( 'NONE',  ( 0.9998941247116546194, -0.01455087607601020239, 0.0001066420868422379362 ) ) ;
#29400=CARTESIAN_POINT ( 'NONE',  ( 0.3473220467592102456, -1.065780441090952380, 0.7836742237912034392 ) ) ;
#29403=CARTESIAN_POINT ( 'NONE',  ( 0.5291583206849711507, -1.148825028536799131, 0.6606389499358795714 ) ) ;
#29404=CARTESIAN_POINT ( 'NONE',  ( 0.1153471662232078698, -0.4465907064269051263, 0.1457432652200511269 ) ) ;
#29405=ORIENTED_EDGE ( 'NONE', *, *, #3469, .F. ) ;
#29407=CARTESIAN_POINT ( 'NONE',  ( 0.3282947148789615577, -1.639384686062084873, 0.5920012551663509370 ) ) ;
#29410=CARTESIAN_POINT ( 'NONE',  ( 0.1436225252650951412, -1.283668529478381393, 0.4687417262808780127 ) ) ;
#29414=CARTESIAN_POINT ( 'NONE',  ( 0.2325478330093098400, -0.9400742174009236729, 0.4405423773235361273 ) ) ;
#29415=CARTESIAN_POINT ( 'NONE',  ( 0.1876095839365603535, -1.270310460104811856, 0.4182417262808778013 ) ) ;
#29417=CARTESIAN_POINT ( 'NONE',  ( 0.2325139813020924151, -1.016947346993363421, 0.7211346862436321947 ) ) ;
#29420=CARTESIAN_POINT ( 'NONE',  ( 0.4753071910876713324, -1.208389221472485398, 0.5182417262812494263 ) ) ;
#29427=CARTESIAN_POINT ( 'NONE',  ( 0.06484759698365868963, -1.340577315853712870, 0.5772880505119728500 ) ) ;
#29431=CARTESIAN_POINT ( 'NONE',  ( 0.1048700943662639051, -1.410537776362986273, 0.5685515072117806046 ) ) ;
#29435=CARTESIAN_POINT ( 'NONE',  ( 0.3484677573834720765, -1.177852168535794330, 0.4282417262808829173 ) ) ;
#29436=ORIENTED_EDGE ( 'NONE', *, *, #10360, .F. ) ;
#29437=CARTESIAN_POINT ( 'NONE',  ( 0.1793623188593787554, -0.5490816427375126985, 0.2524024542104499891 ) ) ;
#29439=CARTESIAN_POINT ( 'NONE',  ( 0.2691042938161366527, -1.674173831038697102, 0.5802809422378258919 ) ) ;
#29440=CARTESIAN_POINT ( 'NONE',  ( 0.6019083329451311304, -1.483125660342571983, 0.5719604998333318591 ) ) ;
#29442=CARTESIAN_POINT ( 'NONE',  ( 0.5486165725604377208, -1.177731164730050351, 0.6033567833160039529 ) ) ;
#29447=CARTESIAN_POINT ( 'NONE',  ( 0.3292770240519934943, -1.177399294473852054, 0.4537878020085868713 ) ) ;
#29448=ORIENTED_EDGE ( 'NONE', *, *, #18734, .F. ) ;
#29450=CARTESIAN_POINT ( 'NONE',  ( -0.01399985835776451290, -0.5261623171122247200, 0.1652506798037701730 ) ) ;
#29457=CARTESIAN_POINT ( 'NONE',  ( 0.2889289658470847177, -1.018197464890844062, 0.6953121150017608221 ) ) ;
#29459=CARTESIAN_POINT ( 'NONE',  ( 0.1097081844868753736, -0.6901120672167371239, 0.4988169094206756915 ) ) ;
#29460=CARTESIAN_POINT ( 'NONE',  ( 0.1100478739389431637, -0.5471989581415684922, 0.1536785690647612113 ) ) ;
#29461=CARTESIAN_POINT ( 'NONE',  ( 0.03152558948873496192, -1.070130582242933892, 0.6176914086455537189 ) ) ;
#29466=CARTESIAN_POINT ( 'NONE',  ( 0.06086249397362281099, -1.332142734742522538, 0.5449151288494182843 ) ) ;
#29469=CARTESIAN_POINT ( 'NONE',  ( 0.01155337267041268469, -0.8469566264145796941, -0.05879553897425002923 ) ) ;
#29470=CARTESIAN_POINT ( 'NONE',  ( 0.5630304050329183463, -1.440913006158521359, 0.7429145406160999610 ) ) ;
#29473=CARTESIAN_POINT ( 'NONE',  ( 0.0002700364102348538193, -0.8386493658592084621, 0.3780876778669690075 ) ) ;
#29474=CARTESIAN_POINT ( 'NONE',  ( 0.1892170003689550017, -0.8723299121346327345, 0.2416867767302488257 ) ) ;
#29476=CARTESIAN_POINT ( 'NONE',  ( 0.6396239940202712582, -1.336901993116134779, 0.8551876651762376769 ) ) ;
#29478=CARTESIAN_POINT ( 'NONE',  ( 0.4884077276296390213, -1.184991248043463452, 0.4182417262808778013 ) ) ;
#29482=CARTESIAN_POINT ( 'NONE',  ( 0.09041522251730070570, -1.303513460825282078, 0.4577461224782632954 ) ) ;
#29486=CARTESIAN_POINT ( 'NONE',  ( 0.4845724100169539472, -1.091512197975673670, 0.8037230719241761356 ) ) ;
#29499=CARTESIAN_POINT ( 'NONE',  ( 0.5394930253215350913, -1.186018807470103908, 0.9907910187352456655 ) ) ;
#29501=CARTESIAN_POINT ( 'NONE',  ( 0.09120750288997202249, -0.6506232390852273451, 0.2347779848227966037 ) ) ;
#29503=CARTESIAN_POINT ( 'NONE',  ( 0.4289323656347681646, -1.412113752792893751, 0.8314756505790452668 ) ) ;
#29504=CARTESIAN_POINT ( 'NONE',  ( 0.1135111366450400200, -0.6246916037217551398, -0.08750969994112312023 ) ) ;
#29506=CARTESIAN_POINT ( 'NONE',  ( 0.1591190474269453259, -0.9387514653284979582, 0.3780444062633597224 ) ) ;
#29510=CARTESIAN_POINT ( 'NONE',  ( 0.1909569983300636875, -0.4822605344198281907, 0.2607227880177884760 ) ) ;
#29511=DIRECTION ( 'NONE',  ( -0.9848077530122080203, 0.000000000000000000, -0.1736481776669303589 ) ) ;
#29515=CARTESIAN_POINT ( 'NONE',  ( 0.002079598126425303162, -0.4942866788504220454, 0.1457185332388685473 ) ) ;
#29516=CARTESIAN_POINT ( 'NONE',  ( 0.1169689867097839509, -1.415244282406541210, 0.5045617156522553826 ) ) ;
#29517=CARTESIAN_POINT ( 'NONE',  ( 0.5308880977089266429, -1.160028955924689242, 0.7442320808281387423 ) ) ;
#29519=CARTESIAN_POINT ( 'NONE',  ( 0.02304082380077634995, -0.9164601304410119331, 0.5704413390923104288 ) ) ;
#29521=CARTESIAN_POINT ( 'NONE',  ( 0.2815322486459076456, -1.024220253226221011, 0.7266672233242934542 ) ) ;
#29524=ORIENTED_EDGE ( 'NONE', *, *, #38086, .T. ) ;
#29527=CARTESIAN_POINT ( 'NONE',  ( 0.08991878951126530684, -0.5648332908254826146, 0.1536871759036723961 ) ) ;
#29529=CARTESIAN_POINT ( 'NONE',  ( 0.3922483900791164935, -1.141226917602951474, 0.4803897171336208860 ) ) ;
#29530=CARTESIAN_POINT ( 'NONE',  ( 0.08221648783320979759, -0.8838808657549234171, 0.5149684988968940003 ) ) ;
#29532=ADVANCED_FACE ( 'NONE', ( #29587 ), #6758, .T. ) ;
#29535=CARTESIAN_POINT ( 'NONE',  ( 0.1733459996405724013, -1.382560672001245772, 0.4245314550594288527 ) ) ;
#29538=CARTESIAN_POINT ( 'NONE',  ( 0.3375807384838437897, -1.070557502036374897, 0.7199277723466692702 ) ) ;
#29540=DIRECTION ( 'NONE',  ( 0.2213665493037340615, -0.07887541654787479095, -0.9719956376001678278 ) ) ;
#29542=CARTESIAN_POINT ( 'NONE',  ( 0.2615876942762666579, -0.9557769062746830357, 0.5027841231788432452 ) ) ;
#29546=EDGE_LOOP ( 'NONE', ( #35456, #12143, #14204, #29143, #14324, #11679, #7258 ) ) ;
#29548=CARTESIAN_POINT ( 'NONE',  ( 0.4155094897012233113, -1.589296793549693776, 0.6069686941225849175 ) ) ;
#29549=CARTESIAN_POINT ( 'NONE',  ( 0.06808939212415124342, -0.5886288129379394496, 0.03568275504429443967 ) ) ;
#29553=EDGE_LOOP ( 'NONE', ( #24048, #28183 ) ) ;
#29555=CARTESIAN_POINT ( 'NONE',  ( 0.5672008999325364176, -1.484259169383562726, 0.6868322779169411252 ) ) ;
#29561=CARTESIAN_POINT ( 'NONE',  ( 0.09263126791059923815, -1.302225538099672564, 0.4543134729207104483 ) ) ;
#29565=CARTESIAN_POINT ( 'NONE',  ( 0.7188893830798498419, -1.468416639873279861, 0.6609592937859087858 ) ) ;
#29570=B_SPLINE_CURVE_WITH_KNOTS ( 'NONE', 3,
 ( #6651, #19439, #37516, #2987, #37737, #6453, #3586, #9558 ),
 .UNSPECIFIED., .F., .F.,
 ( 4, 2, 2, 4 ),
 ( 0.000000000000000000, 0.0006248974353471740181, 0.001249794870694348036, 0.002499589741388694771 ),
 .UNSPECIFIED. ) ;
#29573=CARTESIAN_POINT ( 'NONE',  ( 0.1843345887713713493, -0.8498185637792359248, 0.1049832382102776629 ) ) ;
#29574=CARTESIAN_POINT ( 'NONE',  ( 0.6962239684629863978, -1.427522162457817601, 0.6057417262800831592 ) ) ;
#29575=CARTESIAN_POINT ( 'NONE',  ( 0.1504531896226799503, -1.289993790327085499, 0.4182417262808776903 ) ) ;
#29576=CARTESIAN_POINT ( 'NONE',  ( 0.1172021019593823543, -1.233981478044366087, 0.8520562743190572830 ) ) ;
#29579=CARTESIAN_POINT ( 'NONE',  ( 0.1876053338355621880, -0.6785855078148245179, 0.1477569985384105666 ) ) ;
#29584=FACE_OUTER_BOUND ( 'NONE', #37679, .T. ) ;
#29586=CARTESIAN_POINT ( 'NONE',  ( -19685.04449858789303, 285.6128717395195622, -1.951739244310253252 ) ) ;
#29587=FACE_OUTER_BOUND ( 'NONE', #34505, .T. ) ;
#29589=CARTESIAN_POINT ( 'NONE',  ( 0.5680601962060586319, -1.407955926830466442, 0.6709332758665339513 ) ) ;
#29593=CARTESIAN_POINT ( 'NONE',  ( 0.2389902554220701691, -0.8445547280628969977, 0.4765619450694277281 ) ) ;
#29596=ORIENTED_EDGE ( 'NONE', *, *, #25341, .F. ) ;
#29600=CARTESIAN_POINT ( 'NONE',  ( 0.03921977259664061882, -0.6520487650187948292, 0.4637041238408874944 ) ) ;
#29601=CARTESIAN_POINT ( 'NONE',  ( 0.6805229833934419714, -1.519090101737586629, 0.4475704587218782837 ) ) ;
#29602=CARTESIAN_POINT ( 'NONE',  ( 0.1122840140760263117, -0.8147850859242622423, -0.05910278775682942243 ) ) ;
#29603=CARTESIAN_POINT ( 'NONE',  ( 0.3206535937437295369, -1.182295409031864697, 0.3157417262808777658 ) ) ;
#29610=CARTESIAN_POINT ( 'NONE',  ( 0.3139280916366145591, -1.155011946012813429, 0.7357575621586726067 ) ) ;
#29613=FACE_OUTER_BOUND ( 'NONE', #1476, .T. ) ;
#29615=CARTESIAN_POINT ( 'NONE',  ( 0.4264404822470678758, -1.236583032262235982, 0.5509909139845965420 ) ) ;
#29619=CARTESIAN_POINT ( 'NONE',  ( 0.1780079192261909971, -1.275848360495260847, 0.4182417262808778013 ) ) ;
#29622=CARTESIAN_POINT ( 'NONE',  ( 0.3860850745295709152, -1.140406926820327183, 0.4308008161134124214 ) ) ;
#29625=AXIS2_PLACEMENT_3D ( 'NONE', #5488, #31004, #21755 ) ;
#29634=CARTESIAN_POINT ( 'NONE',  ( 0.4103422353672772083, -1.716666388523393705, 0.4257348284579867137 ) ) ;
#29638=CARTESIAN_POINT ( 'NONE',  ( 0.1786157546805342555, -0.7241356608248309401, 0.5263052784706855336 ) ) ;
#29639=CARTESIAN_POINT ( 'NONE',  ( -0.002079317817372410872, -0.8425701894467937381, 0.1068513513423657718 ) ) ;
#29640=ORIENTED_EDGE ( 'NONE', *, *, #9314, .F. ) ;
#29643=CARTESIAN_POINT ( 'NONE',  ( 0.4695634368055122132, -1.162243873490485857, 0.8979758211665889167 ) ) ;
#29645=CARTESIAN_POINT ( 'NONE',  ( 0.01047931697485390834, -0.7075287188305212638, 0.5611176339341903407 ) ) ;
#29650=FACE_OUTER_BOUND ( 'NONE', #13280, .T. ) ;
#29651=ORIENTED_EDGE ( 'NONE', *, *, #40140, .F. ) ;
#29654=CARTESIAN_POINT ( 'NONE',  ( 0.1108980406011375874, -0.8361979591902880538, 0.3952538393652093585 ) ) ;
#29655=CARTESIAN_POINT ( 'NONE',  ( 0.01903588135871963488, -0.9012985171311311827, 0.5348354971068303154 ) ) ;
#29656=CARTESIAN_POINT ( 'NONE',  ( 0.1404538855177946133, -0.7360681509722835081, 0.5151525649323883682 ) ) ;
#29658=CARTESIAN_POINT ( 'NONE',  ( 0.5528385491747893621, -1.511151847756054156, 0.5706625526926106806 ) ) ;
#29659=CARTESIAN_POINT ( 'NONE',  ( 0.1883287559378439002, -0.5374260242839021817, 0.2815551403220473148 ) ) ;
#29665=PLANE ( 'NONE',  #28572 ) ;
#29666=CARTESIAN_POINT ( 'NONE',  ( 0.07671776034818365841, -1.321070999986371231, 0.4807624541185260836 ) ) ;
#29668=CARTESIAN_POINT ( 'NONE',  ( 1.988800862544524313E-06, -0.6187814307215226961, -0.1067078381776963153 ) ) ;
#29669=CARTESIAN_POINT ( 'NONE',  ( 0.5016706962953397797, -1.333249415785642489, 0.8067160742835506326 ) ) ;
#29674=CARTESIAN_POINT ( 'NONE',  ( 0.1851448419613674068, -1.516587896426844662, 0.7176110508928341680 ) ) ;
#29675=CARTESIAN_POINT ( 'NONE',  ( 0.2669631944262408907, -0.9256872934665847374, 0.5220607882127416000 ) ) ;
#29677=CARTESIAN_POINT ( 'NONE',  ( 0.7032651991748780640, -1.440401145529036642, 0.7869155231269625572 ) ) ;
#29679=CARTESIAN_POINT ( 'NONE',  ( 0.3110401053545825412, -1.761569117269722540, 0.5684230042337896638 ) ) ;
#29684=CARTESIAN_POINT ( 'NONE',  ( 0.002368078414000984559, -0.5283436918108032065, 0.1537378385375844370 ) ) ;
#29689=CARTESIAN_POINT ( 'NONE',  ( 0.3219857165489924955, -1.758039968903889916, 0.4848815471996642534 ) ) ;
#29690=B_SPLINE_CURVE_WITH_KNOTS ( 'NONE', 3,
 ( #22909, #1504, #32739, #11142, #4357, #10348, #1712, #26593 ),
 .UNSPECIFIED., .F., .F.,
 ( 4, 2, 2, 4 ),
 ( 0.000000000000000000, 0.001004989706391617261, 0.001507484559587425133, 0.002009979412783232788 ),
 .UNSPECIFIED. ) ;
#29691=CARTESIAN_POINT ( 'NONE',  ( 0.3857344834571298509, -0.9392921734164567660, 0.7474990102649032853 ) ) ;
#29695=ORIENTED_EDGE ( 'NONE', *, *, #12982, .T. ) ;
#29697=CARTESIAN_POINT ( 'NONE',  ( 0.3434711319545033503, -1.169169302084718254, 0.4182417262808778013 ) ) ;
#29701=CARTESIAN_POINT ( 'NONE',  ( 0.09601930021752928812, -0.7007513381161541988, 0.3017055919335016601 ) ) ;
#29702=CARTESIAN_POINT ( 'NONE',  ( 0.2635877808603924177, -1.476486208343732676, 1.014510316672303514 ) ) ;
#29703=CARTESIAN_POINT ( 'NONE',  ( 0.4388336691297091141, -1.430740155459193641, 0.8217701134134310914 ) ) ;
#29704=CARTESIAN_POINT ( 'NONE',  ( 0.1621828556419718514, -1.266751494790363086, 0.9433689391485273745 ) ) ;
#29706=CARTESIAN_POINT ( 'NONE',  ( 0.05219137279552537451, -0.9515688809449991403, 0.3440008263018651813 ) ) ;
#29707=ORIENTED_EDGE ( 'NONE', *, *, #26768, .F. ) ;
#29708=ORIENTED_EDGE ( 'NONE', *, *, #27291, .T. ) ;
#29711=CARTESIAN_POINT ( 'NONE',  ( 0.1154393097213636810, -0.4486880550576102245, 0.1802714202231547602 ) ) ;
#29717=CARTESIAN_POINT ( 'NONE',  ( 0.6136594321969363053, -1.288375518029639233, 0.6368171400845314967 ) ) ;
#29723=CARTESIAN_POINT ( 'NONE',  ( 0.3702276848513395002, -1.105716412504990087, 0.7603571629394799691 ) ) ;
#29727=CARTESIAN_POINT ( 'NONE',  ( 0.5385803422324542122, -1.160485748998025368, 0.5861681292462268544 ) ) ;
#29728=CARTESIAN_POINT ( 'NONE',  ( 0.1154601380735851140, -0.6757610506600419953, 0.4323217926036908021 ) ) ;
#29730=CARTESIAN_POINT ( 'NONE',  ( 0.4156154940873745818, -1.130749427098165283, 0.4798916445188330382 ) ) ;
#29731=CARTESIAN_POINT ( 'NONE',  ( 0.2502467635401044999, -1.267705161434652394, 0.6988155349366990121 ) ) ;
#29738=CARTESIAN_POINT ( 'NONE',  ( 0.1993974397309283553, -1.367472865666984783, 0.4182417262808786895 ) ) ;
#29741=CARTESIAN_POINT ( 'NONE',  ( 0.4893458284958691618, -1.274452062364263449, 0.6067319554162099449 ) ) ;
#29749=CARTESIAN_POINT ( 'NONE',  ( 0.1689459712188738916, -0.9783659983241776992, 0.7869633328443620401 ) ) ;
#29751=CARTESIAN_POINT ( 'NONE',  ( 0.08874571000602692050, -0.6053243709266833417, 0.05379243744558167423 ) ) ;
#29752=CARTESIAN_POINT ( 'NONE',  ( 0.1920071873703447507, -0.8110264159798786787, 0.2735051980380696635 ) ) ;
#29757=CARTESIAN_POINT ( 'NONE',  ( 0.5566577208962448786, -1.469770625181828549, 0.7214895520387809569 ) ) ;
#29759=CARTESIAN_POINT ( 'NONE',  ( 0.6091898566437330409, -1.605611940169644258, 0.5996532284048697869 ) ) ;
#29763=CARTESIAN_POINT ( 'NONE',  ( 0.1761881424425499609, -1.253808687867943084, 0.4381683186903178040 ) ) ;
#29768=CARTESIAN_POINT ( 'NONE',  ( 0.1907823988372855106, -0.4944553380418882926, 0.2959634315342150046 ) ) ;
#29778=CARTESIAN_POINT ( 'NONE',  ( 0.1836329606266136616, -0.5161036956692948152, 0.07857586674746268318 ) ) ;
#29780=CARTESIAN_POINT ( 'NONE',  ( 0.5977626385027750011, -1.597637465087648811, 0.4278768775546197278 ) ) ;
#29782=CARTESIAN_POINT ( 'NONE',  ( 0.1429229523316038197, -1.294172713379485584, 0.4193902271515088098 ) ) ;
#29783=CARTESIAN_POINT ( 'NONE',  ( 0.000000000000000000, -0.4262518876079541830, 0.1457185332388682419 ) ) ;
#29786=CARTESIAN_POINT ( 'NONE',  ( 0.3048024544079886988, -1.756867927854032674, 0.5684537085834007186 ) ) ;
#29791=( BOUNDED_SURFACE ( )  B_SPLINE_SURFACE ( 3, 2, ( 
 ( #15520, #12230, #21688 ),
 ( #34218, #6033, #40602 ),
 ( #12420, #24968, #37500 ),
 ( #9325, #21904, #26013 ),
 ( #26202, #727, #16331 ),
 ( #29285, #6844, #10764 ) ),
 .UNSPECIFIED., .F., .F., .T. ) 
 B_SPLINE_SURFACE_WITH_KNOTS ( ( 4, 2, 4 ),
 ( 3, 3 ),
 ( 3.120333852413281761E-16, 0.0003231562290647264500, 0.0006463124581291408667 ),
 ( 0.000000000000000000, 1.000000000000000000 ),
 .UNSPECIFIED. ) 
 GEOMETRIC_REPRESENTATION_ITEM ( )  RATIONAL_B_SPLINE_SURFACE ( (
 ( 1.000000000000000000, 0.8997265729123280487, 1.000000000000000000),
 ( 1.000000000000000000, 0.9023522654549963606, 1.000000000000000000),
 ( 1.000000000000000000, 0.9048744759709612673, 1.000000000000000000),
 ( 1.000000000000000000, 0.9100851747552831661, 1.000000000000000000),
 ( 1.000000000000000000, 0.9127760422757066339, 1.000000000000000000),
 ( 1.000000000000000000, 0.9157534740967101516, 1.000000000000000000) ) ) 
 REPRESENTATION_ITEM ( '' )  SURFACE ( )  );
#29795=LINE ( 'NONE', #29586, #38162 ) ;
#29798=CARTESIAN_POINT ( 'NONE',  ( 0.4933479471158314644, -1.287949358479272055, 0.7760119179218301078 ) ) ;
#29801=CARTESIAN_POINT ( 'NONE',  ( 0.5179624304041525740, -1.133452979592703302, 0.6716967517830890744 ) ) ;
#29805=CARTESIAN_POINT ( 'NONE',  ( 0.3238143371732789544, -1.179505499532595758, 0.5655564271612124605 ) ) ;
#29806=ORIENTED_EDGE ( 'NONE', *, *, #15186, .T. ) ;
#29808=CARTESIAN_POINT ( 'NONE',  ( 0.05169272155612220088, -0.7052237289551500643, 0.5425721195289684440 ) ) ;
#29809=CARTESIAN_POINT ( 'NONE',  ( 0.6849528713309417371, -1.506609029741341255, 0.4574981245801082452 ) ) ;
#29811=CARTESIAN_POINT ( 'NONE',  ( 0.2321526281619643584, -1.233007205928619232, 0.3667417262808778111 ) ) ;
#29821=CARTESIAN_POINT ( 'NONE',  ( 0.4181182131315021033, -1.203184156692840734, 0.6707339718938493123 ) ) ;
#29822=FACE_OUTER_BOUND ( 'NONE', #27436, .T. ) ;
#29824=CARTESIAN_POINT ( 'NONE',  ( 0.1957369265267845937, -0.9763688040310566363, 0.5238895912861436521 ) ) ;
#29831=EDGE_CURVE ( 'NONE', #25265, #29236, #35679, .T. ) ;
#29832=CARTESIAN_POINT ( 'NONE',  ( 0.3683757878646363726, -1.156357368468860392, 0.4257332135735479861 ) ) ;
#29837=CARTESIAN_POINT ( 'NONE',  ( 0.0002547247918985094499, -0.4980400414177595381, -0.01674915368249139946 ) ) ;
#29849=CARTESIAN_POINT ( 'NONE',  ( 0.6026051337862934343, -1.481309381409939618, 0.6176392787056765865 ) ) ;
#29850=CARTESIAN_POINT ( 'NONE',  ( 0.007764572479489010963, -0.7391071013572128034, -0.003941584134019470581 ) ) ;
#29854=CARTESIAN_POINT ( 'NONE',  ( 0.3140415829244854184, -1.186180626463321230, 0.4809987123389981578 ) ) ;
#29856=CARTESIAN_POINT ( 'NONE',  ( 0.2530344669440779404, -1.593468256218861567, 0.8522446305581886650 ) ) ;
#29857=CARTESIAN_POINT ( 'NONE',  ( 0.5922106362852195272, -1.600826850851058802, 0.4254268223615397804 ) ) ;
#29858=CARTESIAN_POINT ( 'NONE',  ( 0.2128381955336136888, -1.241281127606408186, 0.5854230766145357423 ) ) ;
#29864=EDGE_LOOP ( 'NONE', ( #11443, #2743, #38441, #27057, #13747 ) ) ;
#29865=CARTESIAN_POINT ( 'NONE',  ( 0.1376160882066851110, -0.8423595946558073422, 0.4896585138266671966 ) ) ;
#29867=CARTESIAN_POINT ( 'NONE',  ( 0.1119881974088350329, -1.370995722074662693, 0.6752038603878468548 ) ) ;
#29868=TOROIDAL_SURFACE ( 'NONE', #33829, 0.04749999999977554815, 0.01000000000000000021 ) ;
#29869=CARTESIAN_POINT ( 'NONE',  ( 0.09245771922927559228, -0.6466466848293074277, 0.4347549917907825856 ) ) ;
#29871=CARTESIAN_POINT ( 'NONE',  ( 0.5539269415344313385, -1.511025941422516006, 0.5935205164291307289 ) ) ;
#29872=CARTESIAN_POINT ( 'NONE',  ( 0.06498580141003787447, -1.293606482245585498, 0.6256161605704260165 ) ) ;
#29878=VECTOR ( 'NONE', #7838, 39.37007874015748143 ) ;
#29882=CARTESIAN_POINT ( 'NONE',  ( 0.01164198743023061450, -0.7796407181604130265, -0.09629102463154327884 ) ) ;
#29886=CARTESIAN_POINT ( 'NONE',  ( 0.007773584319307426035, -0.7382159792943179255, -0.004238343198677651906 ) ) ;
#29888=CARTESIAN_POINT ( 'NONE',  ( 0.1623712441042921006, -1.412506991498796660, 0.8192480828659791658 ) ) ;
#29889=CARTESIAN_POINT ( 'NONE',  ( 0.1874346505856443745, -0.8710952576279675785, 0.2160754816401605771 ) ) ;
#29891=CARTESIAN_POINT ( 'NONE',  ( 0.5453389350593388363, -1.184144166247469876, 0.8773366473911075047 ) ) ;
#29895=CARTESIAN_POINT ( 'NONE',  ( 0.3136311368843414105, -1.762219552882195783, 0.5683051179383220575 ) ) ;
#29899=CARTESIAN_POINT ( 'NONE',  ( 0.1378941890947338045, -1.196521231248368844, 0.9199180204847504649 ) ) ;
#29901=CARTESIAN_POINT ( 'NONE',  ( 0.08058916068514494768, -1.309220013881624123, 0.4727703015479320370 ) ) ;
#29902=CARTESIAN_POINT ( 'NONE',  ( 0.2813047422443414325, -1.204938683099350705, 0.5682417262808779901 ) ) ;
#29906=AXIS2_PLACEMENT_3D ( 'NONE', #39521, #37054, #23710 ) ;
#29907=CARTESIAN_POINT ( 'NONE',  ( 0.2196261443710258443, -0.6607888217372858142, 0.4354189310569229754 ) ) ;
#29916=CARTESIAN_POINT ( 'NONE',  ( 0.1170761419057074482, -1.261392965458049131, 0.6036835557974136179 ) ) ;
#29917=CARTESIAN_POINT ( 'NONE',  ( 0.2584190914277442186, -0.9487391774685208778, 0.7036860948817510453 ) ) ;
#29918=CARTESIAN_POINT ( 'NONE',  ( 0.2995624311403809470, -1.612171325865530136, 0.9470918590109783652 ) ) ;
#29919=CARTESIAN_POINT ( 'NONE',  ( 0.09887370392402621000, -0.5650284097326406796, 0.2392820984072531743 ) ) ;
#29921=LINE ( 'NONE', #1763, #18300 ) ;
#29922=CARTESIAN_POINT ( 'NONE',  ( 0.2792289373433416988, -1.051500623829179526, 0.6297070940450347765 ) ) ;
#29928=CARTESIAN_POINT ( 'NONE',  ( 0.2407639156934034685, -0.6284568509811103709, 0.5445959906753944368 ) ) ;
#29937=VECTOR ( 'NONE', #3114, 39.37007874015748143 ) ;
#29939=CARTESIAN_POINT ( 'NONE',  ( 0.5804192421706322325, -1.234356152197840117, 0.7108377039426548860 ) ) ;
#29943=ORIENTED_EDGE ( 'NONE', *, *, #37295, .F. ) ;
#29948=CARTESIAN_POINT ( 'NONE',  ( 0.4365432303899622890, -1.033643997532201597, 0.7173331770504315363 ) ) ;
#29949=CARTESIAN_POINT ( 'NONE',  ( 0.5373165049569139651, -1.161628669640105027, 0.5421417554447620635 ) ) ;
#29950=CARTESIAN_POINT ( 'NONE',  ( 0.3416191607863283686, -1.126820519681605903, 0.5182417262812423209 ) ) ;
#29953=CARTESIAN_POINT ( 'NONE',  ( 0.05733805304787521762, -0.8395800731581377629, 0.2495454520759651795 ) ) ;
#29956=CARTESIAN_POINT ( 'NONE',  ( 0.1825980849618502877, -1.261391773294454399, 0.5182417262812422099 ) ) ;
#29958=CARTESIAN_POINT ( 'NONE',  ( 0.1402147235662943858, -1.401774878535922975, 0.4497410000889012216 ) ) ;
#29960=CARTESIAN_POINT ( 'NONE',  ( 0.3900475047517206195, -1.136049760834360711, 0.7018806097820817769 ) ) ;
#29962=CARTESIAN_POINT ( 'NONE',  ( 0.4138729472876766513, -1.128955312352843965, 0.5470489658417444501 ) ) ;
#29964=CARTESIAN_POINT ( 'NONE',  ( 0.2225775331702970761, -0.9343733720331020010, 0.4090965549137709489 ) ) ;
#29966=VECTOR ( 'NONE', #15406, 39.37007874015748854 ) ;
#29968=ORIENTED_EDGE ( 'NONE', *, *, #39716, .F. ) ;
#29970=CARTESIAN_POINT ( 'NONE',  ( 0.1087658859722912819, -0.7576187927048527726, 0.5953713316029712876 ) ) ;
#29971=CARTESIAN_POINT ( 'NONE',  ( 0.08964876120596533549, -0.5474965510609541841, 0.1111581565464928867 ) ) ;
#29974=ORIENTED_EDGE ( 'NONE', *, *, #887, .F. ) ;
#29975=CARTESIAN_POINT ( 'NONE',  ( 0.2614468074032732514, -0.7584085742687330933, 0.1932256475537141860 ) ) ;
#29976=CARTESIAN_POINT ( 'NONE',  ( 0.1193505310152234433, -0.5488392675763952289, 0.1535339596633792936 ) ) ;
#29980=CARTESIAN_POINT ( 'NONE',  ( 0.6095536282444361520, -1.587373553213482280, 0.4182417262808777458 ) ) ;
#29981=CARTESIAN_POINT ( 'NONE',  ( 0.1094588636161752809, -1.304004861155783068, 0.4319985379268259096 ) ) ;
#29985=CARTESIAN_POINT ( 'NONE',  ( 0.2723301224276278298, -0.7044396210649886969, 0.6356112240561296867 ) ) ;
#29991=CARTESIAN_POINT ( 'NONE',  ( 0.6521596339623016991, -1.579655379295860307, 0.6112030275387951850 ) ) ;
#29994=CARTESIAN_POINT ( 'NONE',  ( 0.01197363197122058853, -0.5805133742323803636, 0.4689902101802463363 ) ) ;
#29997=CARTESIAN_POINT ( 'NONE',  ( -0.01736481776669303659, -0.8497080691189130564, 0.1457185332388703236 ) ) ;
#30000=VERTEX_POINT ( 'NONE', #7729 ) ;
#30003=DIRECTION ( 'NONE',  ( 0.9998941247116546194, -0.01455087607601020412, 0.0001066420868422379633 ) ) ;
#30005=CARTESIAN_POINT ( 'NONE',  ( 0.3954536428817021498, -1.141798559182092943, 0.7526865122305215206 ) ) ;
#30008=CARTESIAN_POINT ( 'NONE',  ( 0.5138184642618360831, -1.118801421376873551, 0.5693865086028936373 ) ) ;
#30016=CARTESIAN_POINT ( 'NONE',  ( 0.3304196671140066099, -1.628641716510011994, 0.7020376695473490303 ) ) ;
#30017=CARTESIAN_POINT ( 'NONE',  ( 0.7060640942175693269, -1.498641769205614205, 0.5270363939079757420 ) ) ;
#30018=CARTESIAN_POINT ( 'NONE',  ( 0.1145437834104099661, -0.4941296012437448870, 0.001010760634015512704 ) ) ;
#30019=CARTESIAN_POINT ( 'NONE',  ( 0.1434010736994648927, -1.283284918233685623, 0.5707417262808780478 ) ) ;
#30028=CARTESIAN_POINT ( 'NONE',  ( 0.1181081361290538395, -0.8884863947959633634, 0.5437361635629905932 ) ) ;
#30035=CARTESIAN_POINT ( 'NONE',  ( 0.1852724517579373009, -0.8388905295248703098, 0.1482875376949696067 ) ) ;
#30040=CARTESIAN_POINT ( 'NONE',  ( 0.02162899328625018588, -1.067328559141285771, 0.6314244029302625849 ) ) ;
#30042=APPLICATION_CONTEXT ( 'configuration controlled 3d designs of mechanical parts and assemblies' ) ;
#30044=( BOUNDED_SURFACE ( )  B_SPLINE_SURFACE ( 3, 2, ( 
 ( #17493, #17877, #8420 ),
 ( #4926, #30045, #37009 ),
 ( #24088, #14384, #20583 ),
 ( #11113, #18098, #4714 ),
 ( #30444, #2272, #30652 ),
 ( #26763, #36197, #24476 ),
 ( #8010, #36800, #23880 ),
 ( #20796, #27160, #11721 ),
 ( #1679, #26948, #8611 ),
 ( #21185, #39482, #11311 ),
 ( #14812, #36408, #29837 ),
 ( #27375, #8221, #39693 ),
 ( #11526, #5124, #20987 ),
 ( #33318, #36617, #33503 ),
 ( #5315, #33720, #5536 ),
 ( #2473, #15009, #27563 ),
 ( #40086, #11915, #8833 ),
 ( #17281, #21411, #14028 ),
 ( #23323, #29668, #26803 ),
 ( #22712, #1123, #16514 ),
 ( #23110, #1511, #22916 ),
 ( #38522, #35635, #29054 ),
 ( #16925, #19799, #924 ),
 ( #26193, #13430, #32949 ),
 ( #17120, #13628, #7657 ),
 ( #4366, #26390, #26604 ),
 ( #29882, #35244, #26000 ),
 ( #29271, #3953, #38717 ),
 ( #4551, #4752, #7044 ),
 ( #39138, #20017, #10964 ),
 ( #32336, #10354, #20225 ),
 ( #29469, #32746, #23524 ),
 ( #32546, #35432, #7442 ),
 ( #1313, #7230, #38917 ),
 ( #10749, #32146, #13820 ),
 ( #35845, #19613, #10539 ),
 ( #36041, #7843, #20415 ),
 ( #17326, #4158, #1721 ),
 ( #14238, #10141, #16725 ),
 ( #39520, #24316, #21451 ),
 ( #39736, #2312, #33978 ),
 ( #36237, #17716, #20629 ),
 ( #26989, #30082, #5781 ),
 ( #21228, #36452, #27600 ) ),
 .UNSPECIFIED., .F., .F., .F. ) 
 B_SPLINE_SURFACE_WITH_KNOTS ( ( 4, 2, 2, 2, 2, 2, 2, 2, 2, 2, 2, 2, 2, 2, 2, 2, 2, 2, 2, 2, 2, 4 ),
 ( 3, 3 ),
 ( 0.001346002852697868917, 0.002596997597215204134, 0.003847992341732539567, 0.004473489713991207067, 0.005098987086249874567, 0.006349981830767210435, 0.007600976575284546302, 0.008226473947543213802, 0.008851971319801881302, 0.01010296606431921630, 0.01135396080883655130, 0.01260495555335388804, 0.01323045292561255554, 0.01385595029787122304, 0.01448144767012989054, 0.01510694504238855804, 0.01635793978690589304, 0.01760893453142322804, 0.01885992927594056304, 0.01948542664819923054, 0.02011092402045789804, 0.02136191876497523304 ),
 ( 0.000000000000000000, 1.000000000000000000 ),
 .UNSPECIFIED. ) 
 GEOMETRIC_REPRESENTATION_ITEM ( )  RATIONAL_B_SPLINE_SURFACE ( (
 ( 1.000000000000000000, 0.6289600335726139857, 1.000000000000000000),
 ( 1.000000000000000000, 0.6292818987205170966, 1.000000000000000000),
 ( 1.000000000000000000, 0.6297744943890225544, 1.000000000000000000),
 ( 1.000000000000000000, 0.6308798029848204925, 1.000000000000000000),
 ( 1.000000000000000000, 0.6314937475243069809, 1.000000000000000000),
 ( 1.000000000000000000, 0.6324446813422345270, 1.000000000000000000),
 ( 1.000000000000000000, 0.6327693011710547877, 1.000000000000000000),
 ( 1.000000000000000000, 0.6334165357267688146, 1.000000000000000000),
 ( 1.000000000000000000, 0.6337398306086132749, 1.000000000000000000),
 ( 1.000000000000000000, 0.6347105868218758662, 1.000000000000000000),
 ( 1.000000000000000000, 0.6353603024733837090, 1.000000000000000000),
 ( 1.000000000000000000, 0.6366634021563924994, 1.000000000000000000),
 ( 1.000000000000000000, 0.6372927617045243132, 1.000000000000000000),
 ( 1.000000000000000000, 0.6381953573391411227, 1.000000000000000000),
 ( 1.000000000000000000, 0.6384894769518629776, 1.000000000000000000),
 ( 1.000000000000000000, 0.6390667812190622410, 1.000000000000000000),
 ( 1.000000000000000000, 0.6393504911485946574, 1.000000000000000000),
 ( 1.000000000000000000, 0.6401755864900929849, 1.000000000000000000),
 ( 1.000000000000000000, 0.6406983120072226034, 1.000000000000000000),
 ( 1.000000000000000000, 0.6417455103317676324, 1.000000000000000000),
 ( 1.000000000000000000, 0.6422727239750118944, 1.000000000000000000),
 ( 1.000000000000000000, 0.6433117747521388541, 1.000000000000000000),
 ( 1.000000000000000000, 0.6438273952226162278, 1.000000000000000000),
 ( 1.000000000000000000, 0.6446165130563749068, 1.000000000000000000),
 ( 1.000000000000000000, 0.6448812679222618582, 1.000000000000000000),
 ( 1.000000000000000000, 0.6454115060670834181, 1.000000000000000000),
 ( 1.000000000000000000, 0.6456783656519925474, 1.000000000000000000),
 ( 1.000000000000000000, 0.6462228309538587956, 1.000000000000000000),
 ( 1.000000000000000000, 0.6465004957945182928, 1.000000000000000000),
 ( 1.000000000000000000, 0.6470729932895772363, 1.000000000000000000),
 ( 1.000000000000000000, 0.6473695932598104719, 1.000000000000000000),
 ( 1.000000000000000000, 0.6482737582539809251, 1.000000000000000000),
 ( 1.000000000000000000, 0.6488977369596267142, 1.000000000000000000),
 ( 1.000000000000000000, 0.6501749241777317057, 1.000000000000000000),
 ( 1.000000000000000000, 0.6508319705051489601, 1.000000000000000000),
 ( 1.000000000000000000, 0.6521161713507420687, 1.000000000000000000),
 ( 1.000000000000000000, 0.6527515169048989652, 1.000000000000000000),
 ( 1.000000000000000000, 0.6536932375029560482, 1.000000000000000000),
 ( 1.000000000000000000, 0.6540055346228418331, 1.000000000000000000),
 ( 1.000000000000000000, 0.6546044083911876088, 1.000000000000000000),
 ( 1.000000000000000000, 0.6548926905623442263, 1.000000000000000000),
 ( 1.000000000000000000, 0.6557056282628960231, 1.000000000000000000),
 ( 1.000000000000000000, 0.6561814253999803670, 1.000000000000000000),
 ( 1.000000000000000000, 0.6565078065782231631, 1.000000000000000000) ) ) 
 REPRESENTATION_ITEM ( '' )  SURFACE ( )  );
#30045=CARTESIAN_POINT ( 'NONE',  ( 1.405866954095903676E-05, -0.4259765552297195557, 0.1334928998232308428 ) ) ;
#30046=CARTESIAN_POINT ( 'NONE',  ( 0.4621675984227249789, -1.110867290327286261, 0.5635151220948720896 ) ) ;
#30053=CARTESIAN_POINT ( 'NONE',  ( 0.5604557356148186509, -1.426020855739283943, 0.7554199595131929623 ) ) ;
#30054=CARTESIAN_POINT ( 'NONE',  ( -0.001702386183366518761, -0.8269161091246169937, 0.06756100155804112273 ) ) ;
#30056=ORIENTED_EDGE ( 'NONE', *, *, #34263, .F. ) ;
#30057=CARTESIAN_POINT ( 'NONE',  ( 0.2132426129924576141, -0.7277951702479017460, 0.6835290371355510208 ) ) ;
#30060=CARTESIAN_POINT ( 'NONE',  ( 0.2713787642340086403, -1.664625376075213214, 0.7106118310602838051 ) ) ;
#30062=CARTESIAN_POINT ( 'NONE',  ( 0.1574608366664733972, -1.264793525678033825, 0.6048402482925469004 ) ) ;
#30069=CARTESIAN_POINT ( 'NONE',  ( 0.08531284324210690329, -0.8124773231580394439, 0.1722839607542651641 ) ) ;
#30070=CARTESIAN_POINT ( 'NONE',  ( 0.1157716883191968194, -1.391468844569133223, 0.6465564330999761244 ) ) ;
#30072=CARTESIAN_POINT ( 'NONE',  ( 0.1673863529439155173, -0.7934200884644354579, 0.5807677822519677902 ) ) ;
#30073=CARTESIAN_POINT ( 'NONE',  ( 0.06848556979248547616, -1.327615349530146593, 0.5769412031485705583 ) ) ;
#30082=CARTESIAN_POINT ( 'NONE',  ( -1.050216749492551567E-05, -0.9484751009321573667, 0.1331997927868723564 ) ) ;
#30086=CARTESIAN_POINT ( 'NONE',  ( -8.537024980200822558E-17, -0.6872203660140403514, 0.1122922589469583232 ) ) ;
#30087=CARTESIAN_POINT ( 'NONE',  ( 0.1960870051948097048, -0.8771803234346856604, 0.3014997781122282783 ) ) ;
#30089=CARTESIAN_POINT ( 'NONE',  ( 0.6710503155864784297, -1.387729643236325083, 0.8301965501372990941 ) ) ;
#30090=CARTESIAN_POINT ( 'NONE',  ( 0.1316017208954911588, -1.248059642665102942, 0.5182417262812423209 ) ) ;
#30094=CARTESIAN_POINT ( 'NONE',  ( 0.03214649760163642428, -0.7697735882589110679, 0.6362183684201799805 ) ) ;
#30095=B_SPLINE_CURVE_WITH_KNOTS ( 'NONE', 3,
 ( #8174, #17445, #1830, #14346, #14546, #36572, #20944, #28129, #14764, #37563, #27927, #12291, #12871, #33900, #24234, #8568, #34492, #15157 ),
 .UNSPECIFIED., .F., .F.,
 ( 4, 2, 2, 2, 2, 2, 2, 2, 4 ),
 ( 0.000000000000000000, 0.0006226388165308821988, 0.001245277633061764398, 0.001867916449592646596, 0.002490555266123528795, 0.003113194082654410777, 0.003735832899185293193, 0.004358471715716175608, 0.004981110532247057590 ),
 .UNSPECIFIED. ) ;
#30098=ORIENTED_EDGE ( 'NONE', *, *, #17284, .F. ) ;
#30100=CARTESIAN_POINT ( 'NONE',  ( 0.5804192421706322325, -1.234356152197840117, 0.7108377039426548860 ) ) ;
#30101=ORIENTED_EDGE ( 'NONE', *, *, #1735, .T. ) ;
#30104=ADVANCED_FACE ( 'NONE', ( #38339 ), #22326, .F. ) ;
#30107=CARTESIAN_POINT ( 'NONE',  ( 0.2362368525501326866, -1.230736425956878932, 0.4182417262808779679 ) ) ;
#30110=VERTEX_POINT ( 'NONE', #1150 ) ;
#30112=CARTESIAN_POINT ( 'NONE',  ( 0.08630836114928065739, -0.7249243428820483226, 0.1457185332388690469 ) ) ;
#30113=CARTESIAN_POINT ( 'NONE',  ( 0.1792747913679618443, -1.226898500125762181, 1.015033455503321136 ) ) ;
#30114=CARTESIAN_POINT ( 'NONE',  ( 0.1121846759074304062, -0.6324519228151627148, 0.3961551049443752803 ) ) ;
#30115=CARTESIAN_POINT ( 'NONE',  ( 0.5908959048872449715, -1.601544548465861473, 0.4282886817583849703 ) ) ;
#30117=CARTESIAN_POINT ( 'NONE',  ( 0.2691739887394375974, -1.194277921376554641, 0.6127582284757946418 ) ) ;
#30119=EDGE_CURVE ( 'NONE', #13346, #10719, #31977, .T. ) ;
#30122=CARTESIAN_POINT ( 'NONE',  ( 0.2729734451281876639, -0.7689569267751511505, 0.5866520183762450324 ) ) ;
#30124=ADVANCED_FACE ( 'NONE', ( #19636 ), #32170, .T. ) ;
#30125=CARTESIAN_POINT ( 'NONE',  ( 0.1905436384893574864, -0.5945559727383912252, 0.3046096357648204189 ) ) ;
#30128=CARTESIAN_POINT ( 'NONE',  ( 0.08116418662092184100, -1.318973274706103149, 0.4700956214235573749 ) ) ;
#30133=CARTESIAN_POINT ( 'NONE',  ( 0.3057296174425681579, -0.8572510462883253801, 0.6221769111833096444 ) ) ;
#30142=CARTESIAN_POINT ( 'NONE',  ( 0.5296568109260144652, -1.147337575730582371, 0.6371820472447363715 ) ) ;
#30143=CARTESIAN_POINT ( 'NONE',  ( 0.4337264196245351755, -1.120470219587671457, 0.5446312635246355338 ) ) ;
#30144=CARTESIAN_POINT ( 'NONE',  ( 0.08200662898914722054, -0.9691756016468595636, 0.6660704738325865515 ) ) ;
#30146=CARTESIAN_POINT ( 'NONE',  ( 0.1186103394390872201, -1.414144848331978510, 0.5683298932114988489 ) ) ;
#30151=CARTESIAN_POINT ( 'NONE',  ( 0.4228361166268820304, -1.173637864075360415, 0.6740159186778078571 ) ) ;
#30152=EDGE_CURVE ( 'NONE', #17350, #31635, #22949, .T. ) ;
#30153=CARTESIAN_POINT ( 'NONE',  ( 0.4099390216524483321, -1.131149867669359654, 0.5235510575314094028 ) ) ;
#30160=CARTESIAN_POINT ( 'NONE',  ( 0.1885786782586174326, -0.5477411782657776174, -0.03797464539687132878 ) ) ;
#30161=CARTESIAN_POINT ( 'NONE',  ( 0.1608394401585168665, -0.9087424240471937420, 0.7386883132146533359 ) ) ;
#30162=CARTESIAN_POINT ( 'NONE',  ( 0.7048936116999384716, -1.529749924580348530, 0.5717773534970714833 ) ) ;
#30167=ORIENTED_EDGE ( 'NONE', *, *, #23489, .T. ) ;
#30168=CARTESIAN_POINT ( 'NONE',  ( 0.5606097963238384496, -1.505408366410144083, 0.5243742338725653207 ) ) ;
#30169=CARTESIAN_POINT ( 'NONE',  ( 0.1222183301103683672, -0.5572085505171303632, 0.1987391494479376353 ) ) ;
#30170=ORIENTED_EDGE ( 'NONE', *, *, #28398, .T. ) ;
#30171=CARTESIAN_POINT ( 'NONE',  ( 0.3171299009022257032, -1.761203395594564736, 0.5573299461910276031 ) ) ;
#30173=CARTESIAN_POINT ( 'NONE',  ( 0.6207080634491849436, -1.571428378261625181, 0.4182417262808776903 ) ) ;
#30174=CARTESIAN_POINT ( 'NONE',  ( 0.1358326267964612144, -1.288717780320212558, 0.4219958763549262470 ) ) ;
#30177=CARTESIAN_POINT ( 'NONE',  ( 0.3173647091058168779, -0.7919842589448738979, 0.7159411547141941723 ) ) ;
#30184=CARTESIAN_POINT ( 'NONE',  ( 0.08521903690165112677, -1.316213625887622696, 0.4631828244221000701 ) ) ;
#30185=CARTESIAN_POINT ( 'NONE',  ( 0.0003038568743942667081, -0.4444331504931744448, 0.2553847410507332771 ) ) ;
#30188=CARTESIAN_POINT ( 'NONE',  ( 0.5942223284369342329, -1.599512312265707115, 0.4182417262808810765 ) ) ;
#30190=CARTESIAN_POINT ( 'NONE',  ( 0.4435963532280620680, -1.112752012059924134, 0.5972808037033706663 ) ) ;
#30191=CARTESIAN_POINT ( 'NONE',  ( 0.4090604450045443596, -1.131420581850358653, 0.3667417262808778666 ) ) ;
#30194=CARTESIAN_POINT ( 'NONE',  ( 0.5216898644270308028, -1.329855447211024666, 0.6139483236913935160 ) ) ;
#30197=CARTESIAN_POINT ( 'NONE',  ( 0.5138235575674273692, -1.118575097671381080, 0.5744212141803229921 ) ) ;
#30201=CARTESIAN_POINT ( 'NONE',  ( 0.3204479958614548929, -1.182666560659948907, 0.5682417262808776570 ) ) ;
#30202=CARTESIAN_POINT ( 'NONE',  ( 0.3146425706043863846, -1.494729834945346836, 0.8673829083298324472 ) ) ;
#30203=CARTESIAN_POINT ( 'NONE',  ( 0.6964926828203267251, -1.497596446741557452, 0.4801749555793174973 ) ) ;
#30204=CARTESIAN_POINT ( 'NONE',  ( 0.1871331107182152009, -0.5893403707559643490, 0.009665131869706357695 ) ) ;
#30206=EDGE_LOOP ( 'NONE', ( #3701, #8911, #2843, #24427, #6259 ) ) ;
#30210=CARTESIAN_POINT ( 'NONE',  ( 0.07974598588771943108, -0.8334789133843516495, 0.2137242551589284278 ) ) ;
#30216=CARTESIAN_POINT ( 'NONE',  ( 0.6555154469039060627, -1.476457112320177067, 0.4182417262808776348 ) ) ;
#30219=CARTESIAN_POINT ( 'NONE',  ( 0.05107123952191217064, -1.249085498977453357, 0.6677375136145999868 ) ) ;
#30220=CARTESIAN_POINT ( 'NONE',  ( 0.5247102883936010098, -1.203215684353998727, 0.6057417262809794423 ) ) ;
#30221=FACE_OUTER_BOUND ( 'NONE', #3247, .T. ) ;
#30223=CARTESIAN_POINT ( 'NONE',  ( 0.4182650443266206497, -1.104802627502811774, 0.5963647967864725841 ) ) ;
#30225=AXIS2_PLACEMENT_3D ( 'NONE', #34892, #34694, #35105 ) ;
#30227=ORIENTED_EDGE ( 'NONE', *, *, #26883, .T. ) ;
#30235=CARTESIAN_POINT ( 'NONE',  ( 0.007561979894622030025, -0.7583094115173071303, 0.004127483746527383680 ) ) ;
#30241=CARTESIAN_POINT ( 'NONE',  ( 0.2664190893233142621, -1.675340114736260766, 0.5742097616013166483 ) ) ;
#30243=CARTESIAN_POINT ( 'NONE',  ( 0.1404535776246665646, -1.274393186057628746, 0.6056389588256660961 ) ) ;
#30247=CARTESIAN_POINT ( 'NONE',  ( 0.5382307432915078849, -1.161159458769174257, 0.5682417262808779901 ) ) ;
#30249=ORIENTED_EDGE ( 'NONE', *, *, #16976, .F. ) ;
#30250=CARTESIAN_POINT ( 'NONE',  ( 0.3772117652181573022, -1.120077681141029124, 0.6236847670215859285 ) ) ;
#30252=CARTESIAN_POINT ( 'NONE',  ( 0.1712609145248183695, -0.8202291507405884419, 0.6467119214775935987 ) ) ;
#30253=CARTESIAN_POINT ( 'NONE',  ( 0.1870020358722072895, -0.7208919770472870248, 0.03184132201674819834 ) ) ;
#30255=CARTESIAN_POINT ( 'NONE',  ( 0.5446946726381876047, -1.168318774461527987, 0.4638875385414486519 ) ) ;
#30259=DIRECTION ( 'NONE',  ( 0.4999551463232372317, -0.8660512985181135770, 0.000000000000000000 ) ) ;
#30262=CARTESIAN_POINT ( 'NONE',  ( 0.5696125550597064269, -1.613556559779221189, 0.4687417262808790674 ) ) ;
#30263=( BOUNDED_SURFACE ( )  B_SPLINE_SURFACE ( 3, 2, ( 
 ( #32995, #23570, #4801 ),
 ( #36089, #19854, #17376 ),
 ( #14286, #26849, #20678 ),
 ( #39376, #36283, #35471 ),
 ( #8101, #33213, #5020 ),
 ( #30128, #1957, #16775 ) ),
 .UNSPECIFIED., .F., .F., .F. ) 
 B_SPLINE_SURFACE_WITH_KNOTS ( ( 4, 2, 4 ),
 ( 3, 3 ),
 ( 0.001110443675428536905, 0.001652974123862752283, 0.002195504572296967660 ),
 ( 0.3290584448501475134, 1.000000000000000000 ),
 .UNSPECIFIED. ) 
 GEOMETRIC_REPRESENTATION_ITEM ( )  RATIONAL_B_SPLINE_SURFACE ( (
 ( 0.8719303469039287879, 0.8053998383867736477, 1.000000000000000000),
 ( 0.8859245484685469574, 0.8266638444981970757, 1.000000000000000000),
 ( 0.8926552752790239964, 0.8368910957902011560, 1.000000000000000000),
 ( 0.8925234298264548283, 0.8366907583507090518, 1.000000000000000000),
 ( 0.8858040005613148082, 0.8264806735309744301, 1.000000000000000000),
 ( 0.8716885380514636239, 0.8050324130004183898, 1.000000000000000000) ) ) 
 REPRESENTATION_ITEM ( '' )  SURFACE ( )  );
#30264=CARTESIAN_POINT ( 'NONE',  ( 0.4248662974673952375, -1.105221816243816546, 0.5932897847886877685 ) ) ;
#30269=CARTESIAN_POINT ( 'NONE',  ( 0.2520126056674420467, -1.649747432069603059, 0.6712725404530499596 ) ) ;
#30270=CARTESIAN_POINT ( 'NONE',  ( 0.4709147388527493705, -1.070627459034787954, 0.6206731519243955386 ) ) ;
#30271=CARTESIAN_POINT ( 'NONE',  ( 0.01720488785744077667, -0.9349428739647406283, 0.5880094435653454576 ) ) ;
#30274=CARTESIAN_POINT ( 'NONE',  ( 0.1875000000000000833, -0.4595382586000822389, 0.1581505021253525878 ) ) ;
#30282=CARTESIAN_POINT ( 'NONE',  ( 0.06685945144431634790, -0.9180018650465318064, 0.7887301370685455559 ) ) ;
#30284=CARTESIAN_POINT ( 'NONE',  ( 0.5880818911069165544, -1.487943198408785195, 0.6309528828841184378 ) ) ;
#30285=CARTESIAN_POINT ( 'NONE',  ( 0.2968383989124028233, -1.657645728618910574, 0.4428167958024615269 ) ) ;
#30286=CARTESIAN_POINT ( 'NONE',  ( 0.2617247662751732706, -1.216060305431710509, 0.5682417262808779901 ) ) ;
#30290=CARTESIAN_POINT ( 'NONE',  ( 0.6183701179687098870, -1.298963174629117479, 0.5817474467243960445 ) ) ;
#30300=DIRECTION ( 'NONE',  ( 0.000000000000000000, 7.931692224083225994E-17, -1.000000000000000000 ) ) ;
#30305=CARTESIAN_POINT ( 'NONE',  ( 0.09670515779886533492, -1.286975611907339001, 0.5906344341303084722 ) ) ;
#30306=CARTESIAN_POINT ( 'NONE',  ( 0.1064200553386371317, -0.7359704961837734150, 0.3761014276636525655 ) ) ;
#30307=CARTESIAN_POINT ( 'NONE',  ( 0.1706599417108956573, -1.182744918713773519, 1.015904661483719496 ) ) ;
#30308=CARTESIAN_POINT ( 'NONE',  ( 0.4932909056524756863, -1.526258372065918412, 0.7003863106307628428 ) ) ;
#30309=CARTESIAN_POINT ( 'NONE',  ( 0.3203591660471408753, -1.762054173121580858, 0.5022354395982965292 ) ) ;
#30310=CARTESIAN_POINT ( 'NONE',  ( 0.6984807982178791175, -1.438753897344778432, 0.5682417262808779901 ) ) ;
#30311=CARTESIAN_POINT ( 'NONE',  ( 0.01762532016806284130, -0.9532778069939448207, 0.3090308271854356192 ) ) ;
#30312=ORIENTED_EDGE ( 'NONE', *, *, #13551, .F. ) ;
#30316=CARTESIAN_POINT ( 'NONE',  ( 0.4339004961413100991, -1.102577184751369455, 0.8888993553986003215 ) ) ;
#30318=CARTESIAN_POINT ( 'NONE',  ( 0.4686742901286617413, -1.116548677541408185, 0.5688640544436303070 ) ) ;
#30320=CARTESIAN_POINT ( 'NONE',  ( 0.3764398274533635180, -1.163784180705809579, 0.4182417262808778013 ) ) ;
#30322=CARTESIAN_POINT ( 'NONE',  ( 0.3182873482898154749, -1.183781612718975307, 0.5020472072821947629 ) ) ;
#30323=CARTESIAN_POINT ( 'NONE',  ( 0.3883356530642981808, -0.9654559656950375546, 0.7100763952745350327 ) ) ;
#30324=ADVANCED_FACE ( 'NONE', ( #1336 ), #23737, .T. ) ;
#30327=CIRCLE ( 'NONE', #25080, 0.07749999999977547072 ) ;
#30330=ADVANCED_FACE ( 'NONE', ( #17564 ), #9605, .T. ) ;
#30335=EDGE_CURVE ( 'NONE', #33860, #528, #17029, .T. ) ;
#30337=ORIENTED_EDGE ( 'NONE', *, *, #440, .F. ) ;
#30341=CARTESIAN_POINT ( 'NONE',  ( 0.2042129071158758913, -1.305677593605112152, 0.6884246345324352978 ) ) ;
#30342=ORIENTED_EDGE ( 'NONE', *, *, #7422, .T. ) ;
#30346=EDGE_CURVE ( 'NONE', #13751, #26649, #7169, .T. ) ;
#30350=CARTESIAN_POINT ( 'NONE',  ( 0.4687069519024180120, -1.239395243040063654, 0.5932013480186181242 ) ) ;
#30355=ORIENTED_EDGE ( 'NONE', *, *, #36054, .F. ) ;
#30358=CARTESIAN_POINT ( 'NONE',  ( 0.07317269111354535172, -1.324861932786149055, 0.5593322111943830333 ) ) ;
#30364=CARTESIAN_POINT ( 'NONE',  ( 0.06225588220789115418, -0.5681044914483278641, 0.2679612960194602822 ) ) ;
#30365=CARTESIAN_POINT ( 'NONE',  ( 0.06728514184456915737, -0.6483875930907525564, 0.003017575880453532335 ) ) ;
#30367=CARTESIAN_POINT ( 'NONE',  ( 0.3048172866937527425, -1.756813269515922205, 0.5623665267386828148 ) ) ;
#30372=CARTESIAN_POINT ( 'NONE',  ( 0.1222449228537752230, -0.5597973469825100468, 0.2087343094629943718 ) ) ;
#30373=CARTESIAN_POINT ( 'NONE',  ( 0.4773536554779886365, -1.668348979080164884, 0.5692827505350450679 ) ) ;
#30374=DIRECTION ( 'NONE',  ( 1.000000000000000000, 0.000000000000000000, 0.000000000000000000 ) ) ;
#30376=CARTESIAN_POINT ( 'NONE',  ( 0.1718769070500368867, -1.267826361270228519, 0.4341930484031654158 ) ) ;
#30377=CARTESIAN_POINT ( 'NONE',  ( 0.07775718790500896205, -1.310864069790921738, 0.4781538619239825705 ) ) ;
#30378=CARTESIAN_POINT ( 'NONE',  ( 0.2282946535672089883, -1.235122852095027479, 0.5557842531242198625 ) ) ;
#30379=CARTESIAN_POINT ( 'NONE',  ( 0.1883801994403443147, -0.4771412664261568959, 0.2456734866192890887 ) ) ;
#30381=CARTESIAN_POINT ( 'NONE',  ( 0.3740960844805631957, -1.108072201694596526, 0.5182417262812423209 ) ) ;
#30383=ADVANCED_FACE ( 'NONE', ( #30511 ), #17951, .T. ) ;
#30386=CARTESIAN_POINT ( 'NONE',  ( 0.5912368146451574269, -1.616255995515891941, 0.5832502196827238361 ) ) ;
#30392=CARTESIAN_POINT ( 'NONE',  ( 0.002089204316143729572, -0.4812299151504488837, 0.2002484561318531031 ) ) ;
#30393=DIRECTION ( 'NONE',  ( 0.8660512985181133550, 0.4999551463232372317, 0.000000000000000000 ) ) ;
#30396=B_SPLINE_SURFACE_WITH_KNOTS ( 'NONE', 3, 3, ( 
 ( #37004, #24272, #11519, #12121, #21790, #6135, #5525, #36608, #18091, #8823, #31042, #20980, #2264, #37217, #18485, #30644, #2468, #8412, #33498, #30835, #21401, #27369, #33939, #14803, #24885, #5304, #5737, #21597, #34121, #37407, #18296 ),
 ( #15197, #27755, #40290, #5923, #15407, #27965, #40504, #12327, #9219, #28580, #30841, #21605, #37837, #3080, #9650, #40295, #15418, #12129, #31458, #31050, #18302, #27973, #25081, #22218, #9842, #18709, #27762, #15816, #33944, #34736, #6541 ),
 ( #28171, #19117, #37415, #24693, #12731, #12949, #5930, #37616, #18496, #34127, #2663, #15206, #31656, #37224, #38030, #3476, #9225, #9042, #2867, #40511, #9437, #28369, #12334, #21799, #24891, #25297, #25496, #34331, #22020, #6144, #31266 ),
 ( #16031, #453, #5744, #12526, #15624, #35, #34542, #3265, #235, #6349, #18922, #29576, #22833, #16630, #35750, #20138, #34942, #10053, #38630, #22623, #7145, #35159, #39036, #23017, #32665, #4469, #19528, #22411, #32062, #35354, #1232 ),
 ( #13549, #3870, #19712, #637, #16421, #29176, #28962, #13128, #25692, #38431, #38225, #17037, #29386, #13730, #25911, #19918, #32242, #1043, #10450, #26297, #6747, #1418, #19325, #6958, #38822, #828, #16241, #10271, #4065, #16846, #13933 ),
 ( #10654, #13338, #28779, #26120, #35537, #7341, #31866, #26504, #32453, #4278, #23226, #7564, #3682, #20749, #39246, #36352, #11261, #14542, #14146, #21138, #29994, #5078, #14760, #14343, #4657, #30392, #30601, #23629, #27107, #36146, #11067 ),
 ( #7956, #26906, #33064, #11474, #8169, #17442, #1827, #23831, #24041, #20530, #36569, #33667, #8374, #33272, #39641, #5481, #20941, #17638, #4871, #23442, #2223, #24231, #18044, #27324, #30185, #2015, #27516, #29783, #39438, #33463, #5270 ) ),
 .UNSPECIFIED., .F., .F., .F.,
 ( 4, 1, 1, 1, 4 ),
 ( 4, 1, 1, 1, 1, 1, 1, 1, 1, 1, 1, 1, 1, 1, 1, 1, 1, 1, 1, 1, 1, 1, 1, 1, 1, 3, 4 ),
 ( 0.000000000000000000, 0.2500000000000000000, 0.5000000000000000000, 0.7500000000000000000, 1.000000000000000000 ),
 ( 0.000000000000000000, 0.03051875000000000074, 0.04577812500000000978, 0.06103750000000000148, 0.09155625000000001956, 0.1220750000000000030, 0.1525937500000000002, 0.1831125000000000391, 0.2136312499999999948, 0.2441500000000000059, 0.2993062499999999959, 0.3544624999999999027, 0.4096187500000000314, 0.4647750000000000492, 0.5199312500000002890, 0.5750875000000000847, 0.6302437499999999915, 0.6854000000000000092, 0.7247249999999998415, 0.7640500000000001180, 0.8033749999999999503, 0.8427000000000000046, 0.8820249999999999480, 0.9213500000000000023, 0.9606749999999998346, 1.000000000000000000, 1.037727370758942724 ),
 .UNSPECIFIED. ) ;
#30400=CARTESIAN_POINT ( 'NONE',  ( 0.3948127461878784827, -1.136156435014139099, 0.6057297418123517296 ) ) ;
#30403=CARTESIAN_POINT ( 'NONE',  ( 0.4697754283568603695, -1.248084093760120750, 0.7319325641689681250 ) ) ;
#30406=CARTESIAN_POINT ( 'NONE',  ( 0.3472154721327633808, -0.9812419721698063535, 0.6178014265861627718 ) ) ;
#30411=DIRECTION ( 'NONE',  ( -0.4999551463232372317, 0.8660512985181135770, -0.000000000000000000 ) ) ;
#30414=CARTESIAN_POINT ( 'NONE',  ( 0.03562321441245916431, -0.5363712146287933358, 0.1738714753025889515 ) ) ;
#30415=CARTESIAN_POINT ( 'NONE',  ( 0.7034871982223843689, -1.518834583483278156, 0.5648842057115460724 ) ) ;
#30416=CARTESIAN_POINT ( 'NONE',  ( 0.1882863373429763676, -0.5192882382158404697, 0.1376832038832177529 ) ) ;
#30418=AXIS2_PLACEMENT_3D ( 'NONE', #5919, #18480, #16409 ) ;
#30421=CARTESIAN_POINT ( 'NONE',  ( 0.3856095533780636853, -0.9746514165089328330, 0.6873212698995325720 ) ) ;
#30426=AXIS2_PLACEMENT_3D ( 'NONE', #23627, #33059, #27321 ) ;
#30427=CARTESIAN_POINT ( 'NONE',  ( 0.1072518627510686412, -0.8713630855471795611, 0.4911467596464663132 ) ) ;
#30430=DIRECTION ( 'NONE',  ( -1.000000000000000000, -0.000000000000000000, -0.000000000000000000 ) ) ;
#30432=CARTESIAN_POINT ( 'NONE',  ( 0.3756489996570800405, -1.097449264068310670, 0.6348451176221490133 ) ) ;
#30436=CARTESIAN_POINT ( 'NONE',  ( 0.1852706725762902906, -0.8388893584440290097, 0.1474376482679014555 ) ) ;
#30440=CARTESIAN_POINT ( 'NONE',  ( 0.4768631172705831145, -1.133883247812649930, 0.4707179390482816861 ) ) ;
#30441=CARTESIAN_POINT ( 'NONE',  ( 0.4546337798721356571, -1.243669536373561701, 0.6057417262809813296 ) ) ;
#30443=B_SPLINE_CURVE_WITH_KNOTS ( 'NONE', 3,
 ( #4155, #17117, #29666, #26601 ),
 .UNSPECIFIED., .F., .F.,
 ( 4, 4 ),
 ( 4.336808689942017736E-19, 0.0004444667336122164083 ),
 .UNSPECIFIED. ) ;
#30444=CARTESIAN_POINT ( 'NONE',  ( 0.01211358213722261989, -0.4403755143391286375, 0.06599023287002830918 ) ) ;
#30450=VERTEX_POINT ( 'NONE', #3143 ) ;
#30455=CARTESIAN_POINT ( 'NONE',  ( 0.0007308754721319292262, -0.6160987163282929391, 0.002788468881659194980 ) ) ;
#30462=CARTESIAN_POINT ( 'NONE',  ( 0.2562100995515492197, -1.500925799399086102, 0.8984186356539709539 ) ) ;
#30465=CARTESIAN_POINT ( 'NONE',  ( 0.1840567930975518796, -0.8547793429265486687, 0.1477568935609660794 ) ) ;
#30470=ORIENTED_EDGE ( 'NONE', *, *, #33570, .T. ) ;
#30473=CARTESIAN_POINT ( 'NONE',  ( 0.2805973409072567981, -0.9951498133751814912, 0.7619205245393454451 ) ) ;
#30474=CARTESIAN_POINT ( 'NONE',  ( 0.02011115336535013176, -1.001108279069293339, 0.5117138269811281059 ) ) ;
#30475=FACE_OUTER_BOUND ( 'NONE', #28937, .T. ) ;
#30482=CARTESIAN_POINT ( 'NONE',  ( 0.3067120372624415614, -1.770199942203851240, 0.4177417262808785781 ) ) ;
#30487=CARTESIAN_POINT ( 'NONE',  ( 0.2491647336858476003, -1.658092311124387708, 0.5917354811442696594 ) ) ;
#30491=CARTESIAN_POINT ( 'NONE',  ( 0.6277259471038021399, -1.316916163187945799, 0.8316945246157878557 ) ) ;
#30497=CARTESIAN_POINT ( 'NONE',  ( 0.1072529199298410257, -1.089089271014722859, 0.8806249471138073437 ) ) ;
#30499=CARTESIAN_POINT ( 'NONE',  ( 0.1397421702044318870, -0.6236803416123793964, 0.3668591128627327058 ) ) ;
#30503=VECTOR ( 'NONE', #29511, 39.37007874015748854 ) ;
#30504=CARTESIAN_POINT ( 'NONE',  ( 0.5081268369560435483, -1.127385812641128693, 0.7490048996577514107 ) ) ;
#30507=CARTESIAN_POINT ( 'NONE',  ( 0.6383297146155822999, -1.332514953497987653, 0.7863315818369056576 ) ) ;
#30511=FACE_OUTER_BOUND ( 'NONE', #22173, .T. ) ;
#30513=FACE_OUTER_BOUND ( 'NONE', #16396, .T. ) ;
#30516=CARTESIAN_POINT ( 'NONE',  ( 0.08789146819946426492, -0.7060428058465696433, 0.1983783520454339422 ) ) ;
#30518=CARTESIAN_POINT ( 'NONE',  ( 0.2001820407311839800, -1.287744702331634850, 1.033572112086078132 ) ) ;
#30519=CARTESIAN_POINT ( 'NONE',  ( 0.3218516010127101534, -1.144099206277331637, 0.8304979311448332790 ) ) ;
#30521=CARTESIAN_POINT ( 'NONE',  ( 0.3263383112081457149, -1.765042748300605480, 0.4949248276282361969 ) ) ;
#30522=CARTESIAN_POINT ( 'NONE',  ( -0.001418955495163486775, -0.8211291000492192405, 0.04345076978617073982 ) ) ;
#30523=CARTESIAN_POINT ( 'NONE',  ( 0.06244861065054558430, -1.151270256393961855, 0.6619143190264936694 ) ) ;
#30525=ORIENTED_EDGE ( 'NONE', *, *, #4503, .T. ) ;
#30528=CARTESIAN_POINT ( 'NONE',  ( 0.6324602634195602979, -1.323077396536881611, 0.7914183504951575188 ) ) ;
#30529=EDGE_CURVE ( 'NONE', #35222, #31881, #6842, .T. ) ;
#30534=CARTESIAN_POINT ( 'NONE',  ( 0.5536297569049346556, -1.186194075236972179, 0.6057417262809815517 ) ) ;
#30537=CARTESIAN_POINT ( 'NONE',  ( 0.3200100717190457189, -1.182867460163126827, 0.5426201052292141114 ) ) ;
#30538=CARTESIAN_POINT ( 'NONE',  ( 0.1874999999999996669, -0.6872203660140441261, 0.1527381444932270627 ) ) ;
#30539=AXIS2_PLACEMENT_3D ( 'NONE', #18442, #15366, #37366 ) ;
#30554=CARTESIAN_POINT ( 'NONE',  ( 0.2245284881113566167, -1.347762582730240855, 0.6028807914139896473 ) ) ;
#30560=TOROIDAL_SURFACE ( 'NONE', #35181, 0.08249999999977555842, 0.01000000000000000021 ) ;
#30561=CARTESIAN_POINT ( 'NONE',  ( 0.4462378990239732057, -1.204432223294487736, 0.6536530620140627024 ) ) ;
#30564=FACE_OUTER_BOUND ( 'NONE', #3443, .T. ) ;
#30566=ORIENTED_EDGE ( 'NONE', *, *, #36557, .F. ) ;
#30567=CARTESIAN_POINT ( 'NONE',  ( 0.1665205398182600938, -0.7441302385869247304, 0.6010756574681124231 ) ) ;
#30568=ORIENTED_EDGE ( 'NONE', *, *, #14080, .F. ) ;
#30571=CARTESIAN_POINT ( 'NONE',  ( 0.4422158392730773380, -1.563691297916808942, 0.6860588747619075223 ) ) ;
#30581=CARTESIAN_POINT ( 'NONE',  ( 0.1224514167073170456, -0.5493860373880040671, 0.1534799437718065152 ) ) ;
#30583=CARTESIAN_POINT ( 'NONE',  ( 0.4788258031900825551, -1.664885640230176600, 0.5089736068239121280 ) ) ;
#30588=CARTESIAN_POINT ( 'NONE',  ( 0.1840555659586733950, -0.8547793250687044653, 0.1470778270918790542 ) ) ;
#30589=CARTESIAN_POINT ( 'NONE',  ( 0.4627885704097156050, -1.051432690887019072, 0.8329284434066291931 ) ) ;
#30592=CARTESIAN_POINT ( 'NONE',  ( 0.002591829603766808172, -0.9558483906305602629, 0.3895703071142478380 ) ) ;
#30601=CARTESIAN_POINT ( 'NONE',  ( 0.002083146443013521830, -0.4777046557262296100, 0.1638349238242636507 ) ) ;
#30603=CARTESIAN_POINT ( 'NONE',  ( 0.1700561810475392510, -1.268507724650295154, 0.5481991909815175923 ) ) ;
#30608=CARTESIAN_POINT ( 'NONE',  ( 0.3832544727030278708, -1.109930869253659580, 0.6055776681277141860 ) ) ;
#30611=CARTESIAN_POINT ( 'NONE',  ( 0.5229569312828943328, -1.333528584511481263, 0.5864232016723698315 ) ) ;
#30614=CARTESIAN_POINT ( 'NONE',  ( 0.3243638931714790674, -0.9652511992726795498, 0.5977393664509621507 ) ) ;
#30615=ORIENTED_EDGE ( 'NONE', *, *, #37884, .T. ) ;
#30619=EDGE_CURVE ( 'NONE', #11729, #35903, #25152, .T. ) ;
#30620=ORIENTED_EDGE ( 'NONE', *, *, #8448, .T. ) ;
#30621=CARTESIAN_POINT ( 'NONE',  ( 0.1808581208431125631, -1.125631630136205930, 0.8751935381423019411 ) ) ;
#30622=CARTESIAN_POINT ( 'NONE',  ( 0.06569956760428707909, -0.7774221683014203022, 0.02818812589258910817 ) ) ;
#30623=CARTESIAN_POINT ( 'NONE',  ( 0.1872764685775445970, -0.5763073854982146971, 0.01999799437810716521 ) ) ;
#30626=VERTEX_POINT ( 'NONE', #7028 ) ;
#30628=CARTESIAN_POINT ( 'NONE',  ( 0.5261597028464496395, -1.142846293380767264, 0.6481300216459130459 ) ) ;
#30629=CARTESIAN_POINT ( 'NONE',  ( 0.1162913698539808915, -0.5588670519132078462, 0.2094242198637762120 ) ) ;
#30633=CARTESIAN_POINT ( 'NONE',  ( 0.2262118641390306883, -1.103574613869289234, 0.7477357049086994500 ) ) ;
#30640=CARTESIAN_POINT ( 'NONE',  ( 0.3055995149173200143, -1.768272766478771185, 0.5197417262808792238 ) ) ;
#30641=( BOUNDED_SURFACE ( )  B_SPLINE_SURFACE ( 3, 2, ( 
 ( #25361, #15068, #33991 ),
 ( #34184, #18154, #37896 ),
 ( #2723, #9707, #27620 ),
 ( #24545, #5596, #31507 ) ),
 .UNSPECIFIED., .F., .F., .F. ) 
 B_SPLINE_SURFACE_WITH_KNOTS ( ( 4, 4 ),
 ( 3, 3 ),
 ( 0.01439476971272923671, 0.01576594042374710250 ),
 ( 0.4842859667072808572, 1.000000000000000000 ),
 .UNSPECIFIED. ) 
 GEOMETRIC_REPRESENTATION_ITEM ( )  RATIONAL_B_SPLINE_SURFACE ( (
 ( 0.8474955426738830511, 0.8425471025280649728, 1.000000000000000000),
 ( 0.8464882319828066493, 0.8415071067814141603, 1.000000000000000000),
 ( 0.8455725881407269995, 0.8405617522749588844, 1.000000000000000000),
 ( 0.8449979516945560487, 0.8399684701176437507, 1.000000000000000000) ) ) 
 REPRESENTATION_ITEM ( '' )  SURFACE ( )  );
#30642=DIRECTION ( 'NONE',  ( 0.01455087615875037474, 0.9998941303973200023, 0.000000000000000000 ) ) ;
#30643=CARTESIAN_POINT ( 'NONE',  ( 0.6527381946072837726, -1.527960125060469299, 0.4182417262808776903 ) ) ;
#30644=CARTESIAN_POINT ( 'NONE',  ( 0.01632176102313256591, -1.052923364454138255, 0.5995154855756178458 ) ) ;
#30649=CARTESIAN_POINT ( 'NONE',  ( 0.4837052721322094295, -1.131465354378136334, 0.4851784429646056052 ) ) ;
#30650=CARTESIAN_POINT ( 'NONE',  ( 0.3689410297595501764, -1.154863930213027690, 0.5443150188217301677 ) ) ;
#30652=CARTESIAN_POINT ( 'NONE',  ( 0.0003813859085855243985, -0.4500436584032703746, 0.06912418163519741532 ) ) ;
#30664=CARTESIAN_POINT ( 'NONE',  ( 0.001740155361229381867, -0.5357720371266511128, 0.07346349438433615042 ) ) ;
#30665=ORIENTED_EDGE ( 'NONE', *, *, #31414, .T. ) ;
#30670=CARTESIAN_POINT ( 'NONE',  ( -0.0004184392737591126517, -0.5575462098935206612, 0.2717930660292434131 ) ) ;
#30671=CARTESIAN_POINT ( 'NONE',  ( 0.1655461965905788702, -0.9040591713125657458, 0.5924644706352264478 ) ) ;
#30672=CARTESIAN_POINT ( 'NONE',  ( 0.1118412691610174287, -1.266776148485620146, 0.6017280176731151231 ) ) ;
#30675=EDGE_CURVE ( 'NONE', #11923, #36916, #18700, .T. ) ;
#30680=CARTESIAN_POINT ( 'NONE',  ( 0.3204479958614548929, -1.182666560659948907, 0.5682417262808776570 ) ) ;
#30683=CARTESIAN_POINT ( 'NONE',  ( 0.4749030200414927627, -1.260576499757741553, 0.8114222651001881115 ) ) ;
#30684=CARTESIAN_POINT ( 'NONE',  ( 0.01508763455763984483, -0.9705204025707556692, 0.4143134863502723197 ) ) ;
#30685=CARTESIAN_POINT ( 'NONE',  ( 0.4751248519516730884, -1.681100737592190031, 0.5628962907142390781 ) ) ;
#30686=CARTESIAN_POINT ( 'NONE',  ( 0.1696489863018690591, -1.274013792877867646, 0.9327432631391745499 ) ) ;
#30689=AXIS2_PLACEMENT_3D ( 'NONE', #2367, #39989, #11810 ) ;
#30691=CARTESIAN_POINT ( 'NONE',  ( 1.480025787077754007, -0.6872203660140440151, 0.1457185332388702959 ) ) ;
#30692=CARTESIAN_POINT ( 'NONE',  ( 0.3912168351225406848, -1.712565751828606153, 0.4687417262808791230 ) ) ;
#30693=CARTESIAN_POINT ( 'NONE',  ( 0.4643862794852260945, -1.116283308840022803, 0.5648439556958982921 ) ) ;
#30696=CARTESIAN_POINT ( 'NONE',  ( 0.2518326032030922534, -1.639413698222365046, 0.7148483533190357342 ) ) ;
#30697=CARTESIAN_POINT ( 'NONE',  ( 0.07414496827190548978, -1.147132939374254423, 0.7606844393218312739 ) ) ;
#30699=CARTESIAN_POINT ( 'NONE',  ( 0.6930531720067659718, -1.422936651082730375, 0.7544454077531311809 ) ) ;
#30701=CARTESIAN_POINT ( 'NONE',  ( 0.6653925203977772984, -1.561488534969799113, 0.6071316550003039714 ) ) ;
#30706=CARTESIAN_POINT ( 'NONE',  ( 0.03846717227426538904, -0.7578942448716873281, 0.6192360675337290621 ) ) ;
#30707=CARTESIAN_POINT ( 'NONE',  ( 0.5182826642499327452, -1.390450437559696217, 0.7925567997242233265 ) ) ;
#30710=CARTESIAN_POINT ( 'NONE',  ( 0.6014934134068773419, -1.267756190114700976, 0.6768762346975223387 ) ) ;
#30713=CARTESIAN_POINT ( 'NONE',  ( 0.2821966830767973500, -0.7863026750338284465, 0.6043004553601608597 ) ) ;
#30719=ORIENTED_EDGE ( 'NONE', *, *, #24094, .F. ) ;
#30720=CARTESIAN_POINT ( 'NONE',  ( 0.08707804302881141933, -0.7047988938172153883, 0.1683407647532852991 ) ) ;
#30721=CARTESIAN_POINT ( 'NONE',  ( 0.3158115486623674362, -1.764399868795166304, 0.6580999141868399960 ) ) ;
#30722=CARTESIAN_POINT ( 'NONE',  ( 0.4982596037652018972, -1.542515356531135584, 0.5876215343849920947 ) ) ;
#30724=CARTESIAN_POINT ( 'NONE',  ( 0.001618903166729741003, -0.5421073043963201554, 0.06143527706437781205 ) ) ;
#30727=ORIENTED_EDGE ( 'NONE', *, *, #1364, .T. ) ;
#30729=CARTESIAN_POINT ( 'NONE',  ( 0.3967733525505006686, -1.041653198288154725, 0.8729704400460266411 ) ) ;
#30735=CARTESIAN_POINT ( 'NONE',  ( 0.3169982175285875337, -1.184547601087671875, 0.5195431689978142753 ) ) ;
#30736=CARTESIAN_POINT ( 'NONE',  ( 0.4926052497631904226, -1.101322287461897975, 0.6863075852112333619 ) ) ;
#30737=B_SPLINE_SURFACE_WITH_KNOTS ( 'NONE', 5, 5, ( 
 ( #28800, #261, #12758, #25319, #16058, #37860 ),
 ( #9674, #22243, #25714, #28603, #38245, #6984 ),
 ( #854, #40012, #11835, #26690, #24395, #7738 ),
 ( #20302, #14117, #36318, #11647, #20919, #33245 ),
 ( #1591, #30160, #33439, #32822, #5247, #26878 ),
 ( #4628, #24206, #39608, #27295, #14319, #17202 ) ),
 .UNSPECIFIED., .F., .F., .F.,
 ( 6, 6 ),
 ( 6, 6 ),
 ( -5.904618948009931145, 5.904618948009923152 ),
 ( -4.007879036389231153, 1.896739911619200303 ),
 .UNSPECIFIED. ) ;
#30741=CARTESIAN_POINT ( 'NONE',  ( 0.6077786581711973612, -1.479275016670621667, 0.5594553644565639638 ) ) ;
#30745=CARTESIAN_POINT ( 'NONE',  ( 0.4215912490580301930, -1.142508127983099309, 0.4283266193199111727 ) ) ;
#30751=CARTESIAN_POINT ( 'NONE',  ( 0.01476761613299030704, -0.8638487819985384286, 0.3976658538871967741 ) ) ;
#30756=CARTESIAN_POINT ( 'NONE',  ( 0.7412791958894395794, -1.507305061506947430, 0.6536223584324379887 ) ) ;
#30758=CARTESIAN_POINT ( 'NONE',  ( 0.4591678779736387273, -1.223483637120778011, 0.6328851562681094833 ) ) ;
#30759=CARTESIAN_POINT ( 'NONE',  ( 0.2085781299520444998, -1.361703007109797525, 0.5547567937505603064 ) ) ;
#30763=CARTESIAN_POINT ( 'NONE',  ( 0.1266021694322588542, -1.239399129679921829, 0.5182417262812423209 ) ) ;
#30766=CARTESIAN_POINT ( 'NONE',  ( 0.3497955937797163073, -1.368691204837882980, 0.8715010437854141534 ) ) ;
#30769=CARTESIAN_POINT ( 'NONE',  ( 0.5672950941327136176, -1.626571888027773527, 0.5062501768905920407 ) ) ;
#30773=ORIENTED_EDGE ( 'NONE', *, *, #37884, .F. ) ;
#30776=CARTESIAN_POINT ( 'NONE',  ( 0.1223607623319934723, -0.5629964153041870922, 0.2193006277981656427 ) ) ;
#30777=CARTESIAN_POINT ( 'NONE',  ( 0.4226000438817392180, -1.709616762427841996, 0.4282184315516495143 ) ) ;
#30783=CARTESIAN_POINT ( 'NONE',  ( 0.1840595033465176056, -0.8547675690073376353, 0.1457166466292989515 ) ) ;
#30784=CARTESIAN_POINT ( 'NONE',  ( 0.1900797982425219412, -0.5100199057060679220, 0.2041009711615301980 ) ) ;
#30786=CARTESIAN_POINT ( 'NONE',  ( 0.0003691823678324147721, -0.9420571173525413844, 0.2855820445452574852 ) ) ;
#30787=B_SPLINE_CURVE_WITH_KNOTS ( 'NONE', 3,
 ( #19370, #9691, #24924, #16078, #25124 ),
 .UNSPECIFIED., .F., .F.,
 ( 4, 1, 4 ),
 ( 0.1498428223741591070, 0.2500000000004219403, 0.3316920714935439052 ),
 .UNSPECIFIED. ) ;
#30791=CARTESIAN_POINT ( 'NONE',  ( 0.6254352837214305350, -1.595686027468073753, 0.6076023449066322302 ) ) ;
#30798=ADVANCED_FACE ( 'NONE', ( #14406 ), #26968, .F. ) ;
#30799=CARTESIAN_POINT ( 'NONE',  ( 0.1825980849618502877, -1.261391773294454399, 0.5182417262812422099 ) ) ;
#30804=CARTESIAN_POINT ( 'NONE',  ( 0.3713765372429593259, -1.116629982321883041, 0.6056053568277999233 ) ) ;
#30807=CARTESIAN_POINT ( 'NONE',  ( 0.5305547748358091509, -1.344461649844473694, 0.6320627015115972691 ) ) ;
#30810=CARTESIAN_POINT ( 'NONE',  ( 0.2803482358567763177, -0.9348470554797825294, 0.5439829518127811125 ) ) ;
#30815=CARTESIAN_POINT ( 'NONE',  ( 0.009682433437374710072, -0.5618920970707950158, 0.04941970624388019456 ) ) ;
#30817=CARTESIAN_POINT ( 'NONE',  ( 0.2894994844286561952, -1.428162831126878141, 0.8955990884091332704 ) ) ;
#30819=DIRECTION ( 'NONE',  ( -0.0001066307966867950538, 1.551735798909011778E-06, 0.9999999943137325431 ) ) ;
#30820=CARTESIAN_POINT ( 'NONE',  ( 0.1126304012248214304, -0.7661081300572403219, -0.08267986882272944371 ) ) ;
#30824=CARTESIAN_POINT ( 'NONE',  ( 0.3822464718857132571, -1.102226274216854263, 0.6317401270923076462 ) ) ;
#30825=CARTESIAN_POINT ( 'NONE',  ( 0.1162134951484129625, -0.5489498940799030224, 0.1618951865093009590 ) ) ;
#30831=CARTESIAN_POINT ( 'NONE',  ( 0.4257622994621999557, -1.693842739163180289, 0.4182417262808084124 ) ) ;
#30832=CARTESIAN_POINT ( 'NONE',  ( 0.7471901070607220863, -1.513130089782565468, 0.5197417262808792238 ) ) ;
#30833=DIRECTION ( 'NONE',  ( 0.4999551463232372317, -0.8660512985181135770, 0.000000000000000000 ) ) ;
#30835=CARTESIAN_POINT ( 'NONE',  ( 0.004725042054567132541, -0.9785087964782590575, 0.4373990939698282343 ) ) ;
#30837=CARTESIAN_POINT ( 'NONE',  ( 0.4873057611341404805, -1.123973904486345932, 0.5217046469155847133 ) ) ;
#30838=CARTESIAN_POINT ( 'NONE',  ( 0.4545629988304267788, -1.243546925348286036, 0.6057417262809815517 ) ) ;
#30841=CARTESIAN_POINT ( 'NONE',  ( 0.05825416142610396336, -1.237506905460590723, 0.6972702062804553291 ) ) ;
#30844=CARTESIAN_POINT ( 'NONE',  ( 0.02309053091563895849, -0.6171704500300686513, 0.5838629695588271051 ) ) ;
#30854=CARTESIAN_POINT ( 'NONE',  ( 0.001701916547476807961, -0.5482314149877699494, 0.06752930009528983202 ) ) ;
#30859=EDGE_CURVE ( 'NONE', #6171, #16949, #37642, .T. ) ;
#30860=CARTESIAN_POINT ( 'NONE',  ( 0.2666310949013298015, -1.675413163925608240, 0.5768915532334314422 ) ) ;
#30861=CARTESIAN_POINT ( 'NONE',  ( 0.2318711984724983466, -0.9643490876729370331, 0.6839831110571921169 ) ) ;
#30862=CARTESIAN_POINT ( 'NONE',  ( 0.08672459768460706597, -1.302515868427265078, 0.5757131974872962132 ) ) ;
#30868=ORIENTED_EDGE ( 'NONE', *, *, #18433, .F. ) ;
#30869=ORIENTED_EDGE ( 'NONE', *, *, #37116, .T. ) ;
#30871=CARTESIAN_POINT ( 'NONE',  ( 0.01167908229743947097, -0.7459992564288900896, -0.1065741914396502593 ) ) ;
#30874=CARTESIAN_POINT ( 'NONE',  ( 0.4660932482496507046, -1.246255835518915056, 0.7959364137991218335 ) ) ;
#30877=CARTESIAN_POINT ( 'NONE',  ( 0.2687203115727492264, -1.674044157977605529, 0.5754666865148680976 ) ) ;
#30878=B_SPLINE_CURVE_WITH_KNOTS ( 'NONE', 3,
 ( #15855, #2908, #9264, #2698, #31303, #6575 ),
 .UNSPECIFIED., .F., .F.,
 ( 4, 2, 4 ),
 ( 1.734723475976807094E-18, 0.0003446483068616760137, 0.0006892966137233502927 ),
 .UNSPECIFIED. ) ;
#30879=CARTESIAN_POINT ( 'NONE',  ( 0.3186320389496528627, -1.760431904683431359, 0.5682417262808792113 ) ) ;
#30882=CARTESIAN_POINT ( 'NONE',  ( 0.4790130493689879199, -1.660633143797948241, 0.5197417262808792238 ) ) ;
#30883=CARTESIAN_POINT ( 'NONE',  ( 0.4026494850530986658, -1.127712942440639354, 0.6048530416235159413 ) ) ;
#30887=CARTESIAN_POINT ( 'NONE',  ( 0.04402670621142950463, -0.8156408044542829971, 0.6980404683681784572 ) ) ;
#30888=CARTESIAN_POINT ( 'NONE',  ( 0.06797834727357382478, -1.112657892433854601, 0.7541383320516555910 ) ) ;
#30890=CARTESIAN_POINT ( 'NONE',  ( 0.4077406957728484382, -0.9605384586880818532, 0.7982698588713066368 ) ) ;
#30892=EDGE_CURVE ( 'NONE', #14547, #38007, #29273, .T. ) ;
#30894=EDGE_CURVE ( 'NONE', #35903, #8335, #22684, .T. ) ;
#30899=CARTESIAN_POINT ( 'NONE',  ( 0.2082049042024939622, -1.421168782641690331, 0.9443853284052463604 ) ) ;
#30900=CARTESIAN_POINT ( 'NONE',  ( 0.1370985950931609409, -0.6139791525162832109, 0.3469096356793540670 ) ) ;
#30903=CARTESIAN_POINT ( 'NONE',  ( 0.3883356530642981808, -0.9654559656950375546, 0.7100763952745350327 ) ) ;
#30906=CARTESIAN_POINT ( 'NONE',  ( 0.6176316048552610294, -1.299348609076425465, 0.8015369670086561760 ) ) ;
#30909=AXIS2_PLACEMENT_3D ( 'NONE', #15018, #24286, #34133 ) ;
#30912=CARTESIAN_POINT ( 'NONE',  ( 0.1188348172803932595, -0.7700990686786346462, 0.4311705954416762410 ) ) ;
#30913=CARTESIAN_POINT ( 'NONE',  ( 0.3099360783079950776, -1.765723348835396500, 0.5687896325050014745 ) ) ;
#30915=CARTESIAN_POINT ( 'NONE',  ( 0.1039748750666900368, -0.5515957074706057117, 0.1901347062354882822 ) ) ;
#30916=CARTESIAN_POINT ( 'NONE',  ( 0.3247543563050922510, -1.762377147708333869, 0.4950365382291579963 ) ) ;
#30917=CARTESIAN_POINT ( 'NONE',  ( 0.001718405772027072368, -0.5368582204607379449, 0.07123562922874224212 ) ) ;
#30921=CARTESIAN_POINT ( 'NONE',  ( 0.4551067410287782389, -1.681698096176633017, 0.5857470455520834562 ) ) ;
#30922=CARTESIAN_POINT ( 'NONE',  ( 0.2952210513486213661, -0.8093524416240758246, 0.6262659740586482560 ) ) ;
#30928=CARTESIAN_POINT ( 'NONE',  ( 0.3325622382765076046, -1.175505464167819536, 0.4487935994522243566 ) ) ;
#30929=CARTESIAN_POINT ( 'NONE',  ( 0.2139922239084591227, -0.7322259512090013578, 0.4012976140435131622 ) ) ;
#30932=AXIS2_PLACEMENT_3D ( 'NONE', #9338, #22135, #25412 ) ;
#30938=B_SPLINE_CURVE_WITH_KNOTS ( 'NONE', 3,
 ( #35167, #34951, #6757, #10461, #16251, #7351 ),
 .UNSPECIFIED., .F., .F.,
 ( 4, 2, 4 ),
 ( 0.003112475973527875465, 0.003739261459126928984, 0.004366046944725982502 ),
 .UNSPECIFIED. ) ;
#30942=CARTESIAN_POINT ( 'NONE',  ( 0.7071069014570956490, -1.521634513519168452, 0.5617257377400114438 ) ) ;
#30947=CARTESIAN_POINT ( 'NONE',  ( 0.008832803565516154920, -0.8460330395702395645, 0.2167343075818525255 ) ) ;
#30948=EDGE_LOOP ( 'NONE', ( #36254, #33323, #2687, #38770 ) ) ;
#30949=ORIENTED_EDGE ( 'NONE', *, *, #1364, .F. ) ;
#30959=EDGE_LOOP ( 'NONE', ( #16344, #25421 ) ) ;
#30961=DIRECTION ( 'NONE',  ( 0.8660512985181139101, 0.4999551463232363990, 0.000000000000000000 ) ) ;
#30964=CARTESIAN_POINT ( 'NONE',  ( 0.1138873904656961394, -0.7287558471037995922, 0.5555362357626123515 ) ) ;
#30971=CIRCLE ( 'NONE', #11910, 0.04749999999977556897 ) ;
#30972=CARTESIAN_POINT ( 'NONE',  ( 0.5732843912231511130, -1.499081617108205977, 0.5610695280922421979 ) ) ;
#30973=CARTESIAN_POINT ( 'NONE',  ( 0.4173100523516673488, -1.700895175538478021, 0.4281662355554799460 ) ) ;
#30975=AXIS2_PLACEMENT_3D ( 'NONE', #5606, #4999, #17954 ) ;
#30976=VERTEX_POINT ( 'NONE', #40533 ) ;
#30983=CARTESIAN_POINT ( 'NONE',  ( 0.2870953417136587471, -0.7492508933039718766, 0.6466144559156578042 ) ) ;
#30985=CARTESIAN_POINT ( 'NONE',  ( 0.01347435369769745851, -1.020097873921679943, 0.5726246034863379242 ) ) ;
#30988=CARTESIAN_POINT ( 'NONE',  ( 0.08509807008754367852, -0.8316410974449348625, 0.1906738364949772391 ) ) ;
#30995=CARTESIAN_POINT ( 'NONE',  ( 0.6666468149095314821, -1.488249007687060921, 0.4225787955285728592 ) ) ;
#31003=CARTESIAN_POINT ( 'NONE',  ( 0.3229310443258136543, -1.169691403921407025, 0.5631135211526986373 ) ) ;
#31004=DIRECTION ( 'NONE',  ( 0.4999551463232371762, -0.8660512985181134660, 0.000000000000000000 ) ) ;
#31007=CARTESIAN_POINT ( 'NONE',  ( 0.5121945966484598989, -1.314982590827621811, 0.5851977928667088102 ) ) ;
#31010=CARTESIAN_POINT ( 'NONE',  ( 0.4045633573398161875, -1.022308794230461171, 0.6485999566564401020 ) ) ;
#31013=CARTESIAN_POINT ( 'NONE',  ( 0.1051913758597731452, -1.410370913283630623, 0.5802209346841724624 ) ) ;
#31015=VERTEX_POINT ( 'NONE', #30465 ) ;
#31017=CARTESIAN_POINT ( 'NONE',  ( 0.3586591433503226178, -1.621797892226208404, 0.6182109731304538114 ) ) ;
#31019=CARTESIAN_POINT ( 'NONE',  ( 0.1752196092396576255, -0.8414204078959418576, -0.02572121894636038297 ) ) ;
#31020=CARTESIAN_POINT ( 'NONE',  ( 0.5965761245944036784, -1.493465029535157029, 0.5182417262812423209 ) ) ;
#31022=ORIENTED_EDGE ( 'NONE', *, *, #36557, .T. ) ;
#31023=CARTESIAN_POINT ( 'NONE',  ( 0.4713681159961597977, -1.077402325356330737, 0.7137236214398411382 ) ) ;
#31024=CARTESIAN_POINT ( 'NONE',  ( 0.5418845258822191369, -1.488322812234847525, 0.7085126686041083310 ) ) ;
#31026=CARTESIAN_POINT ( 'NONE',  ( 0.3504057387187116679, -1.153664717295437070, 0.4422128889498895266 ) ) ;
#31038=CARTESIAN_POINT ( 'NONE',  ( 0.7472694261237929902, -1.513267490863592135, 0.4687417262808789009 ) ) ;
#31039=VECTOR ( 'NONE', #26158, 39.37007874015748854 ) ;
#31040=CARTESIAN_POINT ( 'NONE',  ( 0.08105144843878842043, -1.319509989509974002, 0.5764475800623926061 ) ) ;
#31042=CARTESIAN_POINT ( 'NONE',  ( 0.04329528483221436325, -1.226008797194266586, 0.6628706426414217034 ) ) ;
#31044=CARTESIAN_POINT ( 'NONE',  ( 0.2870562969094627714, -0.9697506529368410400, 0.5438065585693926396 ) ) ;
#31045=CARTESIAN_POINT ( 'NONE',  ( 0.4837706980973027759, -1.122837591129260737, 0.5209615820093888017 ) ) ;
#31046=CARTESIAN_POINT ( 'NONE',  ( 0.1590992539432692365, -1.295692464083599171, 0.5182417262812423209 ) ) ;
#31050=CARTESIAN_POINT ( 'NONE',  ( 0.003677659035771949428, -0.9373694290314303901, 0.4460629830528545781 ) ) ;
#31053=CARTESIAN_POINT ( 'NONE',  ( 0.3827394763927673971, -1.608088298394132254, 0.5182417262812428760 ) ) ;
#31064=ORIENTED_EDGE ( 'NONE', *, *, #23007, .F. ) ;
#31069=CARTESIAN_POINT ( 'NONE',  ( 0.1424451214204122962, -1.140609330361415763, 0.8966624996383008028 ) ) ;
#31070=CARTESIAN_POINT ( 'NONE',  ( 0.2259872153612249857, -0.9582317320479798450, 0.6774812835207550954 ) ) ;
#31072=CARTESIAN_POINT ( 'NONE',  ( 0.3605448558321485697, -1.159604706203796631, 0.5182417262812284431 ) ) ;
#31074=CARTESIAN_POINT ( 'NONE',  ( 0.4092319501327035813, -1.708177749814091761, 0.4221986184566056122 ) ) ;
#31081=CARTESIAN_POINT ( 'NONE',  ( 0.5293880808009361338, -1.380208753696393842, 0.7890457912007839969 ) ) ;
#31084=CARTESIAN_POINT ( 'NONE',  ( 0.1968545423636366143, -1.364578978885418126, 0.9371999825232737447 ) ) ;
#31087=CARTESIAN_POINT ( 'NONE',  ( 0.3170005508008052475, -1.687968217625634315, 0.8639454125425393149 ) ) ;
#31090=CARTESIAN_POINT ( 'NONE',  ( 0.5705082898449433948, -1.615108203520839947, 0.3157417262808777658 ) ) ;
#31095=CARTESIAN_POINT ( 'NONE',  ( 0.1958798485499332886, -1.272568564212325670, 1.036395571016125006 ) ) ;
#31096=CARTESIAN_POINT ( 'NONE',  ( 0.08877126294492045100, -1.285961541598747981, 0.7406644231755382668 ) ) ;
#31099=CARTESIAN_POINT ( 'NONE',  ( 0.1875000000000001943, -0.4593131964907913312, 0.1457185332388694909 ) ) ;
#31101=EDGE_CURVE ( 'NONE', #21274, #8445, #26268, .T. ) ;
#31102=ADVANCED_FACE ( 'NONE', ( #16263 ), #30737, .T. ) ;
#31113=CARTESIAN_POINT ( 'NONE',  ( 0.2728372402267926766, -1.642600808974832072, 0.7657233710704415275 ) ) ;
#31114=CARTESIAN_POINT ( 'NONE',  ( 0.1489746679736130563, -0.6542566974029685456, 0.4247869901793544511 ) ) ;
#31118=CARTESIAN_POINT ( 'NONE',  ( 0.4104166757648185504, -0.9945572768306742972, 0.7245767828144217271 ) ) ;
#31121=CARTESIAN_POINT ( 'NONE',  ( 0.6949781612789637242, -1.427105545965590583, 0.6651444036754494693 ) ) ;
#31128=ORIENTED_EDGE ( 'NONE', *, *, #446, .F. ) ;
#31129=CARTESIAN_POINT ( 'NONE',  ( 0.2811537305380201190, -0.9978850141101639482, 0.7019614375224079161 ) ) ;
#31131=CARTESIAN_POINT ( 'NONE',  ( 0.3222111719196821267, -1.761649659472191543, 0.6126613877097355498 ) ) ;
#31133=CARTESIAN_POINT ( 'NONE',  ( 0.1044438712203083208, -0.5602818493527880195, 0.2215003945582872391 ) ) ;
#31134=CARTESIAN_POINT ( 'NONE',  ( 0.3418696078408812178, -1.748333077232472554, 0.4473164556818181037 ) ) ;
#31139=CARTESIAN_POINT ( 'NONE',  ( 0.4307568529685167347, -1.695672135311921958, 0.6147001973947316955 ) ) ;
#31140=CARTESIAN_POINT ( 'NONE',  ( 0.6984873844191630265, -1.438842590160148260, 0.5672913894667556134 ) ) ;
#31143=VECTOR ( 'NONE', #19368, 39.37007874015748143 ) ;
#31144=CARTESIAN_POINT ( 'NONE',  ( -0.002162789170891683647, -0.8547793670402533683, 0.1265725835208540984 ) ) ;
#31147=B_SPLINE_CURVE_WITH_KNOTS ( 'NONE', 3,
 ( #5347, #17707, #31441, #39933, #8645, #8254, #15795, #20826, #27407, #2303, #15043, #24307, #6330, #11749, #36831, #33346, #5568, #33754, #213, #22201, #18129, #21218, #3248, #5156, #36646, #30253, #25061, #11560, #39512, #2501, #40118, #2085, #11342, #37595, #14622, #9416, #14414, #21995, #27191, #34520, #18904, #6523, #39726, #8450, #12707, #19096, #26976, #25270, #37811, #24124, #21017, #33535, #17909, #14844, #7543, #4259, #19508, #35729, #28556, #7124, #25888, #29155, #26281, #4044, #31845, #38408, #16402 ),
 .UNSPECIFIED., .F., .F.,
 ( 4, 2, 2, 2, 2, 2, 2, 2, 2, 2, 2, 2, 2, 2, 1, 1, 2, 2, 1, 2, 2, 2, 2, 2, 2, 2, 2, 2, 1, 1, 2, 2, 1, 2, 2, 1, 4 ),
 ( 0.000000000000000000, 0.04613892571620765992, 0.09227785143241531984, 0.1384167771486229936, 0.1845557028648306397, 0.2768335542972459873, 0.3691114057296612794, 0.4152503314458689254, 0.4613892571620765715, 0.5075281828782842730, 0.5305976457363886789, 0.5421323771654402712, 0.5536671085944919746, 0.5652018400235435669, 0.5767365714525951592, 0.5882713028816467515, 0.5911549857389092333, 0.5940386685961718261, 0.5998060343106970116, 0.6228754971687950892, 0.6257591800260565718, 0.6286428628833180543, 0.6344102285978422406, 0.6459449600268917235, 0.6517123257414164650, 0.6574796914559412064, 0.6690144228849906893, 0.6718981057422531711, 0.6747817885995157638, 0.6805491543140408384, 0.6863165200285659129, 0.6920838857430909874, 0.7151533486011910634, 0.7180370314584534341, 0.7209207143157160269, 0.7266880800302409904, 0.7382228114592909174 ),
 .UNSPECIFIED. ) ;
#31149=CARTESIAN_POINT ( 'NONE',  ( 0.3101988348943303664, -1.188457521969344954, 0.5390384569713482232 ) ) ;
#31150=CARTESIAN_POINT ( 'NONE',  ( 0.5520143099787153673, -1.183365530476261585, 0.6129298035784942478 ) ) ;
#31152=CARTESIAN_POINT ( 'NONE',  ( 0.6002284735530656334, -1.599240903479319131, 0.6081811307598909977 ) ) ;
#31157=CARTESIAN_POINT ( 'NONE',  ( 0.5610715841008669935, -1.505132754039335552, 0.5357057820217212551 ) ) ;
#31162=CARTESIAN_POINT ( 'NONE',  ( 0.4685502202651029569, -1.116536938686066183, 0.5688043585934901003 ) ) ;
#31169=CARTESIAN_POINT ( 'NONE',  ( 0.07936604219207132882, -1.300224580243717565, 0.7373157962401226673 ) ) ;
#31177=CARTESIAN_POINT ( 'NONE',  ( 0.2317288817819283253, -1.348463341396027637, 0.5280675649570982788 ) ) ;
#31180=CARTESIAN_POINT ( 'NONE',  ( 0.06909380327002452582, -1.315850677508620281, 0.5176656306823473885 ) ) ;
#31183=CARTESIAN_POINT ( 'NONE',  ( 0.4715550156134034054, -1.554656505831566227, 0.6419049491724836409 ) ) ;
#31185=CARTESIAN_POINT ( 'NONE',  ( 0.5654497241578824163, -1.618822071068416912, 0.5682417262808787672 ) ) ;
#31186=CARTESIAN_POINT ( 'NONE',  ( 0.06844683568258899675, -1.327643015831073914, 0.5607579029421154715 ) ) ;
#31190=CARTESIAN_POINT ( 'NONE',  ( 0.2722331219925429036, -1.671874623808670135, 0.4849083929475441201 ) ) ;
#31192=CARTESIAN_POINT ( 'NONE',  ( 0.1253914729212589063, -0.5518637161767581123, 0.1703337146848046546 ) ) ;
#31193=CARTESIAN_POINT ( 'NONE',  ( 0.4745856284632649080, -1.668843919975977474, 0.5513519273944286203 ) ) ;
#31194=B_SPLINE_CURVE_WITH_KNOTS ( 'NONE', 3,
 ( #2868, #12130, #15625, #18710 ),
 .UNSPECIFIED., .F., .F.,
 ( 4, 4 ),
 ( 0.001920789045071016584, 0.002034319970777410426 ),
 .UNSPECIFIED. ) ;
#31200=CARTESIAN_POINT ( 'NONE',  ( 0.2233408083240900899, -1.237973100587790976, 0.5437015457833099807 ) ) ;
#31202=CARTESIAN_POINT ( 'NONE',  ( 0.2284408465079907080, -1.235179063166289781, 0.4809151899966361832 ) ) ;
#31204=CARTESIAN_POINT ( 'NONE',  ( 0.1898244942508440503, -0.5073357646527311138, 0.1864979583367220028 ) ) ;
#31206=CARTESIAN_POINT ( 'NONE',  ( 0.03300239046062679316, -1.160323239369614123, 0.6643093511034796617 ) ) ;
#31208=CARTESIAN_POINT ( 'NONE',  ( 0.1857430203655688061, -0.8056635886342108366, 0.2698372336795828996 ) ) ;
#31209=CARTESIAN_POINT ( 'NONE',  ( 0.1291546474001438460, -0.8766933867304865791, 0.5184058891243923384 ) ) ;
#31216=CARTESIAN_POINT ( 'NONE',  ( 0.6465835049539359058, -1.539613817736341872, 0.4182417262808776903 ) ) ;
#31222=CIRCLE ( 'NONE', #2969, 0.03749999999977557397 ) ;
#31225=CARTESIAN_POINT ( 'NONE',  ( 0.3902357488131970031, -1.138878306233123805, 0.6057535050277017552 ) ) ;
#31227=CARTESIAN_POINT ( 'NONE',  ( 0.3283149244379453546, -1.763791535429168889, 0.4875464477737077029 ) ) ;
#31229=CARTESIAN_POINT ( 'NONE',  ( 0.5014320656698512124, -1.296437944250064422, 0.5839483198575456946 ) ) ;
#31231=CARTESIAN_POINT ( 'NONE',  ( 0.5135568109339374576, -1.117989077717415292, 0.5796127612779116145 ) ) ;
#31238=CARTESIAN_POINT ( 'NONE',  ( 0.3671697839738085611, -1.545107799971002560, 0.8005747561286837843 ) ) ;
#31240=CARTESIAN_POINT ( 'NONE',  ( 0.1115501525409109546, -0.8938576055124605180, 0.02086076245356002085 ) ) ;
#31241=CARTESIAN_POINT ( 'NONE',  ( 0.6215940427273412006, -1.611809246851749311, 0.5182417262812423209 ) ) ;
#31243=ORIENTED_EDGE ( 'NONE', *, *, #27558, .T. ) ;
#31244=CARTESIAN_POINT ( 'NONE',  ( 0.3197192075068525097, -1.053170137840971687, 0.6328512510037338501 ) ) ;
#31245=CARTESIAN_POINT ( 'NONE',  ( 0.4770251848494882485, -1.362019963231613673, 0.8156266216142553649 ) ) ;
#31254=CARTESIAN_POINT ( 'NONE',  ( 0.4047110712422638534, -1.701609880936963970, 0.4182417262808776903 ) ) ;
#31258=CARTESIAN_POINT ( 'NONE',  ( 0.002290818369124609372, -0.5198888459286679087, 0.1457185332388686583 ) ) ;
#31261=CARTESIAN_POINT ( 'NONE',  ( 0.4737957855049246270, -1.072208190283344909, 0.6181471139717461538 ) ) ;
#31262=CARTESIAN_POINT ( 'NONE',  ( 0.4447797348688822261, -1.136753334708936247, 0.4441811018978158443 ) ) ;
#31263=CARTESIAN_POINT ( 'NONE',  ( 0.4538227971951512285, -1.220717492415648975, 0.5856983068965044836 ) ) ;
#31265=CARTESIAN_POINT ( 'NONE',  ( 0.3121344959780879558, -1.175754444927441300, 0.5182417262812437642 ) ) ;
#31266=CARTESIAN_POINT ( 'NONE',  ( -0.003124719664520024271, -0.8057675726412024675, 0.09674340762273991867 ) ) ;
#31268=FACE_OUTER_BOUND ( 'NONE', #38001, .T. ) ;
#31270=ORIENTED_EDGE ( 'NONE', *, *, #35088, .F. ) ;
#31272=PLANE ( 'NONE',  #30909 ) ;
#31277=CARTESIAN_POINT ( 'NONE',  ( 0.3646774744596967821, -1.088638349586324994, 0.8066222157141976767 ) ) ;
#31278=CARTESIAN_POINT ( 'NONE',  ( 0.009698722596325677972, -0.5609003310328917191, 0.05071314360984191527 ) ) ;
#31281=AXIS2_PLACEMENT_3D ( 'NONE', #7082, #38160, #9984 ) ;
#31283=ORIENTED_EDGE ( 'NONE', *, *, #38175, .T. ) ;
#31284=CARTESIAN_POINT ( 'NONE',  ( 0.1890965627226634804, -1.347655541994686068, 0.5182417262812423209 ) ) ;
#31285=CARTESIAN_POINT ( 'NONE',  ( 0.2857623305721883611, -1.591320169725852551, 0.8243244337802699828 ) ) ;
#31286=CARTESIAN_POINT ( 'NONE',  ( 0.1149644705236894937, -0.8668712750652664001, 0.4808557319664010787 ) ) ;
#31289=CARTESIAN_POINT ( 'NONE',  ( 0.01184929641461734615, -0.5804339378642296987, -0.09026199020224340286 ) ) ;
#31297=CARTESIAN_POINT ( 'NONE',  ( 0.5517015749519356138, -1.382230921397820556, 0.7776688410150216502 ) ) ;
#31299=CARTESIAN_POINT ( 'NONE',  ( 0.1289960929160810510, -0.8267361313214416363, 0.2449634403921974735 ) ) ;
#31302=CARTESIAN_POINT ( 'NONE',  ( 0.1174434333147871268, -0.9515856618589675353, 0.9146188126943564090 ) ) ;
#31303=CARTESIAN_POINT ( 'NONE',  ( 0.4003933387480922423, -1.713626439352980091, 0.4219370341759499099 ) ) ;
#31305=CARTESIAN_POINT ( 'NONE',  ( 0.4679778500672936992, -1.237826332153874942, 0.6057417262809768888 ) ) ;
#31309=CARTESIAN_POINT ( 'NONE',  ( 0.01054327228848483088, -0.5372198261166355460, 0.4758561573974433023 ) ) ;
#31311=CARTESIAN_POINT ( 'NONE',  ( 0.08536197900831818397, -1.283296901138165191, 0.7335830683232681393 ) ) ;
#31313=CARTESIAN_POINT ( 'NONE',  ( 0.7228851465660607323, -1.479175389011975428, 0.5919814340071456460 ) ) ;
#31316=B_SPLINE_CURVE_WITH_KNOTS ( 'NONE', 3,
 ( #34529, #28161, #15807, #37825, #22005, #22210, #34119, #18912, #16022, #31449, #34320, #3256, #28566, #28355, #27, #21594, #5735, #9640, #12514, #12720, #5921, #25486, #34727, #31040, #19107, #25070 ),
 .UNSPECIFIED., .F., .F.,
 ( 4, 2, 2, 2, 2, 2, 2, 2, 2, 2, 2, 2, 4 ),
 ( -5.999999996337358855E-08, 0.0003477659952063618613, 0.0006955919904126871538, 0.001391243980825333619, 0.002086895971237980735, 0.002782547961650626116, 0.003130373956856948373, 0.003478199952063270196, 0.003826025947269592452, 0.004173851942475916878, 0.004869503932888550116, 0.005217329928094866301, 0.005565155923301183354 ),
 .UNSPECIFIED. ) ;
#31318=TOROIDAL_SURFACE ( 'NONE', #17507, 0.07749999999977548459, 0.01000000000000000021 ) ;
#31319=CARTESIAN_POINT ( 'NONE',  ( 0.3704697912810962501, -1.166474544107111377, 0.4182417262808778013 ) ) ;
#31325=CARTESIAN_POINT ( 'NONE',  ( 0.2697570704576938150, -1.625148811348557043, 0.7999399077722737506 ) ) ;
#31327=CARTESIAN_POINT ( 'NONE',  ( 0.3070561426719275455, -1.006156790695110548, 0.7639484575383966858 ) ) ;
#31332=CARTESIAN_POINT ( 'NONE',  ( 0.3136710858027207949, -0.8676775186001693951, 0.6334163436129683911 ) ) ;
#31335=CARTESIAN_POINT ( 'NONE',  ( 0.4987283714208217700, -1.112815979792688204, 0.8110521570308895090 ) ) ;
#31339=CARTESIAN_POINT ( 'NONE',  ( 0.3186320557803343223, -1.760432376530343568, 0.5682926660822772424 ) ) ;
#31342=CARTESIAN_POINT ( 'NONE',  ( 0.2153886340467147109, -0.9136054407777869368, 0.6428213724677314111 ) ) ;
#31343=CARTESIAN_POINT ( 'NONE',  ( 0.3166419384220154898, -1.752632602668677597, 0.7236431125229072503 ) ) ;
#31344=CARTESIAN_POINT ( 'NONE',  ( 0.5253970528185427646, -1.521450895406853965, 0.6493258987034100649 ) ) ;
#31351=CARTESIAN_POINT ( 'NONE',  ( 0.7432944383420270196, -1.516446101903487165, 0.5674244750120348568 ) ) ;
#31354=DIRECTION ( 'NONE',  ( 0.4999551463232372317, -0.8660512985181134660, -6.869252350113302335E-17 ) ) ;
#31355=CARTESIAN_POINT ( 'NONE',  ( 0.2684390043173380258, -1.673772033336743181, 0.5388446858685563834 ) ) ;
#31357=CARTESIAN_POINT ( 'NONE',  ( 0.5554409461590971153, -1.190971970253151824, 0.5682417262808781011 ) ) ;
#31359=CARTESIAN_POINT ( 'NONE',  ( 0.5908959048872449715, -1.601544548465861473, 0.4282886817583849703 ) ) ;
#31360=FACE_OUTER_BOUND ( 'NONE', #32027, .T. ) ;
#31368=CARTESIAN_POINT ( 'NONE',  ( 0.1896960494042899126, -0.8386842184079319473, 0.2498764039407927462 ) ) ;
#31372=CARTESIAN_POINT ( 'NONE',  ( -0.01212677295819645021, -0.8635911836337304415, 0.3648026836272298401 ) ) ;
#31380=CARTESIAN_POINT ( 'NONE',  ( 0.006142123377964069098, -0.4287598720593460699, 0.1457185332388686305 ) ) ;
#31382=ORIENTED_EDGE ( 'NONE', *, *, #27037, .T. ) ;
#31383=CARTESIAN_POINT ( 'NONE',  ( 0.09080745303567185067, -0.5677619141264073077, 0.2083789338475214581 ) ) ;
#31386=CARTESIAN_POINT ( 'NONE',  ( 0.4413773429406284143, -1.573661458614751485, 0.5688663500546452534 ) ) ;
#31389=CARTESIAN_POINT ( 'NONE',  ( 0.5667697670958626865, -1.627219054903903395, 0.5179411731989888024 ) ) ;
#31391=CARTESIAN_POINT ( 'NONE',  ( 0.2352442375527352414, -0.9584679667894288047, 0.4983825088159561378 ) ) ;
#31395=CARTESIAN_POINT ( 'NONE',  ( 0.1153472994790071260, -0.4465945824750962023, 0.1471405910905037306 ) ) ;
#31396=CARTESIAN_POINT ( 'NONE',  ( 0.5807592067643548850, -1.495225062396434046, 0.5704271586488920409 ) ) ;
#31402=CARTESIAN_POINT ( 'NONE',  ( 0.6810725650087121608, -1.407094454800211558, 0.5876998678990568159 ) ) ;
#31404=CARTESIAN_POINT ( 'NONE',  ( 0.02344934057377633801, -1.099133950262376258, 0.6397433352409148677 ) ) ;
#31407=CARTESIAN_POINT ( 'NONE',  ( 0.07670936359779292890, -0.8423313109294351397, 0.3268936787692559576 ) ) ;
#31408=CARTESIAN_POINT ( 'NONE',  ( 0.2663522331702417034, -1.675380074340676151, 0.5698030654214122359 ) ) ;
#31409=CARTESIAN_POINT ( 'NONE',  ( 0.09912479720125623450, -1.266807960652112097, 0.5182417262812423209 ) ) ;
#31410=ORIENTED_EDGE ( 'NONE', *, *, #25582, .F. ) ;
#31412=CARTESIAN_POINT ( 'NONE',  ( 0.4879523740783364150, -1.280237457375205334, 0.7926971813901000363 ) ) ;
#31414=EDGE_CURVE ( 'NONE', #9135, #7249, #1301, .T. ) ;
#31415=CARTESIAN_POINT ( 'NONE',  ( 0.08510361377861434817, -0.8106636051554854117, 0.1454306519311501233 ) ) ;
#31420=CARTESIAN_POINT ( 'NONE',  ( 0.1156610620243726933, -1.416230906443656901, 0.4172996703284162501 ) ) ;
#31423=CARTESIAN_POINT ( 'NONE',  ( 0.3785755849098691450, -1.119414945699769959, 0.7435571456696157266 ) ) ;
#31425=CARTESIAN_POINT ( 'NONE',  ( 0.4790383449168201802, -1.075084602395082634, 0.6124719440393814329 ) ) ;
#31427=PRODUCT_CONTEXT ( 'NONE', #7424, 'mechanical' ) ;
#31428=CIRCLE ( 'NONE', #581, 0.009999999999999995004 ) ;
#31429=CARTESIAN_POINT ( 'NONE',  ( 0.08062789043467089023, -1.253025610042452831, 0.7448910529509513712 ) ) ;
#31431=CARTESIAN_POINT ( 'NONE',  ( 0.3843449031254181913, -1.605279702831362787, 0.5608835269958394321 ) ) ;
#31432=CARTESIAN_POINT ( 'NONE',  ( 0.06455621155043581028, -0.8342858573599853944, 0.1261830515498010841 ) ) ;
#31433=CARTESIAN_POINT ( 'NONE',  ( 0.1116987077102032100, -0.8808449370242167342, 0.0008922463578378222755 ) ) ;
#31434=CARTESIAN_POINT ( 'NONE',  ( 0.06705167635834106965, -0.6680383592416772043, -0.0009537033254834985244 ) ) ;
#31437=ORIENTED_EDGE ( 'NONE', *, *, #39085, .T. ) ;
#31439=CARTESIAN_POINT ( 'NONE',  ( 0.5282826409240604093, -1.443108049827171335, 0.7657529498032049631 ) ) ;
#31441=CARTESIAN_POINT ( 'NONE',  ( 0.1853053032850285331, -0.8367218493003313329, 0.1362433201977383268 ) ) ;
#31447=DIRECTION ( 'NONE',  ( -0.4999551463232372317, 0.8660512985181135770, -0.000000000000000000 ) ) ;
#31449=CARTESIAN_POINT ( 'NONE',  ( 0.1525961459700538314, -1.248272379099432339, 0.6216296366653764061 ) ) ;
#31453=CARTESIAN_POINT ( 'NONE',  ( 0.4162441775219429263, -1.040631601589554034, 0.6343403631529308528 ) ) ;
#31454=CARTESIAN_POINT ( 'NONE',  ( 0.3121344959780879558, -1.175754444927441300, 0.5182417262812437642 ) ) ;
#31455=DIRECTION ( 'NONE',  ( -0.0001066307966867950538, 1.551735798909011778E-06, 0.9999999943137325431 ) ) ;
#31456=CARTESIAN_POINT ( 'NONE',  ( 0.3229289876128840775, -1.169687821100875658, 0.5631135379446852163 ) ) ;
#31458=CARTESIAN_POINT ( 'NONE',  ( 0.006005486288604863949, -0.9514584861060970677, 0.4879672165010910390 ) ) ;
#31459=CARTESIAN_POINT ( 'NONE',  ( 0.0003079261067442713869, -0.4760981469167980817, 0.01389499447167343027 ) ) ;
#31461=CARTESIAN_POINT ( 'NONE',  ( 0.3556570129879135789, -1.173715053083399740, 0.4182417262808778013 ) ) ;
#31468=CARTESIAN_POINT ( 'NONE',  ( 0.5741579611739540123, -1.419304924894309927, 0.6377566456345815649 ) ) ;
#31469=CARTESIAN_POINT ( 'NONE',  ( 0.001493246241084611415, -0.5596943232668920576, 0.04990435613214081606 ) ) ;
#31470=ORIENTED_EDGE ( 'NONE', *, *, #23188, .T. ) ;
#31472=CARTESIAN_POINT ( 'NONE',  ( 0.2004046765218066295, -0.7505902666037495008, 0.3314731723568724586 ) ) ;
#31474=CARTESIAN_POINT ( 'NONE',  ( 0.01468336712996881274, -0.5833551626382605937, 0.3318062457441503521 ) ) ;
#31475=CARTESIAN_POINT ( 'NONE',  ( 0.4226721025871904014, -1.212929281597423525, 0.6550521210678496020 ) ) ;
#31476=CARTESIAN_POINT ( 'NONE',  ( 0.2948777445940948261, -1.312432472972675290, 0.4182417262808776348 ) ) ;
#31478=CARTESIAN_POINT ( 'NONE',  ( 0.01194082430585321694, -0.5163470803647776108, -0.04948302235635338581 ) ) ;
#31484=CARTESIAN_POINT ( 'NONE',  ( 0.1862143093560909568, -0.9153542374866630027, 0.1397141703224119846 ) ) ;
#31486=CARTESIAN_POINT ( 'NONE',  ( 0.5578360211051590634, -1.391431592590435251, 0.7485196725347594837 ) ) ;
#31487=CARTESIAN_POINT ( 'NONE',  ( 0.1943267261999117590, -0.8912486778694943546, 0.5787461573889725042 ) ) ;
#31488=CARTESIAN_POINT ( 'NONE',  ( 0.2693423574607928805, -1.623096489475305271, 0.8033103420475437018 ) ) ;
#31489=CARTESIAN_POINT ( 'NONE',  ( 0.2357496974250468946, -1.376590845310902145, 1.030782602123143876 ) ) ;
#31491=CARTESIAN_POINT ( 'NONE',  ( 0.6059691746655119227, -1.480133143157562170, 0.5526975506195443977 ) ) ;
#31495=CARTESIAN_POINT ( 'NONE',  ( 0.08953535957268946022, -1.239962282013243877, 0.7545938977955062299 ) ) ;
#31498=CARTESIAN_POINT ( 'NONE',  ( 0.6937844480354340426, -1.537461556741912760, 0.5870152100781083071 ) ) ;
#31499=EDGE_CURVE ( 'NONE', #40356, #2485, #21405, .T. ) ;
#31502=CARTESIAN_POINT ( 'NONE',  ( 0.2709623010280027278, -1.672610760848568967, 0.4891849873696615392 ) ) ;
#31504=CARTESIAN_POINT ( 'NONE',  ( 0.2662581717953377836, -1.658323607150117285, 0.7400210192072117499 ) ) ;
#31505=CARTESIAN_POINT ( 'NONE',  ( 0.5820653343257259360, -1.465606132385127935, 0.6997249523535519211 ) ) ;
#31506=ORIENTED_EDGE ( 'NONE', *, *, #11893, .T. ) ;
#31507=CARTESIAN_POINT ( 'NONE',  ( 0.3499317094845075249, -1.754137739073151181, 0.4513909310129907704 ) ) ;
#31512=CARTESIAN_POINT ( 'NONE',  ( 0.1109092093543055241, -0.9286325583098424818, 0.1457252011008478843 ) ) ;
#31516=ORIENTED_EDGE ( 'NONE', *, *, #2387, .F. ) ;
#31517=CARTESIAN_POINT ( 'NONE',  ( 0.1035168011811207489, -0.7883913148987408137, 0.3594284199549346304 ) ) ;
#31519=CARTESIAN_POINT ( 'NONE',  ( 0.1042374422282348334, -0.5569725106795370140, 0.2106683946891434178 ) ) ;
#31524=CARTESIAN_POINT ( 'NONE',  ( 0.4153535842760917585, -1.704503823779182081, 0.6190792889780868391 ) ) ;
#31526=CARTESIAN_POINT ( 'NONE',  ( 0.6984060551207101897, -1.438828591659085054, 0.5657311187875787573 ) ) ;
#31529=EDGE_CURVE ( 'NONE', #24330, #17955, #19240, .T. ) ;
#31530=CARTESIAN_POINT ( 'NONE',  ( 0.1820744924655830210, -0.7238696534340168798, 0.5246764128789646042 ) ) ;
#31531=CARTESIAN_POINT ( 'NONE',  ( 0.1927077495703349852, -0.8180328145591141409, 0.2791508387892263077 ) ) ;
#31532=ADVANCED_FACE ( 'NONE', ( #22538 ), #158, .T. ) ;
#31533=CARTESIAN_POINT ( 'NONE',  ( 0.05560027925352286488, -1.335209592177159843, 0.5707417262808780478 ) ) ;
#31536=CARTESIAN_POINT ( 'NONE',  ( 0.05086546246741921462, -1.198860143930047473, 0.7015125153497857591 ) ) ;
#31537=CARTESIAN_POINT ( 'NONE',  ( 0.2067623920994063613, -0.8133810345767992223, 0.3693416354660131184 ) ) ;
#31545=DIRECTION ( 'NONE',  ( 0.4999551463232372317, -0.8660512985181135770, 0.000000000000000000 ) ) ;
#31547=CARTESIAN_POINT ( 'NONE',  ( 0.08805730728144700592, -0.6472740652894640734, 0.02916467596460211448 ) ) ;
#31549=CARTESIAN_POINT ( 'NONE',  ( 0.2319960710055803677, -1.232736008543062090, 0.4687417262808780127 ) ) ;
#31550=CARTESIAN_POINT ( 'NONE',  ( 0.01072073033491486443, -0.9808573846632955284, 0.6679598757981023427 ) ) ;
#31559=DIRECTION ( 'NONE',  ( 0.4999551463232372317, -0.8660512985181135770, 0.000000000000000000 ) ) ;
#31560=EDGE_LOOP ( 'NONE', ( #22332, #25761, #33922, #40063, #24454 ) ) ;
#31564=CARTESIAN_POINT ( 'NONE',  ( 0.09119287031673356525, -0.6099748663625392808, 0.2139121366898841525 ) ) ;
#31568=CARTESIAN_POINT ( 'NONE',  ( 0.2024955851830932685, -0.9687359790435555729, 0.7686808776775244656 ) ) ;
#31572=CARTESIAN_POINT ( 'NONE',  ( 0.1938692902500353255, -0.9317700634581833619, 0.3727138502448550383 ) ) ;
#31575=B_SPLINE_CURVE_WITH_KNOTS ( 'NONE', 3,
 ( #8822, #27964, #12326, #24884, #3673, #6739 ),
 .UNSPECIFIED., .F., .F.,
 ( 4, 2, 4 ),
 ( 0.001507239257244120598, 0.001922639214874271663, 0.002338039172504422728 ),
 .UNSPECIFIED. ) ;
#31576=CARTESIAN_POINT ( 'NONE',  ( 0.1153481622643483390, -0.4466190433387221548, 0.1494994773299645197 ) ) ;
#31577=CARTESIAN_POINT ( 'NONE',  ( 0.1281471506186622478, -0.5867175007372630313, 0.2851988856149638707 ) ) ;
#31584=CARTESIAN_POINT ( 'NONE',  ( 0.06924866487494936440, -0.5400458411302934136, 0.1497098795544565819 ) ) ;
#31586=ADVANCED_FACE ( 'NONE', ( #18574 ), #30560, .T. ) ;
#31587=CARTESIAN_POINT ( 'NONE',  ( 0.3418186750811026964, -0.8703758711135023418, 0.7017026408156415984 ) ) ;
#31589=( BOUNDED_SURFACE ( )  B_SPLINE_SURFACE ( 3, 2, ( 
 ( #29146, #13104, #1012 ),
 ( #16601, #25664, #32030 ),
 ( #38004, #38198, #13309 ),
 ( #38400, #35328, #10023 ),
 ( #22986, #22593, #7534 ),
 ( #6928, #7313, #19501 ),
 ( #19683, #32218, #10425 ),
 ( #4036, #13524, #26086 ),
 ( #38605, #35505, #4249 ),
 ( #13706, #16817, #1203 ),
 ( #10622, #23198, #32640 ),
 ( #24209, #11447, #36733 ),
 ( #8541, #5055, #21111 ),
 ( #39008, #36120, #23803 ),
 ( #24014, #17412, #39827 ),
 ( #11650, #29752, #36540 ) ),
 .UNSPECIFIED., .F., .F., .T. ) 
 B_SPLINE_SURFACE_WITH_KNOTS ( ( 4, 2, 2, 2, 2, 2, 2, 4 ),
 ( 3, 3 ),
 ( 0.000000000000000000, 0.0008227173377846956582, 0.001645434675569391316, 0.002468152013354086866, 0.003290869351138782633, 0.004113586688923477966, 0.004936304026708173733, 0.006581738702277565266 ),
 ( 0.000000000000000000, 1.000000000000000000 ),
 .UNSPECIFIED. ) 
 GEOMETRIC_REPRESENTATION_ITEM ( )  RATIONAL_B_SPLINE_SURFACE ( (
 ( 1.000000000000000000, 0.9337218516597696194, 1.000000000000000000),
 ( 1.000000000000000000, 0.9361136716705305005, 1.000000000000000000),
 ( 1.000000000000000000, 0.9384872499382632682, 1.000000000000000000),
 ( 1.000000000000000000, 0.9429186473287669568, 1.000000000000000000),
 ( 1.000000000000000000, 0.9449938870051080020, 1.000000000000000000),
 ( 1.000000000000000000, 0.9484294354700106844, 1.000000000000000000),
 ( 1.000000000000000000, 0.9497728432793278719, 1.000000000000000000),
 ( 1.000000000000000000, 0.9515742818507496592, 1.000000000000000000),
 ( 1.000000000000000000, 0.9520286448580135286, 1.000000000000000000),
 ( 1.000000000000000000, 0.9520600083455192930, 1.000000000000000000),
 ( 1.000000000000000000, 0.9516561831818339812, 1.000000000000000000),
 ( 1.000000000000000000, 0.9502672014312925075, 1.000000000000000000),
 ( 1.000000000000000000, 0.9492778443961910062, 1.000000000000000000),
 ( 1.000000000000000000, 0.9459276863539570757, 1.000000000000000000),
 ( 1.000000000000000000, 0.9431151263514566674, 1.000000000000000000),
 ( 1.000000000000000000, 0.9405852554627032180, 1.000000000000000000) ) ) 
 REPRESENTATION_ITEM ( '' )  SURFACE ( )  );
#31590=CARTESIAN_POINT ( 'NONE',  ( 0.4469149852457636185, -1.151100400589097239, 0.3906371383882983328 ) ) ;
#31591=CARTESIAN_POINT ( 'NONE',  ( 0.03048720409776598320, -1.144242443753076932, 0.6605958360182316857 ) ) ;
#31593=CIRCLE ( 'NONE', #25679, 0.009999999999999925615 ) ;
#31603=CARTESIAN_POINT ( 'NONE',  ( 0.6568168296554719454, -1.515518412142557558, 0.4182417262808776903 ) ) ;
#31607=B_SPLINE_CURVE_WITH_KNOTS ( 'NONE', 3,
 ( #22662, #25727, #26151, #38858, #6785, #35196 ),
 .UNSPECIFIED., .F., .F.,
 ( 4, 2, 4 ),
 ( 0.1257255050569696386, 0.5628627525284848332, 1.000000000000000000 ),
 .UNSPECIFIED. ) ;
#31613=CARTESIAN_POINT ( 'NONE',  ( 0.5014444851153065930, -1.296109412195814548, 0.5893235223995025862 ) ) ;
#31616=CARTESIAN_POINT ( 'NONE',  ( 0.3182134860132462828, -1.756684620118125206, 0.4922052827999418012 ) ) ;
#31617=CARTESIAN_POINT ( 'NONE',  ( 0.4544126380536514520, -1.061573323663441704, 0.6302127423442334120 ) ) ;
#31623=CIRCLE ( 'NONE', #17813, 0.01000000000000002970 ) ;
#31624=CARTESIAN_POINT ( 'NONE',  ( 0.3848986351367806868, -1.605492212228826876, 0.5691465893987337488 ) ) ;
#31625=CARTESIAN_POINT ( 'NONE',  ( 0.08657002633575118511, -0.7500003421022021222, 0.03948150975026209347 ) ) ;
#31626=CARTESIAN_POINT ( 'NONE',  ( 0.1757587063316443377, -0.7188061800751018859, -0.08258769630449679100 ) ) ;
#31627=CARTESIAN_POINT ( 'NONE',  ( 0.06682908180107070828, -0.6872203660146791737, -0.001923513761143209400 ) ) ;
#31632=ORIENTED_EDGE ( 'NONE', *, *, #15028, .F. ) ;
#31634=CARTESIAN_POINT ( 'NONE',  ( 0.1210244766436220920, -0.5944767803591236577, 0.3087138919969779627 ) ) ;
#31635=VERTEX_POINT ( 'NONE', #13203 ) ;
#31636=CARTESIAN_POINT ( 'NONE',  ( 0.01730070817424270158, -0.9840727812340169800, 0.4636228551657111674 ) ) ;
#31640=CARTESIAN_POINT ( 'NONE',  ( 0.4351293263873937667, -1.231514889939106849, 0.5832342842089121016 ) ) ;
#31643=CARTESIAN_POINT ( 'NONE',  ( 0.08588225126352896921, -0.7695447752400129682, 0.06148066954598682687 ) ) ;
#31651=CARTESIAN_POINT ( 'NONE',  ( 0.2448569360945407336, -0.9465973144586597998, 0.4687868266098103587 ) ) ;
#31653=CARTESIAN_POINT ( 'NONE',  ( 0.4509566158158128113, -1.245465350927563275, 0.6057417262809816627 ) ) ;
#31656=CARTESIAN_POINT ( 'NONE',  ( 0.06257380981966247091, -1.147456929947968884, 0.7547943717889301629 ) ) ;
#31659=CARTESIAN_POINT ( 'NONE',  ( 0.6894051875735035528, -1.431063707384874206, 0.5165551067006461938 ) ) ;
#31661=CARTESIAN_POINT ( 'NONE',  ( 0.3663975874019590462, -1.157438136726376410, 0.4269148889825734039 ) ) ;
#31663=VERTEX_POINT ( 'NONE', #1110 ) ;
#31667=CARTESIAN_POINT ( 'NONE',  ( 0.7053080889764471451, -1.513942001867420339, 0.5667347313869608438 ) ) ;
#31669=CARTESIAN_POINT ( 'NONE',  ( 0.4043733228583301087, -1.150869673211134758, 0.8142501428070664238 ) ) ;
#31670=CARTESIAN_POINT ( 'NONE',  ( 0.6047538891612445067, -1.605163873594933843, 0.4396382108053981108 ) ) ;
#31673=ORIENTED_EDGE ( 'NONE', *, *, #36301, .T. ) ;
#31674=CARTESIAN_POINT ( 'NONE',  ( 0.1946548089260772552, -0.8036002232862070604, 0.2951871216237044182 ) ) ;
#31676=CARTESIAN_POINT ( 'NONE',  ( 0.01780422884439210318, -0.6047825753528456305, 0.3790601057835611964 ) ) ;
#31677=CARTESIAN_POINT ( 'NONE',  ( 0.6411073885017467555, -1.563549741984003871, 0.4256454981679176908 ) ) ;
#31678=CARTESIAN_POINT ( 'NONE',  ( 0.09455834122667663988, -1.311775142721860465, 0.5782422391874576517 ) ) ;
#31679=CARTESIAN_POINT ( 'NONE',  ( 0.01175241438441537722, -0.6703469306311590215, -0.1131776774227842425 ) ) ;
#31682=ORIENTED_EDGE ( 'NONE', *, *, #18541, .T. ) ;
#31684=CARTESIAN_POINT ( 'NONE',  ( 0.1204209576885674760, -0.9337813714611812310, 0.2981324907430850657 ) ) ;
#31686=CARTESIAN_POINT ( 'NONE',  ( 0.5852598773693732381, -1.437030116779531852, 0.6911710792806706749 ) ) ;
#31689=CARTESIAN_POINT ( 'NONE',  ( 0.1427198293237539606, -0.8385480555221326293, 0.3785612601687390333 ) ) ;
#31692=ADVANCED_FACE ( 'NONE', ( #34804 ), #28006, .F. ) ;
#31694=CARTESIAN_POINT ( 'NONE',  ( 0.2706084658143584898, -1.502104413432969521, 1.006559446342335296 ) ) ;
#31696=CARTESIAN_POINT ( 'NONE',  ( 0.08222542156927918622, -1.327483614382551913, 0.4683366274853996702 ) ) ;
#31697=CARTESIAN_POINT ( 'NONE',  ( 0.5876212857572584713, -1.642967741421476058, 0.5182417262812423209 ) ) ;
#31701=CARTESIAN_POINT ( 'NONE',  ( -3.414809992080329023E-17, -0.4300901116921415634, 0.2008512132480425316 ) ) ;
#31702=CARTESIAN_POINT ( 'NONE',  ( 0.1070510364273958154, -1.394009378634261109, 0.6504313826203965698 ) ) ;
#31710=ORIENTED_EDGE ( 'NONE', *, *, #31101, .T. ) ;
#31711=CARTESIAN_POINT ( 'NONE',  ( 0.1971908949274000789, -0.5803567546090362406, 0.3041702164619223270 ) ) ;
#31714=CARTESIAN_POINT ( 'NONE',  ( 0.2391977394211191044, -1.507150632361212272, 0.9053633066493101955 ) ) ;
#31715=CARTESIAN_POINT ( 'NONE',  ( 0.5949735957244766116, -1.487199741921636509, 0.5738185825883982405 ) ) ;
#31720=ORIENTED_EDGE ( 'NONE', *, *, #18768, .T. ) ;
#31728=CARTESIAN_POINT ( 'NONE',  ( 0.08697380094426622466, -0.7473793666617782883, 0.2016807350946292765 ) ) ;
#31729=CARTESIAN_POINT ( 'NONE',  ( 0.1131952306228060368, -0.6121952599734634681, 0.3538291842944602528 ) ) ;
#31733=AXIS2_PLACEMENT_3D ( 'NONE', #8819, #31447, #40285 ) ;
#31734=CARTESIAN_POINT ( 'NONE',  ( 0.4718170957853269898, -1.683435688723164292, 0.5702107750036669032 ) ) ;
#31735=CARTESIAN_POINT ( 'NONE',  ( 0.6931178826097424972, -1.423648263565181704, 0.6754457899003547539 ) ) ;
#31736=B_SPLINE_CURVE_WITH_KNOTS ( 'NONE', 3,
 ( #26916, #35764, #36360, #39446, #14772, #11486 ),
 .UNSPECIFIED., .F., .F.,
 ( 4, 2, 4 ),
 ( 0.000000000000000000, 0.5000000000000000000, 1.000000000000000000 ),
 .UNSPECIFIED. ) ;
#31737=ORIENTED_EDGE ( 'NONE', *, *, #12763, .T. ) ;
#31740=CARTESIAN_POINT ( 'NONE',  ( 0.5669781996639940980, -1.422531521005945043, 0.7532994004924005171 ) ) ;
#31742=CARTESIAN_POINT ( 'NONE',  ( 0.005968620458395522063, -0.8455642846060320572, 0.1487736266978308408 ) ) ;
#31744=CARTESIAN_POINT ( 'NONE',  ( 0.3207919832889619127, -1.182535135427784878, 0.4177417262808780229 ) ) ;
#31746=CARTESIAN_POINT ( 'NONE',  ( 0.05825416142610396336, -1.237506905460590723, 0.6972702062804553291 ) ) ;
#31748=CARTESIAN_POINT ( 'NONE',  ( 0.5017447040277105419, -1.102516469585429260, 0.6180670868896422920 ) ) ;
#31753=ORIENTED_EDGE ( 'NONE', *, *, #2155, .F. ) ;
#31757=FACE_OUTER_BOUND ( 'NONE', #28597, .T. ) ;
#31759=CARTESIAN_POINT ( 'NONE',  ( 0.3366372923301772513, -1.754154571440896593, 0.4608008921661775337 ) ) ;
#31761=CARTESIAN_POINT ( 'NONE',  ( 0.05446806353428223363, -1.187490080796402170, 0.7666483277446362044 ) ) ;
#31765=DIRECTION ( 'NONE',  ( 0.000000000000000000, -0.8660489055767767175, -0.4999592914920847897 ) ) ;
#31768=CARTESIAN_POINT ( 'NONE',  ( 0.3303674864723026849, -1.765107817504619980, 0.5532596536417452304 ) ) ;
#31771=CARTESIAN_POINT ( 'NONE',  ( 0.5958380658908700722, -1.598773897477913319, 0.4314101756398622256 ) ) ;
#31775=CARTESIAN_POINT ( 'NONE',  ( 0.1718750000000005274, -0.4925660985513966028, 0.3136681013253508898 ) ) ;
#31779=CARTESIAN_POINT ( 'NONE',  ( 0.09029415657535862227, -0.5650508117823077603, 0.1858836665007985722 ) ) ;
#31780=ORIENTED_EDGE ( 'NONE', *, *, #33516, .T. ) ;
#31782=ORIENTED_EDGE ( 'NONE', *, *, #26053, .T. ) ;
#31783=CARTESIAN_POINT ( 'NONE',  ( 0.01223808240847633344, -0.4396073437767880621, 0.2324838087239345930 ) ) ;
#31784=CARTESIAN_POINT ( 'NONE',  ( 0.4577816522039453995, -1.524573175657774282, 0.7453819971993982385 ) ) ;
#31786=CARTESIAN_POINT ( 'NONE',  ( 0.01431878725343691504, -0.6569777124000869550, 0.5019137659709727028 ) ) ;
#31789=CARTESIAN_POINT ( 'NONE',  ( 0.1745125816602956792, -0.9195344838042885938, 0.2322212926758656093 ) ) ;
#31791=CARTESIAN_POINT ( 'NONE',  ( 0.1153471661799889414, -0.4465907051537492123, 0.1406012133455230018 ) ) ;
#31792=CARTESIAN_POINT ( 'NONE',  ( 0.3341561371861889174, -1.068396439941279530, 0.7924052243473069801 ) ) ;
#31794=ADVANCED_FACE ( 'NONE', ( #10304 ), #18950, .T. ) ;
#31798=CARTESIAN_POINT ( 'NONE',  ( 0.1479676914811787758, -0.7747515144801853104, 0.6021013852491187146 ) ) ;
#31800=CARTESIAN_POINT ( 'NONE',  ( 0.6622529324379804461, -1.370658042826599310, 0.7087354899337895420 ) ) ;
#31804=CARTESIAN_POINT ( 'NONE',  ( 0.03820739074425011372, -1.193531024389712369, 0.6672744448627624392 ) ) ;
#31807=CARTESIAN_POINT ( 'NONE',  ( 0.2058175959260750976, -0.8974321954632414888, 0.6308810174354192446 ) ) ;
#31809=CARTESIAN_POINT ( 'NONE',  ( 0.6845239711983126529, -1.512855307908938185, 0.4537933262130811052 ) ) ;
#31813=CARTESIAN_POINT ( 'NONE',  ( 0.005980720888701209978, -0.8455916207747946611, 0.1457185332388707122 ) ) ;
#31815=CARTESIAN_POINT ( 'NONE',  ( 0.3556569928175498663, -1.173715065104882216, 0.4182417262808778013 ) ) ;
#31819=CARTESIAN_POINT ( 'NONE',  ( 0.1801801353197204358, -0.5022319782753607020, 0.1625915292881466023 ) ) ;
#31823=CARTESIAN_POINT ( 'NONE',  ( 0.4019058561636069116, -1.150920537793857390, 0.7414317717734241198 ) ) ;
#31826=CARTESIAN_POINT ( 'NONE',  ( 0.3767165169986340101, -1.018944133209149783, 0.6225985890371608100 ) ) ;
#31831=CARTESIAN_POINT ( 'NONE',  ( 0.09044078639664698827, -1.315030787261194156, 0.7167242329630961750 ) ) ;
#31832=ORIENTED_EDGE ( 'NONE', *, *, #30894, .T. ) ;
#31834=ORIENTED_EDGE ( 'NONE', *, *, #22274, .T. ) ;
#31835=CARTESIAN_POINT ( 'NONE',  ( 0.3475135998290112549, -1.498927023588051188, 0.8450769405235730725 ) ) ;
#31836=CARTESIAN_POINT ( 'NONE',  ( 0.5602799925893692246, -1.505597493397644149, 0.5182417262812344383 ) ) ;
#31837=CARTESIAN_POINT ( 'NONE',  ( 0.1108945586471002803, -0.9285926214858456484, 0.1502493406847869584 ) ) ;
#31840=ORIENTED_EDGE ( 'NONE', *, *, #1154, .T. ) ;
#31841=CARTESIAN_POINT ( 'NONE',  ( 0.4146010801322109196, -1.125553305772108104, 0.5889438968355630299 ) ) ;
#31842=CARTESIAN_POINT ( 'NONE',  ( 0.5679433476211590559, -1.501425632804762822, 0.6203578022940468006 ) ) ;
#31845=CARTESIAN_POINT ( 'NONE',  ( 0.1874563621180923845, -0.6894654218958394809, 0.06001567365385099967 ) ) ;
#31850=CARTESIAN_POINT ( 'NONE',  ( 0.1850841550199354701, -0.8515884040318244530, 0.1812164098636643572 ) ) ;
#31856=CARTESIAN_POINT ( 'NONE',  ( 0.08788382977687533848, -1.333624949218704225, 0.7170191112640089681 ) ) ;
#31860=DIRECTION ( 'NONE',  ( 0.4999551463232371762, -0.8660512985181134660, 0.000000000000000000 ) ) ;
#31861=CARTESIAN_POINT ( 'NONE',  ( 0.4409575364527853480, -1.228144365775162727, 0.5856983068965044836 ) ) ;
#31866=CARTESIAN_POINT ( 'NONE',  ( 0.2844183530474730937, -1.648412185216814541, 0.8663902821515296893 ) ) ;
#31867=CARTESIAN_POINT ( 'NONE',  ( 0.0003498636168733311783, -0.4606750075364664521, 0.04272264150788647463 ) ) ;
#31868=CARTESIAN_POINT ( 'NONE',  ( 0.6588040530991939869, -1.448684765798575080, 0.4330110937685633377 ) ) ;
#31869=CARTESIAN_POINT ( 'NONE',  ( 0.2567678775328935958, -1.218994432343741163, 0.4282360825589090481 ) ) ;
#31870=ORIENTED_EDGE ( 'NONE', *, *, #35147, .F. ) ;
#31874=EDGE_LOOP ( 'NONE', ( #23499, #12893, #23357, #12389 ) ) ;
#31878=CARTESIAN_POINT ( 'NONE',  ( 0.3465686840206718689, -1.059727123120684400, 0.8002934259178389187 ) ) ;
#31881=VERTEX_POINT ( 'NONE', #35987 ) ;
#31882=CARTESIAN_POINT ( 'NONE',  ( 0.2018967578894778903, -0.6341889671314926424, 0.3404161510980175942 ) ) ;
#31884=CARTESIAN_POINT ( 'NONE',  ( 0.01081499117344541377, -0.5305016636949330122, 0.1645499100564967454 ) ) ;
#31888=CARTESIAN_POINT ( 'NONE',  ( 0.01210987442631182576, -0.4416276171603741307, 0.06224955564382433915 ) ) ;
#31889=AXIS2_PLACEMENT_3D ( 'NONE', #22867, #35385, #270 ) ;
#31895=CARTESIAN_POINT ( 'NONE',  ( 0.1110471613688909648, -0.9287055108011992299, 0.1649583684456411847 ) ) ;
#31897=CARTESIAN_POINT ( 'NONE',  ( 0.5671292872122295492, -1.407209245721033675, 0.7602874898437926854 ) ) ;
#31899=CARTESIAN_POINT ( 'NONE',  ( 0.3288109612775019230, -1.078958935667085894, 0.7405084338778586961 ) ) ;
#31901=CARTESIAN_POINT ( 'NONE',  ( 0.1193992653793402442, -1.100149244796670978, 0.8813937183720087498 ) ) ;
#31903=CARTESIAN_POINT ( 'NONE',  ( 0.4403505402492592369, -1.147073999512834508, 0.4182417262808918457 ) ) ;
#31906=CARTESIAN_POINT ( 'NONE',  ( 0.4717768270077258852, -1.210421857018928460, 0.5378582626174832626 ) ) ;
#31919=CARTESIAN_POINT ( 'NONE',  ( 0.1909151965350180669, -0.5465291738026563095, 0.2914815663883933983 ) ) ;
#31923=CARTESIAN_POINT ( 'NONE',  ( 0.2713285965202352767, -1.671844724629077961, 0.7237048008743941496 ) ) ;
#31925=CARTESIAN_POINT ( 'NONE',  ( 0.5130770162454134642, -1.369941357579992580, 0.7991392945303081863 ) ) ;
#31938=EDGE_LOOP ( 'NONE', ( #38237, #32519, #8545, #31782 ) ) ;
#31939=CARTESIAN_POINT ( 'NONE',  ( 0.09656389424368523600, -0.7804001749690797629, 0.3156549668601592029 ) ) ;
#31940=CARTESIAN_POINT ( 'NONE',  ( 0.06924781316064872183, -0.5400285655940516572, 0.1484324165790556205 ) ) ;
#31941=CARTESIAN_POINT ( 'NONE',  ( 0.4754402869458209668, -1.412207419392573993, 0.8084286269221809818 ) ) ;
#31946=CARTESIAN_POINT ( 'NONE',  ( 0.6663302113144387029, -1.561568830604052716, 0.5775187608084981772 ) ) ;
#31947=CIRCLE ( 'NONE', #28683, 0.009999999999999956840 ) ;
#31949=CARTESIAN_POINT ( 'NONE',  ( 0.5831096498430272668, -1.442877891438895555, 0.7273179858556853006 ) ) ;
#31950=CARTESIAN_POINT ( 'NONE',  ( -0.002232160660486151842, -0.8557013418396056670, 0.1376595806906051045 ) ) ;
#31953=CARTESIAN_POINT ( 'NONE',  ( 0.4670213778778394831, -1.236191465557153757, 0.6057417262809817737 ) ) ;
#31955=CARTESIAN_POINT ( 'NONE',  ( 0.02666925540767700956, -1.119321828221852888, 0.6528166539191706530 ) ) ;
#31956=CARTESIAN_POINT ( 'NONE',  ( 0.1971950993027475063, -0.8036775079564704161, 0.3187204964795984363 ) ) ;
#31959=CARTESIAN_POINT ( 'NONE',  ( 0.4115766028365042128, -1.733048369835246794, 0.5182417262812423209 ) ) ;
#31961=CARTESIAN_POINT ( 'NONE',  ( 0.4233859075605026501, -1.153205106124581381, 0.4182417262808776903 ) ) ;
#31965=CARTESIAN_POINT ( 'NONE',  ( 0.08771792644201747979, -0.6708790313995512955, 0.02355072261337067333 ) ) ;
#31968=CARTESIAN_POINT ( 'NONE',  ( 0.1435064959217801916, -1.283467536720964697, 0.5197417262808780025 ) ) ;
#31969=CARTESIAN_POINT ( 'NONE',  ( 0.1288202176491853868, -1.269087133838645354, 0.7371036684735357003 ) ) ;
#31977=LINE ( 'NONE', #29084, #37716 ) ;
#31978=CARTESIAN_POINT ( 'NONE',  ( 0.5947695011133637966, -1.599389987319376649, 0.4269865408061249146 ) ) ;
#31981=CARTESIAN_POINT ( 'NONE',  ( 0.3802414748335787298, -1.273567264344565686, 1.090231875592916788 ) ) ;
#31984=CARTESIAN_POINT ( 'NONE',  ( 0.1943063309424913621, -0.8117621587600959421, 0.6459455874387924901 ) ) ;
#31985=CARTESIAN_POINT ( 'NONE',  ( 0.08509875786982322443, -0.8822929212134896781, 0.8597185319039459817 ) ) ;
#31986=CARTESIAN_POINT ( 'NONE',  ( 0.08687719282835834611, -0.5652987713911060697, 0.2467322302443580861 ) ) ;
#31990=CARTESIAN_POINT ( 'NONE',  ( 0.4470293266345468641, -1.057522354523741326, 0.6334801600245920650 ) ) ;
#31993=CARTESIAN_POINT ( 'NONE',  ( 0.1897112319679104542, -0.5340524121046181794, 0.1461038013937293045 ) ) ;
#31998=CARTESIAN_POINT ( 'NONE',  ( 0.6508285628959425972, -1.351727978844563749, 0.7336055660202295270 ) ) ;
#32000=CARTESIAN_POINT ( 'NONE',  ( 0.06294018881815957589, -1.325673485305720156, 0.6118058600197731067 ) ) ;
#32002=CARTESIAN_POINT ( 'NONE',  ( 0.1957937320930590308, -0.6579955005685824698, 0.3309870665194843964 ) ) ;
#32003=CARTESIAN_POINT ( 'NONE',  ( 0.3543763647980864295, -1.087156323264319546, 0.7394228186721942819 ) ) ;
#32013=ORIENTED_EDGE ( 'NONE', *, *, #37059, .F. ) ;
#32016=CARTESIAN_POINT ( 'NONE',  ( 0.1856296090430102352, -0.5404013791656668841, 0.2574253807303713004 ) ) ;
#32020=CARTESIAN_POINT ( 'NONE',  ( 0.4713312593100775216, -1.246385543292204412, 0.6820353531022836924 ) ) ;
#32023=CARTESIAN_POINT ( 'NONE',  ( 0.3535325904207607950, -1.006223909752091972, 0.6094712593526115940 ) ) ;
#32027=EDGE_LOOP ( 'NONE', ( #24991, #40170, #12358, #32037 ) ) ;
#32028=CARTESIAN_POINT ( 'NONE',  ( 0.04813743803674420257, -0.5451878913138745730, 0.2046468533792761557 ) ) ;
#32029=CARTESIAN_POINT ( 'NONE',  ( 0.08533513956138601142, -0.8071986176931464918, 0.1158118763067559620 ) ) ;
#32030=CARTESIAN_POINT ( 'NONE',  ( 0.1914787914739641550, -0.6027522233316701117, 0.3101915462042573179 ) ) ;
#32032=ORIENTED_EDGE ( 'NONE', *, *, #13037, .F. ) ;
#32033=ORIENTED_EDGE ( 'NONE', *, *, #18311, .T. ) ;
#32035=CARTESIAN_POINT ( 'NONE',  ( 0.3463719972086996557, -1.282768887459493579, 0.5758666892380096547 ) ) ;
#32036=CARTESIAN_POINT ( 'NONE',  ( 0.5665446819737203210, -1.503126282076129083, 0.5658065823788898108 ) ) ;
#32037=ORIENTED_EDGE ( 'NONE', *, *, #12304, .F. ) ;
#32041=EDGE_CURVE ( 'NONE', #8281, #22890, #30971, .T. ) ;
#32042=CARTESIAN_POINT ( 'NONE',  ( 0.1864550573006002465, -0.7573172630633775437, 0.1903174488078394899 ) ) ;
#32055=EDGE_CURVE ( 'NONE', #26063, #15823, #27691, .T. ) ;
#32060=CARTESIAN_POINT ( 'NONE',  ( 0.2589997918842421032, -1.679437038669657101, 0.5654899826020431952 ) ) ;
#32061=CARTESIAN_POINT ( 'NONE',  ( 0.2631702476264848878, -1.684641432726900812, 0.5623523273860218108 ) ) ;
#32062=CARTESIAN_POINT ( 'NONE',  ( -8.537024980200822558E-17, -0.6872203660140400183, 0.1290053960929137267 ) ) ;
#32066=CARTESIAN_POINT ( 'NONE',  ( 0.3261429079507188744, -1.179155933352486141, 0.4282554876890583562 ) ) ;
#32075=CARTESIAN_POINT ( 'NONE',  ( 0.4315594706875046094, -1.193550431808111156, 0.7933049988976597078 ) ) ;
#32078=CARTESIAN_POINT ( 'NONE',  ( 0.5505100836374232642, -1.180854739677868359, 0.6191363254822006557 ) ) ;
#32080=CARTESIAN_POINT ( 'NONE',  ( 0.2012152395183745279, -0.6237198413727698121, 0.3371149615413488454 ) ) ;
#32082=CARTESIAN_POINT ( 'NONE',  ( 0.2982621269202000436, -1.656938567095597614, 0.5878592735844545558 ) ) ;
#32086=CARTESIAN_POINT ( 'NONE',  ( 0.01187895423176401136, -0.5576892020588504195, -0.07857960794242428715 ) ) ;
#32091=CARTESIAN_POINT ( 'NONE',  ( 0.1144355769441696286, -0.9305145192040954472, 0.2393571899215944099 ) ) ;
#32093=CARTESIAN_POINT ( 'NONE',  ( 0.5956095749048035959, -1.454553929209333463, 0.7022256299952198688 ) ) ;
#32094=CARTESIAN_POINT ( 'NONE',  ( 0.3439005628038807050, -1.201380011439704409, 0.7079972624627315358 ) ) ;
#32097=CARTESIAN_POINT ( 'NONE',  ( 0.4591732152518574472, -1.217687017036588770, 0.5510147970674943441 ) ) ;
#32114=ORIENTED_EDGE ( 'NONE', *, *, #16199, .T. ) ;
#32115=CARTESIAN_POINT ( 'NONE',  ( 0.3631564311673132206, -1.147350365566272012, 0.4353599662575116658 ) ) ;
#32117=CARTESIAN_POINT ( 'NONE',  ( 0.1052687179629149677, -1.411243498674495056, 0.5672272397140760702 ) ) ;
#32120=CARTESIAN_POINT ( 'NONE',  ( 0.5943352790997880053, -1.487036568974021478, 0.5610698389965180777 ) ) ;
#32122=ORIENTED_EDGE ( 'NONE', *, *, #25629, .T. ) ;
#32126=CARTESIAN_POINT ( 'NONE',  ( 0.6667424451566161814, -1.554879396669469616, 0.6527706085860663920 ) ) ;
#32132=CARTESIAN_POINT ( 'NONE',  ( -0.001778489194304756814, -0.8469330747986113517, -0.01138449076159475312 ) ) ;
#32134=CARTESIAN_POINT ( 'NONE',  ( 0.1227777051252067902, -0.8276546441510483909, 0.4419462746931263064 ) ) ;
#32137=CARTESIAN_POINT ( 'NONE',  ( 0.2441247229987116574, -0.9568115778297857643, 0.7460559785473861449 ) ) ;
#32141=CARTESIAN_POINT ( 'NONE',  ( 0.6984911126381643243, -1.438784201617487213, 0.5700049453098480212 ) ) ;
#32142=CARTESIAN_POINT ( 'NONE',  ( 0.3580783248953228193, -1.750072000699193886, 0.5928448878684623446 ) ) ;
#32145=CARTESIAN_POINT ( 'NONE',  ( 0.5577295431261173331, -1.410318962983360569, 0.7650052283543964382 ) ) ;
#32146=CARTESIAN_POINT ( 'NONE',  ( -2.184821959533202540E-05, -0.8965584091505671704, -0.01106805737880345482 ) ) ;
#32151=CARTESIAN_POINT ( 'NONE',  ( 0.009238630504655715933, -0.9704941665429688280, 0.5327612241319219510 ) ) ;
#32152=CARTESIAN_POINT ( 'NONE',  ( 0.5137780172988268834, -1.118801028709976109, 0.5682417262808779901 ) ) ;
#32154=PLANE ( 'NONE',  #10301 ) ;
#32158=CARTESIAN_POINT ( 'NONE',  ( 0.4575003298888031256, -1.565075629471692320, 0.5772771306695322346 ) ) ;
#32159=CARTESIAN_POINT ( 'NONE',  ( 0.002367394983765177055, -0.5282119844061777814, 0.1369805761320312121 ) ) ;
#32160=CARTESIAN_POINT ( 'NONE',  ( 0.08693319772243246479, -0.7265168537571531360, 0.02880095135038760606 ) ) ;
#32161=ORIENTED_EDGE ( 'NONE', *, *, #9139, .F. ) ;
#32163=CARTESIAN_POINT ( 'NONE',  ( 0.4972320539234349468, -1.080138254241686413, 0.5197417262808780025 ) ) ;
#32164=CARTESIAN_POINT ( 'NONE',  ( 0.4683780286950792182, -1.066659082333339059, 0.7984748632466120988 ) ) ;
#32165=ORIENTED_EDGE ( 'NONE', *, *, #28012, .T. ) ;
#32170=CYLINDRICAL_SURFACE ( 'NONE', #20025, 0.09249999999977555343 ) ;
#32172=CARTESIAN_POINT ( 'NONE',  ( 0.009057834069440865235, -0.6081530143950221179, 0.008737474963860569765 ) ) ;
#32174=CARTESIAN_POINT ( 'NONE',  ( 0.08992510688325755508, -0.6057077997829157789, 0.1457185332388716836 ) ) ;
#32175=CARTESIAN_POINT ( 'NONE',  ( 0.02313328105944277915, -0.6057138157609148754, 0.5881823741868851263 ) ) ;
#32176=CARTESIAN_POINT ( 'NONE',  ( 0.08665346048445875249, -0.5632608708817946619, 0.2407920386536964441 ) ) ;
#32178=CARTESIAN_POINT ( 'NONE',  ( 0.3768783096114195486, -1.720370743462858343, 0.4222122349756301518 ) ) ;
#32179=CARTESIAN_POINT ( 'NONE',  ( 0.4929465528686921560, -1.082715557938388029, 0.5757886449898332870 ) ) ;
#32181=ORIENTED_EDGE ( 'NONE', *, *, #18740, .T. ) ;
#32182=CARTESIAN_POINT ( 'NONE',  ( 0.3242776434854518497, -1.641852578769815718, 0.5412648777784947463 ) ) ;
#32188=CARTESIAN_POINT ( 'NONE',  ( 0.5429545225213536774, -1.169342262964648826, 0.5420566649409339632 ) ) ;
#32189=CARTESIAN_POINT ( 'NONE',  ( 0.6566606523871314494, -1.361328185136354119, 0.7219929986176217840 ) ) ;
#32191=CARTESIAN_POINT ( 'NONE',  ( 0.01609855503149690281, -0.8901359181507617624, 0.5067106340194477143 ) ) ;
#32195=CARTESIAN_POINT ( 'NONE',  ( 0.3198275229399000219, -1.030254701108176185, 0.7542690204297112233 ) ) ;
#32198=AXIS2_PLACEMENT_3D ( 'NONE', #18604, #31545, #5829 ) ;
#32201=CARTESIAN_POINT ( 'NONE',  ( 0.5828811169494957367, -1.432893170591135190, 0.6998973824865686311 ) ) ;
#32203=CARTESIAN_POINT ( 'NONE',  ( 0.3918182118607624331, -1.107073211027153725, 0.6042946153017959565 ) ) ;
#32204=CARTESIAN_POINT ( 'NONE',  ( 0.07659484908144738313, -0.8729867003811840886, 0.4791183106292659089 ) ) ;
#32207=CARTESIAN_POINT ( 'NONE',  ( 0.4869195250931122043, -1.660191309538731286, 0.5031962290216808187 ) ) ;
#32209=CARTESIAN_POINT ( 'NONE',  ( 0.4500590111990616093, -1.213600599699063531, 0.6848325471722976898 ) ) ;
#32210=CARTESIAN_POINT ( 'NONE',  ( 0.4419048264408250715, -1.686280600454902245, 0.4284299735159858291 ) ) ;
#32211=CARTESIAN_POINT ( 'NONE',  ( 0.3161404488835721782, -1.757546004036539600, 0.4995768716934911868 ) ) ;
#32212=CARTESIAN_POINT ( 'NONE',  ( 0.3845716336272441138, -1.023253965646789831, 0.6260147105531964629 ) ) ;
#32216=CARTESIAN_POINT ( 'NONE',  ( 0.3728004488347659295, -1.485653693715612622, 0.8362323834158711389 ) ) ;
#32217=CARTESIAN_POINT ( 'NONE',  ( 0.06660121735839297230, -0.7068563761969431924, -0.0009791055646058395914 ) ) ;
#32218=CARTESIAN_POINT ( 'NONE',  ( 0.2019560640872724577, -0.6669419321649556753, 0.3380954050266351540 ) ) ;
#32223=CARTESIAN_POINT ( 'NONE',  ( 0.1201110248123422458, -0.5699891019612776111, 0.2421155355894170913 ) ) ;
#32225=CARTESIAN_POINT ( 'NONE',  ( 0.07279848815817739627, -1.323290893158621584, 0.4931731530909873040 ) ) ;
#32231=CARTESIAN_POINT ( 'NONE',  ( 0.08752222435001974499, -0.6850407580105462024, 0.1042154167643189189 ) ) ;
#32232=CARTESIAN_POINT ( 'NONE',  ( 0.7426951793279046310, -1.510662807742832348, 0.6358527240479500131 ) ) ;
#32235=CARTESIAN_POINT ( 'NONE',  ( 0.09721366830544136972, -1.364942592095733209, 0.6896469871951299568 ) ) ;
#32242=CARTESIAN_POINT ( 'NONE',  ( 0.04402670621142950463, -0.8156408044542829971, 0.6980404683681784572 ) ) ;
#32243=CARTESIAN_POINT ( 'NONE',  ( -3.228764966566807510E-05, -0.7201249671145206754, -0.1017258316044593325 ) ) ;
#32246=CARTESIAN_POINT ( 'NONE',  ( 0.7305197500123582488, -1.560475142278366478, 0.5182417262812423209 ) ) ;
#32251=VERTEX_POINT ( 'NONE', #3066 ) ;
#32256=CARTESIAN_POINT ( 'NONE',  ( 0.5211167752495460270, -1.329540253312506914, 0.7191629022700860574 ) ) ;
#32259=CARTESIAN_POINT ( 'NONE',  ( 0.1912825281910040254, -0.6944471949468554728, 0.2480975638430023278 ) ) ;
#32266=CARTESIAN_POINT ( 'NONE',  ( 0.02322713698175598793, -0.5357957426655662880, 0.1845586416323105050 ) ) ;
#32268=LINE ( 'NONE', #25712, #1867 ) ;
#32277=CARTESIAN_POINT ( 'NONE',  ( 0.2988694321510503848, -0.9099035776915582741, 0.5838633149813420298 ) ) ;
#32279=CARTESIAN_POINT ( 'NONE',  ( 0.5672114294812768964, -1.448954238197414757, 0.7332268910936999839 ) ) ;
#32280=CARTESIAN_POINT ( 'NONE',  ( 0.3950454177327251681, -1.172102527061769983, 0.7080655069546051283 ) ) ;
#32281=CARTESIAN_POINT ( 'NONE',  ( 0.06420656066988442157, -0.8824955108432496198, 0.7451941067001949248 ) ) ;
#32283=CARTESIAN_POINT ( 'NONE',  ( 0.4687039633801927674, -1.165676228951822546, 0.4182417262808778013 ) ) ;
#32306=CARTESIAN_POINT ( 'NONE',  ( 0.4067172716121477127, -1.179764143288656086, 0.8178903262834292809 ) ) ;
#32311=CARTESIAN_POINT ( 'NONE',  ( 0.6019566843391931377, -1.400796273631349509, 0.8618335802499477172 ) ) ;
#32321=CARTESIAN_POINT ( 'NONE',  ( -0.002121425808298199340, -0.4210325180397653244, -0.06462206035643883184 ) ) ;
#32324=CARTESIAN_POINT ( 'NONE',  ( 0.2845110416328373026, -1.007666087979148806, 0.6983705601599040635 ) ) ;
#32325=CARTESIAN_POINT ( 'NONE',  ( 0.08991294088452159161, -0.5647436697761467617, 0.1521524643572742530 ) ) ;
#32326=CARTESIAN_POINT ( 'NONE',  ( 0.4419887564222924614, -1.353243676712053700, 0.8323238201494266297 ) ) ;
#32328=CARTESIAN_POINT ( 'NONE',  ( 0.1766676265724269612, -0.4909283402585992717, 0.1805520534859691439 ) ) ;
#32330=CARTESIAN_POINT ( 'NONE',  ( 0.7205019089780672070, -1.476770077061609454, 0.5381834689638800295 ) ) ;
#32332=CARTESIAN_POINT ( 'NONE',  ( 0.6657177695133712492, -1.561535871981375223, 0.5657877757939010488 ) ) ;
#32333=DIRECTION ( 'NONE',  ( 0.4999551463232372317, -0.8660512985181135770, 0.000000000000000000 ) ) ;
#32335=CARTESIAN_POINT ( 'NONE',  ( 0.4721987900744024635, -1.279206107442438123, 0.8150767136317752515 ) ) ;
#32336=CARTESIAN_POINT ( 'NONE',  ( 0.01158385750371686805, -0.8255970240247688663, -0.07329882424099665172 ) ) ;
#32342=CARTESIAN_POINT ( 'NONE',  ( 0.09860045244982779122, -1.306187320691368337, 0.7507959704929506595 ) ) ;
#32343=CARTESIAN_POINT ( 'NONE',  ( 0.1843752803354802017, -0.7900634509218507073, 0.1541083617713018827 ) ) ;
#32346=AXIS2_PLACEMENT_3D ( 'NONE', #31046, #3263, #37413 ) ;
#32352=CARTESIAN_POINT ( 'NONE',  ( 0.002299670934844304584, -0.5203385876834750734, 0.1590128112158734619 ) ) ;
#32353=CARTESIAN_POINT ( 'NONE',  ( 0.2210032901071049827, -1.227910525351944893, 0.5087335351181689891 ) ) ;
#32355=CARTESIAN_POINT ( 'NONE',  ( 0.4971324743577882899, -1.079965756743124006, 0.4177417262808780229 ) ) ;
#32356=CARTESIAN_POINT ( 'NONE',  ( 0.6205349385892930947, -1.302967389835202772, 0.7736340727560927499 ) ) ;
#32368=CARTESIAN_POINT ( 'NONE',  ( 0.2292120464367194133, -0.8985078094207066268, 0.6777055952005869299 ) ) ;
#32369=CARTESIAN_POINT ( 'NONE',  ( 0.08687450833421726804, -0.8754084042801643095, 0.8684160286065422119 ) ) ;
#32371=CARTESIAN_POINT ( 'NONE',  ( 0.4181162624911300418, -1.391114915320552647, 0.8390373960833495959 ) ) ;
#32372=CARTESIAN_POINT ( 'NONE',  ( 0.1152873670910658371, -0.4465801609609503786, 0.1298222201462807257 ) ) ;
#32374=CARTESIAN_POINT ( 'NONE',  ( 0.09902269473968819402, -0.9382648416710920314, 0.3009685187709933984 ) ) ;
#32379=CARTESIAN_POINT ( 'NONE',  ( 0.2153037633907589343, -0.6407961093961948018, 0.4236369251119138646 ) ) ;
#32389=FACE_OUTER_BOUND ( 'NONE', #14678, .T. ) ;
#32390=CARTESIAN_POINT ( 'NONE',  ( 0.5799898087634006716, -1.239070881731211049, 0.8001874111395332889 ) ) ;
#32391=CARTESIAN_POINT ( 'NONE',  ( 0.4891551093075355294, -1.126829402807817626, 0.4573268544095612231 ) ) ;
#32397=CARTESIAN_POINT ( 'NONE',  ( 0.2456149479727556262, -0.9794485632045497603, 0.6980560059640830151 ) ) ;
#32399=CARTESIAN_POINT ( 'NONE',  ( 0.4893454517239185231, -1.274357042672645157, 0.6057417262808995062 ) ) ;
#32404=CARTESIAN_POINT ( 'NONE',  ( 0.5337844292675856250, -1.163613296893691418, 0.5164530006208986057 ) ) ;
#32405=CARTESIAN_POINT ( 'NONE',  ( 0.3048982267989297501, -1.756746414302344350, 0.5594309555313059512 ) ) ;
#32408=CARTESIAN_POINT ( 'NONE',  ( 0.2700465502981880261, -1.304386535474396869, 0.6466137386760588690 ) ) ;
#32414=CARTESIAN_POINT ( 'NONE',  ( 0.1857376701173840405, -0.7573068233460694687, 0.1312443193538671837 ) ) ;
#32415=CARTESIAN_POINT ( 'NONE',  ( 0.4672008347720292831, -1.238708369555474809, 0.6671083618078329502 ) ) ;
#32420=CARTESIAN_POINT ( 'NONE',  ( 0.2530466182501821537, -0.9510907114987208200, 0.4863111693326979679 ) ) ;
#32424=( BOUNDED_SURFACE ( )  B_SPLINE_SURFACE ( 3, 2, ( 
 ( #19410, #9920, #32141 ),
 ( #4148, #32330, #38517 ),
 ( #916, #29263, #13812 ),
 ( #20215, #17112, #16718 ),
 ( #32740, #22490, #13212 ),
 ( #13421, #25572, #7651 ),
 ( #23315, #7222, #10739 ),
 ( #6828, #4547, #38911 ) ),
 .UNSPECIFIED., .F., .F., .T. ) 
 B_SPLINE_SURFACE_WITH_KNOTS ( ( 4, 2, 2, 4 ),
 ( 3, 3 ),
 ( 0.01175530705606903266, 0.01325526436763865314, 0.01400524302342346337, 0.01475522167920827361 ),
 ( 0.4190931457273361360, 1.000000000000000000 ),
 .UNSPECIFIED. ) 
 GEOMETRIC_REPRESENTATION_ITEM ( )  RATIONAL_B_SPLINE_SURFACE ( (
 ( 0.8578808472140506680, 0.8304444319420907217, 1.000000000000000000),
 ( 0.8578018857223783655, 0.8303502267606441833, 1.000000000000000000),
 ( 0.8574190045897945867, 0.8298934295826334573, 1.000000000000000000),
 ( 0.8568921888178224755, 0.8292649108662777380, 1.000000000000000000),
 ( 0.8567216579868570658, 0.8290614586830293842, 1.000000000000000000),
 ( 0.8564019985838529081, 0.8286800883286544739, 1.000000000000000000),
 ( 0.8562511564427921495, 0.8285001257802345753, 1.000000000000000000),
 ( 0.8561112709294405043, 0.8283332350606202876, 1.000000000000000000) ) ) 
 REPRESENTATION_ITEM ( '' )  SURFACE ( )  );
#32425=CARTESIAN_POINT ( 'NONE',  ( 0.04965443803015197333, -0.5664236144437935216, 0.2699224481367241135 ) ) ;
#32427=CARTESIAN_POINT ( 'NONE',  ( 0.2936582543218392294, -1.659717270275419487, 0.5856070495615782745 ) ) ;
#32428=ORIENTED_EDGE ( 'NONE', *, *, #33516, .F. ) ;
#32431=CARTESIAN_POINT ( 'NONE',  ( 0.4708981006924713997, -1.339116817097131262, 0.8202851355120116539 ) ) ;
#32437=CARTESIAN_POINT ( 'NONE',  ( 0.1852770244791848431, -0.8385451057929541596, 0.1525445887411581436 ) ) ;
#32439=CARTESIAN_POINT ( 'NONE',  ( 0.4194637470453334571, -1.704445962963519134, 0.4281874859184326976 ) ) ;
#32442=CARTESIAN_POINT ( 'NONE',  ( 0.6952872927582756102, -1.427253715223001374, 0.8000406204621429707 ) ) ;
#32447=EDGE_CURVE ( 'NONE', #1211, #16949, #3343, .T. ) ;
#32451=CARTESIAN_POINT ( 'NONE',  ( 0.6960571170990073053, -1.427233132848869435, 0.5266323208858617599 ) ) ;
#32452=CARTESIAN_POINT ( 'NONE',  ( 0.1548759089261000366, -1.279768374172243650, 0.4182417262808777458 ) ) ;
#32453=CARTESIAN_POINT ( 'NONE',  ( 0.2565019309081923438, -1.535068652515254151, 0.9594965307338887417 ) ) ;
#32455=CIRCLE ( 'NONE', #7457, 0.1762268159172233339 ) ;
#32459=EDGE_LOOP ( 'NONE', ( #21862, #10207, #13792, #11327 ) ) ;
#32466=CARTESIAN_POINT ( 'NONE',  ( 0.3808652519481688925, -1.119552471694881257, 0.7720269669908987886 ) ) ;
#32469=CARTESIAN_POINT ( 'NONE',  ( 0.5214254866212318928, -1.138125297403113523, 0.6686424646332703725 ) ) ;
#32474=CARTESIAN_POINT ( 'NONE',  ( 0.02324396854566065235, -0.5381434244155830493, 0.1953742764374014340 ) ) ;
#32477=CARTESIAN_POINT ( 'NONE',  ( 0.1438070510857625550, -1.283988175806205723, 0.3667417262808778111 ) ) ;
#32482=CARTESIAN_POINT ( 'NONE',  ( 0.1852701303283973699, -0.8388891762519852247, 0.1468424033789395289 ) ) ;
#32485=CARTESIAN_POINT ( 'NONE',  ( 0.4352861832349482762, -1.225511609506093835, 0.6135475364930662590 ) ) ;
#32488=CARTESIAN_POINT ( 'NONE',  ( 0.4615846830202947615, -1.152285184765094117, 0.4229742390834214660 ) ) ;
#32491=CARTESIAN_POINT ( 'NONE',  ( 0.4512927739169904640, -1.222232343183551784, 0.5547766907096001177 ) ) ;
#32492=CARTESIAN_POINT ( 'NONE',  ( 0.6666052399636229753, -1.487988217786094136, 0.4225755393100666946 ) ) ;
#32496=CARTESIAN_POINT ( 'NONE',  ( 0.1316017208954911588, -1.248059642665102942, 0.5182417262812423209 ) ) ;
#32499=CARTESIAN_POINT ( 'NONE',  ( 0.003854562734146099994, -0.9635350917426001027, 0.4274684093136688623 ) ) ;
#32503=CARTESIAN_POINT ( 'NONE',  ( 0.1095009179483210360, -1.409958579616226393, 0.6174315292831226154 ) ) ;
#32506=ADVANCED_FACE ( 'NONE', ( #9852 ), #35169, .F. ) ;
#32507=CARTESIAN_POINT ( 'NONE',  ( 0.2388732087844057106, -1.438419725007294314, 1.017786028862666559 ) ) ;
#32508=DIRECTION ( 'NONE',  ( -0.8667346922030155776, -0.4987694591008393075, -3.159300867369172999E-12 ) ) ;
#32511=CARTESIAN_POINT ( 'NONE',  ( 0.1887384672550382336, -0.5142388724832238633, 0.08767850434337061405 ) ) ;
#32515=CARTESIAN_POINT ( 'NONE',  ( 0.6019331370556211258, -1.483128407181113939, 0.5723791298540690242 ) ) ;
#32517=ORIENTED_EDGE ( 'NONE', *, *, #40116, .T. ) ;
#32519=ORIENTED_EDGE ( 'NONE', *, *, #887, .T. ) ;
#32520=VERTEX_POINT ( 'NONE', #6760 ) ;
#32521=CARTESIAN_POINT ( 'NONE',  ( 0.3938429588588502339, -1.036934036128653647, 0.8714819481111626409 ) ) ;
#32524=ADVANCED_FACE ( 'NONE', ( #25507 ), #24510, .F. ) ;
#32530=CARTESIAN_POINT ( 'NONE',  ( 0.0002183020222796143764, -0.9534082139883228724, 0.09509064842809067386 ) ) ;
#32532=ORIENTED_EDGE ( 'NONE', *, *, #8667, .F. ) ;
#32533=CARTESIAN_POINT ( 'NONE',  ( 0.08636792212753842402, -0.7903263359433837509, 0.2049882209949519252 ) ) ;
#32535=CARTESIAN_POINT ( 'NONE',  ( 0.09291248155910060424, -0.5915724845055667647, 0.2542574423113423965 ) ) ;
#32536=CARTESIAN_POINT ( 'NONE',  ( 0.5389492827143899101, -1.519008290879962697, 0.5707740500833556885 ) ) ;
#32538=CARTESIAN_POINT ( 'NONE',  ( 0.05894831851802598277, -1.250166165718733291, 0.6518816580813121542 ) ) ;
#32541=CARTESIAN_POINT ( 'NONE',  ( 0.3084565412903440551, -1.760887085980910483, 0.5691548551326652827 ) ) ;
#32542=CARTESIAN_POINT ( 'NONE',  ( 0.7429086483856627288, -1.516424694377827898, 0.5595610635296612845 ) ) ;
#32543=CARTESIAN_POINT ( 'NONE',  ( 0.06936654275856572738, -1.327133429011284393, 0.5458395137742207970 ) ) ;
#32546=CARTESIAN_POINT ( 'NONE',  ( 0.01153255118075396934, -0.8600574543152128548, -0.04784606081928678006 ) ) ;
#32547=CARTESIAN_POINT ( 'NONE',  ( 0.5388299548087387425, -1.396690896044502139, 0.7799327982793118341 ) ) ;
#32549=CARTESIAN_POINT ( 'NONE',  ( 0.4970273525888077026, -1.079783658718535877, 0.3157417262808778213 ) ) ;
#32550=B_SPLINE_CURVE_WITH_KNOTS ( 'NONE', 3,
 ( #27538, #33919, #11885, #18465 ),
 .UNSPECIFIED., .F., .F.,
 ( 4, 4 ),
 ( 7.949501638480626889E-18, 0.0004616409723689751383 ),
 .UNSPECIFIED. ) ;
#32554=CARTESIAN_POINT ( 'NONE',  ( -0.003124719664520040317, -0.8057675726412020234, 0.1293934913668264852 ) ) ;
#32556=CARTESIAN_POINT ( 'NONE',  ( 0.4473065160884135416, -1.054428903401835704, 0.6531518022732211159 ) ) ;
#32562=ADVANCED_FACE ( 'NONE', ( #38290 ), #16491, .T. ) ;
#32565=ORIENTED_EDGE ( 'NONE', *, *, #4694, .F. ) ;
#32567=CARTESIAN_POINT ( 'NONE',  ( 0.01056005445531711488, -0.5296673602274948323, 0.1478910490635437502 ) ) ;
#32568=CARTESIAN_POINT ( 'NONE',  ( 0.1736343712300759123, -1.255284373594809155, 0.4365611478178134663 ) ) ;
#32571=CARTESIAN_POINT ( 'NONE',  ( 0.5016144086874707586, -1.117686766064061255, 0.8075564334577929326 ) ) ;
#32573=ORIENTED_EDGE ( 'NONE', *, *, #1554, .T. ) ;
#32578=CARTESIAN_POINT ( 'NONE',  ( 0.4434829238260091233, -1.227582997348585447, 0.5913743549708686542 ) ) ;
#32582=CARTESIAN_POINT ( 'NONE',  ( 0.1718750000000003608, -0.4565580874172215364, 0.1457185332388697130 ) ) ;
#32583=CARTESIAN_POINT ( 'NONE',  ( 0.1108361821491160165, -0.7252665196136722781, 0.3985623511072731717 ) ) ;
#32585=CARTESIAN_POINT ( 'NONE',  ( 0.1162424483802486364, -0.9470763074633095080, 0.9119154921836929439 ) ) ;
#32586=CARTESIAN_POINT ( 'NONE',  ( 0.08646685978301947573, -0.5613322375003841902, 0.2349906393216993905 ) ) ;
#32587=CARTESIAN_POINT ( 'NONE',  ( 0.1787384279610586268, -1.322427451166070300, 0.9491502850971088590 ) ) ;
#32588=CARTESIAN_POINT ( 'NONE',  ( 0.3172206172883819120, -1.646250959826369709, 0.6002829085295777745 ) ) ;
#32589=CARTESIAN_POINT ( 'NONE',  ( 0.04687500000000023592, -0.9399235171994245741, 0.1623004675701537336 ) ) ;
#32595=CARTESIAN_POINT ( 'NONE',  ( 0.2498664206433944546, -0.6480277882228060449, 0.5700154607156771025 ) ) ;
#32600=CARTESIAN_POINT ( 'NONE',  ( 0.4065730081747980229, -1.089323883707587370, 0.5182417262812423209 ) ) ;
#32601=CARTESIAN_POINT ( 'NONE',  ( 0.4594195809631357874, -1.060066247262113182, 0.7450334795338161564 ) ) ;
#32604=CARTESIAN_POINT ( 'NONE',  ( 0.0004377143710694352875, -0.8614844325866355401, 0.3723279202124662457 ) ) ;
#32609=CARTESIAN_POINT ( 'NONE',  ( 0.2994521289839266465, -1.048896011437137510, 0.7355833716002573297 ) ) ;
#32617=CARTESIAN_POINT ( 'NONE',  ( 0.4974456442574050619, -1.184401136727558868, 0.4224083929475309640 ) ) ;
#32619=FACE_OUTER_BOUND ( 'NONE', #18068, .T. ) ;
#32621=CARTESIAN_POINT ( 'NONE',  ( 0.2791220714032660588, -1.321220139306267694, 0.5799651797159807165 ) ) ;
#32622=ORIENTED_EDGE ( 'NONE', *, *, #488, .T. ) ;
#32626=CARTESIAN_POINT ( 'NONE',  ( 0.1252902061131786204, -1.410433472168242552, 0.4751538658811860216 ) ) ;
#32629=CARTESIAN_POINT ( 'NONE',  ( 0.3636433330243779016, -1.102202853961738782, 0.7268133992109953034 ) ) ;
#32631=CARTESIAN_POINT ( 'NONE',  ( 0.3229289876128840775, -1.169687821100875658, 0.5631135379446852163 ) ) ;
#32632=CARTESIAN_POINT ( 'NONE',  ( 0.1947294528115406376, -0.9190940877486376559, 0.2754987677893815934 ) ) ;
#32635=CARTESIAN_POINT ( 'NONE',  ( 0.4368279861777725204, -1.677667223885754844, 0.4182417262808776903 ) ) ;
#32638=CARTESIAN_POINT ( 'NONE',  ( 0.4141285076484039207, -1.589661339031622322, 0.5810052816111468399 ) ) ;
#32639=CARTESIAN_POINT ( 'NONE',  ( 0.06694291677841214538, -0.6774102696622015252, -0.001900350697965435751 ) ) ;
#32640=CARTESIAN_POINT ( 'NONE',  ( 0.1949235715289977799, -0.7262771972565351675, 0.3260392721664385762 ) ) ;
#32642=EDGE_LOOP ( 'NONE', ( #18579, #40570, #11233, #32161 ) ) ;
#32645=CARTESIAN_POINT ( 'NONE',  ( 0.5602801778932028354, -1.505597814391692824, 0.5212860325390119565 ) ) ;
#32646=CARTESIAN_POINT ( 'NONE',  ( 0.1192883206712807842, -0.5593364352323437760, 0.2090905374237496672 ) ) ;
#32651=CARTESIAN_POINT ( 'NONE',  ( 0.2211874525952635950, -1.239324575930034644, 0.4870531881579039934 ) ) ;
#32654=CARTESIAN_POINT ( 'NONE',  ( 0.4045891740076953402, -0.9484829520717948936, 0.8148132024759134895 ) ) ;
#32661=CARTESIAN_POINT ( 'NONE',  ( 0.1845448093765023889, -0.6265762398594633131, -0.02094390412501702034 ) ) ;
#32663=FACE_OUTER_BOUND ( 'NONE', #34645, .T. ) ;
#32664=CARTESIAN_POINT ( 'NONE',  ( 0.1255475574219608592, -1.293490214176332254, 0.4290848500164155532 ) ) ;
#32665=CARTESIAN_POINT ( 'NONE',  ( 0.0003293075040918708759, -0.6974492147978401668, 0.2474296275395909961 ) ) ;
#32668=CARTESIAN_POINT ( 'NONE',  ( 0.3048238845683336473, -1.756859000771363366, 0.5688729523718247805 ) ) ;
#32671=ORIENTED_EDGE ( 'NONE', *, *, #32041, .F. ) ;
#32672=ORIENTED_EDGE ( 'NONE', *, *, #28525, .F. ) ;
#32674=CARTESIAN_POINT ( 'NONE',  ( 0.4971920908461615607, -1.080069027881642052, 0.4687417262808780127 ) ) ;
#32675=EDGE_LOOP ( 'NONE', ( #17261, #14002, #15883, #2480, #5137 ) ) ;
#32677=CARTESIAN_POINT ( 'NONE',  ( 0.6952357793749982529, -1.543270793921424744, 0.4282417262808777547 ) ) ;
#32678=CARTESIAN_POINT ( 'NONE',  ( 0.5497128959811709015, -1.376878964193947397, 0.6508683836033526404 ) ) ;
#32680=VERTEX_POINT ( 'NONE', #19776 ) ;
#32681=CARTESIAN_POINT ( 'NONE',  ( 0.3071794164948500327, -0.9095699098325729093, 0.5987596725107463547 ) ) ;
#32684=EDGE_LOOP ( 'NONE', ( #5094, #21463, #40228, #34151 ) ) ;
#32687=CARTESIAN_POINT ( 'NONE',  ( 0.02886328582901781167, -0.5951803392457304387, 0.3522513419751048258 ) ) ;
#32688=CARTESIAN_POINT ( 'NONE',  ( 0.6892485586469115910, -1.501120256590844360, 0.4658724615422447646 ) ) ;
#32689=CARTESIAN_POINT ( 'NONE',  ( 0.1112482850659993472, -0.9162505102043612126, 0.06796212585817107410 ) ) ;
#32692=EDGE_LOOP ( 'NONE', ( #36767, #566, #36517, #34808 ) ) ;
#32694=CARTESIAN_POINT ( 'NONE',  ( 0.1586721817899592324, -1.274732504449104242, 0.4246823382044858097 ) ) ;
#32696=CARTESIAN_POINT ( 'NONE',  ( 0.4388835414683294744, -1.230108148053269401, 0.5775320749789016883 ) ) ;
#32697=CARTESIAN_POINT ( 'NONE',  ( 0.5980972052530336702, -1.476321197844801647, 0.6100096754393737886 ) ) ;
#32698=CARTESIAN_POINT ( 'NONE',  ( 0.4719477840738105501, -1.167887988919352749, 0.4182417262808778013 ) ) ;
#32700=CARTESIAN_POINT ( 'NONE',  ( 0.6605589060724770256, -1.466964374737534937, 0.4224021371703464145 ) ) ;
#32702=CARTESIAN_POINT ( 'NONE',  ( 0.3183193540680943623, -1.763265185351239106, 0.5161083673949912187 ) ) ;
#32703=DIRECTION ( 'NONE',  ( 0.8660512985181129109, 0.4999551463232381199, 0.000000000000000000 ) ) ;
#32705=CARTESIAN_POINT ( 'NONE',  ( 0.04291294112961202556, -1.197002576549752284, 0.6781355655905598745 ) ) ;
#32706=CARTESIAN_POINT ( 'NONE',  ( 0.1802568680720616767, -0.4967246651221558507, 0.1220688697886482543 ) ) ;
#32707=PRODUCT_DEFINITION_CONTEXT ( 'detailed design', #30042, 'design' ) ;
#32711=CARTESIAN_POINT ( 'NONE',  ( 0.2035125522712091239, -1.312695684735130097, 1.024845729304089126 ) ) ;
#32715=CARTESIAN_POINT ( 'NONE',  ( 0.1755442188764480826, -0.5359865673549585319, 0.2258108374879264080 ) ) ;
#32716=ORIENTED_EDGE ( 'NONE', *, *, #1875, .T. ) ;
#32718=CARTESIAN_POINT ( 'NONE',  ( 0.6023664826634441694, -1.483121557002085478, 0.5812678940365340052 ) ) ;
#32719=CARTESIAN_POINT ( 'NONE',  ( -0.001119162526905346329, -0.7995298731302591388, 0.02018642203061219928 ) ) ;
#32721=ORIENTED_EDGE ( 'NONE', *, *, #12922, .T. ) ;
#32723=CARTESIAN_POINT ( 'NONE',  ( 0.1689060685570120401, -0.6335038543973973146, 0.5777283047956938145 ) ) ;
#32725=CARTESIAN_POINT ( 'NONE',  ( -0.01296308306156608581, -0.5559130093646982296, 0.2739470918511063280 ) ) ;
#32733=CARTESIAN_POINT ( 'NONE',  ( 0.08507626058706437011, -0.7891241300377983547, 0.1457185332388674370 ) ) ;
#32734=AXIS2_PLACEMENT_3D ( 'NONE', #7586, #1254, #22858 ) ;
#32735=CARTESIAN_POINT ( 'NONE',  ( 0.09571612354954127377, -1.278066085047872669, 0.7427547889169190398 ) ) ;
#32736=CARTESIAN_POINT ( 'NONE',  ( 0.07229973480053927815, -0.5685354101550715855, 0.2638894623840417064 ) ) ;
#32737=CARTESIAN_POINT ( 'NONE',  ( 0.5391388180847991318, -1.519055229545304586, 0.5740328089454040938 ) ) ;
#32738=CARTESIAN_POINT ( 'NONE',  ( 0.1931892079297521658, -0.5558303771799478765, 0.2996417238165024477 ) ) ;
#32739=CARTESIAN_POINT ( 'NONE',  ( 0.5974135625431907792, -1.483567655257939544, 0.6235288986217942808 ) ) ;
#32740=CARTESIAN_POINT ( 'NONE',  ( 0.6808109290445034656, -1.529880038401493447, 0.4663894423524581057 ) ) ;
#32741=CARTESIAN_POINT ( 'NONE',  ( 0.3904547891981581254, -1.730724516036661331, 0.6095245837950131751 ) ) ;
#32746=CARTESIAN_POINT ( 'NONE',  ( -1.332134553831062102E-05, -0.8481898185222114250, -0.06042459179974628974 ) ) ;
#32747=CARTESIAN_POINT ( 'NONE',  ( 0.06931620475622646271, -0.5411911513605178747, 0.1654370273737149066 ) ) ;
#32751=CARTESIAN_POINT ( 'NONE',  ( -0.001163483333746527255, -0.8281092574587937127, 0.3345003353200291518 ) ) ;
#32752=CARTESIAN_POINT ( 'NONE',  ( 0.4130926557567901058, -1.028576094973266963, 0.6508837067575374835 ) ) ;
#32754=CARTESIAN_POINT ( 'NONE',  ( 0.2622253439111549289, -0.6837502657356347990, 0.6133988000875116864 ) ) ;
#32757=DIRECTION ( 'NONE',  ( 0.8660512985181134660, 0.4999551463232371762, 0.000000000000000000 ) ) ;
#32758=CARTESIAN_POINT ( 'NONE',  ( 0.3048535705585853073, -1.756846727098643868, 0.5694515197924591154 ) ) ;
#32761=CARTESIAN_POINT ( 'NONE',  ( 0.01243718341181578382, -0.5782126198877061141, 0.3200173145254873730 ) ) ;
#32763=ORIENTED_EDGE ( 'NONE', *, *, #14285, .F. ) ;
#32765=CARTESIAN_POINT ( 'NONE',  ( 0.3979743647030599130, -0.9582897341353557863, 0.7577590062044536889 ) ) ;
#32773=CARTESIAN_POINT ( 'NONE',  ( 0.5748924173612297572, -1.497770436704561225, 0.5496990462718794879 ) ) ;
#32776=DIRECTION ( 'NONE',  ( 0.01455087616121368381, 0.9998941303972840311, 0.000000000000000000 ) ) ;
#32778=CARTESIAN_POINT ( 'NONE',  ( 0.1016264643281319241, -0.7104890642553463032, 0.3444698009293519214 ) ) ;
#32779=ADVANCED_FACE ( 'NONE', ( #23086 ), #8378, .T. ) ;
#32780=CARTESIAN_POINT ( 'NONE',  ( 0.2384583617500354302, -1.436931818112165304, 1.018057733393896713 ) ) ;
#32781=CARTESIAN_POINT ( 'NONE',  ( 0.1197289683102586016, -0.7024797939781459721, 0.5140782378632711147 ) ) ;
#32782=CARTESIAN_POINT ( 'NONE',  ( 0.1147219897069867295, -0.4787606155756814474, 0.02504200487939481010 ) ) ;
#32783=CARTESIAN_POINT ( 'NONE',  ( 0.09405652007159635841, -0.9320331711797807950, 0.1940232244174328602 ) ) ;
#32784=ORIENTED_EDGE ( 'NONE', *, *, #4228, .T. ) ;
#32788=CARTESIAN_POINT ( 'NONE',  ( 0.1928073709365069055, -0.5609073072382156910, 0.2588347484435389867 ) ) ;
#32794=CARTESIAN_POINT ( 'NONE',  ( 0.6149708076787919753, -1.290796914294373154, 0.6294291921256529587 ) ) ;
#32800=CARTESIAN_POINT ( 'NONE',  ( 0.4137847586607279471, -1.167177869783954769, 0.7350384739651065757 ) ) ;
#32804=CARTESIAN_POINT ( 'NONE',  ( 0.5382321766149029685, -1.161161941655082241, 0.5682417262808779901 ) ) ;
#32805=CARTESIAN_POINT ( 'NONE',  ( 0.09270007612672712116, -0.5904679391847083014, 0.2514941034432642275 ) ) ;
#32807=CARTESIAN_POINT ( 'NONE',  ( 0.4190933895477946258, -1.125838976618574794, 0.5206150500282121785 ) ) ;
#32809=CARTESIAN_POINT ( 'NONE',  ( 0.03443964932668500817, -0.8458729558187815245, 0.2864153933819110764 ) ) ;
#32813=CARTESIAN_POINT ( 'NONE',  ( 0.1294752625188461959, -1.408006024206290618, 0.4661737917874986259 ) ) ;
#32815=CARTESIAN_POINT ( 'NONE',  ( 0.4413656098955364149, -1.203038416578624537, 0.7052521412975559789 ) ) ;
#32820=ORIENTED_EDGE ( 'NONE', *, *, #1664, .F. ) ;
#32822=CARTESIAN_POINT ( 'NONE',  ( 0.1905024329569575126, -0.5477411782657776174, 0.05501147976861575639 ) ) ;
#32823=CARTESIAN_POINT ( 'NONE',  ( 0.05799458868365583303, -0.6184633329593671736, 0.3905354639499808433 ) ) ;
#32824=CARTESIAN_POINT ( 'NONE',  ( 0.08980247528055333717, -0.5441805327445274898, 0.1299383132500184224 ) ) ;
#32825=CARTESIAN_POINT ( 'NONE',  ( 0.08512636967132125587, -0.7679112480786964845, 0.1451308451931132282 ) ) ;
#32827=EDGE_LOOP ( 'NONE', ( #34454, #24944, #32672, #26095, #15832, #20998 ) ) ;
#32832=CARTESIAN_POINT ( 'NONE',  ( 0.5748742142425384838, -1.498333522039650978, 0.6063947612278407506 ) ) ;
#32837=CARTESIAN_POINT ( 'NONE',  ( 0.2095916371365568465, -1.234515458870462989, 0.4716905264182155721 ) ) ;
#32842=CARTESIAN_POINT ( 'NONE',  ( 0.1875419504463087250, -0.4620869884079685241, 0.1831780322516418646 ) ) ;
#32844=CARTESIAN_POINT ( 'NONE',  ( 0.07556315841227359553, -1.331191507351498160, 0.4849083929475443422 ) ) ;
#32852=CARTESIAN_POINT ( 'NONE',  ( 0.4039331521932674751, -1.711434328629108714, 0.5182417262808777236 ) ) ;
#32857=CARTESIAN_POINT ( 'NONE',  ( 0.3047917418918154042, -1.756872425756282219, 0.5682432986887175907 ) ) ;
#32861=CARTESIAN_POINT ( 'NONE',  ( 0.1626176757286639796, -0.6782218769987641283, 0.05683303076865411224 ) ) ;
#32866=CARTESIAN_POINT ( 'NONE',  ( 0.4872548453982092354, -1.278504979452121937, 0.7792526119054953293 ) ) ;
#32870=CARTESIAN_POINT ( 'NONE',  ( 0.1843752803354802017, -0.7900634509218507073, 0.1541083617713018827 ) ) ;
#32875=CARTESIAN_POINT ( 'NONE',  ( 0.02413263538073280590, -0.5564134470917985187, 0.2552522691244957787 ) ) ;
#32876=CARTESIAN_POINT ( 'NONE',  ( 0.7037767268368668727, -1.494333256273129074, 0.5114234088782623200 ) ) ;
#32877=CARTESIAN_POINT ( 'NONE',  ( 0.1150181919530900154, -0.4575939575325503328, 0.07184729873914598441 ) ) ;
#32878=CARTESIAN_POINT ( 'NONE',  ( 0.4089992519647981384, -1.131314579718122992, 0.3157417262808777658 ) ) ;
#32884=CARTESIAN_POINT ( 'NONE',  ( 0.1742696185895059313, -1.268084925919871431, 0.4182417262808778013 ) ) ;
#32886=CARTESIAN_POINT ( 'NONE',  ( 0.1284000471068089122, -0.8566673793669413728, 0.4510511576820184776 ) ) ;
#32887=CARTESIAN_POINT ( 'NONE',  ( 0.5985082606850495868, -1.473464502187743941, 0.6023744451300401259 ) ) ;
#32888=DIRECTION ( 'NONE',  ( -0.8660512985181135770, -0.4999551463232371207, 0.000000000000000000 ) ) ;
#32889=CARTESIAN_POINT ( 'NONE',  ( 0.1343890788881223208, -0.9415398979786367972, 0.3700653858661135387 ) ) ;
#32893=CARTESIAN_POINT ( 'NONE',  ( 0.2755305116007160104, -1.669965222996684151, 0.4753282117146875874 ) ) ;
#32899=CARTESIAN_POINT ( 'NONE',  ( 0.4136407012227684699, -1.144011212594888027, 0.4262611942485852734 ) ) ;
#32901=DIRECTION ( 'NONE',  ( -0.4999551463232372317, 0.8660512985181135770, -0.000000000000000000 ) ) ;
#32903=EDGE_CURVE ( 'NONE', #31663, #3174, #20563, .T. ) ;
#32912=CARTESIAN_POINT ( 'NONE',  ( 0.1805708897690167514, -0.4954670953086038887, 0.09376884823743399100 ) ) ;
#32915=CARTESIAN_POINT ( 'NONE',  ( 0.1348549594756914827, -0.5515731166344398639, 0.1457185332388696020 ) ) ;
#32916=CARTESIAN_POINT ( 'NONE',  ( 0.006527597169688036625, -0.8304684498530628955, 0.07759244090682963779 ) ) ;
#32917=VERTEX_POINT ( 'NONE', #27201 ) ;
#32920=CARTESIAN_POINT ( 'NONE',  ( 0.2545402541793244100, -0.8054584187335094292, 0.7501033274436699205 ) ) ;
#32921=ORIENTED_EDGE ( 'NONE', *, *, #39578, .T. ) ;
#32922=CARTESIAN_POINT ( 'NONE',  ( 0.02304533052768314300, -0.7671398829736530978, 0.6375630150525929407 ) ) ;
#32924=FACE_OUTER_BOUND ( 'NONE', #21974, .T. ) ;
#32927=AXIS2_PLACEMENT_3D ( 'NONE', #6510, #25466, #22380 ) ;
#32934=CARTESIAN_POINT ( 'NONE',  ( 0.1042439066782299417, -0.8091407591346367889, 0.3631625727402441051 ) ) ;
#32935=CARTESIAN_POINT ( 'NONE',  ( 0.1186935531864466153, -1.414102003872103275, 0.5711544693646362081 ) ) ;
#32936=CARTESIAN_POINT ( 'NONE',  ( 0.1345564120588943480, -0.7468426462781448949, 0.5714576363270958970 ) ) ;
#32938=CARTESIAN_POINT ( 'NONE',  ( 0.1162496453231299381, -0.5482924977647862796, 0.1457185332388695187 ) ) ;
#32939=CARTESIAN_POINT ( 'NONE',  ( 0.03811508589225207772, -1.111219027208512289, 0.6472413928917138959 ) ) ;
#32942=CARTESIAN_POINT ( 'NONE',  ( 0.3211351646105950475, -1.297358875900399999, 0.4290006342139815465 ) ) ;
#32944=CARTESIAN_POINT ( 'NONE',  ( -1.920743219377653022, -2.938248161666755287, 0.6057417262804746239 ) ) ;
#32949=CARTESIAN_POINT ( 'NONE',  ( -5.815845300111390967E-05, -0.7445727859702501172, -0.09684046364400783480 ) ) ;
#32950=CARTESIAN_POINT ( 'NONE',  ( 0.06925724349164365246, -0.5402022796555754347, 0.1536732814500230693 ) ) ;
#32951=CARTESIAN_POINT ( 'NONE',  ( 0.006952085198512917251, -0.8063998755378689598, 0.04117179503985820416 ) ) ;
#32953=CARTESIAN_POINT ( 'NONE',  ( -0.003124719664520048124, -0.8057675726412016903, 0.1457185332388697963 ) ) ;
#32954=CARTESIAN_POINT ( 'NONE',  ( 0.2179926414509053834, -0.8923039640295803432, 0.4033837261968737375 ) ) ;
#32956=CARTESIAN_POINT ( 'NONE',  ( 0.1952857665188987568, -0.5148003437455072051, 0.3467747870930740217 ) ) ;
#32960=CARTESIAN_POINT ( 'NONE',  ( 0.3061685498075335521, -1.759171299767175567, 0.5690271169898788450 ) ) ;
#32965=CARTESIAN_POINT ( 'NONE',  ( 0.03078253484063611309, -0.7501471350750349432, 0.6269559300169642579 ) ) ;
#32970=CARTESIAN_POINT ( 'NONE',  ( 0.1896879205916190136, -0.5058468364965200692, 0.1731371019803292222 ) ) ;
#32972=ORIENTED_EDGE ( 'NONE', *, *, #15008, .F. ) ;
#32978=VERTEX_POINT ( 'NONE', #14630 ) ;
#32981=CARTESIAN_POINT ( 'NONE',  ( 0.09897633131546774987, -0.6690318149839973305, 0.3230829238930963410 ) ) ;
#32982=CARTESIAN_POINT ( 'NONE',  ( 0.1481019126683178200, -1.101867350517807154, 0.9906736688113091382 ) ) ;
#32983=CARTESIAN_POINT ( 'NONE',  ( 0.4971680109405678394, -1.542412852845005622, 0.5685800135497441898 ) ) ;
#32984=CARTESIAN_POINT ( 'NONE',  ( 0.2638148871170554743, -1.623480815898712848, 0.8273393273315299279 ) ) ;
#32985=CARTESIAN_POINT ( 'NONE',  ( 0.3405242896115074913, -1.744906522954273731, 0.4484829386636806081 ) ) ;
#32986=CARTESIAN_POINT ( 'NONE',  ( 0.1421613555067215151, -0.9980800295453481352, 0.5465807779430843505 ) ) ;
#32990=CARTESIAN_POINT ( 'NONE',  ( 0.1888885414493101933, -0.4614316578175808314, 0.1777954161997660487 ) ) ;
#32995=CARTESIAN_POINT ( 'NONE',  ( 0.07002615672170085792, -1.325404962382359830, 0.5075059737783654823 ) ) ;
#32998=CARTESIAN_POINT ( 'NONE',  ( 0.6014934134068773419, -1.267756190114700976, 0.6768762346975223387 ) ) ;
#33002=VERTEX_POINT ( 'NONE', #21450 ) ;
#33004=CARTESIAN_POINT ( 'NONE',  ( 0.4544434295504399812, -1.214367261269359233, 0.6181573591564563097 ) ) ;
#33008=ADVANCED_FACE ( 'NONE', ( #11957 ), #11678, .F. ) ;
#33010=CARTESIAN_POINT ( 'NONE',  ( 0.4145682426820113120, -1.006442754038745724, 0.7096782495508600075 ) ) ;
#33012=EDGE_CURVE ( 'NONE', #37890, #11376, #19104, .T. ) ;
#33013=CIRCLE ( 'NONE', #24488, 0.009999999999999996739 ) ;
#33016=CARTESIAN_POINT ( 'NONE',  ( 0.2057862311405771472, -1.177123548154546562, 0.7473132801419769544 ) ) ;
#33026=CARTESIAN_POINT ( 'NONE',  ( 0.4471179260400731659, -1.207645768960549093, 0.6708866534528135084 ) ) ;
#33031=CARTESIAN_POINT ( 'NONE',  ( 0.5959315179729184342, -1.587052097778459236, 0.4182417262808776903 ) ) ;
#33032=ORIENTED_EDGE ( 'NONE', *, *, #14788, .T. ) ;
#33034=CARTESIAN_POINT ( 'NONE',  ( 0.4136966911965741511, -1.589565852169850135, 0.5748244833461771952 ) ) ;
#33037=CARTESIAN_POINT ( 'NONE',  ( 0.08957455089030209872, -0.5701463690649801741, 0.1081760157455312760 ) ) ;
#33038=CARTESIAN_POINT ( 'NONE',  ( 0.08873781644304089278, -0.6437611796408930775, 0.1460192843988557254 ) ) ;
#33041=VERTEX_POINT ( 'NONE', #35199 ) ;
#33043=CARTESIAN_POINT ( 'NONE',  ( 0.5742732429853925069, -1.495958998523723382, 0.6323022671693150354 ) ) ;
#33045=CARTESIAN_POINT ( 'NONE',  ( 0.3135981152340067135, -1.763401867015618185, 0.5450985680089832641 ) ) ;
#33047=CARTESIAN_POINT ( 'NONE',  ( 0.6449624452930813323, -1.552575692319365652, 0.4182417262808776348 ) ) ;
#33048=CARTESIAN_POINT ( 'NONE',  ( 0.2120822108312993837, -1.233077460334429443, 0.4766410756411681438 ) ) ;
#33050=CARTESIAN_POINT ( 'NONE',  ( 0.08058916068514494768, -1.309220013881624123, 0.4727703015479320370 ) ) ;
#33052=CARTESIAN_POINT ( 'NONE',  ( 0.2803613453953150980, -0.7205873319272890765, 0.6521004353453685454 ) ) ;
#33058=CARTESIAN_POINT ( 'NONE',  ( 0.2325938614944302874, -1.347997356825076487, 0.5182417262812506475 ) ) ;
#33059=DIRECTION ( 'NONE',  ( 0.4999551463232372317, -0.8660512985181135770, 0.000000000000000000 ) ) ;
#33064=CARTESIAN_POINT ( 'NONE',  ( 0.3149693831142335032, -1.765269515322325899, 0.6420921437412323574 ) ) ;
#33067=CARTESIAN_POINT ( 'NONE',  ( 0.1211641685807053614, -1.296837725294725407, 0.5378582170338975788 ) ) ;
#33068=CARTESIAN_POINT ( 'NONE',  ( 0.6835481475269313822, -1.411548362123609790, 0.5857417262805110214 ) ) ;
#33071=VERTEX_POINT ( 'NONE', #16463 ) ;
#33072=ORIENTED_EDGE ( 'NONE', *, *, #30335, .F. ) ;
#33073=CARTESIAN_POINT ( 'NONE',  ( 0.4247531631588282730, -1.110879369639613756, 0.6102655838170102376 ) ) ;
#33079=CARTESIAN_POINT ( 'NONE',  ( 0.5317449915470191524, -1.346863324614599344, 0.6223190780326449678 ) ) ;
#33082=CARTESIAN_POINT ( 'NONE',  ( 0.5137780172988268834, -1.118801028709976109, 0.5682417262808779901 ) ) ;
#33088=CARTESIAN_POINT ( 'NONE',  ( 0.2277887942778757668, -1.330934816884134841, 0.9229718230307302207 ) ) ;
#33089=EDGE_CURVE ( 'NONE', #36909, #12111, #34979, .T. ) ;
#33090=CARTESIAN_POINT ( 'NONE',  ( 0.6747034693327369492, -1.517398054291565046, 0.4407624208754166162 ) ) ;
#33091=CARTESIAN_POINT ( 'NONE',  ( 0.1144408672107467828, -0.5040670884152405051, -0.01142007189417859440 ) ) ;
#33092=CARTESIAN_POINT ( 'NONE',  ( 0.2322138788700108258, -1.233113307957229177, 0.3157417262808777658 ) ) ;
#33099=CARTESIAN_POINT ( 'NONE',  ( 0.3319403630591543641, -1.291129383779237472, 0.5791928922408521307 ) ) ;
#33106=DIRECTION ( 'NONE',  ( -0.5077740042737255433, 0.8614903136912374082, 0.000000000000000000 ) ) ;
#33109=CARTESIAN_POINT ( 'NONE',  ( 0.3669024016988304271, -1.145827175174834123, 0.4338469531130782486 ) ) ;
#33126=CARTESIAN_POINT ( 'NONE',  ( 0.3980468560452211646, -1.724211293688185487, 0.4257487098170510409 ) ) ;
#33127=EDGE_LOOP ( 'NONE', ( #19781, #8577, #39456 ) ) ;
#33129=CARTESIAN_POINT ( 'NONE',  ( 0.1693691421777691608, -0.7003464674209329832, 0.4928941103632852871 ) ) ;
#33130=CARTESIAN_POINT ( 'NONE',  ( 9.985549626383408877E-05, -0.6770222147840202487, -0.01371064749713882085 ) ) ;
#33135=EDGE_CURVE ( 'NONE', #38375, #16750, #33817, .T. ) ;
#33136=CARTESIAN_POINT ( 'NONE',  ( 0.2675939308526570914, -1.646160075673759993, 0.7657054049786949923 ) ) ;
#33142=CARTESIAN_POINT ( 'NONE',  ( 0.6985364634159124675, -1.438850461896725275, 0.5682400285031795617 ) ) ;
#33147=CARTESIAN_POINT ( 'NONE',  ( 0.01163423095162381508, -0.7864269613462812059, -0.09388360016666105756 ) ) ;
#33148=CARTESIAN_POINT ( 'NONE',  ( 0.1175647116005374415, -1.401988507280150120, 0.6256832329251384994 ) ) ;
#33150=CARTESIAN_POINT ( 'NONE',  ( 0.1608696483632978125, -0.7559743210487993581, 0.5743405515187776089 ) ) ;
#33152=CARTESIAN_POINT ( 'NONE',  ( 0.1161508510350168916, -0.5536193762935293083, 0.1892461907774328489 ) ) ;
#33156=CARTESIAN_POINT ( 'NONE',  ( 0.06517543881758507129, -1.341089537907319551, 0.5527912483730096360 ) ) ;
#33158=CARTESIAN_POINT ( 'NONE',  ( 0.4048428100840241184, -1.714396146459797654, 0.4257347495283832495 ) ) ;
#33164=CARTESIAN_POINT ( 'NONE',  ( 0.4534726104141680314, -1.109102898972393225, 0.5733675676254303966 ) ) ;
#33165=LINE ( 'NONE', #24134, #20040 ) ;
#33168=CARTESIAN_POINT ( 'NONE',  ( 0.1873045545006853108, -1.548079183614573306, 0.6123590530682133659 ) ) ;
#33169=CARTESIAN_POINT ( 'NONE',  ( 0.3074110389119673048, -0.9534851582863556052, 0.5796648297427198226 ) ) ;
#33171=CARTESIAN_POINT ( 'NONE',  ( 0.2256281918571345080, -0.6025195051315143102, 0.5087991896564706407 ) ) ;
#33173=TOROIDAL_SURFACE ( 'NONE', #13477, 0.04749999999977547877, 0.01000000000000000021 ) ;
#33175=EDGE_CURVE ( 'NONE', #26668, #14931, #18753, .T. ) ;
#33181=CARTESIAN_POINT ( 'NONE',  ( 0.08045902273983134012, -0.9874980346209583093, 0.8248919155433931394 ) ) ;
#33183=CARTESIAN_POINT ( 'NONE',  ( 0.1626176757286639796, -0.6782218769987641283, 0.05683303076865411224 ) ) ;
#33187=CARTESIAN_POINT ( 'NONE',  ( 0.5591717342432651616, -1.201875270489466407, 0.7301083282254506868 ) ) ;
#33193=CARTESIAN_POINT ( 'NONE',  ( 0.3484677573834971120, -1.177852168535778565, 0.4182417262808778013 ) ) ;
#33198=CARTESIAN_POINT ( 'NONE',  ( 0.09038474980893905497, -0.6484375426880288895, 0.2188470046619405418 ) ) ;
#33199=CARTESIAN_POINT ( 'NONE',  ( 0.2982782193571763552, -1.650121741622242899, 0.9210486992908254456 ) ) ;
#33200=CARTESIAN_POINT ( 'NONE',  ( 0.1070046036752630297, -0.6117146700487942068, 0.3554384173735813390 ) ) ;
#33201=CARTESIAN_POINT ( 'NONE',  ( 0.1152231430944956614, -0.4481617324789591295, 0.1139065117562511747 ) ) ;
#33202=DIRECTION ( 'NONE',  ( 0.01265474379914247223, 0.8659329421511292590, -0.4999999971568669932 ) ) ;
#33203=CARTESIAN_POINT ( 'NONE',  ( 0.1516750352782837430, -1.012591555047931413, 0.5723390026005544806 ) ) ;
#33208=CARTESIAN_POINT ( 'NONE',  ( 0.1890114826851027052, -0.4630349058840709797, 0.1881648106416238253 ) ) ;
#33209=DIRECTION ( 'NONE',  ( 0.8660512985181135770, 0.4999551463232369541, 0.000000000000000000 ) ) ;
#33213=CARTESIAN_POINT ( 'NONE',  ( 0.08060092049549716364, -1.315521956732087716, 0.4779325244181578114 ) ) ;
#33217=CARTESIAN_POINT ( 'NONE',  ( 0.3484275328463246058, -0.9131724924592886650, 0.6749714385622568313 ) ) ;
#33222=CARTESIAN_POINT ( 'NONE',  ( 0.4226803827459378327, -1.212955488335365706, 0.6549176275605582687 ) ) ;
#33226=CARTESIAN_POINT ( 'NONE',  ( 0.2570033106424722824, -0.8827906082398013776, 0.5132624092235830160 ) ) ;
#33230=CARTESIAN_POINT ( 'NONE',  ( 0.05896163446183822626, -0.9045474224942531283, 0.5580107087153096668 ) ) ;
#33237=CARTESIAN_POINT ( 'NONE',  ( 0.4562328291855674012, -1.220725676369126766, 0.6612685506176263495 ) ) ;
#33245=CARTESIAN_POINT ( 'NONE',  ( 0.1924928095266713046, -0.6407273034312881421, 0.1479976049341028554 ) ) ;
#33246=CARTESIAN_POINT ( 'NONE',  ( 0.07850612262371522987, -0.6528207494238292830, 0.4497086622102388631 ) ) ;
#33247=CARTESIAN_POINT ( 'NONE',  ( 0.7062175672384829461, -1.525603138082098686, 0.5668970561574433464 ) ) ;
#33251=CARTESIAN_POINT ( 'NONE',  ( 0.5737068280812576138, -1.499206715230487319, 0.5693098563960987679 ) ) ;
#33253=CARTESIAN_POINT ( 'NONE',  ( 0.3273010810244016966, -1.767032151526223505, 0.5424958386988285586 ) ) ;
#33256=CARTESIAN_POINT ( 'NONE',  ( 0.2162048916983708990, -1.230695052506779241, 0.4870512237330100191 ) ) ;
#33260=CARTESIAN_POINT ( 'NONE',  ( 0.7227036224969136669, -1.477504586156484612, 0.6121051687398550989 ) ) ;
#33266=LINE ( 'NONE', #11859, #22129 ) ;
#33272=CARTESIAN_POINT ( 'NONE',  ( 0.1249840844849290228, -1.018512954913863844, 0.9570223520903572423 ) ) ;
#33275=CARTESIAN_POINT ( 'NONE',  ( 0.5909188805876246509, -1.601585752074789148, 0.4182417262808776903 ) ) ;
#33277=CARTESIAN_POINT ( 'NONE',  ( 0.3965913301904470112, -1.111811593118468666, 0.6217369508112339238 ) ) ;
#33278=CARTESIAN_POINT ( 'NONE',  ( 0.4092450614235220163, -1.131740385117829817, 0.4687417262808780127 ) ) ;
#33281=CARTESIAN_POINT ( 'NONE',  ( 0.5227806196671862526, -1.332469647702360094, 0.5985616508300974914 ) ) ;
#33284=CARTESIAN_POINT ( 'NONE',  ( 0.1843752803354802849, -0.7900634509218503743, 0.1457185332388700461 ) ) ;
#33285=AXIS2_PLACEMENT_3D ( 'NONE', #2322, #20235, #24742 ) ;
#33286=CARTESIAN_POINT ( 'NONE',  ( 0.5669405059600367558, -1.627145089617755058, 0.5182417262812432091 ) ) ;
#33289=CARTESIAN_POINT ( 'NONE',  ( 0.2800739882076511700, -1.402756909172277577, 0.9018012001688786583 ) ) ;
#33290=CARTESIAN_POINT ( 'NONE',  ( 0.7078192764890761657, -1.501499620364393106, 0.5258185712464616968 ) ) ;
#33291=CARTESIAN_POINT ( 'NONE',  ( 0.1772207660457670864, -0.4584906788804246625, 0.1194733215096158291 ) ) ;
#33301=CARTESIAN_POINT ( 'NONE',  ( 0.1013622771692264529, -0.8626241053983823015, 0.4561048637332515421 ) ) ;
#33302=CARTESIAN_POINT ( 'NONE',  ( 0.3363290849198692367, -1.747766234461343604, 0.4536831844799349978 ) ) ;
#33304=DIRECTION ( 'NONE',  ( -0.9390634835782838419, -0.2947238591715443667, 0.1769113355465114223 ) ) ;
#33307=CARTESIAN_POINT ( 'NONE',  ( 0.3368016641934968303, -1.066382448447511289, 0.6377147322532498164 ) ) ;
#33314=CARTESIAN_POINT ( 'NONE',  ( 0.3590698163857336533, -1.160211858102977445, 0.4287992454472202009 ) ) ;
#33315=CARTESIAN_POINT ( 'NONE',  ( 0.5624624041831085552, -1.181422097061986864, 0.6057417262809811076 ) ) ;
#33318=CARTESIAN_POINT ( 'NONE',  ( 0.01189099588732479666, -0.5490168688727182777, -0.07334142730708625990 ) ) ;
#33320=CARTESIAN_POINT ( 'NONE',  ( 0.1043520668920405597, -0.9555303118660302131, 0.9080984478619723577 ) ) ;
#33323=ORIENTED_EDGE ( 'NONE', *, *, #24480, .F. ) ;
#33325=ORIENTED_EDGE ( 'NONE', *, *, #4281, .T. ) ;
#33328=CARTESIAN_POINT ( 'NONE',  ( 0.008960703219233765240, -0.6168145289279985954, 0.004056642792912171745 ) ) ;
#33329=ORIENTED_EDGE ( 'NONE', *, *, #37441, .F. ) ;
#33331=CARTESIAN_POINT ( 'NONE',  ( 0.3082516761123384463, -1.189542454948390615, 0.5190639696864913777 ) ) ;
#33333=CARTESIAN_POINT ( 'NONE',  ( -0.001584010976415890478, -0.5275152449236482077, 0.1550235232006954844 ) ) ;
#33340=ORIENTED_EDGE ( 'NONE', *, *, #26556, .F. ) ;
#33345=CARTESIAN_POINT ( 'NONE',  ( 0.1546160709011058509, -0.7880494215839132233, 0.6157047316182207020 ) ) ;
#33346=CARTESIAN_POINT ( 'NONE',  ( 0.1864468077516607813, -0.7589597239772698511, 0.04357516743049526936 ) ) ;
#33351=DIRECTION ( 'NONE',  ( 0.9998941247116546194, -0.01455087607601020239, 0.0001066420868422379362 ) ) ;
#33355=CARTESIAN_POINT ( 'NONE',  ( 0.1625982857068778153, -0.6782215948270849948, 0.2386756342038218459 ) ) ;
#33357=CARTESIAN_POINT ( 'NONE',  ( 0.4104553069130719711, -1.122406575547196361, 0.6026975231386706433 ) ) ;
#33358=DIRECTION ( 'NONE',  ( -0.8660512985181134660, -0.4999551463232372317, -0.000000000000000000 ) ) ;
#33361=CARTESIAN_POINT ( 'NONE',  ( 0.1023011615166706662, -1.050388104772951969, 0.8771683563204210055 ) ) ;
#33362=CARTESIAN_POINT ( 'NONE',  ( 0.4678749147552476173, -1.068959612060700115, 0.6229948197350051453 ) ) ;
#33363=CARTESIAN_POINT ( 'NONE',  ( 0.06469670161903409711, -1.338666824997349236, 0.5872657038676230012 ) ) ;
#33365=CARTESIAN_POINT ( 'NONE',  ( 0.1875419504463087250, -0.4620869884079685241, 0.1831780322516418646 ) ) ;
#33368=EDGE_CURVE ( 'NONE', #30000, #14919, #17570, .T. ) ;
#33376=CARTESIAN_POINT ( 'NONE',  ( 0.008477321368347218514, -0.6246571256772747160, 0.4284521230191858931 ) ) ;
#33377=CARTESIAN_POINT ( 'NONE',  ( 0.4947650380838903850, -1.353202518180897318, 0.8084467676771096567 ) ) ;
#33378=CARTESIAN_POINT ( 'NONE',  ( 0.3111947872004536819, -1.649353374317168441, 0.4306238479843111366 ) ) ;
#33382=CARTESIAN_POINT ( 'NONE',  ( 0.6181559592477333664, -1.299230524387357866, 0.5730398182776358373 ) ) ;
#33383=VERTEX_POINT ( 'NONE', #27553 ) ;
#33386=VERTEX_POINT ( 'NONE', #12119 ) ;
#33388=CARTESIAN_POINT ( 'NONE',  ( 0.4650894839780398415, -1.233502665152375721, 0.6057417262809881020 ) ) ;
#33392=CARTESIAN_POINT ( 'NONE',  ( 0.1692070155042805502, -1.239154833823281621, 0.5978573722032971549 ) ) ;
#33393=CARTESIAN_POINT ( 'NONE',  ( 0.08699155097204941400, -0.7258079871161503549, 0.1901423733659434456 ) ) ;
#33394=CARTESIAN_POINT ( 'NONE',  ( 0.2714330136670746185, -1.557485186306450942, 0.9773871042817656729 ) ) ;
#33395=CARTESIAN_POINT ( 'NONE',  ( 0.4988887069359189685, -1.539164871451035976, 0.6394187024492539173 ) ) ;
#33396=CARTESIAN_POINT ( 'NONE',  ( 0.3390251969953095301, -1.754624289129053993, 0.4617338307200986591 ) ) ;
#33398=CARTESIAN_POINT ( 'NONE',  ( 0.01562499999999997571, -0.9454337353465637195, 0.1457185332388702959 ) ) ;
#33399=ORIENTED_EDGE ( 'NONE', *, *, #40116, .F. ) ;
#33401=ADVANCED_FACE ( 'NONE', ( #36789 ), #17589, .F. ) ;
#33403=CARTESIAN_POINT ( 'NONE',  ( 0.3275534972937365064, -0.8611932717542801763, 0.6716240152411563358 ) ) ;
#33411=CARTESIAN_POINT ( 'NONE',  ( 0.2882448896600493526, -0.8342145444298804113, 0.5948296420995525802 ) ) ;
#33421=EDGE_CURVE ( 'NONE', #15168, #38375, #35204, .T. ) ;
#33425=CARTESIAN_POINT ( 'NONE',  ( 0.05616483301611079754, -0.8972638835280528635, 0.5395877283156539361 ) ) ;
#33427=CARTESIAN_POINT ( 'NONE',  ( 0.3245308759113119113, -1.295391163961464365, 0.5682442948123348492 ) ) ;
#33431=CARTESIAN_POINT ( 'NONE',  ( 0.4176213340141963770, -1.167371637102367687, 0.6772357243189727205 ) ) ;
#33436=ORIENTED_EDGE ( 'NONE', *, *, #28577, .F. ) ;
#33439=CARTESIAN_POINT ( 'NONE',  ( 0.1893217774032603107, -0.5477411782657776174, 0.008518417185872213804 ) ) ;
#33440=CARTESIAN_POINT ( 'NONE',  ( 0.06689121793234006907, -0.5986300435503874029, 0.3429109681586494096 ) ) ;
#33441=CARTESIAN_POINT ( 'NONE',  ( 0.06863494493474814329, -0.5581937468183988393, 0.07394117948283039643 ) ) ;
#33443=CARTESIAN_POINT ( 'NONE',  ( 0.5842233870797494122, -1.491766587394369736, 0.4817266676845166629 ) ) ;
#33447=CARTESIAN_POINT ( 'NONE',  ( 0.3604753679111668552, -1.128369292247676903, 0.8103591614715777158 ) ) ;
#33450=CARTESIAN_POINT ( 'NONE',  ( 0.6372068045576322337, -1.562167934798605939, 0.4182417262808776903 ) ) ;
#33452=CARTESIAN_POINT ( 'NONE',  ( 0.1522398948605527824, -1.279186700788397024, 0.4305827652437771436 ) ) ;
#33455=CARTESIAN_POINT ( 'NONE',  ( 0.2170862770790429608, -0.5809856703168675418, 0.4747658466717744608 ) ) ;
#33457=CARTESIAN_POINT ( 'NONE',  ( 0.0009067107390556438567, -0.9454806478692553418, 0.3203524331525413604 ) ) ;
#33459=CARTESIAN_POINT ( 'NONE',  ( 0.6290530482886385055, -1.474716711548147874, 0.5182417262812423209 ) ) ;
#33461=CARTESIAN_POINT ( 'NONE',  ( 0.6984807982178791175, -1.438753897344778432, 0.5682417262808779901 ) ) ;
#33463=CARTESIAN_POINT ( 'NONE',  ( -6.552157794917040043E-17, -0.4262518876079541830, 0.1106581735831166785 ) ) ;
#33464=CARTESIAN_POINT ( 'NONE',  ( 0.5483671017596566388, -1.512491453477940784, 0.5432759641508111415 ) ) ;
#33467=CARTESIAN_POINT ( 'NONE',  ( 0.5908959048872565178, -1.601544548465854145, 0.4282886817583845818 ) ) ;
#33469=CARTESIAN_POINT ( 'NONE',  ( 0.4313479286575270244, -1.111437664270688241, 0.6062354644816806415 ) ) ;
#33470=CARTESIAN_POINT ( 'NONE',  ( 0.3752269303716003757, -1.114063827499609305, 0.6058347348966837131 ) ) ;
#33473=CARTESIAN_POINT ( 'NONE',  ( 0.3873111840515663373, -1.130537909310332489, 0.7530708704260813402 ) ) ;
#33475=ORIENTED_EDGE ( 'NONE', *, *, #16230, .F. ) ;
#33476=CARTESIAN_POINT ( 'NONE',  ( 0.4898164652207312453, -1.090206986453526872, 0.6335228833721541220 ) ) ;
#33477=ORIENTED_EDGE ( 'NONE', *, *, #40140, .T. ) ;
#33482=CARTESIAN_POINT ( 'NONE',  ( 0.3533442921551203653, -1.594940975894655111, 0.7477099863953585723 ) ) ;
#33483=CARTESIAN_POINT ( 'NONE',  ( 0.6671001712924167215, -1.531666483480435215, 0.4356495569555794423 ) ) ;
#33484=CARTESIAN_POINT ( 'NONE',  ( 0.1769134874695769410, -0.4794902306152409865, 0.04633223984654367966 ) ) ;
#33490=CARTESIAN_POINT ( 'NONE',  ( 0.3263515015897640037, -1.281719106140628117, 0.6270899215385365988 ) ) ;
#33492=CARTESIAN_POINT ( 'NONE',  ( 0.1890965627226634804, -1.347655541994686068, 0.5182417262812423209 ) ) ;
#33494=CARTESIAN_POINT ( 'NONE',  ( 0.3943456310756559002, -1.717985633627846287, 0.3157417262808776548 ) ) ;
#33498=CARTESIAN_POINT ( 'NONE',  ( 0.006497850577614296130, -0.9898846675935381034, 0.4770811589384994500 ) ) ;
#33500=CARTESIAN_POINT ( 'NONE',  ( 0.4878678730304148448, -1.127350573924966071, 0.5059297001645776115 ) ) ;
#33503=CARTESIAN_POINT ( 'NONE',  ( 0.0001552339697111116302, -0.5543275554542274053, -0.06489989973435746073 ) ) ;
#33508=EDGE_CURVE ( 'NONE', #38131, #33071, #33726, .T. ) ;
#33513=CARTESIAN_POINT ( 'NONE',  ( 0.3484677573834994435, -1.177852168535778565, 0.4182417262808778013 ) ) ;
#33516=EDGE_CURVE ( 'NONE', #17214, #32251, #1407, .T. ) ;
#33518=CARTESIAN_POINT ( 'NONE',  ( 0.009380176198049450589, -0.5822127350993825390, 0.02749488402267697210 ) ) ;
#33519=EDGE_LOOP ( 'NONE', ( #39464, #346, #4729, #34515, #39831 ) ) ;
#33524=CARTESIAN_POINT ( 'NONE',  ( 0.03758983668052903043, -0.7652432842712353356, 0.6299102424528236766 ) ) ;
#33529=CARTESIAN_POINT ( 'NONE',  ( 0.5382312210666780894, -1.161160286399032238, 0.5682417267075779987 ) ) ;
#33533=CARTESIAN_POINT ( 'NONE',  ( 0.2163934667642251342, -1.230460931614065112, 0.5491515737641515793 ) ) ;
#33534=CARTESIAN_POINT ( 'NONE',  ( 0.3370383036578078473, -1.050006858144904909, 0.7785456481707841991 ) ) ;
#33535=CARTESIAN_POINT ( 'NONE',  ( 0.1874330190944655250, -0.6911990066440627523, 0.04234871480744431538 ) ) ;
#33537=DIRECTION ( 'NONE',  ( 0.4999551463232372317, -0.8660512985181134660, 0.000000000000000000 ) ) ;
#33538=CARTESIAN_POINT ( 'NONE',  ( 0.5446897993962578344, -1.168310332749241898, 0.4402873239467990918 ) ) ;
#33541=CARTESIAN_POINT ( 'NONE',  ( 0.01220488718634634047, -0.4284039509524131817, 0.1484612068426492959 ) ) ;
#33542=CARTESIAN_POINT ( 'NONE',  ( 0.4104015424280102464, -1.716720069944782656, 0.4259487396392561687 ) ) ;
#33546=CARTESIAN_POINT ( 'NONE',  ( 0.3055995149173200143, -1.768272766478771185, 0.5197417262808792238 ) ) ;
#33552=CARTESIAN_POINT ( 'NONE',  ( 0.1492358308521446464, -1.145521527551625951, 0.9752184947445524665 ) ) ;
#33553=CARTESIAN_POINT ( 'NONE',  ( -0.002362956543387900038, -0.8470628362243999288, 0.1457185332388702959 ) ) ;
#33555=CARTESIAN_POINT ( 'NONE',  ( 0.3073438066573006555, -0.7730596496961650299, 0.7003458109913517360 ) ) ;
#33557=B_SPLINE_CURVE_WITH_KNOTS ( 'NONE', 3,
 ( #38104, #27848, #9309, #25381 ),
 .UNSPECIFIED., .F., .F.,
 ( 4, 4 ),
 ( 2.698596413362738298E-17, 0.0007105667304030845177 ),
 .UNSPECIFIED. ) ;
#33558=ADVANCED_FACE ( 'NONE', ( #12719 ), #19106, .T. ) ;
#33562=CARTESIAN_POINT ( 'NONE',  ( 0.04086830232926540879, -0.7705385959941278839, 0.6340295093763037571 ) ) ;
#33565=CARTESIAN_POINT ( 'NONE',  ( 0.1327793517848841753, -0.5956663927647375401, 0.3057313821641756135 ) ) ;
#33566=CARTESIAN_POINT ( 'NONE',  ( 0.3449116085746372629, -1.629888100695539688, 0.4182417262808778569 ) ) ;
#33570=EDGE_CURVE ( 'NONE', #11702, #20753, #16410, .T. ) ;
#33571=CARTESIAN_POINT ( 'NONE',  ( 0.5761226916817485666, -1.227707429964641328, 0.7155794456320599961 ) ) ;
#33585=CARTESIAN_POINT ( 'NONE',  ( 0.2754527148808368353, -0.9793155036609090258, 0.7096650894199401094 ) ) ;
#33586=CARTESIAN_POINT ( 'NONE',  ( 0.1677963985810169978, -1.186112715867778888, 1.005752358474822028 ) ) ;
#33587=CARTESIAN_POINT ( 'NONE',  ( 0.2358021257645211977, -0.9592120825771568438, 0.7505977746809007201 ) ) ;
#33589=CARTESIAN_POINT ( 'NONE',  ( -0.0006941592203410161229, -0.7620002068169634546, -0.005094063534273165009 ) ) ;
#33591=CARTESIAN_POINT ( 'NONE',  ( 0.09409306777181461467, -1.290726425726503201, 0.6139492122977521227 ) ) ;
#33595=CARTESIAN_POINT ( 'NONE',  ( 0.6243188685325448128, -1.312786121592256938, 0.8640797252984854238 ) ) ;
#33601=FACE_OUTER_BOUND ( 'NONE', #15107, .T. ) ;
#33602=CARTESIAN_POINT ( 'NONE',  ( 0.5553494029534283838, -1.189621637772522389, 0.5881472999875582142 ) ) ;
#33607=AXIS2_PLACEMENT_3D ( 'NONE', #2325, #13182, #25968 ) ;
#33613=ORIENTED_EDGE ( 'NONE', *, *, #4228, .F. ) ;
#33616=CARTESIAN_POINT ( 'NONE',  ( 0.1130068117282509443, -0.8274064342018203622, 0.4102281928929959465 ) ) ;
#33618=CARTESIAN_POINT ( 'NONE',  ( 0.1665889528249037688, -1.217160154129576455, 0.7453979173672002911 ) ) ;
#33625=CARTESIAN_POINT ( 'NONE',  ( 0.4014432137977476667, -1.148788978479662326, 0.6861530365891023164 ) ) ;
#33628=CARTESIAN_POINT ( 'NONE',  ( 0.4835406691325078166, -1.674675384168304415, 0.5338177255081320016 ) ) ;
#33629=CARTESIAN_POINT ( 'NONE',  ( 0.1266021694322588820, -1.239399129679921829, 0.5182417262812423209 ) ) ;
#33632=CARTESIAN_POINT ( 'NONE',  ( 0.2418900393794059245, -0.8808406326854840707, 0.7271447531890425919 ) ) ;
#33637=CARTESIAN_POINT ( 'NONE',  ( 0.4439955536442621864, -1.572094061263507925, 0.6295494919070759865 ) ) ;
#33646=ADVANCED_FACE ( 'NONE', ( #11802 ), #18254, .T. ) ;
#33648=CARTESIAN_POINT ( 'NONE',  ( 0.1251904040544656038, -0.5863800375748553506, 0.2858950053321839824 ) ) ;
#33649=CARTESIAN_POINT ( 'NONE',  ( 0.4830736825586152139, -1.664257883331242693, 0.5549537226658294298 ) ) ;
#33653=DIRECTION ( 'NONE',  ( 0.4999551463232372317, -0.8660512985181135770, 0.000000000000000000 ) ) ;
#33654=CARTESIAN_POINT ( 'NONE',  ( 0.2225889308918536924, -1.238345268919997855, 0.5682417262808776570 ) ) ;
#33655=CARTESIAN_POINT ( 'NONE',  ( 0.5517781715537678489, -1.195290833855036983, 0.8540039827052086086 ) ) ;
#33656=CARTESIAN_POINT ( 'NONE',  ( 0.07690341661973157383, -1.324345918287141322, 0.4736064436466723149 ) ) ;
#33657=CARTESIAN_POINT ( 'NONE',  ( -0.0003043527560127933592, -0.9376677575348233429, 0.2158120078562527078 ) ) ;
#33661=CARTESIAN_POINT ( 'NONE',  ( 0.6653925203977641978, -1.561488534969810438, 0.6071316550003091894 ) ) ;
#33667=CARTESIAN_POINT ( 'NONE',  ( 0.1958798485499332886, -1.272568564212325670, 1.036395571016125006 ) ) ;
#33676=CARTESIAN_POINT ( 'NONE',  ( 0.4002999475594375967, -1.110987091864168885, 0.6207864592343738108 ) ) ;
#33678=CARTESIAN_POINT ( 'NONE',  ( 0.3249672098042813984, -1.168533503727528400, 0.5670347247539490043 ) ) ;
#33679=DIRECTION ( 'NONE',  ( 0.01455087616121368381, 0.9998941303972840311, 0.000000000000000000 ) ) ;
#33681=CARTESIAN_POINT ( 'NONE',  ( 0.4745309070972864030, -1.255194402924658670, 0.7290776394288778217 ) ) ;
#33683=ORIENTED_EDGE ( 'NONE', *, *, #17284, .T. ) ;
#33684=CARTESIAN_POINT ( 'NONE',  ( 0.4473065160884135416, -1.054428903401835704, 0.6531518022732211159 ) ) ;
#33686=DIRECTION ( 'NONE',  ( 0.000000000000000000, 0.000000000000000000, -1.000000000000000000 ) ) ;
#33689=ORIENTED_EDGE ( 'NONE', *, *, #18286, .T. ) ;
#33690=CARTESIAN_POINT ( 'NONE',  ( 0.3560862010677396938, -1.622388544012473233, 0.5735089325637127144 ) ) ;
#33691=CARTESIAN_POINT ( 'NONE',  ( 0.06637855911726646407, -0.7256089028387239237, 0.002745430285754289681 ) ) ;
#33692=CARTESIAN_POINT ( 'NONE',  ( 0.1142833079139667918, -0.5209214772459205278, -0.02864359220122766891 ) ) ;
#33693=DIRECTION ( 'NONE',  ( 0.007183093100618577476, 0.4999484090412817938, 0.8660253988599867503 ) ) ;
#33697=CARTESIAN_POINT ( 'NONE',  ( 0.5121281216239255141, -1.125982481116337919, 0.6765354010138239227 ) ) ;
#33698=B_SPLINE_CURVE_WITH_KNOTS ( 'NONE', 3,
 ( #36263, #11598, #36685, #2734 ),
 .UNSPECIFIED., .F., .F.,
 ( 4, 4 ),
 ( 0.000000000000000000, 1.000000000000000000 ),
 .UNSPECIFIED. ) ;
#33701=CARTESIAN_POINT ( 'NONE',  ( 0.4165761542997364897, -1.741708882820427906, 0.5182417262812423209 ) ) ;
#33704=CARTESIAN_POINT ( 'NONE',  ( 0.2154757676707194647, -1.081506276767553176, 0.7440243676801590045 ) ) ;
#33711=CARTESIAN_POINT ( 'NONE',  ( 0.07344416302227160798, -1.332345902377664260, 0.4917314202680824198 ) ) ;
#33715=FACE_OUTER_BOUND ( 'NONE', #35361, .T. ) ;
#33717=CARTESIAN_POINT ( 'NONE',  ( 0.4647723852893586582, -1.134116793214159147, 0.4600189020470820123 ) ) ;
#33718=CARTESIAN_POINT ( 'NONE',  ( 0.3623650104644992598, -1.158602411851195724, 0.5324242784680641716 ) ) ;
#33720=CARTESIAN_POINT ( 'NONE',  ( 1.002343701812023279E-05, -0.5552538295932334389, -0.07958962418979929898 ) ) ;
#33723=CARTESIAN_POINT ( 'NONE',  ( 0.07272417404265385521, -0.8336665982203107506, 0.8213584970460865442 ) ) ;
#33726=B_SPLINE_CURVE_WITH_KNOTS ( 'NONE', 3,
 ( #5522, #18692, #31254, #28160 ),
 .UNSPECIFIED., .F., .F.,
 ( 4, 4 ),
 ( 1.734723475976807094E-18, 0.0004255989732717012559 ),
 .UNSPECIFIED. ) ;
#33734=CARTESIAN_POINT ( 'NONE',  ( 0.001639899432043153858, -0.5409522198614201693, 0.06344722032422416003 ) ) ;
#33737=ORIENTED_EDGE ( 'NONE', *, *, #18835, .T. ) ;
#33738=CARTESIAN_POINT ( 'NONE',  ( 0.1978587402095111636, -0.5849795632145003976, 0.3178455878192510409 ) ) ;
#33741=CARTESIAN_POINT ( 'NONE',  ( 0.2663068527664966267, -1.675293026590164880, 0.5727052833931987053 ) ) ;
#33743=CARTESIAN_POINT ( 'NONE',  ( 0.1273065581027945647, -1.282153141076411318, 0.6035032530794141037 ) ) ;
#33744=CARTESIAN_POINT ( 'NONE',  ( 0.1590992539432692365, -1.295692464083599171, 0.5182417262812423209 ) ) ;
#33749=CARTESIAN_POINT ( 'NONE',  ( 0.01140841165526322240, -0.9199322217433030247, 0.03086158767695902291 ) ) ;
#33750=CARTESIAN_POINT ( 'NONE',  ( 0.1862143093560868212, -0.9153542374866747711, 0.1423358669777752550 ) ) ;
#33752=CARTESIAN_POINT ( 'NONE',  ( 0.2556524848986769793, -0.9586451026735138825, 0.7438133644576581105 ) ) ;
#33754=CARTESIAN_POINT ( 'NONE',  ( 0.1866433404661365369, -0.7454955835292522703, 0.03807266482934637541 ) ) ;
#33755=CARTESIAN_POINT ( 'NONE',  ( 0.3511079287476752686, -1.164805985122749687, 0.4335040596137051394 ) ) ;
#33756=LINE ( 'NONE', #39323, #17833 ) ;
#33759=DIRECTION ( 'NONE',  ( -0.7525498468814693087, -0.4343474113619809063, 0.4949859131347307817 ) ) ;
#33762=CIRCLE ( 'NONE', #10806, 0.03749999999977551152 ) ;
#33764=CARTESIAN_POINT ( 'NONE',  ( 0.4814184380812144282, -1.664799897621735303, 0.3157417262808778213 ) ) ;
#33766=CARTESIAN_POINT ( 'NONE',  ( 0.4001190030211318471, -1.111027321722804606, 0.6208328323685005090 ) ) ;
#33772=CARTESIAN_POINT ( 'NONE',  ( 0.06825878040686909898, -0.8404074238475144343, 0.8024108098889147778 ) ) ;
#33773=VECTOR ( 'NONE', #16173, 39.37007874015748854 ) ;
#33774=CARTESIAN_POINT ( 'NONE',  ( 0.08014420339816276384, -1.182225237729999101, 0.7631665397026843323 ) ) ;
#33776=CARTESIAN_POINT ( 'NONE',  ( 0.6998761188508713094, -1.434392152549301747, 0.7385670194571644087 ) ) ;
#33785=B_SPLINE_CURVE_WITH_KNOTS ( 'NONE', 3,
 ( #36062, #23941, #1746, #10772, #27012, #23344 ),
 .UNSPECIFIED., .F., .F.,
 ( 4, 2, 4 ),
 ( 0.000000000000000000, 0.5000000000000000000, 1.000000000000000000 ),
 .UNSPECIFIED. ) ;
#33786=CARTESIAN_POINT ( 'NONE',  ( 0.1683595846758117187, -1.287579619409340292, 0.9462029255750337153 ) ) ;
#33788=CARTESIAN_POINT ( 'NONE',  ( 0.5888136248176969456, -1.490730112924630424, 0.5990021645472617395 ) ) ;
#33792=CARTESIAN_POINT ( 'NONE',  ( 0.6177995476601370051, -1.296677486146512681, 0.6035100636680229558 ) ) ;
#33795=CARTESIAN_POINT ( 'NONE',  ( 0.5885374655969598523, -1.253074615311095652, 0.8149014300617682949 ) ) ;
#33802=CYLINDRICAL_SURFACE ( 'NONE', #30975, 0.03749999999977554621 ) ;
#33804=CARTESIAN_POINT ( 'NONE',  ( 0.1463705207591960988, -0.7909580375454078327, 0.5232196913181064168 ) ) ;
#33805=CARTESIAN_POINT ( 'NONE',  ( 0.3112602777207036375, -1.738619137813147031, 0.7428781199237085575 ) ) ;
#33806=CARTESIAN_POINT ( 'NONE',  ( 0.4782480661408347600, -1.500260821454189042, 0.7558612605875917323 ) ) ;
#33807=AXIS2_PLACEMENT_3D ( 'NONE', #28958, #31860, #34938 ) ;
#33808=CARTESIAN_POINT ( 'NONE',  ( 0.5953197980378833742, -1.599064723402610300, 0.4311035055375501135 ) ) ;
#33810=CARTESIAN_POINT ( 'NONE',  ( 0.05992090360963508999, -1.332693131100006312, 0.5767975242531366842 ) ) ;
#33814=CARTESIAN_POINT ( 'NONE',  ( 0.3784499407546133010, -1.011947937249764173, 0.8629558619193703484 ) ) ;
#33817=B_SPLINE_CURVE_WITH_KNOTS ( 'NONE', 3,
 ( #6389, #9690, #9478, #31696 ),
 .UNSPECIFIED., .F., .F.,
 ( 4, 4 ),
 ( 0.000000000000000000, 0.0004633377961365348703 ),
 .UNSPECIFIED. ) ;
#33827=CARTESIAN_POINT ( 'NONE',  ( 0.3225244551428645967, -1.181327507850448155, 0.4853335682619487335 ) ) ;
#33828=CARTESIAN_POINT ( 'NONE',  ( 0.4978751173634345939, -1.107738205778658669, 0.6841874689585324409 ) ) ;
#33829=AXIS2_PLACEMENT_3D ( 'NONE', #32496, #26338, #39474 ) ;
#33832=CARTESIAN_POINT ( 'NONE',  ( 0.1895842342730561514, -0.5876096019965807438, 0.2995157642027707623 ) ) ;
#33836=AXIS2_PLACEMENT_3D ( 'NONE', #6529, #7325, #28765 ) ;
#33845=CARTESIAN_POINT ( 'NONE',  ( 0.03443144359732585452, -0.9312087828476524054, 0.6026922210726547435 ) ) ;
#33846=ORIENTED_EDGE ( 'NONE', *, *, #27413, .F. ) ;
#33853=CARTESIAN_POINT ( 'NONE',  ( 0.4488667739067040974, -1.208173968264157905, 0.6504506168610796335 ) ) ;
#33860=VERTEX_POINT ( 'NONE', #31953 ) ;
#33861=CARTESIAN_POINT ( 'NONE',  ( 0.7050990918974278099, -1.519384653903026905, 0.5628786012043504039 ) ) ;
#33862=CARTESIAN_POINT ( 'NONE',  ( 0.4433254787940574815, -1.568196705436662342, 0.6582884301997589116 ) ) ;
#33864=CARTESIAN_POINT ( 'NONE',  ( 0.5673723352274240295, -1.614853471436807242, 0.4836300718228428996 ) ) ;
#33865=CARTESIAN_POINT ( 'NONE',  ( 0.3048982267989297501, -1.756746414302344350, 0.5594309555313059512 ) ) ;
#33870=CARTESIAN_POINT ( 'NONE',  ( 0.3914081408461116407, -1.186566226689276915, 0.8257643602198004862 ) ) ;
#33871=CARTESIAN_POINT ( 'NONE',  ( 0.4737921430874441620, -1.667306459498246296, 0.4630076221598910524 ) ) ;
#33874=ORIENTED_EDGE ( 'NONE', *, *, #12304, .T. ) ;
#33877=CARTESIAN_POINT ( 'NONE',  ( 0.4419048264408291793, -1.686280600454908019, 0.4284299735155673861 ) ) ;
#33882=CARTESIAN_POINT ( 'NONE',  ( 0.4993356427094534644, -1.110845742389603430, 0.8468575151840780357 ) ) ;
#33884=CARTESIAN_POINT ( 'NONE',  ( 0.02071941500637600186, -1.004773761618042993, 0.5203810855262117618 ) ) ;
#33890=CARTESIAN_POINT ( 'NONE',  ( 0.6179826973912112553, -1.588466188088726305, 0.6165989319811293612 ) ) ;
#33893=EDGE_CURVE ( 'NONE', #6212, #40008, #12174, .T. ) ;
#33899=CARTESIAN_POINT ( 'NONE',  ( 0.1337229918471090351, -1.289495155180872876, 0.5510147389724832090 ) ) ;
#33900=CARTESIAN_POINT ( 'NONE',  ( 0.3589389236034170594, -1.749584479564031625, 0.5938934903193374693 ) ) ;
#33905=CARTESIAN_POINT ( 'NONE',  ( 0.3551276078911581591, -1.131964321692829678, 0.6011313928527168837 ) ) ;
#33908=CARTESIAN_POINT ( 'NONE',  ( 0.5168936871241821551, -1.320940109607575019, 0.6421529002730038682 ) ) ;
#33911=CARTESIAN_POINT ( 'NONE',  ( 0.5078487756305317680, -1.109832367716456325, 0.6054007957810670915 ) ) ;
#33918=CARTESIAN_POINT ( 'NONE',  ( 0.03595399678886468386, -0.5498052390641160470, 0.2287210428828644337 ) ) ;
#33919=CARTESIAN_POINT ( 'NONE',  ( 0.3558574630237864023, -1.162065433541755510, 0.4306974791478214160 ) ) ;
#33920=CARTESIAN_POINT ( 'NONE',  ( 0.1133187343594337232, -0.6553192386313622109, -0.09367839676004516281 ) ) ;
#33922=ORIENTED_EDGE ( 'NONE', *, *, #12734, .T. ) ;
#33925=CARTESIAN_POINT ( 'NONE',  ( 0.2471793377096756505, -1.006172282673910123, 0.5861680647017392110 ) ) ;
#33926=CARTESIAN_POINT ( 'NONE',  ( 0.1192653334777903779, -0.6126589172736857103, 0.3521971464290056253 ) ) ;
#33935=AXIS2_PLACEMENT_3D ( 'NONE', #21631, #18326, #9254 ) ;
#33937=CARTESIAN_POINT ( 'NONE',  ( 0.4802217237380822512, -1.662726879635128219, 0.3667417262808781442 ) ) ;
#33939=CARTESIAN_POINT ( 'NONE',  ( 0.001484713323275439105, -0.9577160478316373293, 0.3237126889746802516 ) ) ;
#33941=CARTESIAN_POINT ( 'NONE',  ( 0.4825669698268504892, -1.124365842536106053, 0.5003378186883976619 ) ) ;
#33942=CARTESIAN_POINT ( 'NONE',  ( 0.5595653757848308985, -1.183094497137172629, 0.6057417262809812186 ) ) ;
#33944=CARTESIAN_POINT ( 'NONE',  ( -0.002083146443013340551, -0.8967360763018591419, 0.1296726476164832831 ) ) ;
#33946=CARTESIAN_POINT ( 'NONE',  ( 0.3991140026135005514, -1.226416419011188808, 0.5182417262812423209 ) ) ;
#33960=CARTESIAN_POINT ( 'NONE',  ( 0.08011936691053324344, -0.9288656528420190517, 0.7837102162258990923 ) ) ;
#33961=CARTESIAN_POINT ( 'NONE',  ( 0.06650046747100032962, -0.8363599969432670145, 0.2317722016253256911 ) ) ;
#33962=CARTESIAN_POINT ( 'NONE',  ( 0.1047782527215795206, -1.275408578320203157, 0.5976651094688776311 ) ) ;
#33965=EDGE_LOOP ( 'NONE', ( #9125, #7790, #25609, #2933, #2238, #22429 ) ) ;
#33967=CARTESIAN_POINT ( 'NONE',  ( 0.3915344748440447442, -1.113207836370987636, 0.6228311983407980312 ) ) ;
#33970=CARTESIAN_POINT ( 'NONE',  ( 0.1833549916660507650, -0.8423218050691670955, 0.6657346342128551697 ) ) ;
#33971=CARTESIAN_POINT ( 'NONE',  ( 0.4737412056605618815, -1.678808096592666388, 0.5629907880828596278 ) ) ;
#33973=CARTESIAN_POINT ( 'NONE',  ( 0.01617491007160833452, -0.4928941197314672951, 0.3779610642509277363 ) ) ;
#33974=CARTESIAN_POINT ( 'NONE',  ( 0.4161606292527415540, -1.703533559239368556, 0.4226782797517861789 ) ) ;
#33978=CARTESIAN_POINT ( 'NONE',  ( -0.0003802752418593652317, -0.9311711565920335332, 0.09304606914443409871 ) ) ;
#33980=CARTESIAN_POINT ( 'NONE',  ( 0.2922741047311901985, -1.688215408676643658, 0.8015225518757634893 ) ) ;
#33981=CARTESIAN_POINT ( 'NONE',  ( 0.05225207911860056675, -1.070115161207997101, 0.7386715066487512527 ) ) ;
#33983=CARTESIAN_POINT ( 'NONE',  ( 0.4224057990199354684, -0.9849677903659747047, 0.8092447908785728172 ) ) ;
#33989=CARTESIAN_POINT ( 'NONE',  ( 0.2635503086687465135, -1.597273101066688961, 0.8385226914806884757 ) ) ;
#33990=CARTESIAN_POINT ( 'NONE',  ( 0.1283342468025234773, -0.5638928911301458458, 0.2184306303221273671 ) ) ;
#33991=CARTESIAN_POINT ( 'NONE',  ( 0.3862110256088816529, -1.731934476144517010, 0.4282538419479021141 ) ) ;
#33993=CARTESIAN_POINT ( 'NONE',  ( 0.2089316498445973613, -0.7245868578893045475, 0.3779356710034222910 ) ) ;
#33996=CARTESIAN_POINT ( 'NONE',  ( 0.4539313471337609318, -1.044844956913612677, 0.7902625984474508369 ) ) ;
#33997=( BOUNDED_SURFACE ( )  B_SPLINE_SURFACE ( 3, 2, ( 
 ( #19858, #33553, #26054 ),
 ( #7086, #10590, #20076 ),
 ( #24138, #20843, #13865 ),
 ( #39742, #38573, #23164 ),
 ( #11576, #32604, #10394 ),
 ( #14858, #16781, #38977 ),
 ( #35475, #19656, #32191 ),
 ( #1176, #26238, #36660 ),
 ( #4418, #16977, #29519 ),
 ( #30271, #1356, #26442 ),
 ( #14638, #27421, #10809 ),
 ( #23384, #36458, #5171 ),
 ( #17723, #2101, #27209 ),
 ( #8466, #21030, #5362 ),
 ( #2317, #34377, #11965 ),
 ( #37058, #27811, #21456 ),
 ( #6194, #34171, #24529 ),
 ( #24738, #18542, #37667 ),
 ( #36849, #8880, #40553 ),
 ( #9081, #33981, #286 ),
 ( #34591, #6395, #5786 ),
 ( #24321, #8662, #40347 ),
 ( #15469, #18343, #30888 ),
 ( #37265, #27607, #18762 ),
 ( #12175, #21850, #30697 ),
 ( #21235, #18961, #33774 ),
 ( #12373, #2709, #21647 ),
 ( #5583, #24929, #31495 ),
 ( #15253, #18142, #5979 ),
 ( #3119, #2518, #15057 ),
 ( #31311, #31096, #40136 ),
 ( #15661, #37457, #15866 ),
 ( #2917, #3305, #28210 ),
 ( #28020, #76, #9274 ),
 ( #12570, #25129, #9488 ),
 ( #22067, #28414, #4110 ),
 ( #6582, #28822, #10098 ),
 ( #23063, #19574, #12994 ),
 ( #19164, #31702, #16085 ),
 ( #25542, #10495, #22264 ),
 ( #25346, #681, #25740 ),
 ( #16888, #32503, #19757 ),
 ( #35592, #4326, #13383 ),
 ( #34777, #22673, #28626 ),
 ( #13170, #38485, #497 ),
 ( #29431, #19966, #38070 ) ),
 .UNSPECIFIED., .F., .F., .T. ) 
 B_SPLINE_SURFACE_WITH_KNOTS ( ( 4, 2, 2, 2, 2, 2, 2, 2, 2, 2, 2, 2, 2, 2, 2, 2, 2, 2, 2, 2, 2, 2, 4 ),
 ( 3, 3 ),
 ( 0.004598587694449686458, 0.008053666893016626915, 0.01150874609158356564, 0.01496382529015050436, 0.01582759508979223947, 0.01669136488943397459, 0.01841890448871744482, 0.01928267428835917646, 0.02014644408800091158, 0.02101021388764264669, 0.02187398368728438180, 0.02273775348692611692, 0.02360152328656785203, 0.02532906288585132226, 0.02619283268549305738, 0.02705660248513479249, 0.02792037228477652760, 0.02878414208441826272, 0.02964791188405999783, 0.03051168168370173295, 0.03094356658352260050, 0.03137545148334346806, 0.03223922128298520318 ),
 ( 0.000000000000000000, 1.000000000000000000 ),
 .UNSPECIFIED. ) 
 GEOMETRIC_REPRESENTATION_ITEM ( )  RATIONAL_B_SPLINE_SURFACE ( (
 ( 1.000000000000000000, 0.7632047519019736770, 1.000000000000000000),
 ( 1.000000000000000000, 0.7632286149905481709, 1.000000000000000000),
 ( 1.000000000000000000, 0.7629254557762273903, 1.000000000000000000),
 ( 1.000000000000000000, 0.7637623039598308017, 1.000000000000000000),
 ( 1.000000000000000000, 0.7648987287669885005, 1.000000000000000000),
 ( 1.000000000000000000, 0.7701097848380057398, 1.000000000000000000),
 ( 1.000000000000000000, 0.7743524099804016680, 1.000000000000000000),
 ( 1.000000000000000000, 0.7814619412129618636, 1.000000000000000000),
 ( 1.000000000000000000, 0.7829602748593540440, 1.000000000000000000),
 ( 1.000000000000000000, 0.7860833734074590406, 1.000000000000000000),
 ( 1.000000000000000000, 0.7877007998171637881, 1.000000000000000000),
 ( 1.000000000000000000, 0.7924769341938445733, 1.000000000000000000),
 ( 1.000000000000000000, 0.7956231603520705908, 1.000000000000000000),
 ( 1.000000000000000000, 0.7994035787022366613, 1.000000000000000000),
 ( 1.000000000000000000, 0.8005088628952052865, 1.000000000000000000),
 ( 1.000000000000000000, 0.8022700022555464550, 1.000000000000000000),
 ( 1.000000000000000000, 0.8029714101659524150, 1.000000000000000000),
 ( 1.000000000000000000, 0.8038112144617808319, 1.000000000000000000),
 ( 1.000000000000000000, 0.8039451361680508557, 1.000000000000000000),
 ( 1.000000000000000000, 0.8034950465542111120, 1.000000000000000000),
 ( 1.000000000000000000, 0.8029308292737085129, 1.000000000000000000),
 ( 1.000000000000000000, 0.8014392268801329156, 1.000000000000000000),
 ( 1.000000000000000000, 0.8004564543759468132, 1.000000000000000000),
 ( 1.000000000000000000, 0.7979003383569539531, 1.000000000000000000),
 ( 1.000000000000000000, 0.7962632686529542703, 1.000000000000000000),
 ( 1.000000000000000000, 0.7909923980647605157, 1.000000000000000000),
 ( 1.000000000000000000, 0.7869922070366083267, 1.000000000000000000),
 ( 1.000000000000000000, 0.7800571597425866033, 1.000000000000000000),
 ( 1.000000000000000000, 0.7775874025926204913, 1.000000000000000000),
 ( 1.000000000000000000, 0.7724354519564852195, 1.000000000000000000),
 ( 1.000000000000000000, 0.7697310273206949827, 1.000000000000000000),
 ( 1.000000000000000000, 0.7640258123504037879, 1.000000000000000000),
 ( 1.000000000000000000, 0.7609241244781310698, 1.000000000000000000),
 ( 1.000000000000000000, 0.7541134444708277318, 1.000000000000000000),
 ( 1.000000000000000000, 0.7504651226881818848, 1.000000000000000000),
 ( 1.000000000000000000, 0.7429106411578584312, 1.000000000000000000),
 ( 1.000000000000000000, 0.7390392288429025180, 1.000000000000000000),
 ( 1.000000000000000000, 0.7307215126039489084, 1.000000000000000000),
 ( 1.000000000000000000, 0.7264137187239084748, 1.000000000000000000),
 ( 1.000000000000000000, 0.7203301539224434835, 1.000000000000000000),
 ( 1.000000000000000000, 0.7183325906642731296, 1.000000000000000000),
 ( 1.000000000000000000, 0.7145333189904975457, 1.000000000000000000),
 ( 1.000000000000000000, 0.7127256081940787080, 1.000000000000000000),
 ( 1.000000000000000000, 0.7076437807589661677, 1.000000000000000000),
 ( 1.000000000000000000, 0.7048615031870756331, 1.000000000000000000),
 ( 1.000000000000000000, 0.7032008504187987619, 1.000000000000000000) ) ) 
 REPRESENTATION_ITEM ( '' )  SURFACE ( )  );
#34002=CARTESIAN_POINT ( 'NONE',  ( 0.08731704049279917501, -0.7051593094029652287, 0.1785453983726967564 ) ) ;
#34005=CARTESIAN_POINT ( 'NONE',  ( 0.1048038408359760476, -0.5640354025563051321, 0.2328515503754501059 ) ) ;
#34006=CARTESIAN_POINT ( 'NONE',  ( 0.3180120677078723812, -1.763266930125749088, 0.5173096362706023355 ) ) ;
#34007=CARTESIAN_POINT ( 'NONE',  ( -0.0004942178885020764119, -0.7418118112770993866, -0.01346943646478583612 ) ) ;
#34010=FACE_OUTER_BOUND ( 'NONE', #18115, .T. ) ;
#34011=CARTESIAN_POINT ( 'NONE',  ( 0.6069988657307503477, -1.282399503386861372, 0.8072536527268652229 ) ) ;
#34016=CARTESIAN_POINT ( 'NONE',  ( 0.3824648761353414694, -1.161281635105729793, 0.4182417262808778013 ) ) ;
#34018=CARTESIAN_POINT ( 'NONE',  ( 0.3157767417926863884, -1.173633493893747604, 0.4907895864628127325 ) ) ;
#34019=CARTESIAN_POINT ( 'NONE',  ( 0.4767475950167052168, -1.082687895696078595, 0.6905128956159171105 ) ) ;
#34021=CARTESIAN_POINT ( 'NONE',  ( 0.6575684296065228418, -1.565022818668032167, 0.6191063639631391169 ) ) ;
#34026=ORIENTED_EDGE ( 'NONE', *, *, #1154, .F. ) ;
#34027=DIRECTION ( 'NONE',  ( 0.9998941247116546194, -0.01455087607601020239, 0.0001066420868422379362 ) ) ;
#34028=DIRECTION ( 'NONE',  ( -0.4494955276729005189, -0.2607972048181872449, 0.8543644354495810722 ) ) ;
#34032=CARTESIAN_POINT ( 'NONE',  ( 0.1946323581323236296, -1.284704817078259120, 0.7082202489593650840 ) ) ;
#34044=CARTESIAN_POINT ( 'NONE',  ( 0.009280570092012071712, -0.4278883025115321481, 0.1457185332388686028 ) ) ;
#34049=CARTESIAN_POINT ( 'NONE',  ( 0.06947962733063202390, -1.315600342532642797, 0.5272843072721160596 ) ) ;
#34050=ORIENTED_EDGE ( 'NONE', *, *, #18768, .F. ) ;
#34052=CARTESIAN_POINT ( 'NONE',  ( 0.4414602493135039718, -1.573691556144694692, 0.5701842070315025213 ) ) ;
#34054=CARTESIAN_POINT ( 'NONE',  ( 0.5692155472414205386, -1.626790725381059177, 0.5412322144065360163 ) ) ;
#34055=CARTESIAN_POINT ( 'NONE',  ( 0.5602796947073411804, -1.505596977389118685, 0.5133479035088003295 ) ) ;
#34057=ORIENTED_EDGE ( 'NONE', *, *, #35417, .T. ) ;
#34060=CARTESIAN_POINT ( 'NONE',  ( 0.1223192797020816736, -0.5513356496355160674, 0.1705091651870799807 ) ) ;
#34061=CARTESIAN_POINT ( 'NONE',  ( 0.4598108443664392087, -1.687057064927079297, 0.4518108406592880599 ) ) ;
#34065=CARTESIAN_POINT ( 'NONE',  ( 0.4909954411287530407, -1.657501613187781775, 0.4182417262808775793 ) ) ;
#34066=CARTESIAN_POINT ( 'NONE',  ( 0.1590992539432692365, -1.295692464083599171, 0.5182417262812423209 ) ) ;
#34067=CARTESIAN_POINT ( 'NONE',  ( 0.3434800707737146741, -1.169184835483404905, 0.4282596159937968605 ) ) ;
#34068=CARTESIAN_POINT ( 'NONE',  ( 0.6005716857727874114, -1.273429356927226364, 0.8451723082856259506 ) ) ;
#34070=CARTESIAN_POINT ( 'NONE',  ( 0.002922095070481303073, -0.9671335970068797305, 0.3874888977936652990 ) ) ;
#34074=CARTESIAN_POINT ( 'NONE',  ( 0.2677971797784672314, -1.674570292523664294, 0.5743078772006583455 ) ) ;
#34078=CARTESIAN_POINT ( 'NONE',  ( 0.4841245483858538368, -1.549657009352272352, 0.5686873558213612068 ) ) ;
#34081=B_SPLINE_CURVE_WITH_KNOTS ( 'NONE', 3,
 ( #29962, #10832, #30153, #38782, #36310, #17195 ),
 .UNSPECIFIED., .F., .F.,
 ( 4, 2, 4 ),
 ( 0.0005396597967631549695, 0.001451180847823622336, 0.002362701898884089595 ),
 .UNSPECIFIED. ) ;
#34086=CARTESIAN_POINT ( 'NONE',  ( 0.1850841550199354701, -0.8515884040318244530, 0.1812164098636643572 ) ) ;
#34087=B_SPLINE_CURVE_WITH_KNOTS ( 'NONE', 3,
 ( #16988, #38584, #987, #32405 ),
 .UNSPECIFIED., .F., .F.,
 ( 4, 4 ),
 ( 1.734723475976807094E-18, 0.0007662876003044726252 ),
 .UNSPECIFIED. ) ;
#34090=CARTESIAN_POINT ( 'NONE',  ( 0.4001801618615863920, -1.148636508920398258, 0.7310201398396796169 ) ) ;
#34093=CARTESIAN_POINT ( 'NONE',  ( 0.2060221519102763132, -0.8840977030479291177, 0.3560353928791143985 ) ) ;
#34094=ORIENTED_EDGE ( 'NONE', *, *, #38075, .T. ) ;
#34098=VERTEX_POINT ( 'NONE', #37263 ) ;
#34099=ORIENTED_EDGE ( 'NONE', *, *, #7180, .F. ) ;
#34100=CARTESIAN_POINT ( 'NONE',  ( 0.03842595133820840558, -0.5761514843590607171, 0.3024418328014801816 ) ) ;
#34101=CARTESIAN_POINT ( 'NONE',  ( 0.06592485238751269461, -0.7613911970652081918, 0.01751281745013728505 ) ) ;
#34102=CARTESIAN_POINT ( 'NONE',  ( 0.1762309537805641091, -0.5849416173095501881, -0.06031293326471942606 ) ) ;
#34106=CARTESIAN_POINT ( 'NONE',  ( 0.2981519290491080887, -1.037850129404853883, 0.6229852180713888465 ) ) ;
#34107=CARTESIAN_POINT ( 'NONE',  ( 0.4535351762197513681, -1.347617495928803866, 0.8275486820836309709 ) ) ;
#34113=EDGE_CURVE ( 'NONE', #15872, #2643, #34169, .T. ) ;
#34117=CARTESIAN_POINT ( 'NONE',  ( 0.5985082606850495868, -1.473464502187743941, 0.6023744451300401259 ) ) ;
#34118=CARTESIAN_POINT ( 'NONE',  ( 0.3060205578877235877, -1.769002121529782423, 0.4687417262808789009 ) ) ;
#34119=CARTESIAN_POINT ( 'NONE',  ( 0.1939671707469822481, -1.242525794052198096, 0.6031029377704193450 ) ) ;
#34121=CARTESIAN_POINT ( 'NONE',  ( 1.365923996832131609E-16, -0.9481888444201341803, 0.1298224387748352637 ) ) ;
#34123=CARTESIAN_POINT ( 'NONE',  ( 0.4851165728318759252, -1.078419517084477697, 0.6030839855583299824 ) ) ;
#34124=CARTESIAN_POINT ( 'NONE',  ( 0.4737035873274689224, -1.116906127828866335, 0.5614642110315988255 ) ) ;
#34125=CARTESIAN_POINT ( 'NONE',  ( 0.5435348920822987706, -1.168928385231105427, 0.5856983068965041506 ) ) ;
#34127=CARTESIAN_POINT ( 'NONE',  ( 0.09860045244982779122, -1.306187320691368337, 0.7507959704929506595 ) ) ;
#34130=CARTESIAN_POINT ( 'NONE',  ( 0.3484677573834994435, -1.177852168535778565, 0.4182417262808778013 ) ) ;
#34133=DIRECTION ( 'NONE',  ( 0.9998941303973200023, -0.01455087615875037474, 0.000000000000000000 ) ) ;
#34135=CARTESIAN_POINT ( 'NONE',  ( 0.2686719937394452806, -1.673937497439395461, 0.4971255110577562086 ) ) ;
#34139=DIRECTION ( 'NONE',  ( 0.8660512985181134660, 0.4999551463232372317, 0.000000000000000000 ) ) ;
#34144=ORIENTED_EDGE ( 'NONE', *, *, #33012, .T. ) ;
#34145=CARTESIAN_POINT ( 'NONE',  ( -0.0007768880743327374406, -0.5529413628073850395, 0.2588803452509780278 ) ) ;
#34147=CARTESIAN_POINT ( 'NONE',  ( 0.08496507042635949303, -1.314462971446856754, 0.5855767900618368271 ) ) ;
#34149=CARTESIAN_POINT ( 'NONE',  ( 0.4075534289126498955, -1.705687498146139847, 0.4182417262809068337 ) ) ;
#34151=ORIENTED_EDGE ( 'NONE', *, *, #18740, .F. ) ;
#34155=CARTESIAN_POINT ( 'NONE',  ( 0.3583355372769085334, -1.108236462397462097, 0.8023416462808365957 ) ) ;
#34157=CARTESIAN_POINT ( 'NONE',  ( 0.2022720587426989902, -1.382578450136434212, 0.9362826073282410899 ) ) ;
#34159=CARTESIAN_POINT ( 'NONE',  ( 0.2475864609571435671, -1.418823566509069378, 1.026491066079080250 ) ) ;
#34161=B_SPLINE_CURVE_WITH_KNOTS ( 'NONE', 3,
 ( #449, #6952, #22829, #35348, #19706, #15812, #22012, #28364, #231, #12725, #25290, #7760, #36140, #13926, #19912, #4058, #23624, #33058 ),
 .UNSPECIFIED., .F., .F.,
 ( 4, 2, 2, 2, 2, 2, 2, 2, 4 ),
 ( 0.000000000000000000, 0.0003722442504740213886, 0.0007444885009480427772, 0.001116732751422064166, 0.001488977001896085554, 0.001861221252370106943, 0.002233465502844128332, 0.002605709753318149503, 0.002977954003792171109 ),
 .UNSPECIFIED. ) ;
#34169=LINE ( 'NONE', #2516, #5447 ) ;
#34170=CARTESIAN_POINT ( 'NONE',  ( -8.537024980200822558E-17, -0.6872203660140397963, 0.1457185332388691301 ) ) ;
#34171=CARTESIAN_POINT ( 'NONE',  ( 0.04158943244807711270, -1.020592330009299609, 0.7078592779458576789 ) ) ;
#34173=CARTESIAN_POINT ( 'NONE',  ( 0.7220926616001757115, -1.479655736425856682, 0.5682417262808782121 ) ) ;
#34174=AXIS2_PLACEMENT_3D ( 'NONE', #37727, #34028, #18822 ) ;
#34176=DIRECTION ( 'NONE',  ( 0.01455087616121368381, 0.9998941303972840311, 0.000000000000000000 ) ) ;
#34180=CARTESIAN_POINT ( 'NONE',  ( 0.2316878579425200868, -1.510780966898643385, 0.9085919253409524554 ) ) ;
#34182=ADVANCED_FACE ( 'NONE', ( #3912 ), #3507, .F. ) ;
#34183=CARTESIAN_POINT ( 'NONE',  ( 0.1349389734390225581, -0.6048227726405104310, 0.3263205089217648402 ) ) ;
#34184=CARTESIAN_POINT ( 'NONE',  ( 0.3676072623606497225, -1.734636822330196448, 0.4290806300446088350 ) ) ;
#34186=CARTESIAN_POINT ( 'NONE',  ( 0.1886295724182434630, -0.6892155111403490686, 0.2012867199884409153 ) ) ;
#34189=CARTESIAN_POINT ( 'NONE',  ( 0.6315607611771009156, -1.321640318787267843, 0.7919778341148684397 ) ) ;
#34196=CARTESIAN_POINT ( 'NONE',  ( 0.1616880641390656403, -0.8518218427985874142, 0.5517047459742124849 ) ) ;
#34199=CARTESIAN_POINT ( 'NONE',  ( 0.1041061586474624351, -0.5542841090750713073, 0.2004015504623158361 ) ) ;
#34200=CARTESIAN_POINT ( 'NONE',  ( 0.3432523969717229395, -1.751972077818550799, 0.4558970387576508076 ) ) ;
#34201=CARTESIAN_POINT ( 'NONE',  ( 0.001101228876466371154, -0.5768926175761717179, 0.01911525350802194614 ) ) ;
#34202=CARTESIAN_POINT ( 'NONE',  ( 0.007701696793370658295, -0.9976095849859260012, 0.4998176050132062120 ) ) ;
#34206=CARTESIAN_POINT ( 'NONE',  ( 0.2810522391648209162, -0.7111171087874781360, 0.6409053233574648623 ) ) ;
#34210=CARTESIAN_POINT ( 'NONE',  ( 0.3798561561205663351, -1.154581612852501715, 0.4182417262808776903 ) ) ;
#34212=CARTESIAN_POINT ( 'NONE',  ( 0.3234561073823307709, -1.180921653228079737, 0.5535308386742264775 ) ) ;
#34213=CARTESIAN_POINT ( 'NONE',  ( 0.5179624304041525740, -1.133452979592703302, 0.6716967517830890744 ) ) ;
#34218=CARTESIAN_POINT ( 'NONE',  ( 0.4004575997975503565, -1.713586824669576902, 0.4219389359880015289 ) ) ;
#34222=( BOUNDED_SURFACE ( )  B_SPLINE_SURFACE ( 3, 2, ( 
 ( #11958, #18338, #23922 ),
 ( #8262, #8656, #33766 ),
 ( #20835, #30883, #11569 ),
 ( #24523, #11151, #23709 ),
 ( #5578, #33357, #15051 ),
 ( #1911, #39940, #8874 ),
 ( #30264, #15249, #2094 ),
 ( #18137, #14631, #11758 ),
 ( #37053, #27203, #24133 ),
 ( #33164, #17919, #8459 ),
 ( #21023, #4967, #2702 ),
 ( #36840, #30693, #39329 ) ),
 .UNSPECIFIED., .F., .F., .F. ) 
 B_SPLINE_SURFACE_WITH_KNOTS ( ( 4, 2, 2, 2, 2, 4 ),
 ( 3, 3 ),
 ( -1.965116437629976787E-19, 0.0002905500556263221671, 0.0005811001112526445510, 0.001162200222505289319, 0.001743300333757933978, 0.002324400445010578638 ),
 ( 0.000000000000000000, 1.000000000000000000 ),
 .UNSPECIFIED. ) 
 GEOMETRIC_REPRESENTATION_ITEM ( )  RATIONAL_B_SPLINE_SURFACE ( (
 ( 1.000000000000000000, 0.3554223140987168850, 1.000000000000000000),
 ( 1.000000000000000000, 0.3781116103073136059, 1.000000000000000000),
 ( 1.000000000000000000, 0.4049359264755946763, 1.000000000000000000),
 ( 1.000000000000000000, 0.4598140129575411517, 1.000000000000000000),
 ( 1.000000000000000000, 0.4879366426973186788, 1.000000000000000000),
 ( 1.000000000000000000, 0.5702646001839052348, 1.000000000000000000),
 ( 1.000000000000000000, 0.6198565573272236673, 1.000000000000000000),
 ( 1.000000000000000000, 0.7059671795725417365, 1.000000000000000000),
 ( 1.000000000000000000, 0.7435989477609952214, 1.000000000000000000),
 ( 1.000000000000000000, 0.8093167251978203858, 1.000000000000000000),
 ( 1.000000000000000000, 0.8374450039889510533, 1.000000000000000000),
 ( 1.000000000000000000, 0.8603775106309528020, 1.000000000000000000) ) ) 
 REPRESENTATION_ITEM ( '' )  SURFACE ( )  );
#34224=CARTESIAN_POINT ( 'NONE',  ( 0.4364024856657339191, -1.140120363169106588, 0.4343543486376312823 ) ) ;
#34225=CIRCLE ( 'NONE', #14526, 0.01000000000000002970 ) ;
#34231=CARTESIAN_POINT ( 'NONE',  ( 0.1105865011551944721, -1.209543234154132341, 0.7561629657869882726 ) ) ;
#34234=CARTESIAN_POINT ( 'NONE',  ( 0.3186320389496528627, -1.760431904683431359, 0.5682417262808792113 ) ) ;
#34244=FACE_OUTER_BOUND ( 'NONE', #27567, .T. ) ;
#34245=EDGE_LOOP ( 'NONE', ( #18446, #948, #38749 ) ) ;
#34247=CARTESIAN_POINT ( 'NONE',  ( 0.3840491615834836225, -1.381380984370014442, 0.8560923923499079713 ) ) ;
#34249=CARTESIAN_POINT ( 'NONE',  ( 0.5656120792695429333, -1.615920895601612228, 0.4892587525384312630 ) ) ;
#34254=CARTESIAN_POINT ( 'NONE',  ( 0.1254727147607625215, -0.5505682354593325334, 0.1615710687873511131 ) ) ;
#34255=CARTESIAN_POINT ( 'NONE',  ( 0.4747166437277507978, -1.681399074042227770, 0.5637963070471054827 ) ) ;
#34256=CARTESIAN_POINT ( 'NONE',  ( 0.3792944791200489885, -1.718975934191981469, 0.4318151841061548257 ) ) ;
#34259=CARTESIAN_POINT ( 'NONE',  ( 0.2207803211308198288, -1.228036517901200719, 0.5094220132429284620 ) ) ;
#34261=CARTESIAN_POINT ( 'NONE',  ( 0.2206336596962433783, -1.239453910453733876, 0.5669030946385860137 ) ) ;
#34263=EDGE_CURVE ( 'NONE', #35870, #5559, #4798, .T. ) ;
#34265=CARTESIAN_POINT ( 'NONE',  ( 0.2954936729740054724, -0.7648845942614268534, 0.6619870385404000857 ) ) ;
#34266=EDGE_CURVE ( 'NONE', #7711, #25042, #921, .T. ) ;
#34269=ADVANCED_FACE ( 'NONE', ( #7390 ), #8514, .F. ) ;
#34271=CARTESIAN_POINT ( 'NONE',  ( 0.1866832830560181955, -0.7995344403538681144, 0.2774612360649313936 ) ) ;
#34279=CARTESIAN_POINT ( 'NONE',  ( 0.6579514796806046339, -1.538074113211328697, 0.4238364680776416371 ) ) ;
#34288=CARTESIAN_POINT ( 'NONE',  ( 0.3738069751030371757, -1.122463183855469948, 0.6233846043333758358 ) ) ;
#34289=CARTESIAN_POINT ( 'NONE',  ( 0.3249483201304784741, -1.768002432019315728, 0.5182417262812728520 ) ) ;
#34292=CARTESIAN_POINT ( 'NONE',  ( 0.4303872151682832659, -1.189052686049667074, 0.7234122301098351304 ) ) ;
#34295=CARTESIAN_POINT ( 'NONE',  ( 0.4430687885351943245, -1.051147784193108281, 0.6535119922057798236 ) ) ;
#34300=ORIENTED_EDGE ( 'NONE', *, *, #447, .F. ) ;
#34301=CARTESIAN_POINT ( 'NONE',  ( 0.1289379552302614418, -0.9164046769963616335, 0.7560741064833712555 ) ) ;
#34302=CARTESIAN_POINT ( 'NONE',  ( 0.06626660213556555268, -0.7348254893761211326, 0.005522339898145539085 ) ) ;
#34303=CARTESIAN_POINT ( 'NONE',  ( 0.1749985090116134290, -0.8722846205208456549, 0.008124829994509464443 ) ) ;
#34307=CARTESIAN_POINT ( 'NONE',  ( 0.3620239859624554968, -1.000756814187188315, 0.6096560215957895768 ) ) ;
#34308=CARTESIAN_POINT ( 'NONE',  ( 0.5529025669954783506, -1.511171647080765679, 0.5718623976496952643 ) ) ;
#34320=CARTESIAN_POINT ( 'NONE',  ( 0.1438259253235277535, -1.251381717279140160, 0.6230599517298043288 ) ) ;
#34326=CARTESIAN_POINT ( 'NONE',  ( 0.3611884512188844321, -1.010424417365897831, 0.6143157383772529512 ) ) ;
#34327=CARTESIAN_POINT ( 'NONE',  ( 0.4839995430037176138, -1.120831722135291697, 0.5371002527360760892 ) ) ;
#34329=CARTESIAN_POINT ( 'NONE',  ( 0.4374001795570605089, -1.230147717240742677, 0.6057417262809753344 ) ) ;
#34331=CARTESIAN_POINT ( 'NONE',  ( -0.003124719664520048124, -0.8057675726412016903, 0.1457185332388697963 ) ) ;
#34333=DIRECTION ( 'NONE',  ( 0.4999551463232372317, -0.8660512985181135770, 0.000000000000000000 ) ) ;
#34334=CARTESIAN_POINT ( 'NONE',  ( 0.3792114031565354537, -1.610124904551262226, 0.4986251887174527608 ) ) ;
#34337=ADVANCED_FACE ( 'NONE', ( #3473 ), #25906, .F. ) ;
#34339=ORIENTED_EDGE ( 'NONE', *, *, #31499, .T. ) ;
#34342=AXIS2_PLACEMENT_3D ( 'NONE', #28501, #15743, #7439 ) ;
#34344=CARTESIAN_POINT ( 'NONE',  ( 0.01018941234914808383, -0.5369207985381054815, 0.09707054648710758404 ) ) ;
#34345=ORIENTED_EDGE ( 'NONE', *, *, #12815, .F. ) ;
#34351=CARTESIAN_POINT ( 'NONE',  ( 0.1390698109426623252, -1.062601491521927288, 0.8567851293273262003 ) ) ;
#34352=CARTESIAN_POINT ( 'NONE',  ( 0.3951243486924778114, -1.180114500222565033, 0.7033046486683809384 ) ) ;
#34353=CARTESIAN_POINT ( 'NONE',  ( 0.1093547303742859189, -1.269651521606318889, 0.6004988576366063757 ) ) ;
#34357=ORIENTED_EDGE ( 'NONE', *, *, #28577, .T. ) ;
#34362=CARTESIAN_POINT ( 'NONE',  ( 0.5161999997979804800, -1.324679096059732331, 0.7828784074225845213 ) ) ;
#34363=VECTOR ( 'NONE', #25481, 39.37007874015748143 ) ;
#34365=CARTESIAN_POINT ( 'NONE',  ( 0.1870037891866919988, -0.7120005297123722654, 0.07613086658547316143 ) ) ;
#34366=CARTESIAN_POINT ( 'NONE',  ( 0.3228554848850782033, -1.719965048204380231, 0.8062249495306545999 ) ) ;
#34370=CARTESIAN_POINT ( 'NONE',  ( 0.4465751558565839163, -1.208568754259124800, 0.6870635310481745250 ) ) ;
#34371=LINE ( 'NONE', #5782, #29937 ) ;
#34372=B_SPLINE_CURVE_WITH_KNOTS ( 'NONE', 3,
 ( #39468, #33302, #17476, #7597, #5109, #1453 ),
 .UNSPECIFIED., .F., .F.,
 ( 4, 2, 4 ),
 ( 0.000000000000000000, 0.0005460346488701544763, 0.001092069297740308953 ),
 .UNSPECIFIED. ) ;
#34374=EDGE_CURVE ( 'NONE', #2583, #35372, #15522, .T. ) ;
#34376=CARTESIAN_POINT ( 'NONE',  ( 3.414809992080329023E-17, -0.4262518876079541830, 0.1639910581422319991 ) ) ;
#34377=CARTESIAN_POINT ( 'NONE',  ( 0.03538878874458249030, -0.9945019241485085759, 0.6847322700004405682 ) ) ;
#34380=CARTESIAN_POINT ( 'NONE',  ( 0.7218807932984940834, -1.475040712527332376, 0.6299232363116300526 ) ) ;
#34381=TOROIDAL_SURFACE ( 'NONE', #5468, 0.04749999999977554815, 0.01000000000000000021 ) ;
#34384=CARTESIAN_POINT ( 'NONE',  ( 0.6754612668510717732, -1.566418238229341897, 0.6053376557078533615 ) ) ;
#34391=CARTESIAN_POINT ( 'NONE',  ( 0.2400417667449158410, -1.530793041395833720, 0.9076943226153151301 ) ) ;
#34393=CARTESIAN_POINT ( 'NONE',  ( 0.1313096082175202184, -0.5612069155677682497, 0.2075466349573875935 ) ) ;
#34394=CARTESIAN_POINT ( 'NONE',  ( 0.1614670899430008522, -0.7569536277469717245, 0.1022936816274460647 ) ) ;
#34397=CARTESIAN_POINT ( 'NONE',  ( 0.2393369856776542404, -0.7683812882957752333, 0.4887749849253086309 ) ) ;
#34398=EDGE_LOOP ( 'NONE', ( #27621, #17009, #26623, #26180, #32033, #30615 ) ) ;
#34399=ORIENTED_EDGE ( 'NONE', *, *, #6993, .F. ) ;
#34400=CARTESIAN_POINT ( 'NONE',  ( 0.5213874123744923761, -1.147839253744530774, 0.8164622333705154889 ) ) ;
#34405=CARTESIAN_POINT ( 'NONE',  ( 0.3186308459106851343, -1.760406140419759069, 0.5654457401203095701 ) ) ;
#34407=CARTESIAN_POINT ( 'NONE',  ( 0.1503728836000403912, -0.8245688327091527103, 0.5282395445164650427 ) ) ;
#34411=CARTESIAN_POINT ( 'NONE',  ( 0.5201261370170202625, -1.511049808878615952, 0.6955162974028021861 ) ) ;
#34415=CARTESIAN_POINT ( 'NONE',  ( 0.4665252869708542138, -1.674583161905657702, 0.5704180265848416420 ) ) ;
#34416=CARTESIAN_POINT ( 'NONE',  ( 0.6759764701317674263, -1.395871262418312497, 0.8266306626867110374 ) ) ;
#34418=CARTESIAN_POINT ( 'NONE',  ( 0.5965761245944036784, -1.493465029535157029, 0.5182417262812423209 ) ) ;
#34421=EDGE_CURVE ( 'NONE', #11729, #10550, #34161, .T. ) ;
#34422=CARTESIAN_POINT ( 'NONE',  ( 0.2321526281619643584, -1.233007205928619232, 0.3667417262808778111 ) ) ;
#34426=CARTESIAN_POINT ( 'NONE',  ( 0.2195574306699510647, -0.7404155031343288007, 0.4240249586596535059 ) ) ;
#34434=CARTESIAN_POINT ( 'NONE',  ( 0.4879674388967786824, -1.124945552576106289, 0.5170992273679249074 ) ) ;
#34437=CARTESIAN_POINT ( 'NONE',  ( 0.08927640104142192667, -0.5804883439722833272, 0.08457828714984440277 ) ) ;
#34441=CARTESIAN_POINT ( 'NONE',  ( 0.1177782521778383135, -1.233918990886516465, 0.7507158840856879012 ) ) ;
#34444=CARTESIAN_POINT ( 'NONE',  ( 0.2209956536232957902, -1.227897296991992793, 0.5182417262820130377 ) ) ;
#34453=CARTESIAN_POINT ( 'NONE',  ( 0.7053080889764471451, -1.513942001867420339, 0.5667347313869608438 ) ) ;
#34454=ORIENTED_EDGE ( 'NONE', *, *, #20859, .F. ) ;
#34455=CARTESIAN_POINT ( 'NONE',  ( 0.1302229724485401419, -0.6987652251196058151, 0.4850897968509496616 ) ) ;
#34458=CARTESIAN_POINT ( 'NONE',  ( 0.07393562383578071440, -0.5614078526008612346, 0.2422426369645085398 ) ) ;
#34460=CARTESIAN_POINT ( 'NONE',  ( 0.5960294191658490615, -1.609979221294132179, 0.4458189870587250803 ) ) ;
#34462=CARTESIAN_POINT ( 'NONE',  ( 0.1771372480334198196, -0.9211842106723756585, 0.2626135244724711049 ) ) ;
#34467=CARTESIAN_POINT ( 'NONE',  ( 0.1397689641161724283, -0.6337347103700835538, 0.3872242776158923427 ) ) ;
#34468=CARTESIAN_POINT ( 'NONE',  ( 0.4814626134252603107, -1.674667815061178455, 0.4945816651399402297 ) ) ;
#34474=CARTESIAN_POINT ( 'NONE',  ( 0.2343914929394679270, -1.231693708927193986, 0.5277184083482510113 ) ) ;
#34478=CARTESIAN_POINT ( 'NONE',  ( 0.4715326458378593655, -1.065703591122391103, 0.8369151567944118630 ) ) ;
#34480=CARTESIAN_POINT ( 'NONE',  ( 0.03249461378931156608, -1.132065962088204980, 0.6695808836488423843 ) ) ;
#34483=CARTESIAN_POINT ( 'NONE',  ( 0.1713655093773583105, -0.9087330125397632408, 0.6023929517496198205 ) ) ;
#34484=CARTESIAN_POINT ( 'NONE',  ( 0.3727347521531706454, -1.154750239813580714, 0.4257713460756237245 ) ) ;
#34486=ORIENTED_EDGE ( 'NONE', *, *, #29393, .T. ) ;
#34490=CARTESIAN_POINT ( 'NONE',  ( 0.6568730927750903170, -1.460570608776345036, 0.4224083929475443422 ) ) ;
#34492=CARTESIAN_POINT ( 'NONE',  ( 0.3388158023681371311, -1.760717924938912438, 0.5703872202102562294 ) ) ;
#34494=CIRCLE ( 'NONE', #27928, 0.1762268159172233339 ) ;
#34497=CARTESIAN_POINT ( 'NONE',  ( 0.1514353721145317300, -1.395111566407175152, 0.4677691116936663618 ) ) ;
#34499=CARTESIAN_POINT ( 'NONE',  ( 0.1876514731215554732, -0.8468096824363462449, 0.2227353535533353190 ) ) ;
#34501=CARTESIAN_POINT ( 'NONE',  ( 0.5117419007255246122, -1.313278830500390182, 0.6011698456470916385 ) ) ;
#34504=CARTESIAN_POINT ( 'NONE',  ( 0.4878597496520711285, -1.079924603896147195, 0.5970707234729024648 ) ) ;
#34505=EDGE_LOOP ( 'NONE', ( #7031, #24106, #16255, #23726 ) ) ;
#34508=DIRECTION ( 'NONE',  ( -0.4999551463232372317, 0.8660512985181134660, 0.000000000000000000 ) ) ;
#34510=CARTESIAN_POINT ( 'NONE',  ( 0.04758055007403567266, -0.6291802298475768218, 0.4158285656181007761 ) ) ;
#34512=CARTESIAN_POINT ( 'NONE',  ( 0.1852687023069083672, -0.7992365650813095801, 0.02179029107226419792 ) ) ;
#34515=ORIENTED_EDGE ( 'NONE', *, *, #9716, .T. ) ;
#34517=CARTESIAN_POINT ( 'NONE',  ( 0.3443385366210869325, -1.072482504630695388, 0.6392052143392089603 ) ) ;
#34518=CARTESIAN_POINT ( 'NONE',  ( 0.4889399104974117560, -1.382089549755538327, 0.8085469255259594146 ) ) ;
#34520=CARTESIAN_POINT ( 'NONE',  ( 0.1873216024392761192, -0.6989317540256104744, 0.03190675745988370837 ) ) ;
#34521=CARTESIAN_POINT ( 'NONE',  ( 0.5433433239293584682, -1.169038973927291503, 0.5856983068965047057 ) ) ;
#34529=CARTESIAN_POINT ( 'NONE',  ( 0.2225889308918536924, -1.238345268919997855, 0.5682417262808776570 ) ) ;
#34532=CARTESIAN_POINT ( 'NONE',  ( 0.1145268569410018006, -1.410781586862627224, 0.6062388606988194928 ) ) ;
#34536=CARTESIAN_POINT ( 'NONE',  ( 0.1897171943901793389, -0.9163440338727294465, 0.2193954077252403545 ) ) ;
#34538=CARTESIAN_POINT ( 'NONE',  ( 0.5523217627366585614, -1.163855889859017889, 0.5856983068965044836 ) ) ;
#34541=EDGE_LOOP ( 'NONE', ( #12912, #17198, #17287 ) ) ;
#34542=CARTESIAN_POINT ( 'NONE',  ( 0.1799043607419438529, -1.488798643046104875, 0.7589116457392215409 ) ) ;
#34545=CARTESIAN_POINT ( 'NONE',  ( 0.3459486122327841695, -1.629317532511044497, 0.4807459044743475629 ) ) ;
#34552=CARTESIAN_POINT ( 'NONE',  ( 0.5912128005600242320, -1.447495737070808142, 0.6721173034932466095 ) ) ;
#34553=CARTESIAN_POINT ( 'NONE',  ( 0.6020307166002785149, -1.477835242481402078, 0.5986708909347367991 ) ) ;
#34557=B_SPLINE_CURVE_WITH_KNOTS ( 'NONE', 3,
 ( #3560, #19200, #6235, #31531 ),
 .UNSPECIFIED., .F., .F.,
 ( 4, 4 ),
 ( 7.823333095578703919E-15, 0.001097874967820342733 ),
 .UNSPECIFIED. ) ;
#34562=CARTESIAN_POINT ( 'NONE',  ( 0.1618130643425950421, -1.132953745604308393, 0.8857258589616595623 ) ) ;
#34563=CARTESIAN_POINT ( 'NONE',  ( 0.3354003383065387589, -1.100282042489750811, 0.7404311049156548918 ) ) ;
#34564=CARTESIAN_POINT ( 'NONE',  ( 0.08765592157946001939, -1.316965293376829216, 0.5674773004636822771 ) ) ;
#34567=CARTESIAN_POINT ( 'NONE',  ( 0.01215609957436605652, -0.4301083516152499620, 0.1115223648745343049 ) ) ;
#34571=B_SPLINE_CURVE_WITH_KNOTS ( 'NONE', 3,
 ( #22913, #920, #35632, #7654 ),
 .UNSPECIFIED., .F., .F.,
 ( 4, 4 ),
 ( 1.734723475976806902E-18, 0.0007336933749192815985 ),
 .UNSPECIFIED. ) ;
#34574=B_SPLINE_CURVE_WITH_KNOTS ( 'NONE', 3,
 ( #22277, #21867, #18973, #299 ),
 .UNSPECIFIED., .F., .F.,
 ( 4, 4 ),
 ( 0.004092191055103780277, 0.004352811462213712450 ),
 .UNSPECIFIED. ) ;
#34575=EDGE_CURVE ( 'NONE', #15823, #27338, #17634, .T. ) ;
#34579=CARTESIAN_POINT ( 'NONE',  ( 0.1261292094506277772, -0.8244062005499848134, 0.1457185332388709897 ) ) ;
#34580=DIRECTION ( 'NONE',  ( 0.8660512985181139101, 0.4999551463232363990, 0.000000000000000000 ) ) ;
#34581=CARTESIAN_POINT ( 'NONE',  ( 0.09862427037191998092, -0.8798430304322220064, 0.8669395311361297596 ) ) ;
#34582=CARTESIAN_POINT ( 'NONE',  ( 0.07030502144589019509, -1.326531751660471548, 0.5682417262808779901 ) ) ;
#34589=CARTESIAN_POINT ( 'NONE',  ( 0.6540709664215760277, -1.593060928864740156, 0.5182417262812423209 ) ) ;
#34590=CARTESIAN_POINT ( 'NONE',  ( 0.2556072607908594918, -1.486118078215695082, 1.019147448260280475 ) ) ;
#34591=CARTESIAN_POINT ( 'NONE',  ( 0.05224697855747006958, -1.083945988322971843, 0.7370724361663850699 ) ) ;
#34595=CARTESIAN_POINT ( 'NONE',  ( 0.7012556518089668733, -1.538026872409016255, 0.5808264824219138145 ) ) ;
#34599=ORIENTED_EDGE ( 'NONE', *, *, #875, .F. ) ;
#34601=CARTESIAN_POINT ( 'NONE',  ( 0.2663611043439514936, -1.609278709772456795, 0.8236604638598111761 ) ) ;
#34602=CARTESIAN_POINT ( 'NONE',  ( 0.5938776191701434781, -1.482008058293285746, 0.6415007704987426562 ) ) ;
#34603=CARTESIAN_POINT ( 'NONE',  ( 0.5433433239293584682, -1.169038973927291503, 0.5856983068965047057 ) ) ;
#34605=B_SPLINE_CURVE_WITH_KNOTS ( 'NONE', 3,
 ( #396, #10213, #25451, #35304, #37982, #22364, #34887, #6696, #26450, #29728, #26251, #16578, #16987, #1185, #32805, #1368, #10404, #29124, #4427, #13686, #38988, #29527, #38771, #13875 ),
 .UNSPECIFIED., .F., .F.,
 ( 4, 2, 2, 2, 2, 2, 2, 2, 2, 2, 2, 4 ),
 ( 0.01813101908972761245, 0.02053964073319797246, 0.02294826237666833246, 0.02535688402013869247, 0.02776550566360905248, 0.03258274895054977249, 0.03378705977228495250, 0.03499137059402013250, 0.03619568141575531250, 0.03679783682662289557, 0.03709891453205669404, 0.03739999223749048557 ),
 .UNSPECIFIED. ) ;
#34608=CARTESIAN_POINT ( 'NONE',  ( 0.3278576390227929127, -0.8618518445022319563, 0.6723808983945177564 ) ) ;
#34609=EDGE_CURVE ( 'NONE', #9161, #18789, #2811, .T. ) ;
#34616=TOROIDAL_SURFACE ( 'NONE', #40514, 0.07749999999977548459, 0.01000000000000000021 ) ;
#34617=EDGE_CURVE ( 'NONE', #30000, #2251, #38991, .T. ) ;
#34618=CARTESIAN_POINT ( 'NONE',  ( 0.1816443464261394691, -0.8741777808320030374, 0.5909987484381754586 ) ) ;
#34619=CARTESIAN_POINT ( 'NONE',  ( 0.5252056258530563015, -1.526865455870212163, 0.5731947314661878234 ) ) ;
#34623=CARTESIAN_POINT ( 'NONE',  ( 0.4524429500423481909, -1.683290388497794776, 0.5885333811653102876 ) ) ;
#34624=CARTESIAN_POINT ( 'NONE',  ( 0.6663429882773612700, -1.552917541305505189, 0.6639169729098425288 ) ) ;
#34626=CARTESIAN_POINT ( 'NONE',  ( 0.4119022438926009388, -1.177436575425700571, 0.8152005758745497488 ) ) ;
#34635=CARTESIAN_POINT ( 'NONE',  ( 0.0003547581337898165674, -0.9504652791025145486, 0.2394745140284491591 ) ) ;
#34636=CARTESIAN_POINT ( 'NONE',  ( 0.2577558225373174916, -0.8624250852862554995, 0.5195666343558283939 ) ) ;
#34639=CARTESIAN_POINT ( 'NONE',  ( 0.5375396755134189686, -1.518737640874254335, 0.5483303752197447034 ) ) ;
#34644=CARTESIAN_POINT ( 'NONE',  ( 0.1873984653709714066, -0.8522402958051090716, 0.2163211054440509484 ) ) ;
#34645=EDGE_LOOP ( 'NONE', ( #3437, #9251, #17295, #31022, #36533, #4992, #19631, #2635, #15274, #3845, #21616, #28838, #38685, #778, #37590, #505, #18274 ) ) ;
#34646=CARTESIAN_POINT ( 'NONE',  ( 0.2318589737339854795, -1.232498520698479982, 0.5197417262808780025 ) ) ;
#34647=CARTESIAN_POINT ( 'NONE',  ( 0.07600224412002334895, -1.084198183792790315, 0.7459357625971153594 ) ) ;
#34660=CARTESIAN_POINT ( 'NONE',  ( 0.2195632003157210466, -0.8548457781082356988, 0.6847411545281603118 ) ) ;
#34664=CARTESIAN_POINT ( 'NONE',  ( 0.08156795407636466266, -0.6096982493729176111, 0.3618699794873930786 ) ) ;
#34665=CARTESIAN_POINT ( 'NONE',  ( 0.002316381905007189150, -0.5232263146340704330, 0.1844568262363025790 ) ) ;
#34668=CARTESIAN_POINT ( 'NONE',  ( 0.2707375556126198068, -0.9607971206205383474, 0.5189254608558738768 ) ) ;
#34670=CARTESIAN_POINT ( 'NONE',  ( 0.1255523023994105092, -0.5499328071996130163, 0.1457185332388692689 ) ) ;
#34674=CARTESIAN_POINT ( 'NONE',  ( 0.06926373081126928344, -0.5403174658036256073, 0.1556459889883224090 ) ) ;
#34678=CARTESIAN_POINT ( 'NONE',  ( 0.3050116026255210722, -0.8112037691066587008, 0.6500339927034136656 ) ) ;
#34680=CARTESIAN_POINT ( 'NONE',  ( 0.05318916154647986699, -1.262669248688604862, 0.6621301725941526328 ) ) ;
#34683=CARTESIAN_POINT ( 'NONE',  ( 0.1203098315036280619, -0.8529650373737380775, 0.4308920117485077195 ) ) ;
#34685=CARTESIAN_POINT ( 'NONE',  ( -2.070903537920736781, -2.678131749591557309, 0.6057417262810178560 ) ) ;
#34688=CARTESIAN_POINT ( 'NONE',  ( 0.5951553339360416972, -1.455642694606908760, 0.6304964123869174486 ) ) ;
#34692=VERTEX_POINT ( 'NONE', #15571 ) ;
#34694=DIRECTION ( 'NONE',  ( -0.4999551463232372317, 0.8660512985181135770, -0.000000000000000000 ) ) ;
#34695=CARTESIAN_POINT ( 'NONE',  ( 0.4869779214331270700, -1.661191848117253178, 0.5366761509299960986 ) ) ;
#34697=CARTESIAN_POINT ( 'NONE',  ( 0.4097880553864961528, -1.161594837369823940, 0.7403270510053888698 ) ) ;
#34701=CARTESIAN_POINT ( 'NONE',  ( 0.3768783096114195486, -1.720370743462858343, 0.4222122349756301518 ) ) ;
#34702=CARTESIAN_POINT ( 'NONE',  ( 0.4885592119991905014, -1.080308374838712782, 0.5952236481819053182 ) ) ;
#34706=CARTESIAN_POINT ( 'NONE',  ( 0.004754326254995749901, -0.8878146167104555841, 0.4619373158225143494 ) ) ;
#34708=CARTESIAN_POINT ( 'NONE',  ( 0.3811835917169881793, -1.578736998356156773, 0.7419389678365337915 ) ) ;
#34710=CARTESIAN_POINT ( 'NONE',  ( 0.1856512491390554243, -0.7629151448678782588, -0.003031259884144057136 ) ) ;
#34712=VERTEX_POINT ( 'NONE', #9591 ) ;
#34714=CARTESIAN_POINT ( 'NONE',  ( 0.5959315179729194334, -1.587052097778459014, 0.4282417262808783653 ) ) ;
#34715=CARTESIAN_POINT ( 'NONE',  ( 0.4386138752512657724, -1.295316779970371313, 0.8303206930615300019 ) ) ;
#34717=CARTESIAN_POINT ( 'NONE',  ( 0.01814701835283376308, -0.9892295991911050912, 0.4798887309902147846 ) ) ;
#34720=CARTESIAN_POINT ( 'NONE',  ( 0.1852939438208618395, -0.8373517857265262432, 0.1567296349695768420 ) ) ;
#34722=CARTESIAN_POINT ( 'NONE',  ( 0.3423116886662437297, -1.747674139269914884, 0.5964707725471621869 ) ) ;
#34724=CARTESIAN_POINT ( 'NONE',  ( 0.08638421507254147313, -0.7700017860723418206, 0.02001464231056792470 ) ) ;
#34725=LINE ( 'NONE', #40500, #27135 ) ;
#34727=CARTESIAN_POINT ( 'NONE',  ( 0.08428283282631070239, -1.315430133339995145, 0.5840562972504370620 ) ) ;
#34728=CARTESIAN_POINT ( 'NONE',  ( 0.6179353394495009644, -1.299228382567916285, 0.5682417262808779901 ) ) ;
#34732=CARTESIAN_POINT ( 'NONE',  ( 0.3384799338905536970, -0.9979650346196410338, 0.5984318192120324786 ) ) ;
#34733=CARTESIAN_POINT ( 'NONE',  ( 0.3130168538663060662, -1.175229136912986361, 0.5028472835892379145 ) ) ;
#34736=CARTESIAN_POINT ( 'NONE',  ( -0.002083146443013342720, -0.8967360763018593639, 0.1136267619940960899 ) ) ;
#34737=CARTESIAN_POINT ( 'NONE',  ( 0.0004250980212677150211, -0.4402291855641986551, 0.1128034438869898043 ) ) ;
#34739=CARTESIAN_POINT ( 'NONE',  ( 0.3319227099733979003, -1.175833534577056527, 0.4282569450358217344 ) ) ;
#34744=CARTESIAN_POINT ( 'NONE',  ( 0.7053185306253882958, -1.513916414415744649, 0.5667975048583363540 ) ) ;
#34746=CARTESIAN_POINT ( 'NONE',  ( 0.5953576370465231138, -1.455492272848171398, 0.6457864647264339730 ) ) ;
#34747=CARTESIAN_POINT ( 'NONE',  ( 0.5734482455647949006, -1.622651489275899195, 0.4800729107877242385 ) ) ;
#34751=CARTESIAN_POINT ( 'NONE',  ( 0.1852724517579373009, -0.8388905295248703098, 0.1482875376949696067 ) ) ;
#34753=CARTESIAN_POINT ( 'NONE',  ( 0.02183045352075156653, -0.6280315654919215174, 0.4241349530551878355 ) ) ;
#34754=CARTESIAN_POINT ( 'NONE',  ( 0.4286824899518620891, -1.220626395943066766, 0.6356727319996533510 ) ) ;
#34759=VERTEX_POINT ( 'NONE', #3620 ) ;
#34761=CARTESIAN_POINT ( 'NONE',  ( 0.7066109249242027435, -1.499057094600571238, 0.5182417262806440217 ) ) ;
#34762=CARTESIAN_POINT ( 'NONE',  ( 0.2703269693566499043, -0.8913611900814359945, 0.5391764932455734849 ) ) ;
#34764=CARTESIAN_POINT ( 'NONE',  ( 0.6044909876012586336, -1.470555607199449666, 0.6611702863572196387 ) ) ;
#34767=CARTESIAN_POINT ( 'NONE',  ( 0.3248332791687661425, -1.755151979504451676, 0.6785705204500919185 ) ) ;
#34775=EDGE_CURVE ( 'NONE', #20093, #24651, #9167, .T. ) ;
#34776=CARTESIAN_POINT ( 'NONE',  ( 0.3137727395043992673, -1.722325404801505089, 0.8203598276066251804 ) ) ;
#34777=CARTESIAN_POINT ( 'NONE',  ( 0.1052213198848533787, -1.408629276248457574, 0.5918252877697837144 ) ) ;
#34781=CARTESIAN_POINT ( 'NONE',  ( 0.3351195522891313172, -1.762354232558481337, 0.5631496603913015431 ) ) ;
#34785=CARTESIAN_POINT ( 'NONE',  ( 0.1978587402095143555, -0.5849795632144964008, 0.3178455878192523731 ) ) ;
#34787=DIRECTION ( 'NONE',  ( 0.9998941247116546194, -0.01455087607601020412, 0.0001066420868422379362 ) ) ;
#34788=CARTESIAN_POINT ( 'NONE',  ( 0.2463166633156871344, -1.532156299544739309, 0.8923198964620434603 ) ) ;
#34789=CARTESIAN_POINT ( 'NONE',  ( 0.1972707534773566473, -0.7764867367545040810, 0.5873998428394819893 ) ) ;
#34794=VERTEX_POINT ( 'NONE', #35478 ) ;
#34803=CARTESIAN_POINT ( 'NONE',  ( 0.2123995819314469513, -0.9001393775761254989, 0.6432088496448890025 ) ) ;
#34804=FACE_OUTER_BOUND ( 'NONE', #11413, .T. ) ;
#34805=CARTESIAN_POINT ( 'NONE',  ( 0.1054506471514282812, -0.5698990576301153910, 0.2500573047465119991 ) ) ;
#34808=ORIENTED_EDGE ( 'NONE', *, *, #1224, .F. ) ;
#34810=CARTESIAN_POINT ( 'NONE',  ( 0.4081734154113714208, -1.720235488236536714, 0.6107698181414052963 ) ) ;
#34811=CARTESIAN_POINT ( 'NONE',  ( 0.6433413964517614714, -1.490184457409822416, 0.7922965759278289832 ) ) ;
#34815=CARTESIAN_POINT ( 'NONE',  ( 0.6095958906658129894, -1.477207775979266113, 0.6170772022735478979 ) ) ;
#34819=CARTESIAN_POINT ( 'NONE',  ( 0.006497850577614296130, -0.9898846675935381034, 0.4770811589384994500 ) ) ;
#34820=CARTESIAN_POINT ( 'NONE',  ( 0.5137183020217809259, -1.118314259765692764, 0.5770968910244165251 ) ) ;
#34821=EDGE_CURVE ( 'NONE', #12702, #7023, #835, .T. ) ;
#34826=CARTESIAN_POINT ( 'NONE',  ( 0.4665061541563142455, -1.559087575406794546, 0.5615006216634282898 ) ) ;
#34830=CARTESIAN_POINT ( 'NONE',  ( 0.4369325048625125052, -1.577024436001213337, 0.5877075299981957546 ) ) ;
#34833=CARTESIAN_POINT ( 'NONE',  ( 0.08895852713552732105, -0.5944957032902286054, 0.06479970134998659648 ) ) ;
#34835=CARTESIAN_POINT ( 'NONE',  ( 0.3380199588881184769, -1.750814078658277095, 0.4537226720579596861 ) ) ;
#34836=CARTESIAN_POINT ( 'NONE',  ( 0.1597909806901142149, -1.352425750947476413, 0.6653032890432879487 ) ) ;
#34838=ORIENTED_EDGE ( 'NONE', *, *, #37063, .F. ) ;
#34845=CARTESIAN_POINT ( 'NONE',  ( 0.4315909263077353786, -1.207668101024179430, 0.5182417262812423209 ) ) ;
#34853=CARTESIAN_POINT ( 'NONE',  ( 0.2666460212928653539, -0.9446779231603621430, 0.7263499614607815680 ) ) ;
#34857=CARTESIAN_POINT ( 'NONE',  ( 0.4417433136407998839, -1.573784526376230231, 0.5745458250901962494 ) ) ;
#34861=CARTESIAN_POINT ( 'NONE',  ( 0.4816455246181599592, -1.076515072263177109, 0.6112998809387040211 ) ) ;
#34864=CARTESIAN_POINT ( 'NONE',  ( 0.1627274426518589001, -0.7006462241110582578, 0.4958264140424790134 ) ) ;
#34869=CARTESIAN_POINT ( 'NONE',  ( 0.5429359209136535025, -1.169310040315109545, 0.5682417262808779901 ) ) ;
#34871=CARTESIAN_POINT ( 'NONE',  ( 0.5104750172518451867, -1.131314744720151477, 0.8088526445616294192 ) ) ;
#34875=CARTESIAN_POINT ( 'NONE',  ( 0.06624353298525109679, -1.303414041770764698, 0.6164754190481782636 ) ) ;
#34876=B_SPLINE_CURVE_WITH_KNOTS ( 'NONE', 3,
 ( #19128, #461, #34744, #31667 ),
 .UNSPECIFIED., .F., .F.,
 ( 4, 4 ),
 ( 0.000000000000000000, 1.000000000000000000 ),
 .UNSPECIFIED. ) ;
#34882=CARTESIAN_POINT ( 'NONE',  ( 0.1747268316551206235, -0.8716118499233347361, 0.5764457051807095889 ) ) ;
#34887=CARTESIAN_POINT ( 'NONE',  ( 0.1641337306192110213, -0.7872022314479601990, 0.5748589285422562867 ) ) ;
#34889=CARTESIAN_POINT ( 'NONE',  ( 0.4368279861777725204, -1.677667223885754844, 0.4182417262808776903 ) ) ;
#34891=DIRECTION ( 'NONE',  ( 0.000000000000000000, 0.000000000000000000, -1.000000000000000000 ) ) ;
#34892=CARTESIAN_POINT ( 'NONE',  ( 0.4115766028365042128, -1.733048369835246794, 0.5182417262812423209 ) ) ;
#34893=CARTESIAN_POINT ( 'NONE',  ( 0.4605182701905176090, -1.675111011033613817, 0.4442546633674782641 ) ) ;
#34896=CARTESIAN_POINT ( 'NONE',  ( 0.4790257464341468041, -1.258124379487450817, 0.6720361128856358057 ) ) ;
#34900=CARTESIAN_POINT ( 'NONE',  ( 0.4319471385618090520, -1.049247276449186916, 0.6348846931381728620 ) ) ;
#34905=CARTESIAN_POINT ( 'NONE',  ( 0.09776457712155511848, -1.359218914602520201, 0.6812646313418837529 ) ) ;
#34908=AXIS2_PLACEMENT_3D ( 'NONE', #33629, #27482, #37140 ) ;
#34909=CARTESIAN_POINT ( 'NONE',  ( 0.3860616713828277091, -1.605769424550066882, 0.5860242868412063322 ) ) ;
#34910=CARTESIAN_POINT ( 'NONE',  ( 0.06503451718542789528, -0.8165451492604878236, 0.07317945280641556527 ) ) ;
#34919=CARTESIAN_POINT ( 'NONE',  ( 0.5669932279378018247, -1.503243827336946392, 0.5741771593363358406 ) ) ;
#34920=ORIENTED_EDGE ( 'NONE', *, *, #1524, .F. ) ;
#34921=CARTESIAN_POINT ( 'NONE',  ( 0.07296648554936861764, -1.326663526568328422, 0.4848661492846343402 ) ) ;
#34925=EDGE_LOOP ( 'NONE', ( #21518, #3779, #28795, #39918, #16387, #31283, #26088, #942, #20431, #5648, #21154, #30342 ) ) ;
#34926=CARTESIAN_POINT ( 'NONE',  ( 0.1840567930975518796, -0.8547793429265486687, 0.1477568935609660794 ) ) ;
#34929=AXIS2_PLACEMENT_3D ( 'NONE', #38005, #21985, #19502 ) ;
#34930=CARTESIAN_POINT ( 'NONE',  ( 0.7185399166019250661, -1.465950542831855330, 0.7545741816404391011 ) ) ;
#34938=DIRECTION ( 'NONE',  ( 0.8660512985181126888, 0.4999551463232384529, 0.000000000000000000 ) ) ;
#34940=CARTESIAN_POINT ( 'NONE',  ( 0.4568997192848022748, -1.218890999244366613, 0.6057417262810179670 ) ) ;
#34942=CARTESIAN_POINT ( 'NONE',  ( 0.03167879690716527558, -0.8799939210571326997, 0.6541495583543271986 ) ) ;
#34951=CARTESIAN_POINT ( 'NONE',  ( 0.3549495572495519058, -1.751088804252343145, 0.4457772353421656786 ) ) ;
#34953=CARTESIAN_POINT ( 'NONE',  ( 0.3941551577388408556, -1.134933593074018310, 0.8127732636010218670 ) ) ;
#34958=CARTESIAN_POINT ( 'NONE',  ( 0.1978587402095111636, -0.5849795632145003976, 0.3178455878192510409 ) ) ;
#34959=ORIENTED_EDGE ( 'NONE', *, *, #35299, .T. ) ;
#34960=CARTESIAN_POINT ( 'NONE',  ( 0.2972703710326047299, -1.656711430450878986, 0.5747086054135303046 ) ) ;
#34961=CARTESIAN_POINT ( 'NONE',  ( 0.6205237272702224249, -1.594602023479971153, 0.4300673587497688133 ) ) ;
#34962=CARTESIAN_POINT ( 'NONE',  ( 0.1121305562899380798, -0.8343818903186780434, -0.04602629424161558402 ) ) ;
#34966=CARTESIAN_POINT ( 'NONE',  ( 0.4141786054075141665, -1.705102989373699529, 0.4226014444323759611 ) ) ;
#34970=CARTESIAN_POINT ( 'NONE',  ( 0.1862284309081393141, -0.9153619266321347814, 0.1521157592012398474 ) ) ;
#34972=CARTESIAN_POINT ( 'NONE',  ( 0.5955365829513108444, -1.457654325452099275, 0.6080873925085832354 ) ) ;
#34975=CARTESIAN_POINT ( 'NONE',  ( 0.3692778306978620750, -1.136428696002824701, 0.7302004567001213475 ) ) ;
#34976=CARTESIAN_POINT ( 'NONE',  ( 0.01703122118373576882, -0.6267681536281951571, 0.4285498985508694458 ) ) ;
#34978=CARTESIAN_POINT ( 'NONE',  ( -0.002308984842514968851, -0.8531871666706627444, 0.1457185332388709897 ) ) ;
#34979=LINE ( 'NONE', #25337, #31143 ) ;
#34980=CARTESIAN_POINT ( 'NONE',  ( 0.4299615998478440448, -1.187820293361493640, 0.7150245015202120191 ) ) ;
#34983=DIRECTION ( 'NONE',  ( 0.000000000000000000, 0.000000000000000000, -1.000000000000000000 ) ) ;
#34991=AXIS2_PLACEMENT_3D ( 'NONE', #4514, #8219, #10916 ) ;
#34993=ORIENTED_EDGE ( 'NONE', *, *, #25847, .T. ) ;
#34994=CARTESIAN_POINT ( 'NONE',  ( 0.3854339232390436298, -1.140486404647998775, 0.4306521322894901194 ) ) ;
#34997=CARTESIAN_POINT ( 'NONE',  ( 0.2739389673431911199, -1.670182469438165507, 0.6632468065124506040 ) ) ;
#34998=CARTESIAN_POINT ( 'NONE',  ( 0.5244453523138082884, -1.387307315266893104, 0.7902440572305963196 ) ) ;
#35005=CIRCLE ( 'NONE', #2824, 0.01000000000000002970 ) ;
#35009=ORIENTED_EDGE ( 'NONE', *, *, #23579, .F. ) ;
#35010=CARTESIAN_POINT ( 'NONE',  ( 0.09262370799349907424, -0.7550308318057149526, 0.2814015553635414446 ) ) ;
#35011=CARTESIAN_POINT ( 'NONE',  ( 0.06924732741833404537, -0.5400192420372453839, 0.1478676264384281847 ) ) ;
#35012=CARTESIAN_POINT ( 'NONE',  ( 0.4649247847684765400, -1.394123109563673468, 0.8177829614335009323 ) ) ;
#35017=CARTESIAN_POINT ( 'NONE',  ( 0.3424019376673626547, -1.758881546318450395, 0.5758682293985877276 ) ) ;
#35018=CARTESIAN_POINT ( 'NONE',  ( 0.7337022410813530682, -1.492415808383954046, 0.7062599971678739097 ) ) ;
#35022=CARTESIAN_POINT ( 'NONE',  ( 0.1358623780661346869, -0.5778457909491311328, 0.2559053680288311816 ) ) ;
#35026=FACE_OUTER_BOUND ( 'NONE', #24187, .T. ) ;
#35028=CARTESIAN_POINT ( 'NONE',  ( 0.05992090360963521489, -1.332693131100006978, 0.5682417262808777680 ) ) ;
#35030=CARTESIAN_POINT ( 'NONE',  ( 0.3382833150183324755, -0.9396054708716727877, 0.6333258291577809063 ) ) ;
#35037=CARTESIAN_POINT ( 'NONE',  ( 0.4076976354719489271, -1.154888438488554270, 0.4182417262808778013 ) ) ;
#35039=CARTESIAN_POINT ( 'NONE',  ( 0.4338200250350727205, -1.578845347063857707, 0.5905617543171319817 ) ) ;
#35042=CARTESIAN_POINT ( 'NONE',  ( 0.08636663003170327868, -0.7620321640752294456, 0.04754930498978150732 ) ) ;
#35044=CARTESIAN_POINT ( 'NONE',  ( 0.3211756810167746834, -1.183199798883805887, 0.5707417262808780478 ) ) ;
#35045=CARTESIAN_POINT ( 'NONE',  ( -0.01481790428398078660, -0.8502221965164611373, 0.2178672377299346041 ) ) ;
#35053=CARTESIAN_POINT ( 'NONE',  ( 0.3177856290042974652, -1.645584934368151009, 0.5182417262812344383 ) ) ;
#35059=CARTESIAN_POINT ( 'NONE',  ( 0.01562500000000000694, -0.4290069966815239777, 0.1457185332388690469 ) ) ;
#35062=CARTESIAN_POINT ( 'NONE',  ( 0.09694602640260427395, -0.6285277416443179055, 0.3013455349893560675 ) ) ;
#35065=EDGE_CURVE ( 'NONE', #34712, #15439, #10633, .T. ) ;
#35066=CARTESIAN_POINT ( 'NONE',  ( 0.03852295281450220099, -0.6922990027746789288, 0.6869434594017632678 ) ) ;
#35067=CARTESIAN_POINT ( 'NONE',  ( 0.2743735404850286552, -1.090822434421504505, 0.8247435112018880465 ) ) ;
#35070=DIRECTION ( 'NONE',  ( -1.000000000000000000, 0.000000000000000000, 0.000000000000000000 ) ) ;
#35072=CARTESIAN_POINT ( 'NONE',  ( 0.3048716024861035101, -0.9795252986220516211, 0.5672847750834353331 ) ) ;
#35077=CARTESIAN_POINT ( 'NONE',  ( 0.1897112079047654776, -0.5340520988485685239, 0.1446142472693987546 ) ) ;
#35084=CARTESIAN_POINT ( 'NONE',  ( 0.6265937217076796850, -1.312621381056858993, 0.7675331558851111735 ) ) ;
#35088=EDGE_CURVE ( 'NONE', #28384, #10719, #28257, .T. ) ;
#35089=CARTESIAN_POINT ( 'NONE',  ( 0.02106135308996504724, -1.064028623006035845, 0.6283655268256098658 ) ) ;
#35092=CARTESIAN_POINT ( 'NONE',  ( 0.1905436384893574864, -0.5945559727383912252, 0.3046096357648204189 ) ) ;
#35093=CARTESIAN_POINT ( 'NONE',  ( 0.3303338544634616958, -1.053644867167129240, 0.7371517169581325302 ) ) ;
#35099=CARTESIAN_POINT ( 'NONE',  ( 0.4621675984227249789, -1.110867290327286261, 0.5635151220948720896 ) ) ;
#35100=CARTESIAN_POINT ( 'NONE',  ( 0.4013540502050752523, -1.148216799725839232, 0.7886735227232307688 ) ) ;
#35102=CARTESIAN_POINT ( 'NONE',  ( 0.3445284778472457732, -1.145141864321415515, 0.5942735951974011943 ) ) ;
#35105=DIRECTION ( 'NONE',  ( 0.8660512985181133550, 0.4999551463232373982, 0.000000000000000000 ) ) ;
#35106=CARTESIAN_POINT ( 'NONE',  ( 0.1856347024191063455, -0.7573053249172038148, 0.1605899983602313563 ) ) ;
#35109=CARTESIAN_POINT ( 'NONE',  ( 0.4897466037307776077, -1.275248307527913960, 0.6033332196752250187 ) ) ;
#35112=CARTESIAN_POINT ( 'NONE',  ( 0.4646871136015383597, -1.067210575163276776, 0.6251146133038130159 ) ) ;
#35116=CARTESIAN_POINT ( 'NONE',  ( 0.0004665802737306216875, -0.8700472974049004993, 0.3726199621362326075 ) ) ;
#35118=CIRCLE ( 'NONE', #30539, 0.01000000000000000194 ) ;
#35121=VECTOR ( 'NONE', #37574, 39.37007874015748143 ) ;
#35122=CARTESIAN_POINT ( 'NONE',  ( 0.04802164911735522929, -0.5370111569602100676, 0.1635350359062409942 ) ) ;
#35123=CARTESIAN_POINT ( 'NONE',  ( 0.06637331517990789631, -0.7260456777667779749, 0.002854135229572256870 ) ) ;
#35124=CARTESIAN_POINT ( 'NONE',  ( 0.1743516220684620532, -0.9173990847765624013, 0.1503757705193672634 ) ) ;
#35131=CARTESIAN_POINT ( 'NONE',  ( 0.5667909668417350222, -1.503200344063986282, 0.5705455483130308370 ) ) ;
#35144=CARTESIAN_POINT ( 'NONE',  ( 0.07043814880410684265, -1.334972480813831242, 0.5056242588139928662 ) ) ;
#35147=EDGE_CURVE ( 'NONE', #39770, #27951, #21948, .T. ) ;
#35149=CARTESIAN_POINT ( 'NONE',  ( 0.1637488714925408873, -0.5994898440788770655, 0.1932149833450298726 ) ) ;
#35153=CARTESIAN_POINT ( 'NONE',  ( 0.6638964227572436982, -1.375154404986101531, 0.8002223753517787586 ) ) ;
#35155=B_SPLINE_CURVE_WITH_KNOTS ( 'NONE', 3,
 ( #25208, #9153, #31186, #28492 ),
 .UNSPECIFIED., .F., .F.,
 ( 4, 4 ),
 ( 0.000000000000000000, 0.0005696446236587841307 ),
 .UNSPECIFIED. ) ;
#35159=CARTESIAN_POINT ( 'NONE',  ( 0.004343411016521666126, -0.7362306918419727619, 0.3916307744012189618 ) ) ;
#35160=CARTESIAN_POINT ( 'NONE',  ( -0.0003491300308188850007, -0.9207945218656948816, 0.05792235683160573689 ) ) ;
#35164=ORIENTED_EDGE ( 'NONE', *, *, #514, .T. ) ;
#35167=CARTESIAN_POINT ( 'NONE',  ( 0.3499317094845083576, -1.754137739073151847, 0.4513909310129906038 ) ) ;
#35169=CYLINDRICAL_SURFACE ( 'NONE', #9853, 0.03749999999977557397 ) ;
#35170=CARTESIAN_POINT ( 'NONE',  ( 0.5669405059600367558, -1.627145089617755058, 0.5182417262812432091 ) ) ;
#35172=CARTESIAN_POINT ( 'NONE',  ( 0.1880247778135462344, -0.6881053353252821747, 0.1842137475136224611 ) ) ;
#35174=CARTESIAN_POINT ( 'NONE',  ( 0.5596770508836024227, -1.621439871647906816, 0.5567351769756754276 ) ) ;
#35176=CARTESIAN_POINT ( 'NONE',  ( 0.03160920193218080126, -0.6779490433875170474, 0.5099419547340309222 ) ) ;
#35179=CARTESIAN_POINT ( 'NONE',  ( 0.3169360506679547163, -1.762143365380179461, 0.5416432108594028128 ) ) ;
#35180=CARTESIAN_POINT ( 'NONE',  ( 0.01191963247266815060, -0.5294101887948575724, -0.06017522680174922783 ) ) ;
#35181=AXIS2_PLACEMENT_3D ( 'NONE', #12598, #25157, #9520 ) ;
#35185=EDGE_LOOP ( 'NONE', ( #19295, #4133, #9234, #26227 ) ) ;
#35190=CARTESIAN_POINT ( 'NONE',  ( 0.1109049718728688100, -0.9286333055842341810, 0.1423358669777867735 ) ) ;
#35193=CARTESIAN_POINT ( 'NONE',  ( 0.2925246921984026582, -1.120422423083942132, 0.7434686055759071044 ) ) ;
#35195=CARTESIAN_POINT ( 'NONE',  ( 0.01071266088865911389, -0.5421084299554996822, 0.2199866464733553073 ) ) ;
#35196=CARTESIAN_POINT ( 'NONE',  ( 0.1109092093543055241, -0.9286325583098424818, 0.1457252011008478843 ) ) ;
#35199=CARTESIAN_POINT ( 'NONE',  ( 0.06843411546424661707, -1.327640554429453168, 0.5682417262808774350 ) ) ;
#35203=CARTESIAN_POINT ( 'NONE',  ( 0.1793995099104103708, -0.4942854820514369085, 0.1284778566484219009 ) ) ;
#35204=B_SPLINE_CURVE_WITH_KNOTS ( 'NONE', 3,
 ( #8601, #5301, #33711, #27749 ),
 .UNSPECIFIED., .F., .F.,
 ( 4, 4 ),
 ( 2.168404344971008868E-19, 0.0005504881370414333418 ),
 .UNSPECIFIED. ) ;
#35217=CARTESIAN_POINT ( 'NONE',  ( 0.2652262113535000521, -1.687579907045415828, 0.5753159517177408588 ) ) ;
#35218=CARTESIAN_POINT ( 'NONE',  ( 0.5956431972771878414, -1.485373576684963171, 0.6181930061425162659 ) ) ;
#35222=VERTEX_POINT ( 'NONE', #12335 ) ;
#35223=ORIENTED_EDGE ( 'NONE', *, *, #37116, .F. ) ;
#35232=CARTESIAN_POINT ( 'NONE',  ( 0.09535391716454494349, -0.8218467293612060631, 0.3072227578265157022 ) ) ;
#35233=CARTESIAN_POINT ( 'NONE',  ( 0.08990550160137456004, -0.5646315916194289963, 0.1465534274451210095 ) ) ;
#35234=CARTESIAN_POINT ( 'NONE',  ( 0.5394272294032712578, -1.519093360441811313, 0.5788999028638697197 ) ) ;
#35239=CARTESIAN_POINT ( 'NONE',  ( 0.3255272214173159928, -1.756778541186221121, 0.5750899042416465212 ) ) ;
#35240=CARTESIAN_POINT ( 'NONE',  ( 0.6986210655803636316, -1.438860270996676904, 0.5699262351845304497 ) ) ;
#35241=AXIS2_PLACEMENT_3D ( 'NONE', #31020, #24869, #2641 ) ;
#35243=CARTESIAN_POINT ( 'NONE',  ( 0.6094178491768812433, -1.479016531803970746, 0.5810952581285231400 ) ) ;
#35244=CARTESIAN_POINT ( 'NONE',  ( -4.800059970049352646E-06, -0.7803577571415442060, -0.09821680784411590537 ) ) ;
#35246=CARTESIAN_POINT ( 'NONE',  ( 0.3206535937437295369, -1.182295409031864697, 0.3157417262808777658 ) ) ;
#35249=CARTESIAN_POINT ( 'NONE',  ( 1.365923996832131609E-16, -0.9481888444201347355, 0.09803024984676507458 ) ) ;
#35250=CARTESIAN_POINT ( 'NONE',  ( 0.5089221226418110255, -1.111225213825750568, 0.6024461477417591970 ) ) ;
#35255=ORIENTED_EDGE ( 'NONE', *, *, #14285, .T. ) ;
#35258=CARTESIAN_POINT ( 'NONE',  ( 0.08603282679394133603, -0.7798095055049161228, 0.06400130418535010524 ) ) ;
#35259=ORIENTED_EDGE ( 'NONE', *, *, #28657, .F. ) ;
#35262=CARTESIAN_POINT ( 'NONE',  ( 0.6508285628959425972, -1.351727978844563749, 0.7336055660202295270 ) ) ;
#35264=VERTEX_POINT ( 'NONE', #18497 ) ;
#35272=CARTESIAN_POINT ( 'NONE',  ( 0.1376369211866255993, -0.6843090735930908997, 0.7406414737086894906 ) ) ;
#35274=CARTESIAN_POINT ( 'NONE',  ( 0.09128336968152271635, -0.5703653419453503792, 0.2228016259242908137 ) ) ;
#35275=CARTESIAN_POINT ( 'NONE',  ( 0.01633901792732134900, -0.5702388794319304122, 0.5330440696850335947 ) ) ;
#35276=CARTESIAN_POINT ( 'NONE',  ( 0.09962249923029198317, -0.6318392586327593596, 0.3999921429806476691 ) ) ;
#35279=CARTESIAN_POINT ( 'NONE',  ( 0.1519119642568272921, -0.9326923694292597045, 0.3322815801383296463 ) ) ;
#35283=CARTESIAN_POINT ( 'NONE',  ( 0.3177856290042974652, -1.645584934368151009, 0.5182417262812344383 ) ) ;
#35284=CARTESIAN_POINT ( 'NONE',  ( 0.1153471832944766712, -0.4465912132367801934, 0.1463508116155961547 ) ) ;
#35290=CARTESIAN_POINT ( 'NONE',  ( 0.5893014856854912331, -1.253657609334210665, 0.7958531859040811618 ) ) ;
#35292=EDGE_CURVE ( 'NONE', #36006, #15118, #31194, .T. ) ;
#35297=CARTESIAN_POINT ( 'NONE',  ( 0.2282131427976650528, -0.9177001319490483144, 0.6643802175654811570 ) ) ;
#35299=EDGE_CURVE ( 'NONE', #13132, #12586, #7645, .T. ) ;
#35300=CARTESIAN_POINT ( 'NONE',  ( 0.6792220396283762396, -1.521116734023811201, 0.4455427699610711723 ) ) ;
#35304=CARTESIAN_POINT ( 'NONE',  ( 0.2103800470826229507, -0.8725428098432390644, 0.6529641895999598322 ) ) ;
#35310=CARTESIAN_POINT ( 'NONE',  ( 0.09606123864389597145, -0.9124172847158124044, 0.5866022920368346716 ) ) ;
#35316=CARTESIAN_POINT ( 'NONE',  ( 0.4602903487706154206, -1.228384066590711754, 0.6755160344941316675 ) ) ;
#35319=CARTESIAN_POINT ( 'NONE',  ( 0.4928237909781065240, -1.082648202709539431, 0.5731206881285608734 ) ) ;
#35320=ORIENTED_EDGE ( 'NONE', *, *, #17335, .T. ) ;
#35324=( BOUNDED_SURFACE ( )  B_SPLINE_SURFACE ( 3, 2, ( 
 ( #26720, #2227, #4474 ),
 ( #23632, #11071, #36150 ),
 ( #13937, #30188, #26507 ),
 ( #33467, #33275, #1423 ) ),
 .UNSPECIFIED., .F., .F., .F. ) 
 B_SPLINE_SURFACE_WITH_KNOTS ( ( 4, 4 ),
 ( 3, 3 ),
 ( 0.003771772523746863212, 0.004062699796700002322 ),
 ( 0.000000000000000000, 1.000000000000000000 ),
 .UNSPECIFIED. ) 
 GEOMETRIC_REPRESENTATION_ITEM ( )  RATIONAL_B_SPLINE_SURFACE ( (
 ( 1.000000000000000000, 0.7270749630179166312, 1.000000000000000000),
 ( 1.000000000000000000, 0.7198896738069492374, 1.000000000000000000),
 ( 1.000000000000000000, 0.7126463349551879212, 1.000000000000000000),
 ( 1.000000000000000000, 0.7054447009685870240, 1.000000000000000000) ) ) 
 REPRESENTATION_ITEM ( '' )  SURFACE ( )  );
#35325=CARTESIAN_POINT ( 'NONE',  ( 0.07156345257519909631, -0.6773993882840948499, 0.4940002351035037709 ) ) ;
#35327=CARTESIAN_POINT ( 'NONE',  ( 0.08705834347432826748, -0.7253769890809593779, 0.006460193196229412418 ) ) ;
#35328=CARTESIAN_POINT ( 'NONE',  ( 0.2002482725081971004, -0.6266219077336198096, 0.3288090134007002341 ) ) ;
#35329=CARTESIAN_POINT ( 'NONE',  ( 0.06772995496177347530, -0.6134157779729459969, 0.01766292184562558848 ) ) ;
#35333=CARTESIAN_POINT ( 'NONE',  ( 0.4949533726178510507, -1.379071206832592544, 0.8062209685769742284 ) ) ;
#35336=CARTESIAN_POINT ( 'NONE',  ( 0.07115698274084111818, -1.324302356227759825, 0.5002514903164775317 ) ) ;
#35341=CARTESIAN_POINT ( 'NONE',  ( 0.08752988513861870157, -0.6847329015552422460, 0.1457151237251784470 ) ) ;
#35342=DIRECTION ( 'NONE',  ( -0.01265474379914244447, -0.8659329421511298142, 0.4999999971568662160 ) ) ;
#35345=DIRECTION ( 'NONE',  ( 0.9948684839163943749, 2.731847993664264244E-14, 0.1011765768836579149 ) ) ;
#35348=CARTESIAN_POINT ( 'NONE',  ( 0.1717957286698658936, -1.383210011275196827, 0.4993402293719408913 ) ) ;
#35349=CARTESIAN_POINT ( 'NONE',  ( 0.1849152241263185281, -0.7983094181796221989, 0.01806537668523729850 ) ) ;
#35350=CARTESIAN_POINT ( 'NONE',  ( 0.2590198564899700573, -1.679471795743312290, 0.4182417262808776348 ) ) ;
#35351=CARTESIAN_POINT ( 'NONE',  ( 0.2617320194804602096, -1.680740016843867979, 0.5479263650791303952 ) ) ;
#35353=EDGE_CURVE ( 'NONE', #7904, #7711, #12524, .T. ) ;
#35354=CARTESIAN_POINT ( 'NONE',  ( -8.537024980200822558E-17, -0.6872203660140403514, 0.1122922589469583232 ) ) ;
#35361=EDGE_LOOP ( 'NONE', ( #8434, #27766, #6356, #31737, #737 ) ) ;
#35367=CARTESIAN_POINT ( 'NONE',  ( 0.3644834194571767161, -1.092200917885892686, 0.7884070574448115432 ) ) ;
#35370=CARTESIAN_POINT ( 'NONE',  ( 0.5484966004669556972, -1.177603726185705080, 0.6257892858931851654 ) ) ;
#35372=VERTEX_POINT ( 'NONE', #15367 ) ;
#35374=ORIENTED_EDGE ( 'NONE', *, *, #11536, .T. ) ;
#35375=CARTESIAN_POINT ( 'NONE',  ( 0.3270948354918082890, -1.639212714906252311, 0.5750488052645271742 ) ) ;
#35382=CARTESIAN_POINT ( 'NONE',  ( 0.5446687329359086727, -1.168273840204911540, 0.5856983068966360451 ) ) ;
#35383=CARTESIAN_POINT ( 'NONE',  ( 0.1266587039438421824, -0.9372301308308913503, 0.3362830365086449391 ) ) ;
#35385=DIRECTION ( 'NONE',  ( 0.4999551463232371762, -0.8660512985181134660, 0.000000000000000000 ) ) ;
#35386=CARTESIAN_POINT ( 'NONE',  ( 0.1888634695993094692, -0.9417634414638629270, 0.6531452432017001986 ) ) ;
#35387=CARTESIAN_POINT ( 'NONE',  ( 0.02211643768509126765, -0.6637935133132942811, 0.4930904770729322983 ) ) ;
#35388=CARTESIAN_POINT ( 'NONE',  ( 0.4820730268389710194, -1.120100422993975275, 0.5182417262812748504 ) ) ;
#35400=EDGE_CURVE ( 'NONE', #31635, #33002, #38532, .T. ) ;
#35401=CARTESIAN_POINT ( 'NONE',  ( 0.3109023401880776083, -1.751637589031094011, 0.6786626549772374339 ) ) ;
#35402=CARTESIAN_POINT ( 'NONE',  ( 0.6906859043523344566, -1.496443130473642080, 0.4682586448533338497 ) ) ;
#35403=ORIENTED_EDGE ( 'NONE', *, *, #35353, .T. ) ;
#35404=CARTESIAN_POINT ( 'NONE',  ( 0.4519383542666973730, -1.131712119964726648, 0.4502564825975859386 ) ) ;
#35407=CARTESIAN_POINT ( 'NONE',  ( 0.2565234391735137232, -1.677641732679920450, 0.5263822859174334123 ) ) ;
#35408=CARTESIAN_POINT ( 'NONE',  ( 0.3114613613881818677, -1.004621970292722377, 0.7614557701602212569 ) ) ;
#35410=ORIENTED_EDGE ( 'NONE', *, *, #23986, .T. ) ;
#35414=ORIENTED_EDGE ( 'NONE', *, *, #10248, .F. ) ;
#35417=EDGE_CURVE ( 'NONE', #12111, #356, #13425, .T. ) ;
#35422=CARTESIAN_POINT ( 'NONE',  ( 0.2227485520779646233, -0.9426598342782120943, 0.6424711532909392897 ) ) ;
#35424=CARTESIAN_POINT ( 'NONE',  ( 0.5173655358750550715, -1.478930200014486829, 0.7454170918323320683 ) ) ;
#35425=CARTESIAN_POINT ( 'NONE',  ( 0.1915715022251594790, -0.5493874118981464383, 0.2939312971703439414 ) ) ;
#35428=CARTESIAN_POINT ( 'NONE',  ( -19685.03937007874265, 285.9652880572280083, -1.951739244310253252 ) ) ;
#35430=DIRECTION ( 'NONE',  ( -0.9996235034872141823, 0.000000000000000000, -0.02743813543131554469 ) ) ;
#35431=CARTESIAN_POINT ( 'NONE',  ( 0.6090682804592260080, -1.479034850722692696, 0.5736300833207230720 ) ) ;
#35432=CARTESIAN_POINT ( 'NONE',  ( -1.494856848218599248E-05, -0.8613933088276938266, -0.04939037072607115747 ) ) ;
#35435=CARTESIAN_POINT ( 'NONE',  ( 0.1057086693319095883, -1.337907155632660716, 0.7376750060448485913 ) ) ;
#35436=CARTESIAN_POINT ( 'NONE',  ( 0.1851443459949622949, -0.7907988577364570837, 0.1906562862421710969 ) ) ;
#35440=CARTESIAN_POINT ( 'NONE',  ( 0.4904112910084666432, -1.188461936721600720, 0.4182417262808778013 ) ) ;
#35445=EDGE_LOOP ( 'NONE', ( #3102, #22044, #36257 ) ) ;
#35447=CARTESIAN_POINT ( 'NONE',  ( 0.1896045607153576118, -0.5049209053381719103, 0.1595777137938904078 ) ) ;
#35455=B_SPLINE_CURVE_WITH_KNOTS ( 'NONE', 3,
 ( #17830, #36754, #39854, #11674, #8565, #26717 ),
 .UNSPECIFIED., .F., .F.,
 ( 4, 2, 4 ),
 ( 0.000000000000000000, 0.0007689356304541490605, 0.001537871260908298121 ),
 .UNSPECIFIED. ) ;
#35456=ORIENTED_EDGE ( 'NONE', *, *, #28012, .F. ) ;
#35457=CARTESIAN_POINT ( 'NONE',  ( 0.4443883236068807419, -1.706945807527836756, 0.8827363541034584093 ) ) ;
#35458=CARTESIAN_POINT ( 'NONE',  ( 0.1091475376240157724, -0.6888598723991967709, 0.3909236133807777458 ) ) ;
#35459=B_SPLINE_CURVE_WITH_KNOTS ( 'NONE', 3,
 ( #27368, #14189, #20979, #36396, #39893, #1862, #35995, #24271, #23478, #7801 ),
 .UNSPECIFIED., .F., .F.,
 ( 4, 2, 2, 2, 4 ),
 ( 7.271605333268061299E-15, 0.0003768098143164838490, 0.0007536196286256961708, 0.001130429442934908438, 0.001507239257244120598 ),
 .UNSPECIFIED. ) ;
#35460=CARTESIAN_POINT ( 'NONE',  ( 0.003415692958229195764, -0.4932933441065976976, 0.3528940576573719734 ) ) ;
#35461=CARTESIAN_POINT ( 'NONE',  ( 0.3955718155169024031, -1.346764816040846746, 0.8519979171323052158 ) ) ;
#35463=CARTESIAN_POINT ( 'NONE',  ( 0.3455335085159372821, -1.741491928912728637, 0.4422736660380222062 ) ) ;
#35464=CARTESIAN_POINT ( 'NONE',  ( 0.1179759873886401383, -1.125199527543434330, 0.6533949885475268671 ) ) ;
#35465=VERTEX_POINT ( 'NONE', #31813 ) ;
#35468=CARTESIAN_POINT ( 'NONE',  ( 0.1916429764873162911, -0.5530848051578395319, 0.2366777123144251094 ) ) ;
#35471=CARTESIAN_POINT ( 'NONE',  ( 0.07551600056043764053, -1.312274329810509066, 0.4837890602591397582 ) ) ;
#35473=CARTESIAN_POINT ( 'NONE',  ( 0.4683780286950792182, -1.066659082333339059, 0.7984748632466120988 ) ) ;
#35475=CARTESIAN_POINT ( 'NONE',  ( 0.007696911294830250348, -0.8993530900274140372, 0.5044786313595001070 ) ) ;
#35478=CARTESIAN_POINT ( 'NONE',  ( 0.5654596793231598806, -1.618818539163461301, 0.5682417262808788783 ) ) ;
#35480=CARTESIAN_POINT ( 'NONE',  ( 0.2949679976356796018, -0.9947731076855342858, 0.7382632246787314001 ) ) ;
#35489=CARTESIAN_POINT ( 'NONE',  ( 0.2275226583839362604, -1.223163572956847966, 0.7306588133906862792 ) ) ;
#35495=CARTESIAN_POINT ( 'NONE',  ( 0.3987602141185838667, -1.146724837527934193, 0.7205486833366475663 ) ) ;
#35497=CARTESIAN_POINT ( 'NONE',  ( 0.3204139389452054232, -1.755336229099436318, 0.4849083929475442867 ) ) ;
#35503=CARTESIAN_POINT ( 'NONE',  ( 0.4157477866045977688, -1.588835819673688254, 0.6151641792345675652 ) ) ;
#35505=CARTESIAN_POINT ( 'NONE',  ( 0.2018805221389261828, -0.6980253832968265071, 0.3378735216469233582 ) ) ;
#35507=ORIENTED_EDGE ( 'NONE', *, *, #21825, .F. ) ;
#35512=EDGE_CURVE ( 'NONE', #6859, #31663, #9617, .T. ) ;
#35513=CARTESIAN_POINT ( 'NONE',  ( 0.1561817513097121801, -0.7009449418526539910, 0.4986987260078958317 ) ) ;
#35517=AXIS2_PLACEMENT_3D ( 'NONE', #2022, #11273, #23840 ) ;
#35518=CARTESIAN_POINT ( 'NONE',  ( 0.1853469541905378160, -0.8336531673994818092, 0.1643568276252908300 ) ) ;
#35523=CARTESIAN_POINT ( 'NONE',  ( 0.4310150799785918418, -1.695525730796878294, 0.6145840607228283403 ) ) ;
#35525=EDGE_CURVE ( 'NONE', #3174, #17938, #34605, .T. ) ;
#35526=FACE_OUTER_BOUND ( 'NONE', #12793, .T. ) ;
#35528=CARTESIAN_POINT ( 'NONE',  ( 0.3827394763927673971, -1.608088298394132254, 0.5182417262812428760 ) ) ;
#35529=CARTESIAN_POINT ( 'NONE',  ( 0.08016251834805442067, -1.309203902574839207, 0.5631135398343307674 ) ) ;
#35532=CARTESIAN_POINT ( 'NONE',  ( 0.1847778408806958483, -0.8190323103295640284, 0.04085703638754438483 ) ) ;
#35533=CARTESIAN_POINT ( 'NONE',  ( 0.4753073865181790536, -1.208389560008542585, 0.5132863017525766125 ) ) ;
#35534=CARTESIAN_POINT ( 'NONE',  ( 0.2641583310953224961, -1.686482484943033766, 0.5673961214706590983 ) ) ;
#35537=CARTESIAN_POINT ( 'NONE',  ( 0.2949739106045629056, -1.710307911171992323, 0.7406796427396996618 ) ) ;
#35542=CARTESIAN_POINT ( 'NONE',  ( 0.1826134026666640375, -1.261648033191452578, 0.4282186462236585722 ) ) ;
#35545=EDGE_LOOP ( 'NONE', ( #30337, #23415, #14269, #28644, #5831, #22094 ) ) ;
#35548=( BOUNDED_SURFACE ( )  B_SPLINE_SURFACE ( 3, 2, ( 
 ( #25713, #12970, #16656 ),
 ( #35179, #6771, #22859 ),
 ( #19554, #12757, #13363 ),
 ( #9863, #25318, #4087 ) ),
 .UNSPECIFIED., .F., .F., .T. ) 
 B_SPLINE_SURFACE_WITH_KNOTS ( ( 4, 4 ),
 ( 3, 3 ),
 ( 1.965170647738601062E-15, 0.0007359428493836263222 ),
 ( 0.000000000000000000, 1.000000000000000000 ),
 .UNSPECIFIED. ) 
 GEOMETRIC_REPRESENTATION_ITEM ( )  RATIONAL_B_SPLINE_SURFACE ( (
 ( 1.000000000000000000, 0.8602827799852004187, 1.000000000000000000),
 ( 1.000000000000000000, 0.8187812255249553584, 1.000000000000000000),
 ( 1.000000000000000000, 0.7657952688647495787, 1.000000000000000000),
 ( 1.000000000000000000, 0.6984366549430200966, 1.000000000000000000) ) ) 
 REPRESENTATION_ITEM ( '' )  SURFACE ( )  );
#35549=CARTESIAN_POINT ( 'NONE',  ( 0.4094665197507286747, -1.132124008075320098, 0.5707417262808780478 ) ) ;
#35554=TOROIDAL_SURFACE ( 'NONE', #28338, 0.07749999999977555398, 0.01000000000000000021 ) ;
#35556=CARTESIAN_POINT ( 'NONE',  ( 0.5529494632797998799, -1.383080504355475249, 0.6300486131270075507 ) ) ;
#35559=CARTESIAN_POINT ( 'NONE',  ( 0.5136166297679740644, -1.127695158652323615, 0.6751074532211280843 ) ) ;
#35564=CARTESIAN_POINT ( 'NONE',  ( 0.3293980905737597942, -1.639100469172996677, 0.6107778528379868010 ) ) ;
#35565=CARTESIAN_POINT ( 'NONE',  ( 0.6126507545533108612, -1.600805309556822209, 0.4340437436598985066 ) ) ;
#35571=CARTESIAN_POINT ( 'NONE',  ( 0.5447008582413235267, -1.168329489522004216, 0.5018407269173935648 ) ) ;
#35572=CARTESIAN_POINT ( 'NONE',  ( 0.2001178498007331608, -0.8475313208254383612, 0.3327188987815731802 ) ) ;
#35576=CARTESIAN_POINT ( 'NONE',  ( 0.1050961439476602449, -0.8310223100206696190, 0.2465440532630112369 ) ) ;
#35590=CARTESIAN_POINT ( 'NONE',  ( 0.06488195170228858166, -1.341118445645211654, 0.5728004737317409223 ) ) ;
#35591=CARTESIAN_POINT ( 'NONE',  ( 0.1809266711160160690, -0.4989356743641660263, 0.1166738295573907097 ) ) ;
#35592=CARTESIAN_POINT ( 'NONE',  ( 0.1048189938829944684, -1.403947404827792012, 0.6087930347991732383 ) ) ;
#35594=CARTESIAN_POINT ( 'NONE',  ( 0.3504004095185141443, -1.746198910743387733, 0.4438683260553373811 ) ) ;
#35596=CARTESIAN_POINT ( 'NONE',  ( 0.3012979652686071930, -1.678591049238880917, 0.8711002189715364441 ) ) ;
#35598=ORIENTED_EDGE ( 'NONE', *, *, #14283, .T. ) ;
#35599=EDGE_LOOP ( 'NONE', ( #424, #18510, #26469 ) ) ;
#35604=CARTESIAN_POINT ( 'NONE',  ( 0.6024792198024999657, -1.483053084053396420, 0.5847252747985980381 ) ) ;
#35605=CARTESIAN_POINT ( 'NONE',  ( 0.5524261267419869892, -1.184164381802659927, 0.6057417262809862146 ) ) ;
#35610=VECTOR ( 'NONE', #35838, 39.37007874015748143 ) ;
#35613=CARTESIAN_POINT ( 'NONE',  ( -0.01400817393110175522, -0.5278220070374219919, 0.1759774557947419160 ) ) ;
#35618=CARTESIAN_POINT ( 'NONE',  ( 0.004127512716747100754, -0.5275076572294757904, 0.1483282180229316405 ) ) ;
#35621=CARTESIAN_POINT ( 'NONE',  ( 0.09109308586799420848, -0.7953216885135077074, 0.2706080309223847236 ) ) ;
#35624=CARTESIAN_POINT ( 'NONE',  ( 0.5236184131203611702, -1.488138999244633220, 0.7296234892006074890 ) ) ;
#35628=EDGE_CURVE ( 'NONE', #2643, #8839, #3721, .T. ) ;
#35629=CARTESIAN_POINT ( 'NONE',  ( 0.3186320389496528627, -1.760431904683431359, 0.5682417262808792113 ) ) ;
#35632=CARTESIAN_POINT ( 'NONE',  ( 0.4211301194118072244, -1.688827985529782527, 0.4182417262808776903 ) ) ;
#35635=CARTESIAN_POINT ( 'NONE',  ( 3.473743519314094728E-08, -0.7045837285689108276, -0.1152398889879612948 ) ) ;
#35636=CARTESIAN_POINT ( 'NONE',  ( 0.2672861266253624413, -0.9758538585998212112, 0.7531240496249852479 ) ) ;
#35641=CARTESIAN_POINT ( 'NONE',  ( 0.1233923337978296703, -1.433947342477501108, 0.6209663710929820279 ) ) ;
#35642=CARTESIAN_POINT ( 'NONE',  ( 0.2554252512568409572, -0.9178124959013912454, 0.5002157811656953168 ) ) ;
#35655=CARTESIAN_POINT ( 'NONE',  ( 0.002952521020825130300, -0.5558164471492254011, 0.2655225723378386027 ) ) ;
#35658=CARTESIAN_POINT ( 'NONE',  ( 0.3269417016373100116, -1.755644436858573076, 0.4716675315899548360 ) ) ;
#35659=CARTESIAN_POINT ( 'NONE',  ( 0.5195754528810989648, -1.145330933930835959, 0.8096739517683957388 ) ) ;
#35660=ORIENTED_EDGE ( 'NONE', *, *, #36036, .T. ) ;
#35663=ORIENTED_EDGE ( 'NONE', *, *, #15038, .T. ) ;
#35665=CARTESIAN_POINT ( 'NONE',  ( 0.2362067350217224027, -1.230737272509785374, 0.4282273956715025864 ) ) ;
#35669=CARTESIAN_POINT ( 'NONE',  ( 0.09374999999999988898, -0.4830108143257719755, 0.3319492704185081910 ) ) ;
#35670=CARTESIAN_POINT ( 'NONE',  ( 0.09324156912962643096, -0.6558780651247091420, 0.2654224007799687035 ) ) ;
#35672=CARTESIAN_POINT ( 'NONE',  ( 0.07626770091217156822, -0.8479114564755200201, 0.8336461691634142745 ) ) ;
#35674=CARTESIAN_POINT ( 'NONE',  ( 0.1925202373472624240, -0.9012288813172684154, 0.7215585555966789189 ) ) ;
#35675=CARTESIAN_POINT ( 'NONE',  ( 0.1676876122360048404, -1.285305603201868374, 0.9459303112033679017 ) ) ;
#35676=CARTESIAN_POINT ( 'NONE',  ( 0.3137153524386490644, -1.648232696675291375, 0.5962818595802683586 ) ) ;
#35677=CARTESIAN_POINT ( 'NONE',  ( 0.3140370939074847434, -1.084786762411256378, 0.6412117272335754459 ) ) ;
#35679=B_SPLINE_CURVE_WITH_KNOTS ( 'NONE', 3,
 ( #29135, #32414, #7105, #788 ),
 .UNSPECIFIED., .F., .F.,
 ( 4, 4 ),
 ( 1.753349224617995719E-05, 0.001120479941338546354 ),
 .UNSPECIFIED. ) ;
#35683=CARTESIAN_POINT ( 'NONE',  ( 0.3666170748374983357, -1.617430218101400197, 0.5510161745712417458 ) ) ;
#35684=CARTESIAN_POINT ( 'NONE',  ( 0.1897362042065962873, -0.5343739875968438469, 0.1562402822563540850 ) ) ;
#35687=CARTESIAN_POINT ( 'NONE',  ( 0.6935470237484337996, -1.428868995382490237, 0.5856070495622788252 ) ) ;
#35691=CARTESIAN_POINT ( 'NONE',  ( 0.4220340746365390805, -1.009949560908969035, 0.7308913177996746446 ) ) ;
#35693=CARTESIAN_POINT ( 'NONE',  ( 0.06842911028247611327, -1.327649046458937443, 0.5682133453004688528 ) ) ;
#35697=CARTESIAN_POINT ( 'NONE',  ( 0.3113442856022401450, -1.065761248458108046, 0.7391908608033311845 ) ) ;
#35701=FACE_OUTER_BOUND ( 'NONE', #32675, .T. ) ;
#35704=CARTESIAN_POINT ( 'NONE',  ( 0.6590705178848084156, -1.601721441849921268, 0.5182417262812423209 ) ) ;
#35706=CARTESIAN_POINT ( 'NONE',  ( 0.2784898103895053767, -1.320042667948280846, 0.5909764709513882774 ) ) ;
#35708=CARTESIAN_POINT ( 'NONE',  ( 0.4621675984227249789, -1.110867290327286261, 0.5635151220948720896 ) ) ;
#35710=CARTESIAN_POINT ( 'NONE',  ( 0.3204479958614548929, -1.182666560659948907, 0.5682417262808776570 ) ) ;
#35712=CARTESIAN_POINT ( 'NONE',  ( 0.3497762486267798621, -1.084349969738368502, 0.7277452793936995956 ) ) ;
#35714=LINE ( 'NONE', #7523, #40454 ) ;
#35717=DIRECTION ( 'NONE',  ( -0.9848077530122080203, -0.1736481776669303589, 4.095352323445923521E-18 ) ) ;
#35718=ORIENTED_EDGE ( 'NONE', *, *, #21070, .F. ) ;
#35719=CARTESIAN_POINT ( 'NONE',  ( 0.3806051526081477010, -1.502956011673624026, 0.8238138617331723923 ) ) ;
#35720=CARTESIAN_POINT ( 'NONE',  ( 0.08893475363215910812, -0.5779476940138750241, 0.05184119719358894901 ) ) ;
#35721=CARTESIAN_POINT ( 'NONE',  ( 0.1111486238615575634, -0.9218372719158527406, 0.08682267064788348754 ) ) ;
#35727=CARTESIAN_POINT ( 'NONE',  ( 0.1223120210888352516, -0.5860525448271070026, 0.2865477404261148608 ) ) ;
#35729=CARTESIAN_POINT ( 'NONE',  ( 0.1874453682798400689, -0.6903079694140360489, 0.04813715558869984673 ) ) ;
#35735=CARTESIAN_POINT ( 'NONE',  ( 0.2145758709995234104, -1.243149601538450000, 0.4716904324752760336 ) ) ;
#35737=CARTESIAN_POINT ( 'NONE',  ( 0.3434800707737146741, -1.169184835483404905, 0.4282596159937968605 ) ) ;
#35739=CARTESIAN_POINT ( 'NONE',  ( 0.7346172259536333238, -1.494169854247700657, 0.6985599367358283907 ) ) ;
#35747=CARTESIAN_POINT ( 'NONE',  ( 0.1846016914021299526, -0.8353733999320747117, 0.06670577366108822182 ) ) ;
#35748=CARTESIAN_POINT ( 'NONE',  ( 0.4144545104481285880, -1.243517080461129076, 0.4993477989703495878 ) ) ;
#35750=CARTESIAN_POINT ( 'NONE',  ( 0.05848126963139189949, -0.9969932945501481791, 0.7623047753129613691 ) ) ;
#35752=AXIS2_PLACEMENT_3D ( 'NONE', #34845, #3587, #19440 ) ;
#35754=CYLINDRICAL_SURFACE ( 'NONE', #21267, 0.02000000000000003858 ) ;
#35761=CARTESIAN_POINT ( 'NONE',  ( 0.1435064959217801916, -1.283467536720964697, 0.5197417262808780025 ) ) ;
#35764=CARTESIAN_POINT ( 'NONE',  ( 0.08989401589083206856, -0.5588208839049469967, 0.1462139476000107741 ) ) ;
#35765=CARTESIAN_POINT ( 'NONE',  ( 0.3474212099432354983, -1.070521011291321933, 0.7674123779357524544 ) ) ;
#35767=VERTEX_POINT ( 'NONE', #40223 ) ;
#35768=CARTESIAN_POINT ( 'NONE',  ( 0.5265921910155209051, -1.145228776028037521, 0.6635139613180396356 ) ) ;
#35769=CIRCLE ( 'NONE', #39732, 0.009999999999999975922 ) ;
#35770=CARTESIAN_POINT ( 'NONE',  ( 0.1279017468704548299, -0.4488044174422846089, 0.1457404026636500427 ) ) ;
#35774=CARTESIAN_POINT ( 'NONE',  ( 0.3308004652115096866, -1.635985480546734205, 0.6545755976240583696 ) ) ;
#35775=CARTESIAN_POINT ( 'NONE',  ( 0.6318873531608050209, -1.583827858112001552, 0.4267529692672295538 ) ) ;
#35784=CARTESIAN_POINT ( 'NONE',  ( 0.1962839440205723096, -0.9538400423320417820, 0.6688300417027344125 ) ) ;
#35788=CARTESIAN_POINT ( 'NONE',  ( 0.4716580862946758157, -1.112877053019780016, 0.5495408069278913121 ) ) ;
#35795=CARTESIAN_POINT ( 'NONE',  ( 0.4165761542997364897, -1.741708882820427906, 0.5182417262812423209 ) ) ;
#35797=CARTESIAN_POINT ( 'NONE',  ( 0.3554163599750468361, -1.162345695606875839, 0.4422132562362469099 ) ) ;
#35801=CARTESIAN_POINT ( 'NONE',  ( 0.4764113678702300847, -1.677356869750545210, 0.4781561135235793403 ) ) ;
#35803=CARTESIAN_POINT ( 'NONE',  ( 0.3049719670396321414, -1.696434107116652434, 0.8435498759739918917 ) ) ;
#35809=ORIENTED_EDGE ( 'NONE', *, *, #20493, .F. ) ;
#35812=CARTESIAN_POINT ( 'NONE',  ( 0.4942140488756893713, -1.327628134470207222, 0.8104097437034657458 ) ) ;
#35813=CARTESIAN_POINT ( 'NONE',  ( 0.008457857042273673326, -0.6665957502853808725, -0.01121200989691692289 ) ) ;
#35817=ORIENTED_EDGE ( 'NONE', *, *, #17335, .F. ) ;
#35818=ORIENTED_EDGE ( 'NONE', *, *, #7894, .T. ) ;
#35819=CARTESIAN_POINT ( 'NONE',  ( 0.05948319379729941764, -1.278145653519860536, 0.5182417262812423209 ) ) ;
#35822=CARTESIAN_POINT ( 'NONE',  ( 0.1426205952518595221, -1.218146753663991610, 0.9251587076902523243 ) ) ;
#35828=CARTESIAN_POINT ( 'NONE',  ( -0.002762107553692768041, -0.4210325180397656020, -0.1178596299512813528 ) ) ;
#35829=EDGE_LOOP ( 'NONE', ( #18014, #30566 ) ) ;
#35831=CARTESIAN_POINT ( 'NONE',  ( 0.2310385060053183892, -0.9417727088514467049, 0.6570708109900642580 ) ) ;
#35833=CARTESIAN_POINT ( 'NONE',  ( 0.04409305177916850171, -0.9987702684838598577, 0.6897599509476122215 ) ) ;
#35834=CARTESIAN_POINT ( 'NONE',  ( 0.1255995385913393214, -0.7272598595541045485, 0.5480802707321428269 ) ) ;
#35835=CARTESIAN_POINT ( 'NONE',  ( 0.1134734767189682914, -0.5850338423759841033, 0.2884401093049815956 ) ) ;
#35838=DIRECTION ( 'NONE',  ( 0.4999551463232372317, -0.8660512985181134660, 0.000000000000000000 ) ) ;
#35839=FACE_OUTER_BOUND ( 'NONE', #31938, .T. ) ;
#35840=CARTESIAN_POINT ( 'NONE',  ( 0.3853942601747663566, -1.722288293259479852, 0.6094916416589982733 ) ) ;
#35842=CARTESIAN_POINT ( 'NONE',  ( 0.06277511499740180689, -1.333345291044720771, 0.5336558136334552671 ) ) ;
#35845=CARTESIAN_POINT ( 'NONE',  ( 0.01142394431942996696, -0.9136163810232513782, 0.01885333890477661895 ) ) ;
#35846=CARTESIAN_POINT ( 'NONE',  ( 0.5775506772830608648, -1.469745956246417240, 0.6985825451078249149 ) ) ;
#35847=CARTESIAN_POINT ( 'NONE',  ( 0.4972320539234349468, -1.080138254241686413, 0.5197417262808780025 ) ) ;
#35851=CARTESIAN_POINT ( 'NONE',  ( 0.03762609415277568675, -1.032875954121303508, 0.6996461994120862782 ) ) ;
#35852=CARTESIAN_POINT ( 'NONE',  ( 0.4919302148474398173, -1.082157928207513331, 0.5818935738131040258 ) ) ;
#35854=CARTESIAN_POINT ( 'NONE',  ( 0.4624512237511245738, -1.047046041135732741, 0.8530670246638676346 ) ) ;
#35858=CARTESIAN_POINT ( 'NONE',  ( 0.4809364209501173493, -1.175687667482560927, 0.4182417262808778013 ) ) ;
#35861=CARTESIAN_POINT ( 'NONE',  ( 0.3198746602526446603, -1.759624966644469879, 0.5626316659645647089 ) ) ;
#35862=CARTESIAN_POINT ( 'NONE',  ( 0.002367394983744824412, -0.5282119844061545777, 0.1443450864220834906 ) ) ;
#35868=CARTESIAN_POINT ( 'NONE',  ( 0.5289273032196292190, -1.159758851219879094, 0.8099624798310959273 ) ) ;
#35870=VERTEX_POINT ( 'NONE', #19457 ) ;
#35876=ORIENTED_EDGE ( 'NONE', *, *, #241, .F. ) ;
#35877=CARTESIAN_POINT ( 'NONE',  ( 0.008954545898026106121, -0.6173803428054009945, 0.003786539670926606597 ) ) ;
#35880=CARTESIAN_POINT ( 'NONE',  ( 0.09589697510153505355, -0.6621991411919149195, 0.2946228100768590319 ) ) ;
#35881=CARTESIAN_POINT ( 'NONE',  ( 0.1581441334961056766, -1.100692414099352368, 0.9862425334140708655 ) ) ;
#35882=CARTESIAN_POINT ( 'NONE',  ( 0.08736941714279185256, -0.5694091105756469151, 0.2584125436657497832 ) ) ;
#35883=CARTESIAN_POINT ( 'NONE',  ( 0.1144236352178722299, -0.5058114079956718134, -0.01341456787975157591 ) ) ;
#35884=DIRECTION ( 'NONE',  ( 0.01455087615875041117, 0.9998941303973198913, 0.000000000000000000 ) ) ;
#35886=CARTESIAN_POINT ( 'NONE',  ( 0.1362976124207936068, -1.175113777419627858, 0.6553486967042546629 ) ) ;
#35891=EDGE_CURVE ( 'NONE', #9404, #9161, #9977, .T. ) ;
#35892=CARTESIAN_POINT ( 'NONE',  ( 0.2059853976207044468, -0.5424875326118652197, 0.4059703345962285548 ) ) ;
#35898=CARTESIAN_POINT ( 'NONE',  ( 0.6179353394495007423, -1.299228382567916285, 0.5682417262808777680 ) ) ;
#35903=VERTEX_POINT ( 'NONE', #28287 ) ;
#35904=CARTESIAN_POINT ( 'NONE',  ( 0.4254380803681816481, -1.182152342139886514, 0.7222371136035362627 ) ) ;
#35908=ORIENTED_EDGE ( 'NONE', *, *, #8244, .F. ) ;
#35911=B_SPLINE_CURVE_WITH_KNOTS ( 'NONE', 3,
 ( #11442, #24007, #27678, #20916, #5245, #14724 ),
 .UNSPECIFIED., .F., .F.,
 ( 4, 2, 4 ),
 ( 0.000000000000000000, 0.0004951616201126960402, 0.0009903232402253920805 ),
 .UNSPECIFIED. ) ;
#35914=DIRECTION ( 'NONE',  ( 0.01455087615875041117, 0.9998941303973198913, 0.000000000000000000 ) ) ;
#35916=CARTESIAN_POINT ( 'NONE',  ( 0.1955472856704882634, -1.153870291027489170, 0.7502753263242120108 ) ) ;
#35923=CARTESIAN_POINT ( 'NONE',  ( 0.4797981269282615147, -1.258694402034498561, 0.5894615839076718933 ) ) ;
#35931=CARTESIAN_POINT ( 'NONE',  ( 0.4148514316362570953, -1.579328421602780086, 0.6899777374673161656 ) ) ;
#35932=CARTESIAN_POINT ( 'NONE',  ( 0.08965783709418552461, -0.5679113859805221542, 0.1161394655102304663 ) ) ;
#35936=ORIENTED_EDGE ( 'NONE', *, *, #26595, .F. ) ;
#35940=CARTESIAN_POINT ( 'NONE',  ( 0.5745002926870975690, -1.499201178651017763, 0.5855314181424956521 ) ) ;
#35946=CARTESIAN_POINT ( 'NONE',  ( 0.2170659164319594381, -1.241710086118905432, 0.4766412924577621002 ) ) ;
#35948=CARTESIAN_POINT ( 'NONE',  ( 0.08965528283357206141, -0.5631619445760863707, 0.1053715254844957705 ) ) ;
#35949=CARTESIAN_POINT ( 'NONE',  ( 0.2256281918571345080, -0.6025195051315143102, 0.5087991896564706407 ) ) ;
#35951=CARTESIAN_POINT ( 'NONE',  ( 0.08146858378016413882, -1.311453225872572403, 0.5631245198800998164 ) ) ;
#35956=CARTESIAN_POINT ( 'NONE',  ( 0.1464731643940764827, -1.281649693683432734, 0.4243453113979892555 ) ) ;
#35957=CARTESIAN_POINT ( 'NONE',  ( 0.3285791488923691106, -1.750622606776042423, 0.4882417262808776415 ) ) ;
#35964=ORIENTED_EDGE ( 'NONE', *, *, #27649, .F. ) ;
#35965=B_SPLINE_SURFACE_WITH_KNOTS ( 'NONE', 5, 5, ( 
 ( #7587, #20357, #23042, #26528, #26140, #38848 ),
 ( #30019, #19943, #29410, #17658, #32477, #10475 ),
 ( #4495, #4303, #11092, #17057, #29811, #33092 ),
 ( #11286, #39068, #1849, #23652, #36173, #29603 ),
 ( #4900, #17466, #1445, #7982, #10894, #32878 ),
 ( #14364, #4688, #5101, #26739, #20558, #26928 ) ),
 .UNSPECIFIED., .F., .F., .F.,
 ( 6, 6 ),
 ( 6, 6 ),
 ( -6.477000000001651436, 6.477000000001639002 ),
 ( -2.080605796196421498, 4.396394203803585476 ),
 .UNSPECIFIED. ) ;
#35967=CARTESIAN_POINT ( 'NONE',  ( 0.1060760254173120226, -1.412497056228485759, 0.5620039430078178633 ) ) ;
#35968=CARTESIAN_POINT ( 'NONE',  ( 0.1437340355044557927, -1.283861693981850349, 0.4177417262808780229 ) ) ;
#35972=CARTESIAN_POINT ( 'NONE',  ( 0.4813074317656115819, -1.269335260105949770, 0.7818202548325017265 ) ) ;
#35975=CARTESIAN_POINT ( 'NONE',  ( 0.5031347454681565079, -1.114267567382387414, 0.6816460158534795033 ) ) ;
#35979=CARTESIAN_POINT ( 'NONE',  ( 0.03049314378765675612, -0.6057240897949897063, 0.3755447581365881082 ) ) ;
#35980=CARTESIAN_POINT ( 'NONE',  ( 0.6912965087608118342, -1.498753872919812657, 0.4704591923298728218 ) ) ;
#35985=B_SPLINE_CURVE_WITH_KNOTS ( 'NONE', 3,
 ( #33050, #30377, #1817, #4458, #2004, #10856 ),
 .UNSPECIFIED., .F., .F.,
 ( 4, 2, 4 ),
 ( 0.000000000000000000, 0.0004760980429614800708, 0.0009521960859229601417 ),
 .UNSPECIFIED. ) ;
#35987=CARTESIAN_POINT ( 'NONE',  ( 0.3451269221721864899, -1.782955182391982696, 0.5182417262812423209 ) ) ;
#35988=CARTESIAN_POINT ( 'NONE',  ( 0.3819577260478873026, -1.257944084395889783, 0.6070643466492523510 ) ) ;
#35992=CARTESIAN_POINT ( 'NONE',  ( 0.1109049720484397705, -0.9286333197963668740, 0.1741076406654592235 ) ) ;
#35995=CARTESIAN_POINT ( 'NONE',  ( 0.4225253925792876730, -1.126620259732304064, 0.4991778718059378117 ) ) ;
#35998=CARTESIAN_POINT ( 'NONE',  ( 0.0009472761255793785357, -0.9457358089336086460, 0.3226690514330370907 ) ) ;
#36003=CARTESIAN_POINT ( 'NONE',  ( 0.5986518128144662221, -1.465474987463235790, 0.6057417262805031566 ) ) ;
#36006=VERTEX_POINT ( 'NONE', #31190 ) ;
#36008=CARTESIAN_POINT ( 'NONE',  ( 0.1766277944084894969, -0.4884173451829000867, 0.1430110528971104966 ) ) ;
#36011=CARTESIAN_POINT ( 'NONE',  ( 0.6016038281123217146, -1.483041495014917333, 0.5656544979527685646 ) ) ;
#36012=B_SPLINE_CURVE_WITH_KNOTS ( 'NONE', 3,
 ( #813, #9636, #19698, #25896 ),
 .UNSPECIFIED., .F., .F.,
 ( 4, 4 ),
 ( 0.005342362744812973255, 0.005869326880028568477 ),
 .UNSPECIFIED. ) ;
#36013=CARTESIAN_POINT ( 'NONE',  ( -0.0003981876585745823885, -0.7315818264868999554, -0.01661212268152491636 ) ) ;
#36016=CARTESIAN_POINT ( 'NONE',  ( 0.3151595171820714136, -1.185655525176347647, 0.5568032880584220523 ) ) ;
#36018=CARTESIAN_POINT ( 'NONE',  ( -0.0002811468384461541072, -0.6516915277880520607, 0.4786751619668931368 ) ) ;
#36027=CARTESIAN_POINT ( 'NONE',  ( 0.1462251280849438395, -0.8510050163060884909, 0.5114821326872159846 ) ) ;
#36028=CARTESIAN_POINT ( 'NONE',  ( 0.07520564851098779369, -1.153270212343224133, 0.7613220868928463059 ) ) ;
#36029=CARTESIAN_POINT ( 'NONE',  ( 0.08994178283652765060, -0.5440620458595929465, 0.1575062128599965250 ) ) ;
#36030=CARTESIAN_POINT ( 'NONE',  ( 0.4876370588746136159, -1.406030492629142259, 0.8039593740868691274 ) ) ;
#36031=CARTESIAN_POINT ( 'NONE',  ( 0.03693592009331247289, -1.103750244955626236, 0.6430833370955907347 ) ) ;
#36036=EDGE_CURVE ( 'NONE', #5749, #13059, #28714, .T. ) ;
#36037=FACE_OUTER_BOUND ( 'NONE', #12056, .T. ) ;
#36041=CARTESIAN_POINT ( 'NONE',  ( 0.01140463913857075844, -0.9214766123526784147, 0.03400881840692861202 ) ) ;
#36045=CARTESIAN_POINT ( 'NONE',  ( 0.006363676076506938339, -0.8374434632259925015, 0.09472199571917780392 ) ) ;
#36047=EDGE_CURVE ( 'NONE', #38179, #24800, #39983, .T. ) ;
#36048=CARTESIAN_POINT ( 'NONE',  ( -0.001733054258001554731, -0.9004704535694999512, 0.2409329515054920989 ) ) ;
#36049=CARTESIAN_POINT ( 'NONE',  ( 0.4925986438152862856, -1.082524672201789828, 0.5763763218629267548 ) ) ;
#36051=CARTESIAN_POINT ( 'NONE',  ( 0.2803613453953150980, -0.7205873319272890765, 0.6521004353453685454 ) ) ;
#36054=EDGE_CURVE ( 'NONE', #30626, #33071, #5540, .T. ) ;
#36058=CARTESIAN_POINT ( 'NONE',  ( 0.01371903225206740247, -0.6635012362921914875, 0.4961661892038754518 ) ) ;
#36062=CARTESIAN_POINT ( 'NONE',  ( 0.06843411546424661707, -1.327640554429453168, 0.5682417262808774350 ) ) ;
#36063=CARTESIAN_POINT ( 'NONE',  ( 0.4605766076693431632, -1.054687064863744750, 0.7953974510635947182 ) ) ;
#36069=CARTESIAN_POINT ( 'NONE',  ( 0.4575915118593487652, -1.228153751895449952, 0.6022438500237607961 ) ) ;
#36070=B_SPLINE_CURVE_WITH_KNOTS ( 'NONE', 3,
 ( #31265, #21184, #3079, #28170, #34, #31456 ),
 .UNSPECIFIED., .F., .F.,
 ( 4, 2, 4 ),
 ( 0.002342563885389197919, 0.002942418546801120038, 0.003542273208213042156 ),
 .UNSPECIFIED. ) ;
#36073=CARTESIAN_POINT ( 'NONE',  ( 0.6055916563817613785, -1.479479184092913790, 0.5526975506195442867 ) ) ;
#36075=CARTESIAN_POINT ( 'NONE',  ( 0.2731210195084670111, -0.9705246840574025535, 0.7137744440085082021 ) ) ;
#36076=CARTESIAN_POINT ( 'NONE',  ( 0.2855206935027220227, -1.611758747868883290, 0.9420719997129571865 ) ) ;
#36077=CARTESIAN_POINT ( 'NONE',  ( 0.09770673769026198829, -0.5470910535863472424, 0.1715607505604543614 ) ) ;
#36078=CARTESIAN_POINT ( 'NONE',  ( 0.1356501467668746463, -1.176154491973367078, 0.9233203751264872361 ) ) ;
#36079=CARTESIAN_POINT ( 'NONE',  ( 0.3006692146602689131, -1.655694840352218034, 0.5887342810090384626 ) ) ;
#36080=CARTESIAN_POINT ( 'NONE',  ( 0.3816210699381897276, -1.147921404532277645, 0.5682417262808778791 ) ) ;
#36084=CARTESIAN_POINT ( 'NONE',  ( 0.2007258555610571815, -0.5966229082202755274, 0.3439381669633011507 ) ) ;
#36089=CARTESIAN_POINT ( 'NONE',  ( 0.07098271911918006827, -1.324513431496047611, 0.5012323767505566519 ) ) ;
#36091=CARTESIAN_POINT ( 'NONE',  ( 0.1031893334089009490, -1.411522619511051513, 0.5048512516234096026 ) ) ;
#36092=CARTESIAN_POINT ( 'NONE',  ( 0.6181559592477333664, -1.299230524387357866, 0.5730398182776358373 ) ) ;
#36096=CARTESIAN_POINT ( 'NONE',  ( 0.4578775569534166423, -1.222985555920403256, 0.6583285616417049457 ) ) ;
#36103=CARTESIAN_POINT ( 'NONE',  ( 0.4099814236516951538, -1.131125796475745737, 0.5236811888078589661 ) ) ;
#36104=CARTESIAN_POINT ( 'NONE',  ( 0.03817455972094940114, -0.8539075176413860602, 0.3579164544551949878 ) ) ;
#36110=CARTESIAN_POINT ( 'NONE',  ( 0.4760168417944102837, -1.251435095516215235, 0.6187594006579745232 ) ) ;
#36111=CARTESIAN_POINT ( 'NONE',  ( 0.5640992009001688512, -1.512213347522166185, 0.5182417262812423209 ) ) ;
#36112=CARTESIAN_POINT ( 'NONE',  ( 0.5382307432915078849, -1.161159458769174257, 0.5682417262808779901 ) ) ;
#36113=CARTESIAN_POINT ( 'NONE',  ( 0.2042269006659602204, -0.9243050108670398668, 0.3357924985444922794 ) ) ;
#36115=CARTESIAN_POINT ( 'NONE',  ( 0.5360540090424209536, -1.620675673019976504, 0.4182417262808776903 ) ) ;
#36118=CARTESIAN_POINT ( 'NONE',  ( 0.4138156062724669959, -1.589593685339665941, 0.5765124207693830272 ) ) ;
#36119=CARTESIAN_POINT ( 'NONE',  ( 0.08939090954650172338, -0.5761542031603253955, 0.09289087833756660972 ) ) ;
#36120=CARTESIAN_POINT ( 'NONE',  ( 0.1957193385055910895, -0.7828756236076227504, 0.3030586162759186242 ) ) ;
#36121=CARTESIAN_POINT ( 'NONE',  ( 0.1785188695711833751, -1.263798542596899610, 0.4993478297628262119 ) ) ;
#36125=CARTESIAN_POINT ( 'NONE',  ( 0.1192180282511240558, -0.5521284355774265240, 0.1795391081213666140 ) ) ;
#36129=CARTESIAN_POINT ( 'NONE',  ( 0.6109174031409076999, -1.589286328436636975, 0.4250233519115255154 ) ) ;
#36130=CARTESIAN_POINT ( 'NONE',  ( 0.1086196161304056745, -1.292942797799375265, 0.4408190352604076656 ) ) ;
#36133=DIRECTION ( 'NONE',  ( -0.8304108868527259046, -0.5068230121326142701, 0.2314048257260277464 ) ) ;
#36135=CARTESIAN_POINT ( 'NONE',  ( 0.7062706752423565382, -1.445327451526715823, 0.7203384021836691797 ) ) ;
#36137=CARTESIAN_POINT ( 'NONE',  ( 0.07734919244711804809, -1.330214924570791490, 0.4791524173686232957 ) ) ;
#36140=CARTESIAN_POINT ( 'NONE',  ( 0.2200771146567370995, -1.355300809693532837, 0.4882188858632743877 ) ) ;
#36141=CARTESIAN_POINT ( 'NONE',  ( 0.6205175308492241193, -1.587685600206998338, 0.6075176836741390529 ) ) ;
#36146=CARTESIAN_POINT ( 'NONE',  ( 0.002083146443013472390, -0.4777046557262296100, 0.1109577558998209867 ) ) ;
#36150=CARTESIAN_POINT ( 'NONE',  ( 0.5926747167100170355, -1.589032888346250338, 0.4182417262808776903 ) ) ;
#36154=VERTEX_POINT ( 'NONE', #24172 ) ;
#36155=DIRECTION ( 'NONE',  ( 0.8660512985181133550, 0.4999551463232370652, 0.000000000000000000 ) ) ;
#36157=CARTESIAN_POINT ( 'NONE',  ( 0.3206535937437295369, -1.182295409031864697, 0.3157417262808777658 ) ) ;
#36161=CARTESIAN_POINT ( 'NONE',  ( 0.5542078555708851439, -1.385725491393886788, 0.6184366861635991475 ) ) ;
#36165=CARTESIAN_POINT ( 'NONE',  ( 0.4873263706924592098, -1.095012774062378513, 0.6880473194844076712 ) ) ;
#36170=CARTESIAN_POINT ( 'NONE',  ( 0.2469025657576066068, -1.386664304572385431, 0.9158093811668733819 ) ) ;
#36171=CARTESIAN_POINT ( 'NONE',  ( 0.6692142533638006929, -1.524953862027760287, 0.4346820991015040159 ) ) ;
#36173=CARTESIAN_POINT ( 'NONE',  ( 0.3207148961678939481, -1.182401600646133089, 0.3667417262808778111 ) ) ;
#36178=CARTESIAN_POINT ( 'NONE',  ( 0.1536596445529309907, -1.277574755431482023, 0.4245438548657214928 ) ) ;
#36180=CARTESIAN_POINT ( 'NONE',  ( 0.3010285249158310417, -1.239940644847210116, 0.6985209647544882161 ) ) ;
#36187=CARTESIAN_POINT ( 'NONE',  ( 0.3503153873832512422, -1.166694168676842391, 0.4149758699348384816 ) ) ;
#36188=CARTESIAN_POINT ( 'NONE',  ( 0.6589248909250595698, -1.495897505467806310, 0.4182417262808776903 ) ) ;
#36192=CARTESIAN_POINT ( 'NONE',  ( 0.06465794909978246630, -1.338646149722257483, 0.5860318141376208434 ) ) ;
#36193=CARTESIAN_POINT ( 'NONE',  ( 0.3848921974812524738, -1.145728365548885241, 0.5552085920578813116 ) ) ;
#36196=VECTOR ( 'NONE', #34787, 39.37007874015748143 ) ;
#36197=CARTESIAN_POINT ( 'NONE',  ( 2.535788866453828974E-05, -0.4479327805637732252, 0.04122704326806578279 ) ) ;
#36204=CARTESIAN_POINT ( 'NONE',  ( 0.1746424574112480366, -0.5322842895853476808, 0.2164681121527878838 ) ) ;
#36207=CARTESIAN_POINT ( 'NONE',  ( 0.5306537665242748725, -1.384128856765673987, 0.7879015558401659680 ) ) ;
#36209=CARTESIAN_POINT ( 'NONE',  ( -0.001735234428706586285, -0.8394157820079461985, 0.07324090056792484371 ) ) ;
#36211=ORIENTED_EDGE ( 'NONE', *, *, #4697, .T. ) ;
#36212=CARTESIAN_POINT ( 'NONE',  ( 0.1559516411203765995, -0.6020992908152480450, 0.5335147605418883998 ) ) ;
#36213=CARTESIAN_POINT ( 'NONE',  ( 0.04547705972580577682, -0.8635874790222509700, 0.7385780690550703964 ) ) ;
#36215=CARTESIAN_POINT ( 'NONE',  ( 0.1327588654869316098, -1.278667161109435790, 0.6047653525011950082 ) ) ;
#36224=CARTESIAN_POINT ( 'NONE',  ( 0.02818252482944432619, -0.9358868228192540606, 0.6083748332521794477 ) ) ;
#36225=CARTESIAN_POINT ( 'NONE',  ( 0.09604050016782572641, -0.6082561981476365398, 0.2968782915989965354 ) ) ;
#36227=CARTESIAN_POINT ( 'NONE',  ( 0.1162496453231300075, -0.5482924977647862796, 0.1535821627971732661 ) ) ;
#36228=CARTESIAN_POINT ( 'NONE',  ( 0.04800852669519790200, -1.175821727638011405, 0.6650279943451450348 ) ) ;
#36230=CARTESIAN_POINT ( 'NONE',  ( 0.06581764578086063411, -1.340728352476672658, 0.5449258910593480776 ) ) ;
#36233=CARTESIAN_POINT ( 'NONE',  ( 0.3921416614852478721, -1.728153360793264870, 0.4267968442986774802 ) ) ;
#36234=CARTESIAN_POINT ( 'NONE',  ( 0.6540709664215760277, -1.593060928864740156, 0.5182417262812423209 ) ) ;
#36235=CARTESIAN_POINT ( 'NONE',  ( 0.06923712653936904549, -0.5400029222721455247, 0.1457185332388703236 ) ) ;
#36237=CARTESIAN_POINT ( 'NONE',  ( 0.01132828649437914691, -0.9450724994329757767, 0.1162305715099754139 ) ) ;
#36238=CARTESIAN_POINT ( 'NONE',  ( 0.4370955311001439303, -1.230376993490756687, 0.5844175963752731295 ) ) ;
#36240=CARTESIAN_POINT ( 'NONE',  ( 0.001061621656357588511, -0.7083572002807602130, 0.2962098885571950446 ) ) ;
#36241=CARTESIAN_POINT ( 'NONE',  ( 0.2117717001728993131, -0.8880493388543053701, 0.3804667941236127282 ) ) ;
#36243=CARTESIAN_POINT ( 'NONE',  ( 0.4717011137366580176, -1.062550488221034151, 0.8575416557712804977 ) ) ;
#36246=CARTESIAN_POINT ( 'NONE',  ( 0.3187624475196638163, -1.760353637077040068, 0.5684082056346195788 ) ) ;
#36250=CARTESIAN_POINT ( 'NONE',  ( 0.1198448511384348769, -1.120590779523480629, 0.9040002884437861042 ) ) ;
#36251=CIRCLE ( 'NONE', #2761, 0.01000000000000002970 ) ;
#36252=CARTESIAN_POINT ( 'NONE',  ( 0.01054817777343857940, -0.5296544771352952319, 0.1457185332388703236 ) ) ;
#36254=ORIENTED_EDGE ( 'NONE', *, *, #30529, .F. ) ;
#36256=CARTESIAN_POINT ( 'NONE',  ( 0.2143793204313029777, -0.6499299462495844448, 0.4116214953459712556 ) ) ;
#36257=ORIENTED_EDGE ( 'NONE', *, *, #15688, .F. ) ;
#36261=CARTESIAN_POINT ( 'NONE',  ( 0.1826249073287969926, -1.261667980084790530, 0.4182417262808780789 ) ) ;
#36263=CARTESIAN_POINT ( 'NONE',  ( 0.4670213778778394831, -1.236191465557153757, 0.6057417262809817737 ) ) ;
#36266=CARTESIAN_POINT ( 'NONE',  ( 0.2188233872650832412, -0.8909256067445749938, 0.6610102726906746939 ) ) ;
#36267=CARTESIAN_POINT ( 'NONE',  ( 0.2500145865922475119, -1.478584986872982343, 1.008546107030279027 ) ) ;
#36268=CARTESIAN_POINT ( 'NONE',  ( 0.09782311751919105236, -0.5505692872209160260, 0.1905127806560832637 ) ) ;
#36269=CARTESIAN_POINT ( 'NONE',  ( 0.2117622885028031254, -1.433178199125996199, 0.9421946221852213199 ) ) ;
#36271=CARTESIAN_POINT ( 'NONE',  ( 0.09537293942087692045, -0.9336651254918434395, 0.2369052016270806194 ) ) ;
#36275=CARTESIAN_POINT ( 'NONE',  ( 0.1898178091108482235, -0.5354154051322274066, 0.1678590518679249910 ) ) ;
#36279=EDGE_CURVE ( 'NONE', #12586, #36726, #29196, .T. ) ;
#36283=CARTESIAN_POINT ( 'NONE',  ( 0.07814782694598980395, -1.316809471941703613, 0.4837547526852793434 ) ) ;
#36285=CARTESIAN_POINT ( 'NONE',  ( 0.1048644750963132199, -1.410528588406870787, 0.5685427134957244943 ) ) ;
#36286=CARTESIAN_POINT ( 'NONE',  ( 0.3304381985390301701, -0.8896417797241282788, 0.6549085351719812209 ) ) ;
#36287=B_SPLINE_SURFACE_WITH_KNOTS ( 'NONE', 3, 3, ( 
 ( #9574, #25619, #21936, #754, #37752, #963, #6670, #19452, #22152, #13260, #22341, #34668, #6276, #35072, #12645, #25000, #6472, #12870, #28708, #31990, #3802, #34861, #25209, #32179, #25431 ),
 ( #9974, #37532, #19041, #31789, #34462, #9771, #9356, #31572, #18850, #19645, #31391, #15948, #3195, #3390, #3603, #28493, #22544, #15735, #38349, #28285, #7074, #16358, #28893, #10184, #366 ),
 ( #151, #3990, #16171, #572, #25830, #22753, #35279, #29506, #10793, #7880, #23749, #20262, #13661, #26841, #23364, #29922, #19839, #35677, #20058, #7480, #13853, #17575, #29313, #26226, #36080 ),
 ( #1764, #26648, #32783, #36271, #17368, #32374, #1346, #1161, #14276, #16962, #7265, #32986, #33203, #38748, #17157, #10574, #23148, #38561, #10384, #39369, #4200, #30117, #11189, #26426, #16765 ),
 ( #39179, #32589, #11005, #8093, #14073, #38963, #29706, #20670, #1552, #22947, #23562, #20452, #13472, #5008, #26039, #35464, #4585, #35886, #4404, #7697, #4793, #36492, #11607, #15083, #8498 ),
 ( #33398, #27031, #9107, #8910, #17760, #30311, #2138, #14677, #39558, #12210, #2546, #18578, #39777, #24352, #11392, #30523, #1949, #27247, #14464, #37293, #23964, #33591, #8306, #14889, #20877 ),
 ( #5205, #24169, #27638, #21487, #2348, #36693, #11998, #21063, #5400, #34202, #17963, #27448, #5615, #24565, #37095, #11794, #39973, #21673, #36886, #8695, #15287, #40386, #21273, #33810, #18171 ) ),
 .UNSPECIFIED., .F., .F., .F.,
 ( 4, 1, 1, 1, 4 ),
 ( 4, 1, 1, 1, 1, 1, 1, 1, 1, 1, 1, 1, 1, 1, 1, 1, 1, 1, 1, 1, 1, 1, 4 ),
 ( 0.000000000000000000, 0.2500000000000000000, 0.5000000000000000000, 0.7500000000000000000, 1.000000000000000000 ),
 ( 0.000000000000000000, 0.06250000000000000000, 0.1250000000000000000, 0.1666666666666666574, 0.1875000000000000000, 0.2500000000000000000, 0.3125000000000000000, 0.3750000000000000000, 0.4375000000000000000, 0.5000000000000000000, 0.5555555555555555802, 0.5625000000000000000, 0.6250000000000000000, 0.6875000000000000000, 0.7500000000000000000, 0.7812500000000000000, 0.8125000000000000000, 0.8437500000000000000, 0.8750000000000000000, 0.9062500000000000000, 0.9375000000000000000, 0.9687500000000000000, 1.000000000000000000 ),
 .UNSPECIFIED. ) ;
#36288=DIRECTION ( 'NONE',  ( -0.4395832838285286814, -0.2366097102993482970, 0.8664769942535033298 ) ) ;
#36295=CARTESIAN_POINT ( 'NONE',  ( 0.3099399546549871931, -0.9171249783946038292, 0.5994493976520077760 ) ) ;
#36299=CARTESIAN_POINT ( 'NONE',  ( 0.1364971356285234749, -1.133499090544220156, 0.7558102704853532083 ) ) ;
#36301=EDGE_CURVE ( 'NONE', #26649, #12308, #20330, .T. ) ;
#36309=CARTESIAN_POINT ( 'NONE',  ( 0.4780493526100274004, -1.254977130501546467, 0.6087998174934282636 ) ) ;
#36310=CARTESIAN_POINT ( 'NONE',  ( 0.3980789824590564852, -1.137894033439979635, 0.4906765649267371132 ) ) ;
#36316=CARTESIAN_POINT ( 'NONE',  ( 0.5860257985473389386, -1.592810714289445650, 0.4182417262808776903 ) ) ;
#36318=CARTESIAN_POINT ( 'NONE',  ( 0.1895943254151421786, -0.6407273034312881421, 0.008518417185872215538 ) ) ;
#36319=CARTESIAN_POINT ( 'NONE',  ( 0.06062184886820209256, -0.5472141424593505166, 0.2036466807051401096 ) ) ;
#36321=CARTESIAN_POINT ( 'NONE',  ( 0.08990334728944714138, -0.5646811812073189163, 0.1486427366963163632 ) ) ;
#36324=ORIENTED_EDGE ( 'NONE', *, *, #2201, .F. ) ;
#36325=B_SPLINE_CURVE_WITH_KNOTS ( 'NONE', 3,
 ( #29023, #39046, #4667, #14548, #30190, #33469, #33073, #40045, #8179, #24049, #33676, #33277 ),
 .UNSPECIFIED., .F., .F.,
 ( 4, 2, 2, 2, 2, 4 ),
 ( 0.000000000000000000, 0.0005853004908840498495, 0.001170600981768099699, 0.001755901472652149440, 0.002048551718094174419, 0.002341201963536199832 ),
 .UNSPECIFIED. ) ;
#36328=CARTESIAN_POINT ( 'NONE',  ( 0.4635535538083537244, -1.314077908205018241, 0.8227958598471974971 ) ) ;
#36331=CARTESIAN_POINT ( 'NONE',  ( 0.3207912813105621153, -1.758981359444245385, 0.5311847171115458011 ) ) ;
#36334=B_SPLINE_CURVE_WITH_KNOTS ( 'NONE', 3,
 ( #28179, #44, #24701, #18718, #34135, #15430 ),
 .UNSPECIFIED., .F., .F.,
 ( 4, 2, 4 ),
 ( 0.0008728868357568681348, 0.001510076209140402432, 0.002147265582523936404 ),
 .UNSPECIFIED. ) ;
#36337=CARTESIAN_POINT ( 'NONE',  ( 0.1891515964196448796, -1.246317699220909958, 0.4467030175713385121 ) ) ;
#36340=CARTESIAN_POINT ( 'NONE',  ( 0.08988759086353000083, -0.6029188970129375491, 0.1463085495562314320 ) ) ;
#36341=CARTESIAN_POINT ( 'NONE',  ( 0.6419406851146725046, -1.339736372716090917, 0.8215813590131169075 ) ) ;
#36348=CARTESIAN_POINT ( 'NONE',  ( 0.5750090102395998271, -1.613396230683133759, 0.5672260050467223813 ) ) ;
#36350=AXIS2_PLACEMENT_3D ( 'NONE', #15359, #20937, #2216 ) ;
#36352=CARTESIAN_POINT ( 'NONE',  ( 0.06825878040686909898, -0.8404074238475144343, 0.8024108098889147778 ) ) ;
#36355=CARTESIAN_POINT ( 'NONE',  ( 0.3047936848243344432, -1.756875962071034580, 0.5682417262361116883 ) ) ;
#36360=CARTESIAN_POINT ( 'NONE',  ( 0.08778601674903806218, -0.5530204048924579618, 0.1461273381126583226 ) ) ;
#36363=EDGE_CURVE ( 'NONE', #32520, #33386, #15086, .T. ) ;
#36364=CARTESIAN_POINT ( 'NONE',  ( 0.4992372981854732439, -1.293093988718565956, 0.7065005728875947133 ) ) ;
#36367=CARTESIAN_POINT ( 'NONE',  ( 0.3302065591133839240, -0.9317669992161012882, 0.6252562391197076241 ) ) ;
#36375=CARTESIAN_POINT ( 'NONE',  ( 0.1127314162110860801, -0.9204869745937769299, 0.7651726503946431057 ) ) ;
#36376=CARTESIAN_POINT ( 'NONE',  ( 0.6981984480215006617, -1.496421087833687213, 0.4851264061261034710 ) ) ;
#36377=CARTESIAN_POINT ( 'NONE',  ( 0.1878447062321111916, -0.5357678935135709031, 0.07285347281293909349 ) ) ;
#36380=ORIENTED_EDGE ( 'NONE', *, *, #13256, .F. ) ;
#36386=EDGE_CURVE ( 'NONE', #26082, #20946, #33557, .T. ) ;
#36387=CARTESIAN_POINT ( 'NONE',  ( 0.2377172976805353166, -1.126050835660724836, 0.7471600383748348007 ) ) ;
#36391=ADVANCED_FACE ( 'NONE', ( #34010 ), #22251, .F. ) ;
#36392=CARTESIAN_POINT ( 'NONE',  ( 0.2283924689359978499, -0.9952348863919213695, 0.5666251819813739043 ) ) ;
#36393=CARTESIAN_POINT ( 'NONE',  ( 0.6589703859825570831, -1.564329074718757484, 0.3667417262808780887 ) ) ;
#36396=CARTESIAN_POINT ( 'NONE',  ( 0.4095772007298983941, -1.132452871991625143, 0.4852699800312822997 ) ) ;
#36397=B_SPLINE_CURVE_WITH_KNOTS ( 'NONE', 5,
 ( #25901, #13121, #38419, #16411, #10257, #3860 ),
 .UNSPECIFIED., .F., .F.,
 ( 6, 6 ),
 ( 12.39904547089488496, 12.50424887933038676 ),
 .UNSPECIFIED. ) ;
#36400=AXIS2_PLACEMENT_3D ( 'NONE', #32677, #17047, #10062 ) ;
#36401=CARTESIAN_POINT ( 'NONE',  ( 0.06310204368368470262, -1.326805032915164162, 0.6102011665707310906 ) ) ;
#36402=CARTESIAN_POINT ( 'NONE',  ( 0.3605539653964052182, -1.159620486319301813, 0.5253391196606768121 ) ) ;
#36408=CARTESIAN_POINT ( 'NONE',  ( 2.003769519753459454E-05, -0.4887874499424059715, -0.02467011407665378395 ) ) ;
#36410=CARTESIAN_POINT ( 'NONE',  ( 0.0004801912913160456516, -0.4395057766670965038, 0.1677942470109538287 ) ) ;
#36413=VERTEX_POINT ( 'NONE', #17114 ) ;
#36414=ORIENTED_EDGE ( 'NONE', *, *, #17315, .F. ) ;
#36416=CARTESIAN_POINT ( 'NONE',  ( 0.1733962078978711074, -0.5203934806767281929, 0.1236872031806311029 ) ) ;
#36419=EDGE_CURVE ( 'NONE', #30626, #26082, #11011, .T. ) ;
#36421=CARTESIAN_POINT ( 'NONE',  ( -0.001329024702343150049, -0.8150860535562964859, 0.03600470908344870907 ) ) ;
#36424=ORIENTED_EDGE ( 'NONE', *, *, #12225, .F. ) ;
#36425=CARTESIAN_POINT ( 'NONE',  ( 0.5521441265314278590, -1.306365183234622585, 0.8936522956502730430 ) ) ;
#36429=CARTESIAN_POINT ( 'NONE',  ( 0.1658945499291084036, -1.260523426758859644, 0.6030236252751928205 ) ) ;
#36436=CARTESIAN_POINT ( 'NONE',  ( 0.01170466158157320614, -0.7209202686218528777, -0.1115487569099005288 ) ) ;
#36439=CARTESIAN_POINT ( 'NONE',  ( 0.09213258466004858871, -0.5863880887348119630, 0.2398429810774082571 ) ) ;
#36441=CARTESIAN_POINT ( 'NONE',  ( 0.01128729522873459998, -0.9461985897320852601, 0.1796480652156055013 ) ) ;
#36444=CARTESIAN_POINT ( 'NONE',  ( 0.06485935661193353852, -1.341259894741156700, 0.5606283090912991263 ) ) ;
#36446=CARTESIAN_POINT ( 'NONE',  ( 0.4079725984602744493, -1.712446521674362732, 0.4259523847339783953 ) ) ;
#36450=LINE ( 'NONE', #30691, #13959 ) ;
#36452=CARTESIAN_POINT ( 'NONE',  ( -3.837675818371248128E-05, -0.9481486753962028446, 0.1506679456753735602 ) ) ;
#36456=CARTESIAN_POINT ( 'NONE',  ( 0.003441938119505853853, -0.5826794048688673788, 0.2512083064573837898 ) ) ;
#36457=CARTESIAN_POINT ( 'NONE',  ( 0.1854168535569865883, -0.8697360073808750869, 0.1550939566555308846 ) ) ;
#36458=CARTESIAN_POINT ( 'NONE',  ( 0.02418895824641892692, -0.9508555545350739768, 0.6316828188328664773 ) ) ;
#36460=CARTESIAN_POINT ( 'NONE',  ( 0.5573545814012507149, -1.203739305690170402, 0.8778060520269345135 ) ) ;
#36464=CARTESIAN_POINT ( 'NONE',  ( 0.3187246401137938112, -1.760368955180017236, 0.5676021236855325336 ) ) ;
#36469=CARTESIAN_POINT ( 'NONE',  ( 0.07641379623259875187, -0.9713282881620481923, 0.8144253132993416466 ) ) ;
#36472=DIRECTION ( 'NONE',  ( 0.8660512985181133550, 0.4999551463232371207, 0.000000000000000000 ) ) ;
#36473=VERTEX_POINT ( 'NONE', #22708 ) ;
#36474=CARTESIAN_POINT ( 'NONE',  ( 0.3224711051296385578, -1.754080271473366093, 0.4780932018388675542 ) ) ;
#36476=CARTESIAN_POINT ( 'NONE',  ( 0.5155751834530871713, -1.137973747986757544, 0.7479765829993398896 ) ) ;
#36477=ORIENTED_EDGE ( 'NONE', *, *, #38086, .F. ) ;
#36482=CARTESIAN_POINT ( 'NONE',  ( 0.2948640431821396013, -1.208698857570559948, 0.4182417262808778013 ) ) ;
#36487=CARTESIAN_POINT ( 'NONE',  ( 0.1251483427054724540, -0.7782096407036064312, 0.4562269205239417591 ) ) ;
#36488=CARTESIAN_POINT ( 'NONE',  ( 0.3154013571205182553, -1.680250829566968473, 0.8751360567703019289 ) ) ;
#36489=CARTESIAN_POINT ( 'NONE',  ( 0.09985988637870266138, -0.5731286213205528668, 0.2623670383419783314 ) ) ;
#36490=CARTESIAN_POINT ( 'NONE',  ( 0.1146734031460662356, -0.4828071762122547739, 0.01829575716233284438 ) ) ;
#36492=CARTESIAN_POINT ( 'NONE',  ( 0.1659062591970449363, -1.250628541066444388, 0.6134509435559128976 ) ) ;
#36496=CARTESIAN_POINT ( 'NONE',  ( 0.3174184176267951796, -1.762933076790987874, 0.5319023928053561168 ) ) ;
#36497=CARTESIAN_POINT ( 'NONE',  ( 0.3348785992456718708, -0.8147534913312738380, 0.7321433735801530229 ) ) ;
#36503=EDGE_CURVE ( 'NONE', #9452, #14931, #1308, .T. ) ;
#36504=DIRECTION ( 'NONE',  ( 1.912293595564980111E-14, 0.7743343091952541446, -0.6327767201810673425 ) ) ;
#36507=CARTESIAN_POINT ( 'NONE',  ( 0.3504057387187115014, -1.153664717295436404, 0.4422128889498893045 ) ) ;
#36508=CARTESIAN_POINT ( 'NONE',  ( 0.4104166757648185504, -0.9945572768306742972, 0.7245767828144217271 ) ) ;
#36517=ORIENTED_EDGE ( 'NONE', *, *, #17922, .F. ) ;
#36520=CIRCLE ( 'NONE', #7590, 0.01000000000000002623 ) ;
#36522=CARTESIAN_POINT ( 'NONE',  ( 0.1620965704063034862, -1.205491034068324252, 0.7491300204058332080 ) ) ;
#36527=CARTESIAN_POINT ( 'NONE',  ( 0.1613371997446969852, -1.389521869439662938, 0.4310088812813361869 ) ) ;
#36529=CARTESIAN_POINT ( 'NONE',  ( 0.4411176185871907296, -1.199366743384446377, 0.6758596692312155430 ) ) ;
#36532=PLANE ( 'NONE',  #34908 ) ;
#36533=ORIENTED_EDGE ( 'NONE', *, *, #14668, .F. ) ;
#36535=CARTESIAN_POINT ( 'NONE',  ( 0.06979851145747001384, -1.326871333008951881, 0.5494227783323851755 ) ) ;
#36538=CARTESIAN_POINT ( 'NONE',  ( 0.4132723870208870331, -1.504063452548798807, 0.8015072579983955059 ) ) ;
#36539=CARTESIAN_POINT ( 'NONE',  ( 0.08803424184564076493, -0.6404506698634022666, 0.009295576138141414813 ) ) ;
#36540=CARTESIAN_POINT ( 'NONE',  ( 0.1857430203655689172, -0.8056635886342105035, 0.2698372336795832882 ) ) ;
#36541=CARTESIAN_POINT ( 'NONE',  ( 0.4412551199097751176, -1.145691214381745038, 0.4235448160515665195 ) ) ;
#36545=B_SPLINE_CURVE_WITH_KNOTS ( 'NONE', 3,
 ( #7611, #20795, #20985, #13981, #17490, #26553 ),
 .UNSPECIFIED., .F., .F.,
 ( 4, 2, 4 ),
 ( 0.005183784548773252843, 0.005807229420386499606, 0.006430674291999746370 ),
 .UNSPECIFIED. ) ;
#36546=CARTESIAN_POINT ( 'NONE',  ( 0.5566350444588750168, -1.457454591888360573, 0.7347119787586107176 ) ) ;
#36549=CARTESIAN_POINT ( 'NONE',  ( 0.6009414993585495690, -1.584005022665416984, 0.4182417262808776903 ) ) ;
#36550=CARTESIAN_POINT ( 'NONE',  ( 0.09165208117211873229, -1.314337288742353227, 0.4470340182402313123 ) ) ;
#36552=CARTESIAN_POINT ( 'NONE',  ( 0.08911620379650853074, -0.6035282328652368244, 0.06395801244005373809 ) ) ;
#36554=EDGE_CURVE ( 'NONE', #13751, #30110, #16378, .T. ) ;
#36556=CARTESIAN_POINT ( 'NONE',  ( 0.1876258513389257310, -0.4649338269308297966, 0.1998821562507554217 ) ) ;
#36557=EDGE_CURVE ( 'NONE', #23564, #30450, #1906, .T. ) ;
#36558=CARTESIAN_POINT ( 'NONE',  ( 0.07296648554937049114, -1.326663526568331752, 0.4848661492846349508 ) ) ;
#36560=CARTESIAN_POINT ( 'NONE',  ( 0.1484974224218250372, -0.8518925887318784529, 0.5179931425135368972 ) ) ;
#36569=CARTESIAN_POINT ( 'NONE',  ( 0.2292082634166116850, -1.390808673668628259, 1.038138609612698327 ) ) ;
#36572=CARTESIAN_POINT ( 'NONE',  ( 0.4399541867944170570, -1.702001723531057165, 0.6019985635216079656 ) ) ;
#36576=CARTESIAN_POINT ( 'NONE',  ( 0.3558549970762978076, -1.139915900499853585, 0.6174992432461627878 ) ) ;
#36580=CARTESIAN_POINT ( 'NONE',  ( 0.4911901511437292700, -1.279438450280085293, 0.6967407287098164037 ) ) ;
#36583=CARTESIAN_POINT ( 'NONE',  ( 0.4989999315605664343, -1.099494619349625113, 0.6223919996226902063 ) ) ;
#36586=CARTESIAN_POINT ( 'NONE',  ( 0.1699918782215477098, -0.4775673823552313291, 0.1457287000202342475 ) ) ;
#36589=CARTESIAN_POINT ( 'NONE',  ( 0.3562689543733437159, -1.622445070342072304, 0.5759800519041369249 ) ) ;
#36590=CARTESIAN_POINT ( 'NONE',  ( 0.7027426662857245709, -1.495553731087327254, 0.5003482327437285271 ) ) ;
#36596=ORIENTED_EDGE ( 'NONE', *, *, #29831, .T. ) ;
#36597=CARTESIAN_POINT ( 'NONE',  ( 0.1826134026666660082, -1.261648033191451246, 0.4282186462236582392 ) ) ;
#36599=CARTESIAN_POINT ( 'NONE',  ( 0.1041408025812746996, -0.8666933816795890921, 0.4735943452512007545 ) ) ;
#36603=CARTESIAN_POINT ( 'NONE',  ( 0.3092347844015437830, -1.045386296435460549, 0.6288420117150920197 ) ) ;
#36607=CARTESIAN_POINT ( 'NONE',  ( 0.1852718761952666104, -0.8389489029336036907, 0.1457185345930598341 ) ) ;
#36608=CARTESIAN_POINT ( 'NONE',  ( 0.05217694232180475344, -1.283001185023028068, 0.6381678350426021051 ) ) ;
#36610=EDGE_CURVE ( 'NONE', #8445, #13751, #7561, .T. ) ;
#36611=CARTESIAN_POINT ( 'NONE',  ( 0.4393690858571965285, -1.132650523124447473, 0.4426054485940990046 ) ) ;
#36613=CARTESIAN_POINT ( 'NONE',  ( 0.4669612913469819437, -1.236553095564864035, 0.6057417262809811076 ) ) ;
#36617=CARTESIAN_POINT ( 'NONE',  ( 1.097344326769410557E-05, -0.5478823044768206252, -0.07510365260775653251 ) ) ;
#36619=CARTESIAN_POINT ( 'NONE',  ( 0.0008453517450213650667, -0.4570859405462899816, 0.2529032369821648807 ) ) ;
#36622=ORIENTED_EDGE ( 'NONE', *, *, #22893, .F. ) ;
#36623=EDGE_CURVE ( 'NONE', #15439, #27736, #38468, .T. ) ;
#36624=CARTESIAN_POINT ( 'NONE',  ( 0.1767564091517300762, -0.5260537877495167214, 0.08939343933192094027 ) ) ;
#36626=CARTESIAN_POINT ( 'NONE',  ( 0.1849096901904443147, -1.549205955729533235, 0.5682417262808779901 ) ) ;
#36627=ADVANCED_FACE ( 'NONE', ( #868 ), #20918, .T. ) ;
#36629=CARTESIAN_POINT ( 'NONE',  ( 0.001056708435954382790, -0.5892904156828951967, 0.01971284387651792494 ) ) ;
#36634=CARTESIAN_POINT ( 'NONE',  ( -0.0009405724334786376211, -0.5506602586161217783, 0.2523206823539573262 ) ) ;
#36636=CARTESIAN_POINT ( 'NONE',  ( 0.1361711851722846311, -1.247893485105676215, 0.6057349558209625950 ) ) ;
#36643=B_SPLINE_SURFACE_WITH_KNOTS ( 'NONE', 3, 3, ( 
 ( #32758, #1323, #23335, #1738, #7673, #13829, #13636 ),
 ( #10977, #32960, #14250, #20424, #38933, #26402, #36246 ),
 ( #26203, #10765, #4560, #29679, #29895, #1525, #26812 ),
 ( #14041, #23719, #26619, #39152, #19622, #3965, #36464 ) ),
 .UNSPECIFIED., .F., .F., .F.,
 ( 4, 4 ),
 ( 4, 3, 4 ),
 ( 0.01293109825612811029, 0.01296195159122108011 ),
 ( 0.000000000000000000, 0.5039009682608166507, 1.007801936521633301 ),
 .UNSPECIFIED. ) ;
#36644=CARTESIAN_POINT ( 'NONE',  ( 0.09318787492968771957, -0.5716158580642060061, 0.2615376999529335778 ) ) ;
#36646=CARTESIAN_POINT ( 'NONE',  ( 0.1869677562307399121, -0.7232448055034852441, 0.03223249978197218618 ) ) ;
#36649=CARTESIAN_POINT ( 'NONE',  ( 0.01220592763406190724, -0.4286278507047505681, 0.1569170967635542535 ) ) ;
#36650=CARTESIAN_POINT ( 'NONE',  ( 0.4011294921376035161, -1.722319301493235644, 0.4257442406416360736 ) ) ;
#36658=CARTESIAN_POINT ( 'NONE',  ( 0.005948235723147832048, -0.6142029534155015735, 0.3540208382306603840 ) ) ;
#36659=CARTESIAN_POINT ( 'NONE',  ( 0.4241296934850513067, -1.044958113096912777, 0.6349482895397999815 ) ) ;
#36660=CARTESIAN_POINT ( 'NONE',  ( 0.02180608606761921808, -0.9117970258225919222, 0.5599240550155194507 ) ) ;
#36662=CARTESIAN_POINT ( 'NONE',  ( 0.1875000000000003608, -0.4593131964907914422, 0.1498534765393862711 ) ) ;
#36667=CARTESIAN_POINT ( 'NONE',  ( -0.001495529303326669120, -0.9079788901573263571, 0.1457185332388704069 ) ) ;
#36668=CARTESIAN_POINT ( 'NONE',  ( 0.09137532172571469213, -1.015574661215327579, 0.8525896866749620440 ) ) ;
#36671=CARTESIAN_POINT ( 'NONE',  ( 0.1282560915798944823, -0.5581765241255676191, 0.1980671242072916116 ) ) ;
#36673=CARTESIAN_POINT ( 'NONE',  ( 0.1874578000378240850, -0.6893444085712847613, 0.06304793604024336307 ) ) ;
#36677=CARTESIAN_POINT ( 'NONE',  ( 0.6169573538504090626, -1.299218888095586388, 0.5469722621913530869 ) ) ;
#36685=CARTESIAN_POINT ( 'NONE',  ( 0.5247602972291017798, -1.202859872010444198, 0.6057417262809816627 ) ) ;
#36688=CARTESIAN_POINT ( 'NONE',  ( 0.2783032227094284772, -0.9886002588855364870, 0.7058132634711740128 ) ) ;
#36689=CARTESIAN_POINT ( 'NONE',  ( 0.3167411566867828210, -1.686693824585019152, 0.8658616982602641565 ) ) ;
#36690=CARTESIAN_POINT ( 'NONE',  ( 0.4713817688654168281, -1.488542902949906876, 0.7707858769014730438 ) ) ;
#36691=CARTESIAN_POINT ( 'NONE',  ( 0.5938580047360285663, -1.599883625798725673, 0.4301333326164196169 ) ) ;
#36692=CARTESIAN_POINT ( 'NONE',  ( 0.0006870102372341157582, -0.6133945797756367169, -0.005209209353789174407 ) ) ;
#36693=CARTESIAN_POINT ( 'NONE',  ( 0.001265705468310253205, -0.9563107042206788755, 0.3108407331560245068 ) ) ;
#36697=CARTESIAN_POINT ( 'NONE',  ( 0.5806152853151792526, -1.240580746683077606, 0.8162131908780063672 ) ) ;
#36700=EDGE_CURVE ( 'NONE', #13571, #25255, #31607, .T. ) ;
#36703=CARTESIAN_POINT ( 'NONE',  ( 0.3175074107031659598, -1.172635205199522801, 0.4853316727370740047 ) ) ;
#36704=CARTESIAN_POINT ( 'NONE',  ( 0.1912825281910040254, -0.6944471949468554728, 0.2480975638430023278 ) ) ;
#36708=CARTESIAN_POINT ( 'NONE',  ( 0.4568312001397978883, -1.218398625660269907, 0.5976199984034119561 ) ) ;
#36710=CARTESIAN_POINT ( 'NONE',  ( 0.3174184176267951796, -1.762933076790987874, 0.5319023928053561168 ) ) ;
#36715=CARTESIAN_POINT ( 'NONE',  ( 0.2263037797473776980, -1.351310894833297693, 0.5682417262808749925 ) ) ;
#36716=EDGE_LOOP ( 'NONE', ( #36727, #16942, #33846, #28793 ) ) ;
#36721=CARTESIAN_POINT ( 'NONE',  ( 0.3837573706890263781, -1.128755630749517680, 0.7040211244557138537 ) ) ;
#36724=CARTESIAN_POINT ( 'NONE',  ( 0.2164394655998746198, -1.357183666387900667, 0.5509909139819678670 ) ) ;
#36726=VERTEX_POINT ( 'NONE', #16460 ) ;
#36727=ORIENTED_EDGE ( 'NONE', *, *, #38809, .T. ) ;
#36731=CARTESIAN_POINT ( 'NONE',  ( 0.06043370286545072384, -0.5384506411558260819, 0.1542169419559350219 ) ) ;
#36733=CARTESIAN_POINT ( 'NONE',  ( 0.1934695683574406411, -0.7446624497515935692, 0.3188077537673400519 ) ) ;
#36734=CARTESIAN_POINT ( 'NONE',  ( 0.4236478467173229179, -1.144025187649157393, 0.4241618933158771698 ) ) ;
#36738=CARTESIAN_POINT ( 'NONE',  ( 0.4766810985275751200, -1.336280447492598222, 0.8178516970329706703 ) ) ;
#36742=CARTESIAN_POINT ( 'NONE',  ( 0.4368279861777726314, -1.677667223885754622, 0.4182417262808776348 ) ) ;
#36745=CARTESIAN_POINT ( 'NONE',  ( 0.7205914100055046401, -1.471989004879187490, 0.6461535000039996257 ) ) ;
#36747=CARTESIAN_POINT ( 'NONE',  ( 0.01771465363353170661, -0.9865948873696219756, 0.4717780899493672075 ) ) ;
#36750=CARTESIAN_POINT ( 'NONE',  ( 0.5767056209452497972, -1.613046407156268014, 0.5861331466064494400 ) ) ;
#36754=CARTESIAN_POINT ( 'NONE',  ( 0.1826873925087639794, -0.5091858565627841449, 0.09782563527837608019 ) ) ;
#36760=CARTESIAN_POINT ( 'NONE',  ( 0.3504971479267370293, -1.161911706188821780, 0.5926884422481595305 ) ) ;
#36761=CARTESIAN_POINT ( 'NONE',  ( 0.3247288286498336007, -1.767622216147507919, 0.5120194545848663070 ) ) ;
#36763=CARTESIAN_POINT ( 'NONE',  ( 0.4865585680422996884, -1.272250160645541195, 0.7024912634709812309 ) ) ;
#36766=CARTESIAN_POINT ( 'NONE',  ( 0.4638997371337593156, -1.067608878195758448, 0.6494661525283214054 ) ) ;
#36767=ORIENTED_EDGE ( 'NONE', *, *, #26009, .F. ) ;
#36772=CARTESIAN_POINT ( 'NONE',  ( 0.3349041316666306889, -1.546677854842905653, 0.8259521700164116353 ) ) ;
#36774=CARTESIAN_POINT ( 'NONE',  ( 0.1148406439744575763, -0.4693285123388637459, 0.04216440238363276805 ) ) ;
#36775=FACE_OUTER_BOUND ( 'NONE', #6723, .T. ) ;
#36778=CARTESIAN_POINT ( 'NONE',  ( 0.4855685666384785826, -1.075955829526442864, 0.6081528487602839705 ) ) ;
#36779=ADVANCED_FACE ( 'NONE', ( #14184 ), #14796, .T. ) ;
#36781=FACE_OUTER_BOUND ( 'NONE', #10825, .T. ) ;
#36784=CARTESIAN_POINT ( 'NONE',  ( 0.1370286797637513543, -0.9213833723744169202, 0.6131078865398249533 ) ) ;
#36788=CARTESIAN_POINT ( 'NONE',  ( 0.1192809747888602806, -0.9331602493862439784, 0.2873266990398272158 ) ) ;
#36789=FACE_OUTER_BOUND ( 'NONE', #6370, .T. ) ;
#36790=CARTESIAN_POINT ( 'NONE',  ( 0.3620892796180312234, -1.158480933315200634, 0.4329786855189595718 ) ) ;
#36792=CARTESIAN_POINT ( 'NONE',  ( 0.6568168297909239284, -1.515518412183779917, 0.4182417262808776903 ) ) ;
#36797=CARTESIAN_POINT ( 'NONE',  ( 0.4782576142078460157, -1.116195606080568448, 0.5342808753144958622 ) ) ;
#36798=CARTESIAN_POINT ( 'NONE',  ( 0.5536047524870395531, -1.186371981408798737, 0.6057417262809813296 ) ) ;
#36800=CARTESIAN_POINT ( 'NONE',  ( 2.603767063935397472E-05, -0.4515708911803948955, 0.03326049213652611247 ) ) ;
#36802=CARTESIAN_POINT ( 'NONE',  ( 0.0004750592482352814579, -0.4386115460793976739, 0.1457185332388683252 ) ) ;
#36806=ORIENTED_EDGE ( 'NONE', *, *, #34821, .F. ) ;
#36809=DIRECTION ( 'NONE',  ( 0.4999551463232382309, -0.8660512985181127998, 1.639108796198564242E-15 ) ) ;
#36811=CARTESIAN_POINT ( 'NONE',  ( 0.001165796508395512297, -0.5811892146192374486, 0.02646226458924476332 ) ) ;
#36813=EDGE_LOOP ( 'NONE', ( #26208, #37807, #31382, #17850, #18927, #37078, #22417, #26030, #30525 ) ) ;
#36815=ADVANCED_FACE ( 'NONE', ( #29613 ), #4258, .T. ) ;
#36817=CARTESIAN_POINT ( 'NONE',  ( 0.2756304489896920229, -1.560360415575528403, 0.8591560916848097751 ) ) ;
#36818=CARTESIAN_POINT ( 'NONE',  ( 0.1561163534220291194, -1.247536721834538564, 0.6205000180267052912 ) ) ;
#36819=CARTESIAN_POINT ( 'NONE',  ( 0.6055916563817613785, -1.479479184092913790, 0.5526975506195442867 ) ) ;
#36821=EDGE_CURVE ( 'NONE', #34712, #3822, #35769, .T. ) ;
#36828=CARTESIAN_POINT ( 'NONE',  ( 0.3311676996542577411, -1.172455566505741009, 0.5902003772419670558 ) ) ;
#36830=CARTESIAN_POINT ( 'NONE',  ( 0.3883702057743975145, -1.127429566525099069, 0.8010219123841900712 ) ) ;
#36831=CARTESIAN_POINT ( 'NONE',  ( 0.1863214475076807042, -0.7675427701765082933, 0.04791228833432090856 ) ) ;
#36835=DIRECTION ( 'NONE',  ( 0.5495291984759871351, 0.000000000000000000, 0.8354745118926962810 ) ) ;
#36838=CIRCLE ( 'NONE', #7938, 0.01000000000000002276 ) ;
#36839=CARTESIAN_POINT ( 'NONE',  ( 0.4793488899164102257, -1.661214906270700453, 0.4177417262808786336 ) ) ;
#36840=CARTESIAN_POINT ( 'NONE',  ( 0.4626267559758963643, -1.110960807299395503, 0.5629296282522621153 ) ) ;
#36848=CARTESIAN_POINT ( 'NONE',  ( 0.1576987512544144876, -1.257723164589890308, 0.9396174402501648038 ) ) ;
#36849=CARTESIAN_POINT ( 'NONE',  ( 0.04606810292053332284, -1.053385927643326392, 0.7216629152402889158 ) ) ;
#36851=CARTESIAN_POINT ( 'NONE',  ( 0.2954936729740054724, -0.7648845942614268534, 0.6619870385404000857 ) ) ;
#36852=CARTESIAN_POINT ( 'NONE',  ( 0.6901651924715963560, -1.541509145059895447, 0.6010274064238112501 ) ) ;
#36858=CARTESIAN_POINT ( 'NONE',  ( 0.06485312910877945314, -0.9239547295439671792, 0.7816216479469996203 ) ) ;
#36860=CARTESIAN_POINT ( 'NONE',  ( 0.5475335553363155361, -1.432897008145440632, 0.7595943864330529927 ) ) ;
#36865=CARTESIAN_POINT ( 'NONE',  ( 0.2413003582545148740, -0.7023676887333554220, 0.5126316699731913173 ) ) ;
#36868=CARTESIAN_POINT ( 'NONE',  ( 0.2540134399983700608, -0.7317239470612214580, 0.5469083470500127886 ) ) ;
#36870=CIRCLE ( 'NONE', #26378, 0.04749999999977558285 ) ;
#36871=( BOUNDED_SURFACE ( )  B_SPLINE_SURFACE ( 3, 2, ( 
 ( #19229, #37946, #9757 ),
 ( #31771, #3588, #6865 ),
 ( #19441, #31978, #27181 ),
 ( #2072, #29857, #23900 ) ),
 .UNSPECIFIED., .F., .F., .T. ) 
 B_SPLINE_SURFACE_WITH_KNOTS ( ( 4, 4 ),
 ( 3, 3 ),
 ( 0.01585912860563366486, 0.01610830113874010469 ),
 ( 0.000000000000000000, 0.04973070668175570697 ),
 .UNSPECIFIED. ) 
 GEOMETRIC_REPRESENTATION_ITEM ( )  RATIONAL_B_SPLINE_SURFACE ( (
 ( 1.000000000000000000, 0.9852470504322862199, 0.9719614500798579027),
 ( 1.000000000000000000, 0.9852431442513369664, 0.9719540262322374780),
 ( 1.000000000000000000, 0.9852393448778324903, 0.9719468053762871929),
 ( 1.000000000000000000, 0.9852356417021994606, 0.9719397673481035005) ) ) 
 REPRESENTATION_ITEM ( '' )  SURFACE ( )  );
#36881=CARTESIAN_POINT ( 'NONE',  ( 0.1667190806935081038, -0.8308575925635335313, 0.5680044787289236785 ) ) ;
#36882=CARTESIAN_POINT ( 'NONE',  ( 0.3190986850306563594, -1.698610481730714161, 0.8469447252347735988 ) ) ;
#36883=CARTESIAN_POINT ( 'NONE',  ( 0.3509249258713971198, -1.204199599461771797, 0.8461177908718215956 ) ) ;
#36885=CARTESIAN_POINT ( 'NONE',  ( 0.001991186333074667497, -0.5252647267804683162, 0.1020407222978734763 ) ) ;
#36886=CARTESIAN_POINT ( 'NONE',  ( 0.04680495427436304895, -1.248529868540707355, 0.6559205912289112206 ) ) ;
#36890=CARTESIAN_POINT ( 'NONE',  ( 0.4526194128954861284, -1.133629661972199054, 0.8947919898580423137 ) ) ;
#36896=CARTESIAN_POINT ( 'NONE',  ( 0.3725772820214828807, -1.154817030518550780, 0.4257997613619559085 ) ) ;
#36899=CARTESIAN_POINT ( 'NONE',  ( 0.3233135765761497304, -1.169465760711457358, 0.5638487597746312252 ) ) ;
#36900=CARTESIAN_POINT ( 'NONE',  ( 0.5240142186908230970, -1.141661684775556296, 0.6661746706671649587 ) ) ;
#36909=VERTEX_POINT ( 'NONE', #28158 ) ;
#36913=ORIENTED_EDGE ( 'NONE', *, *, #12809, .T. ) ;
#36915=CARTESIAN_POINT ( 'NONE',  ( 0.01992777578774528394, -0.8806741340087591574, 0.4717011239932006328 ) ) ;
#36916=VERTEX_POINT ( 'NONE', #28350 ) ;
#36920=CARTESIAN_POINT ( 'NONE',  ( 0.7433653656267760201, -1.515745490836327924, 0.5775132586956883696 ) ) ;
#36922=CARTESIAN_POINT ( 'NONE',  ( 0.4616341473221652336, -1.227275536790998878, 0.6274102885783789940 ) ) ;
#36926=DIRECTION ( 'NONE',  ( -0.4999551463232372317, 0.8660512985181134660, -0.000000000000000000 ) ) ;
#36933=VECTOR ( 'NONE', #17709, 39.37007874015748854 ) ;
#36935=CARTESIAN_POINT ( 'NONE',  ( 0.4127843276619986290, -1.589234977166629648, 0.5609238619371352819 ) ) ;
#36941=ORIENTED_EDGE ( 'NONE', *, *, #4728, .F. ) ;
#36943=CARTESIAN_POINT ( 'NONE',  ( 0.1228162980791566161, -0.5684618713961013814, 0.2359394659365706692 ) ) ;
#36944=CARTESIAN_POINT ( 'NONE',  ( 0.4714374192161987498, -1.680212440471048563, 0.4684164612439499775 ) ) ;
#36950=CARTESIAN_POINT ( 'NONE',  ( 0.1905506861939139096, -0.5145941129025596306, 0.2257199139534598609 ) ) ;
#36952=DIRECTION ( 'NONE',  ( 0.8660512985181134660, 0.4999551463232371762, 0.000000000000000000 ) ) ;
#36958=CARTESIAN_POINT ( 'NONE',  ( 0.6011193747858227798, -1.595581932925101976, 0.4276689662439276396 ) ) ;
#36963=CARTESIAN_POINT ( 'NONE',  ( 0.5003942916249191075, -1.540239132408833589, 0.5630373515401332352 ) ) ;
#36966=B_SPLINE_SURFACE_WITH_KNOTS ( 'NONE', 3, 1, ( 
 ( #10300, #35382 ),
 ( #19739, #29208 ),
 ( #1070, #26145 ),
 ( #38659, #10479 ),
 ( #23045, #35571 ),
 ( #16872, #10681 ),
 ( #667, #30255 ),
 ( #2087, #33538 ),
 ( #32942, #10957 ),
 ( #17318, #7837 ) ),
 .UNSPECIFIED., .F., .F., .F.,
 ( 4, 2, 2, 2, 4 ),
 ( 2, 2 ),
 ( -0.1094769316984412211, 0.2500000000000000000, 0.5000000000000000000, 0.7500000000000000000, 0.9999999728204846949 ),
 ( 0.000000000000000000, 1.000000000000000000 ),
 .UNSPECIFIED. ) ;
#36971=CYLINDRICAL_SURFACE ( 'NONE', #29625, 0.09249999999977555343 ) ;
#36973=CARTESIAN_POINT ( 'NONE',  ( 0.4639166846825588664, -1.238161140430742213, 0.7208849079774189983 ) ) ;
#36976=CARTESIAN_POINT ( 'NONE',  ( 0.4793721953524077151, -1.080656662118478328, 0.6419491832934718367 ) ) ;
#36983=CARTESIAN_POINT ( 'NONE',  ( 0.09209597571042482667, -0.8538668600629184535, 0.7123787990913729162 ) ) ;
#36984=LINE ( 'NONE', #15390, #26992 ) ;
#36985=CARTESIAN_POINT ( 'NONE',  ( 0.1124264983556580860, -0.7955156797634613808, -0.06988970266567862133 ) ) ;
#36989=CARTESIAN_POINT ( 'NONE',  ( 0.5067133256571466626, -1.119665319208750676, 0.6842747717451090894 ) ) ;
#36990=CARTESIAN_POINT ( 'NONE',  ( 0.2241138682733187781, -0.8936256700826709087, 0.7043492929034889105 ) ) ;
#36992=DIRECTION ( 'NONE',  ( 0.8660512985181134660, 0.4999551463232372317, 0.000000000000000000 ) ) ;
#36997=B_SPLINE_CURVE_WITH_KNOTS ( 'NONE', 3,
 ( #15442, #31476, #18516, #22241, #2891, #38049, #3283 ),
 .UNSPECIFIED., .F., .F.,
 ( 4, 3, 4 ),
 ( 0.0001163120317926839576, 0.002539995921006134392, 0.003592109058172289482 ),
 .UNSPECIFIED. ) ;
#37000=CARTESIAN_POINT ( 'NONE',  ( 0.6588957223800396834, -1.564199738096486714, 0.5197417262808792238 ) ) ;
#37004=CARTESIAN_POINT ( 'NONE',  ( 0.05992090360963521489, -1.332693131100006978, 0.5682417262808777680 ) ) ;
#37006=CARTESIAN_POINT ( 'NONE',  ( 0.4573173800065648553, -1.135161403414604475, 0.4529988214013289660 ) ) ;
#37007=CARTESIAN_POINT ( 'NONE',  ( 0.3911537912183811194, -1.142124775201903475, 0.5563430366993925569 ) ) ;
#37009=CARTESIAN_POINT ( 'NONE',  ( 0.0004467655297966004256, -0.4383329269132242856, 0.1340609614503255331 ) ) ;
#37010=CARTESIAN_POINT ( 'NONE',  ( 0.3410366399252441338, -1.752216166167418043, 0.4548429336037024817 ) ) ;
#37019=ORIENTED_EDGE ( 'NONE', *, *, #19527, .F. ) ;
#37022=CARTESIAN_POINT ( 'NONE',  ( 0.001435883076814227933, -0.5530114004245914039, 0.04489778311629699648 ) ) ;
#37029=EDGE_CURVE ( 'NONE', #1394, #35264, #3128, .T. ) ;
#37030=CARTESIAN_POINT ( 'NONE',  ( 0.1207393138600422744, -1.069125492563510971, 0.8673586701997172410 ) ) ;
#37031=CARTESIAN_POINT ( 'NONE',  ( 0.4309855169775498873, -1.223829803323659426, 0.6254704992157742449 ) ) ;
#37032=CARTESIAN_POINT ( 'NONE',  ( 0.1438553286746209747, -1.251795828929518128, 0.6227151430034421065 ) ) ;
#37039=CARTESIAN_POINT ( 'NONE',  ( 0.3381111732067393350, -1.163545670492880157, 0.6012525635317799155 ) ) ;
#37042=CARTESIAN_POINT ( 'NONE',  ( 0.3202918194079290015, -1.024799612382053970, 0.7687582342706213989 ) ) ;
#37044=CARTESIAN_POINT ( 'NONE',  ( 0.2644847879712617367, -1.601187613148850719, 0.8339127871527183267 ) ) ;
#37046=CARTESIAN_POINT ( 'NONE',  ( 0.08970986014245081741, -0.8451374409715517455, 0.8410174406224033561 ) ) ;
#37050=DIRECTION ( 'NONE',  ( 0.9848077530122080203, -0.1736481776669303589, 4.095352323445923521E-18 ) ) ;
#37051=CARTESIAN_POINT ( 'NONE',  ( 0.3927915226382389657, -1.715293516864650147, 0.5707417262808793801 ) ) ;
#37053=CARTESIAN_POINT ( 'NONE',  ( 0.4427491432746096800, -1.107282895871583905, 0.5823651115457876282 ) ) ;
#37054=DIRECTION ( 'NONE',  ( 0.4999551463232372317, -0.8660512985181135770, 0.000000000000000000 ) ) ;
#37057=CARTESIAN_POINT ( 'NONE',  ( 0.2510700677566410910, -1.656657411791499168, 0.6264822711378978948 ) ) ;
#37058=CARTESIAN_POINT ( 'NONE',  ( 0.03787118657716118109, -1.016424498358915018, 0.6950631583489912391 ) ) ;
#37059=EDGE_CURVE ( 'NONE', #22890, #799, #13487, .T. ) ;
#37061=CARTESIAN_POINT ( 'NONE',  ( 0.4715326458378593655, -1.065703591122391103, 0.8369151567944118630 ) ) ;
#37063=EDGE_CURVE ( 'NONE', #20753, #9404, #19309, .T. ) ;
#37072=CARTESIAN_POINT ( 'NONE',  ( 0.2215769352394466596, -1.475921142408890496, 0.9227110526898859577 ) ) ;
#37074=CARTESIAN_POINT ( 'NONE',  ( 0.5879633267048641754, -1.491232175459922038, 0.5739096314268175014 ) ) ;
#37077=CARTESIAN_POINT ( 'NONE',  ( 0.6182635900321699074, -1.298039841913932513, 0.5932631914600888789 ) ) ;
#37078=ORIENTED_EDGE ( 'NONE', *, *, #34821, .T. ) ;
#37082=VECTOR ( 'NONE', #3431, 39.37007874015748143 ) ;
#37088=ORIENTED_EDGE ( 'NONE', *, *, #4697, .F. ) ;
#37089=CARTESIAN_POINT ( 'NONE',  ( 0.1385871437811476981, -0.7804196182993179409, 0.5000907977187665221 ) ) ;
#37092=CARTESIAN_POINT ( 'NONE',  ( 0.1074718422060760153, -0.5843318630099050282, 0.2896000563418689722 ) ) ;
#37095=CARTESIAN_POINT ( 'NONE',  ( 0.02732781149695911321, -1.123547693055224173, 0.6558377280348957061 ) ) ;
#37097=ORIENTED_EDGE ( 'NONE', *, *, #18734, .T. ) ;
#37099=CARTESIAN_POINT ( 'NONE',  ( 0.5000143371095003841, -1.114760706755517639, 0.8117732093188116949 ) ) ;
#37108=CARTESIAN_POINT ( 'NONE',  ( 0.3415936387057808554, -1.158750661784961444, 0.4480089712593383622 ) ) ;
#37109=B_SPLINE_CURVE_WITH_KNOTS ( 'NONE', 3,
 ( #34521, #12708, #25890, #3662 ),
 .UNSPECIFIED., .F., .F.,
 ( 4, 4 ),
 ( 0.0005090742087139675347, 0.0009526417881629593246 ),
 .UNSPECIFIED. ) ;
#37110=CARTESIAN_POINT ( 'NONE',  ( 0.5214254866212318928, -1.138125297403113523, 0.6686424646332703725 ) ) ;
#37116=EDGE_CURVE ( 'NONE', #13556, #13794, #18282, .T. ) ;
#37122=( BOUNDED_SURFACE ( )  B_SPLINE_SURFACE ( 3, 2, ( 
 ( #37302, #11618, #18183 ),
 ( #27856, #28065, #14898 ),
 ( #9115, #20886, #18591 ),
 ( #34016, #34210, #11801 ),
 ( #30320, #2963, #36896 ),
 ( #5818, #14689, #8707 ) ),
 .UNSPECIFIED., .F., .F., .F. ) 
 B_SPLINE_SURFACE_WITH_KNOTS ( ( 4, 2, 4 ),
 ( 3, 3 ),
 ( -1.019150042136374168E-17, 0.0004951616201126806446, 0.0009903232402253714806 ),
 ( 0.000000000000000000, 1.000000000000000000 ),
 .UNSPECIFIED. ) 
 GEOMETRIC_REPRESENTATION_ITEM ( )  RATIONAL_B_SPLINE_SURFACE ( (
 ( 1.000000000000000000, 0.8170441014560104742, 1.000000000000000000),
 ( 1.000000000000000000, 0.8306458315206579623, 1.000000000000000000),
 ( 1.000000000000000000, 0.8330947640617497596, 1.000000000000000000),
 ( 1.000000000000000000, 0.8126093788735454515, 1.000000000000000000),
 ( 1.000000000000000000, 0.7896249599902737115, 1.000000000000000000),
 ( 1.000000000000000000, 0.7525568848367778507, 1.000000000000000000) ) ) 
 REPRESENTATION_ITEM ( '' )  SURFACE ( )  );
#37124=CARTESIAN_POINT ( 'NONE',  ( 0.4564781620595781408, -1.137377641396571937, 0.4472515671891064692 ) ) ;
#37128=CARTESIAN_POINT ( 'NONE',  ( 0.05817917803143683037, -1.018161828248461021, 0.7083252315212340555 ) ) ;
#37140=DIRECTION ( 'NONE',  ( 0.8660512985181134660, 0.4999551463232372317, 0.000000000000000000 ) ) ;
#37142=EDGE_CURVE ( 'NONE', #21612, #24566, #24022, .T. ) ;
#37147=CARTESIAN_POINT ( 'NONE',  ( 0.06872051704080016366, -0.6086765721664342266, 0.3652306837808803053 ) ) ;
#37149=CARTESIAN_POINT ( 'NONE',  ( 0.5717393591038858469, -1.612291461392513003, 0.4730418959724068673 ) ) ;
#37156=CARTESIAN_POINT ( 'NONE',  ( 0.1901246552320745298, -0.7774690835213511342, 0.5910184091100809667 ) ) ;
#37158=CARTESIAN_POINT ( 'NONE',  ( 0.4796114828161345267, -1.675628263522580763, 0.4877750351082724700 ) ) ;
#37164=CARTESIAN_POINT ( 'NONE',  ( 0.3043431798205027405, -0.7811398438223191576, 0.6771279187310788039 ) ) ;
#37166=CARTESIAN_POINT ( 'NONE',  ( 0.01534025463952351682, -0.9720854558541353052, 0.4214751749065498987 ) ) ;
#37172=CARTESIAN_POINT ( 'NONE',  ( 0.2645503737337568939, -1.676379442750866477, 0.5604219075278777940 ) ) ;
#37175=ORIENTED_EDGE ( 'NONE', *, *, #13037, .T. ) ;
#37177=CARTESIAN_POINT ( 'NONE',  ( 0.4676789493019616883, -1.559177855287317005, 0.5735223705611400824 ) ) ;
#37178=CARTESIAN_POINT ( 'NONE',  ( 0.6531517882810622400, -1.470370464788490317, 0.4182417262808778013 ) ) ;
#37183=FACE_OUTER_BOUND ( 'NONE', #16938, .T. ) ;
#37184=CARTESIAN_POINT ( 'NONE',  ( 0.4076976354719484830, -1.154888438488558267, 0.4282417262808775882 ) ) ;
#37185=EDGE_CURVE ( 'NONE', #27340, #14, #35985, .T. ) ;
#37187=CARTESIAN_POINT ( 'NONE',  ( 0.4942211817909919480, -1.285256733056542977, 0.7126200490527264675 ) ) ;
#37191=CARTESIAN_POINT ( 'NONE',  ( 0.2179926414509053834, -0.8923039640295803432, 0.4033837261968737375 ) ) ;
#37197=CARTESIAN_POINT ( 'NONE',  ( 0.03719017515162942322, -0.5647721775443517167, 0.2719657506221234144 ) ) ;
#37198=CARTESIAN_POINT ( 'NONE',  ( 0.06444297064315794576, -0.8352831487901670737, 0.1457185332388703236 ) ) ;
#37199=CARTESIAN_POINT ( 'NONE',  ( 0.1758095078217830343, -0.7034033841566151857, -0.08419028408879647429 ) ) ;
#37203=CARTESIAN_POINT ( 'NONE',  ( 0.2813884797296905549, -1.026807924004586647, 0.6132444993518527676 ) ) ;
#37204=CARTESIAN_POINT ( 'NONE',  ( 0.5527745311540036566, -1.511132050481931222, 0.5694627077227574219 ) ) ;
#37207=DIRECTION ( 'NONE',  ( 0.8660512985181129109, 0.4999551463232381199, 0.000000000000000000 ) ) ;
#37209=LINE ( 'NONE', #21393, #40206 ) ;
#37213=CARTESIAN_POINT ( 'NONE',  ( 0.4211285406421715893, -1.688829255868648405, 0.4182417262808776903 ) ) ;
#37214=CARTESIAN_POINT ( 'NONE',  ( 0.4815360835401190087, -1.665003689908300277, 0.5707417262808793801 ) ) ;
#37217=CARTESIAN_POINT ( 'NONE',  ( 0.02666925540767700956, -1.119321828221852888, 0.6528166539191706530 ) ) ;
#37221=CARTESIAN_POINT ( 'NONE',  ( 0.4787236986780760151, -1.118179508398265742, 0.5519777869597309872 ) ) ;
#37222=CARTESIAN_POINT ( 'NONE',  ( 0.5245687263101824760, -1.202970462303446952, 0.6057417262809816627 ) ) ;
#37224=CARTESIAN_POINT ( 'NONE',  ( 0.04935217837593552231, -1.087446678362770758, 0.7326706496891072229 ) ) ;
#37226=CARTESIAN_POINT ( 'NONE',  ( 0.3088664963667261398, -1.757905065063135597, 0.5295467280985148850 ) ) ;
#37228=CARTESIAN_POINT ( 'NONE',  ( 0.3434711319545313835, -1.169169302084733797, 0.4182417262808776903 ) ) ;
#37237=DIRECTION ( 'NONE',  ( 0.4999551463232372317, -0.8660512985181134660, 0.000000000000000000 ) ) ;
#37238=VERTEX_POINT ( 'NONE', #1609 ) ;
#37242=ORIENTED_EDGE ( 'NONE', *, *, #33421, .T. ) ;
#37243=CARTESIAN_POINT ( 'NONE',  ( 0.2696218657953411424, -1.674929051967658733, 0.6230054160990766698 ) ) ;
#37244=CARTESIAN_POINT ( 'NONE',  ( 0.1810495352127157176, -0.9167129548756171031, 0.6179360156744274635 ) ) ;
#37245=CARTESIAN_POINT ( 'NONE',  ( 0.08514104884741639789, -1.317777977354982921, 0.5631554082348806389 ) ) ;
#37251=CARTESIAN_POINT ( 'NONE',  ( 0.3631141027881771288, -1.729552718906028685, 0.4270090698524765527 ) ) ;
#37252=CARTESIAN_POINT ( 'NONE',  ( 0.4751248519516730884, -1.681100737592190031, 0.5628962907142390781 ) ) ;
#37253=CARTESIAN_POINT ( 'NONE',  ( 0.5049385406414879096, -1.338700766536453202, 0.8051606239926210051 ) ) ;
#37255=CARTESIAN_POINT ( 'NONE',  ( 0.2481470555835709191, -1.538569375340287371, 0.8889987892862927232 ) ) ;
#37256=CARTESIAN_POINT ( 'NONE',  ( 0.3157029859671476313, -1.681686951297227894, 0.8731147540620630698 ) ) ;
#37259=CARTESIAN_POINT ( 'NONE',  ( 0.3914506609052950670, -1.712970798409825690, 0.5197417262808792238 ) ) ;
#37260=CARTESIAN_POINT ( 'NONE',  ( 0.3336325236675090067, -1.050835064020409160, 0.7593003920438236021 ) ) ;
#37263=CARTESIAN_POINT ( 'NONE',  ( 0.5953197980378833742, -1.599064723402610300, 0.4311035055375501135 ) ) ;
#37264=CARTESIAN_POINT ( 'NONE',  ( 0.003142067210302413628, -0.5716151664902620055, 0.1991251360516817781 ) ) ;
#37265=CARTESIAN_POINT ( 'NONE',  ( 0.06216260169285257875, -1.138180230654762815, 0.7527527421364956783 ) ) ;
#37267=CARTESIAN_POINT ( 'NONE',  ( 0.2232487200984690223, -0.6189500806901601093, 0.4773341886849224447 ) ) ;
#37272=CARTESIAN_POINT ( 'NONE',  ( 0.2601188121435625278, -1.607439648646116215, 0.8467017527915076114 ) ) ;
#37273=CARTESIAN_POINT ( 'NONE',  ( 0.1286200154133211038, -0.5674997884473316212, 0.2294314527738028076 ) ) ;
#37276=CARTESIAN_POINT ( 'NONE',  ( 0.5392338747517343434, -1.163405467613477295, 0.6464276897500325081 ) ) ;
#37279=CARTESIAN_POINT ( 'NONE',  ( 0.6498155928403246406, -1.464591312738813267, 0.4182417262808778013 ) ) ;
#37286=CARTESIAN_POINT ( 'NONE',  ( 0.08735497562171311292, -0.7263075606618498714, 0.2000283160256591530 ) ) ;
#37289=CARTESIAN_POINT ( 'NONE',  ( 0.3083686665179578568, -1.758089317276438024, 0.6134063284622075507 ) ) ;
#37290=CARTESIAN_POINT ( 'NONE',  ( 0.5247960161509089838, -1.526737019399793116, 0.5659639212617542103 ) ) ;
#37291=CARTESIAN_POINT ( 'NONE',  ( 0.3454273455000012594, -1.756874669286808466, 0.4564301676634069937 ) ) ;
#37292=CARTESIAN_POINT ( 'NONE',  ( 0.06953952643797545186, -1.315567610428153511, 0.5260635157698690945 ) ) ;
#37293=CARTESIAN_POINT ( 'NONE',  ( 0.08520462220341532000, -1.252311161969172026, 0.6441909309935092143 ) ) ;
#37295=EDGE_CURVE ( 'NONE', #8335, #35903, #21378, .T. ) ;
#37296=CARTESIAN_POINT ( 'NONE',  ( 0.4601907590469310194, -1.690464365935532731, 0.5857309660096694515 ) ) ;
#37297=CARTESIAN_POINT ( 'NONE',  ( 0.5662013050271856862, -1.332134377766191147, 0.8879307549162257507 ) ) ;
#37302=CARTESIAN_POINT ( 'NONE',  ( 0.4076976354719481499, -1.154888438488558711, 0.4182417262808778013 ) ) ;
#37304=CARTESIAN_POINT ( 'NONE',  ( 0.3116101662948007611, -1.187661518757025192, 0.5454230041139144225 ) ) ;
#37305=CARTESIAN_POINT ( 'NONE',  ( 0.4504611332311936889, -1.053473412190887304, 0.6915920958210214353 ) ) ;
#37312=CARTESIAN_POINT ( 'NONE',  ( 0.5611986379937768943, -1.505946779369399025, 0.5603673003229301397 ) ) ;
#37318=CARTESIAN_POINT ( 'NONE',  ( 0.1022213135577672433, -0.8207663499021961018, 0.3585070046201188076 ) ) ;
#37321=CARTESIAN_POINT ( 'NONE',  ( 0.02220665151295753842, -1.035819085711241039, 0.7188228406368177836 ) ) ;
#37327=CARTESIAN_POINT ( 'NONE',  ( 0.7346172259536333238, -1.494169854247700657, 0.6985599367358283907 ) ) ;
#37331=CARTESIAN_POINT ( 'NONE',  ( 0.2284780739230824753, -1.350302979228993117, 0.5370935808337153894 ) ) ;
#37334=CARTESIAN_POINT ( 'NONE',  ( 0.1191520103465610603, -0.6496890496031613171, 0.4527207694524171822 ) ) ;
#37338=CARTESIAN_POINT ( 'NONE',  ( 0.09827287832808975776, -0.6772034054173794448, 0.4837373503272690001 ) ) ;
#37340=CARTESIAN_POINT ( 'NONE',  ( 0.5618478858959879974, -1.618700185366941824, 0.5182094704982558309 ) ) ;
#37347=CARTESIAN_POINT ( 'NONE',  ( 0.4273369639566782507, -1.239477052644316624, 0.8278212302127097022 ) ) ;
#37348=CARTESIAN_POINT ( 'NONE',  ( 0.4875656111780362068, -1.659925035319771203, 0.5079328609705456854 ) ) ;
#37354=CARTESIAN_POINT ( 'NONE',  ( 0.2079659131559265517, -1.247001267129989710, 0.4467898267690011416 ) ) ;
#37355=CARTESIAN_POINT ( 'NONE',  ( 0.5877184641988779656, -1.252861897328551022, 0.8491679911058225283 ) ) ;
#37356=( BOUNDED_SURFACE ( )  B_SPLINE_SURFACE ( 3, 2, ( 
 ( #32543, #29466, #13816 ),
 ( #26387, #35842, #38914 ),
 ( #10745, #17116, #1508 ),
 ( #14023, #10961, #23522 ) ),
 .UNSPECIFIED., .F., .F., .F. ) 
 B_SPLINE_SURFACE_WITH_KNOTS ( ( 4, 4 ),
 ( 3, 3 ),
 ( 1.516581998872723602E-15, 0.0009752704012298402374 ),
 ( 0.000000000000000000, 1.000000000000000000 ),
 .UNSPECIFIED. ) 
 GEOMETRIC_REPRESENTATION_ITEM ( )  RATIONAL_B_SPLINE_SURFACE ( (
 ( 1.000000000000000000, 0.7101913118074566489, 1.000000000000000000),
 ( 1.000000000000000000, 0.7878845071931158683, 1.000000000000000000),
 ( 1.000000000000000000, 0.8401241550276493664, 1.000000000000000000),
 ( 1.000000000000000000, 0.8671479162383957107, 1.000000000000000000) ) ) 
 REPRESENTATION_ITEM ( '' )  SURFACE ( )  );
#37358=EDGE_CURVE ( 'NONE', #5090, #3536, #22747, .T. ) ;
#37359=CARTESIAN_POINT ( 'NONE',  ( 0.01207181549175943662, -0.9514910684014844522, 0.2846013046921853640 ) ) ;
#37362=CARTESIAN_POINT ( 'NONE',  ( 0.09705974031108312305, -0.8384972796398091344, 0.3241563970570177089 ) ) ;
#37363=CARTESIAN_POINT ( 'NONE',  ( 0.2616322387702281205, -1.678013124025769187, 0.5382687897764735219 ) ) ;
#37366=DIRECTION ( 'NONE',  ( 0.4908277074234744797, -0.8712566565745227809, 0.000000000000000000 ) ) ;
#37368=CARTESIAN_POINT ( 'NONE',  ( 0.6542814889465385919, -1.462066692984673288, 0.4182417262808777458 ) ) ;
#37373=CARTESIAN_POINT ( 'NONE',  ( 0.3782063182305618887, -1.143311561251338260, 0.6049062659591731839 ) ) ;
#37376=CARTESIAN_POINT ( 'NONE',  ( 0.3862339994230782336, -1.129766223146394299, 0.7432368964524667110 ) ) ;
#37379=CARTESIAN_POINT ( 'NONE',  ( 0.2007793764868952557, -0.8804627652107338553, 0.3298308470297674488 ) ) ;
#37382=CARTESIAN_POINT ( 'NONE',  ( 0.1014787326204109191, -1.381130074647918482, 0.6548904690729412392 ) ) ;
#37386=CARTESIAN_POINT ( 'NONE',  ( 0.04318205873092141600, -0.6066656042371337820, 0.3720294104896150755 ) ) ;
#37388=CARTESIAN_POINT ( 'NONE',  ( 0.1849751083739534507, -0.8214528691028653018, 0.04641342327598888678 ) ) ;
#37394=CARTESIAN_POINT ( 'NONE',  ( 0.4724925770889458754, -1.066128429548910628, 0.6254527518579948708 ) ) ;
#37395=CARTESIAN_POINT ( 'NONE',  ( 0.1549538013712574436, -0.7259076401328894423, 0.5372629092130595252 ) ) ;
#37402=CARTESIAN_POINT ( 'NONE',  ( 0.4173132459375147874, -1.699444977922919042, 0.4182417262808778013 ) ) ;
#37407=CARTESIAN_POINT ( 'NONE',  ( 1.365923996832131609E-16, -0.9481888444201345134, 0.1139263443108001761 ) ) ;
#37409=EDGE_CURVE ( 'NONE', #27730, #12740, #28121, .T. ) ;
#37410=CARTESIAN_POINT ( 'NONE',  ( 0.1916709472725509622, -0.9174159909098704713, 0.2459055916410233245 ) ) ;
#37412=CARTESIAN_POINT ( 'NONE',  ( 0.4690336016591764023, -1.116275788733601004, 0.5587719650776661329 ) ) ;
#37413=DIRECTION ( 'NONE',  ( 0.8660512985181134660, 0.4999551463232372317, 0.000000000000000000 ) ) ;
#37415=CARTESIAN_POINT ( 'NONE',  ( 0.1235390412447300995, -1.439500955437662766, 0.5982358349985300583 ) ) ;
#37422=ORIENTED_EDGE ( 'NONE', *, *, #36610, .T. ) ;
#37425=CARTESIAN_POINT ( 'NONE',  ( 0.5547482201398101775, -1.386539788442228582, 0.7573865583411005797 ) ) ;
#37427=B_SPLINE_CURVE_WITH_KNOTS ( 'NONE', 3,
 ( #39009, #26882, #39227, #23199, #29362, #13525, #1595, #19892, #23804, #7535, #4446, #7742, #10845, #39414, #36121, #10426, #11232, #17008 ),
 .UNSPECIFIED., .F., .F.,
 ( 4, 2, 2, 2, 2, 2, 2, 2, 4 ),
 ( 5.275955480050202716E-18, 0.0003722442517452602536, 0.0007444885034905153031, 0.001116732755235770244, 0.001488977006981025185, 0.001861221258726280126, 0.002233465510471535284, 0.002605709762216790008, 0.002977954013962045166 ),
 .UNSPECIFIED. ) ;
#37432=CARTESIAN_POINT ( 'NONE',  ( 0.2484999103478700566, -1.477039049371299040, 0.9074785348539847751 ) ) ;
#37434=CARTESIAN_POINT ( 'NONE',  ( 0.1089099196686046794, -1.297471296687298326, 0.5942357276382801423 ) ) ;
#37435=CARTESIAN_POINT ( 'NONE',  ( 0.3840418824211426774, -1.145968873474952909, 0.4818701983608400519 ) ) ;
#37437=ADVANCED_FACE ( 'NONE', ( #17121 ), #25301, .T. ) ;
#37438=CARTESIAN_POINT ( 'NONE',  ( 0.4042633028792979033, -1.711240744073928122, 0.4220515681607882597 ) ) ;
#37439=ORIENTED_EDGE ( 'NONE', *, *, #23986, .F. ) ;
#37440=VERTEX_POINT ( 'NONE', #11152 ) ;
#37441=EDGE_CURVE ( 'NONE', #528, #40154, #9968, .T. ) ;
#37443=CARTESIAN_POINT ( 'NONE',  ( 0.3453377680719366127, -1.749458763706788433, 0.4498113177181519151 ) ) ;
#37445=CARTESIAN_POINT ( 'NONE',  ( 0.3891419541809565952, -1.130175006036680641, 0.7851655795637670909 ) ) ;
#37446=CARTESIAN_POINT ( 'NONE',  ( 0.6985364634159124675, -1.438850461896725275, 0.5682400285031795617 ) ) ;
#37448=CARTESIAN_POINT ( 'NONE',  ( 0.01327203635574252319, -0.4607175675008980398, 0.2958762723741367728 ) ) ;
#37450=CARTESIAN_POINT ( 'NONE',  ( 0.7472913949145145729, -1.513305546476923613, 0.4177417262808786336 ) ) ;
#37456=CARTESIAN_POINT ( 'NONE',  ( 0.000000000000000000, -0.4262518876079541830, 0.1457185332388682419 ) ) ;
#37457=CARTESIAN_POINT ( 'NONE',  ( 0.09217733281014239832, -1.307048935866454098, 0.7302822141201406048 ) ) ;
#37459=CARTESIAN_POINT ( 'NONE',  ( 0.3679852976493193095, -0.8933044249262621639, 0.7616870389678419562 ) ) ;
#37462=CARTESIAN_POINT ( 'NONE',  ( 0.3453377680719361131, -1.749458763706787545, 0.4498113177181523037 ) ) ;
#37466=CARTESIAN_POINT ( 'NONE',  ( 0.2629916659223787145, -1.620021443655322857, 0.8311813128113193505 ) ) ;
#37467=CARTESIAN_POINT ( 'NONE',  ( 0.5949976145935880201, -1.487201548628922954, 0.5742703033084610720 ) ) ;
#37470=CARTESIAN_POINT ( 'NONE',  ( 0.1874999999999996669, -0.6872203660140437931, 0.1457185332388695742 ) ) ;
#37480=CARTESIAN_POINT ( 'NONE',  ( 0.1145648225167921752, -0.8006048646630788967, 0.4136033892511831733 ) ) ;
#37483=CARTESIAN_POINT ( 'NONE',  ( 0.4182384646632246183, -1.335901635285643207, 0.8423281896759605702 ) ) ;
#37489=CARTESIAN_POINT ( 'NONE',  ( 0.7441752718225284058, -1.515794030150653837, 0.5954587793138176322 ) ) ;
#37490=CARTESIAN_POINT ( 'NONE',  ( 0.1135262681040088983, -1.415870350120112864, 0.5684114953092351818 ) ) ;
#37492=CARTESIAN_POINT ( 'NONE',  ( 0.2318589737339854795, -1.232498520698479982, 0.5197417262808780025 ) ) ;
#37493=B_SPLINE_CURVE_WITH_KNOTS ( 'NONE', 3,
 ( #24810, #5657, #24603, #15542, #11829, #40006 ),
 .UNSPECIFIED., .F., .F.,
 ( 4, 2, 4 ),
 ( 0.000000000000000000, 0.5000000000000000000, 1.000000000000000000 ),
 .UNSPECIFIED. ) ;
#37495=CARTESIAN_POINT ( 'NONE',  ( 0.08096179802327445330, -1.367098532309424685, 0.5880770290185818316 ) ) ;
#37496=CARTESIAN_POINT ( 'NONE',  ( 0.5265921910155209051, -1.145228776028037521, 0.6635139613180396356 ) ) ;
#37500=CARTESIAN_POINT ( 'NONE',  ( 0.3920817863706622663, -1.709816463946002063, 0.4185791750296219416 ) ) ;
#37503=ORIENTED_EDGE ( 'NONE', *, *, #30529, .T. ) ;
#37507=B_SPLINE_CURVE_WITH_KNOTS ( 'NONE', 3,
 ( #21958, #15970, #16372, #393, #18870, #12891, #6692, #19472, #35300, #31809, #37979, #22777, #19269, #777, #9789, #3624, #13084, #25640, #38171, #29119 ),
 .UNSPECIFIED., .F., .F.,
 ( 4, 2, 2, 2, 2, 2, 2, 2, 2, 4 ),
 ( 0.000000000000000000, 0.0006479730685966644116, 0.001295946137193328823, 0.002591892274386650707, 0.003239865342983302109, 0.003563851877281627809, 0.003887838411579953943, 0.004211824945878279644, 0.004535811480176605778, 0.005183784548773252843 ),
 .UNSPECIFIED. ) ;
#37508=CARTESIAN_POINT ( 'NONE',  ( 0.2413666260127980967, -0.9305387420463091530, 0.6820401963294040470 ) ) ;
#37511=CARTESIAN_POINT ( 'NONE',  ( -0.001101659507716951656, -0.9212496868719332044, 0.5732851652631911765 ) ) ;
#37516=CARTESIAN_POINT ( 'NONE',  ( 0.1392976812637733430, -1.285713247446159890, 0.4252422542015512064 ) ) ;
#37520=CARTESIAN_POINT ( 'NONE',  ( 0.4842604987045637799, -1.673939032089394097, 0.5259745941821198922 ) ) ;
#37524=CARTESIAN_POINT ( 'NONE',  ( 0.09435491736042275757, -0.5840496667413408449, 0.2789874680385455163 ) ) ;
#37525=ORIENTED_EDGE ( 'NONE', *, *, #3938, .F. ) ;
#37526=CARTESIAN_POINT ( 'NONE',  ( 0.6902793494311211253, -1.541375760405424566, 0.6008920144000082786 ) ) ;
#37527=CARTESIAN_POINT ( 'NONE',  ( 0.07437268989541760689, -0.5655675014591935446, 0.2541927867883168601 ) ) ;
#37530=CARTESIAN_POINT ( 'NONE',  ( 0.5593818882502148426, -1.619251521524634363, 0.4799587450026789326 ) ) ;
#37532=CARTESIAN_POINT ( 'NONE',  ( 0.1718750000000002776, -0.9178826446108662163, 0.1609973318550534105 ) ) ;
#37535=CARTESIAN_POINT ( 'NONE',  ( 0.1169788285577439829, -1.415237608940837388, 0.5049415650359101448 ) ) ;
#37536=CARTESIAN_POINT ( 'NONE',  ( 0.1887412855916273668, -0.4595320686313604241, 0.1365881794216594058 ) ) ;
#37537=CARTESIAN_POINT ( 'NONE',  ( 0.5809272469664140681, -1.495261656052034871, 0.5735391159125613481 ) ) ;
#37538=CARTESIAN_POINT ( 'NONE',  ( 0.4259795917038463609, -1.695922107943511836, 0.4200542363796885836 ) ) ;
#37543=CARTESIAN_POINT ( 'NONE',  ( 0.2257694031136883717, -1.236620430762222167, 0.5267521799253104264 ) ) ;
#37546=CARTESIAN_POINT ( 'NONE',  ( 0.2321516500765777036, -1.232946919155727183, 0.5425383027153066751 ) ) ;
#37547=CARTESIAN_POINT ( 'NONE',  ( 0.5091714098097919194, -1.126742604313814677, 0.8493738626068785269 ) ) ;
#37549=CARTESIAN_POINT ( 'NONE',  ( 0.06547945893112464000, -1.297457944248764594, 0.6222148637417063144 ) ) ;
#37552=CARTESIAN_POINT ( 'NONE',  ( 0.1737315473343117589, -0.8901614270947242336, 0.5692762810378355631 ) ) ;
#37553=CARTESIAN_POINT ( 'NONE',  ( 0.2660108306589821781, -1.675569572048062561, 0.5682491886492555544 ) ) ;
#37555=EDGE_CURVE ( 'NONE', #18554, #7023, #33165, .T. ) ;
#37558=CARTESIAN_POINT ( 'NONE',  ( 0.4282286496180897628, -1.188361668518445713, 0.7944891104112847824 ) ) ;
#37560=CARTESIAN_POINT ( 'NONE',  ( 0.6665678333534084121, -1.510259890604198407, 0.4229811308471109754 ) ) ;
#37563=CARTESIAN_POINT ( 'NONE',  ( 0.3982365725197472561, -1.726079210701410460, 0.6107553134230500058 ) ) ;
#37569=FACE_BOUND ( 'NONE', #39603, .T. ) ;
#37573=CARTESIAN_POINT ( 'NONE',  ( 0.4540194299641387987, -1.222353591583736687, 0.7124676942563946680 ) ) ;
#37574=DIRECTION ( 'NONE',  ( 0.4999551463232372317, -0.8660512985181134660, 0.000000000000000000 ) ) ;
#37576=CARTESIAN_POINT ( 'NONE',  ( 0.1863616350354748430, -0.8703638341540448353, 0.1952903930469164218 ) ) ;
#37577=ORIENTED_EDGE ( 'NONE', *, *, #510, .T. ) ;
#37582=CARTESIAN_POINT ( 'NONE',  ( 0.3849909235177108591, -1.605527633581090852, 0.5705237664168376632 ) ) ;
#37585=CARTESIAN_POINT ( 'NONE',  ( 0.1748516657612844138, -0.8884282797386773289, 0.03374897621379178286 ) ) ;
#37590=ORIENTED_EDGE ( 'NONE', *, *, #26993, .F. ) ;
#37591=ORIENTED_EDGE ( 'NONE', *, *, #36503, .T. ) ;
#37592=CARTESIAN_POINT ( 'NONE',  ( 0.4347216870940026623, -1.031328747192698625, 0.7169922827082580996 ) ) ;
#37593=CARTESIAN_POINT ( 'NONE',  ( 0.1528991923064401126, -0.7010905126288613509, 0.5001151810244065521 ) ) ;
#37595=CARTESIAN_POINT ( 'NONE',  ( 0.1871790664487952560, -0.7087350574275718129, 0.03072952741108740324 ) ) ;
#37596=PLANE ( 'NONE',  #16073 ) ;
#37609=CARTESIAN_POINT ( 'NONE',  ( 0.4878597496520711285, -1.079924603896147195, 0.5970707234729024648 ) ) ;
#37610=CARTESIAN_POINT ( 'NONE',  ( 0.3121297305841956859, -1.175746190035780403, 0.5106052970165252392 ) ) ;
#37611=CARTESIAN_POINT ( 'NONE',  ( 0.5623208420996907986, -1.181176875011435756, 0.6057417262809816627 ) ) ;
#37612=B_SPLINE_CURVE_WITH_KNOTS ( 'NONE', 3,
 ( #17705, #2081, #33533, #14619, #2300, #27189 ),
 .UNSPECIFIED., .F., .F.,
 ( 4, 2, 4 ),
 ( 0.000000000000000000, 0.0005939623046373305147, 0.001187924609274661029 ),
 .UNSPECIFIED. ) ;
#37616=CARTESIAN_POINT ( 'NONE',  ( 0.1120276941441372132, -1.367097346105948130, 0.7195291715619951400 ) ) ;
#37619=CARTESIAN_POINT ( 'NONE',  ( 0.6747199749832551996, -1.439515243308204795, 0.4672089648579093590 ) ) ;
#37620=CARTESIAN_POINT ( 'NONE',  ( 0.3242889740156271738, -1.641829081526549716, 0.4952036213288416588 ) ) ;
#37625=ORIENTED_EDGE ( 'NONE', *, *, #28513, .T. ) ;
#37628=CIRCLE ( 'NONE', #15316, 0.009999999999999981126 ) ;
#37629=CARTESIAN_POINT ( 'NONE',  ( 0.5749443205740174534, -1.420905134751040855, 0.6314223347319325441 ) ) ;
#37630=FACE_OUTER_BOUND ( 'NONE', #29553, .T. ) ;
#37632=B_SPLINE_CURVE_WITH_KNOTS ( 'NONE', 3,
 ( #34086, #39863, #34499, #9003 ),
 .UNSPECIFIED., .F., .F.,
 ( 4, 4 ),
 ( 0.000000000000000000, 0.001593837860110619521 ),
 .UNSPECIFIED. ) ;
#37637=EDGE_CURVE ( 'NONE', #24607, #356, #34371, .T. ) ;
#37638=CARTESIAN_POINT ( 'NONE',  ( 0.01343172348619905282, -0.5732673182617886720, 0.3074519330991232757 ) ) ;
#37641=CARTESIAN_POINT ( 'NONE',  ( 0.1049266666186983721, -1.284188116108003097, 0.6131522485820786184 ) ) ;
#37642=B_SPLINE_CURVE_WITH_KNOTS ( 'NONE', 3,
 ( #18517, #21433, #9062, #36819 ),
 .UNSPECIFIED., .F., .F.,
 ( 4, 4 ),
 ( -0.0003965198687675489109, 0.0004429401854243748132 ),
 .UNSPECIFIED. ) ;
#37643=CARTESIAN_POINT ( 'NONE',  ( 0.01205285774706865709, -0.4630597876925141021, 0.01601191316080295690 ) ) ;
#37654=CARTESIAN_POINT ( 'NONE',  ( 0.5515293582047056109, -1.419488402371683833, 0.7635374488037771634 ) ) ;
#37658=CARTESIAN_POINT ( 'NONE',  ( 0.2177940209044571529, -1.312915603899528438, 1.030959333779153164 ) ) ;
#37666=CARTESIAN_POINT ( 'NONE',  ( 0.2646723247128293655, -1.687375416948911244, 0.5682417262808783232 ) ) ;
#37667=CARTESIAN_POINT ( 'NONE',  ( 0.05311564377218584709, -1.038294028734484620, 0.7210077450460690152 ) ) ;
#37672=CARTESIAN_POINT ( 'NONE',  ( 0.3338244128917602915, -1.760037155675280518, 0.5632158866801645347 ) ) ;
#37673=CARTESIAN_POINT ( 'NONE',  ( 0.6926962928713769063, -1.550933885067852902, 0.5932296416423278318 ) ) ;
#37679=EDGE_LOOP ( 'NONE', ( #316, #10458, #33325, #24105, #13873 ) ) ;
#37681=CARTESIAN_POINT ( 'NONE',  ( 0.2673801512343003117, -1.641609933369855501, 0.7978219346028294634 ) ) ;
#37682=CARTESIAN_POINT ( 'NONE',  ( 0.1316567728380550195, -0.5516482450355230105, 0.1613228570193817046 ) ) ;
#37683=DIRECTION ( 'NONE',  ( 0.9998941247116546194, -0.01455087607600989881, 0.0001066420868425327849 ) ) ;
#37685=CARTESIAN_POINT ( 'NONE',  ( 0.2322244407957205770, -0.7584751632699872070, 0.4677412183550399005 ) ) ;
#37686=ORIENTED_EDGE ( 'NONE', *, *, #4989, .T. ) ;
#37688=CARTESIAN_POINT ( 'NONE',  ( 0.6104464726719969203, -1.287892560030390099, 0.8054571804883312591 ) ) ;
#37695=CARTESIAN_POINT ( 'NONE',  ( 0.08617281636341815598, -0.7679981000224859189, 0.1929316491008059298 ) ) ;
#37696=CARTESIAN_POINT ( 'NONE',  ( 0.3138383792994305921, -1.724913923476310895, 0.8094178256982638153 ) ) ;
#37698=CARTESIAN_POINT ( 'NONE',  ( 0.5246584051016858208, -1.526692330542510856, 0.5635048083496201343 ) ) ;
#37702=CARTESIAN_POINT ( 'NONE',  ( 0.4347228130698158610, -1.693624708453924876, 0.6021643700774704788 ) ) ;
#37703=CARTESIAN_POINT ( 'NONE',  ( 0.6993589672832161153, -1.438438989639379439, 0.5922646702261220586 ) ) ;
#37705=CARTESIAN_POINT ( 'NONE',  ( 0.5766624839413022618, -1.620837096128123989, 0.5630430456491227753 ) ) ;
#37706=CARTESIAN_POINT ( 'NONE',  ( 0.6090910762621168928, -1.479036187308539807, 0.5740727581542524049 ) ) ;
#37709=CARTESIAN_POINT ( 'NONE',  ( 0.4092450614235220163, -1.131740385117829817, 0.4687417262808780127 ) ) ;
#37712=CARTESIAN_POINT ( 'NONE',  ( 0.5127940875192875669, -1.116701596374397587, 0.5863938561526392812 ) ) ;
#37714=( BOUNDED_SURFACE ( )  B_SPLINE_SURFACE ( 3, 2, ( 
 ( #22208, #37402, #19105 ),
 ( #37213, #30831, #12512 ),
 ( #11900, #15613, #21786 ),
 ( #27551, #2651, #28159 ) ),
 .UNSPECIFIED., .F., .F., .F. ) 
 B_SPLINE_SURFACE_WITH_KNOTS ( ( 4, 4 ),
 ( 3, 3 ),
 ( 1.314703554355922677E-15, 0.0007336933749180589437 ),
 ( 0.000000000000000000, 1.000000000000000000 ),
 .UNSPECIFIED. ) 
 GEOMETRIC_REPRESENTATION_ITEM ( )  RATIONAL_B_SPLINE_SURFACE ( (
 ( 1.000000000000000000, 0.8624897507812552266, 1.000000000000000000),
 ( 1.000000000000000000, 0.8280948711062059431, 1.000000000000000000),
 ( 1.000000000000000000, 0.7730114043998153051, 1.000000000000000000),
 ( 1.000000000000000000, 0.7004196158429182306, 1.000000000000000000) ) ) 
 REPRESENTATION_ITEM ( '' )  SURFACE ( )  );
#37716=VECTOR ( 'NONE', #7066, 39.37007874015748143 ) ;
#37718=ORIENTED_EDGE ( 'NONE', *, *, #22567, .T. ) ;
#37720=CARTESIAN_POINT ( 'NONE',  ( 0.4667682742968850551, -1.559724797038235300, 0.5741068050677242685 ) ) ;
#37724=ORIENTED_EDGE ( 'NONE', *, *, #35417, .F. ) ;
#37725=CARTESIAN_POINT ( 'NONE',  ( 0.4863315821689714880, -1.129918813781339404, 0.4934822903636956193 ) ) ;
#37727=CARTESIAN_POINT ( 'NONE',  ( 0.07318992162220727682, -1.313491455601902613, 0.4675735672926750741 ) ) ;
#37730=CARTESIAN_POINT ( 'NONE',  ( 0.1434010736994648927, -1.283284918233685623, 0.5707417262808780478 ) ) ;
#37732=CARTESIAN_POINT ( 'NONE',  ( 0.09645609262235674275, -1.159589713166229608, 0.7612075701997731425 ) ) ;
#37737=CARTESIAN_POINT ( 'NONE',  ( 0.1185427538159745248, -1.297446678095303563, 0.4322093719855905625 ) ) ;
#37744=CARTESIAN_POINT ( 'NONE',  ( 0.09349442991740078424, -0.6180904650601271033, 0.2586776949927410141 ) ) ;
#37748=CARTESIAN_POINT ( 'NONE',  ( 0.07513757318104685723, -0.5719538737171597775, 0.2718397121403446914 ) ) ;
#37752=CARTESIAN_POINT ( 'NONE',  ( 0.1932155651835060495, -0.9182634696541240871, 0.2611848007271776462 ) ) ;
#37758=CARTESIAN_POINT ( 'NONE',  ( 0.1256422341217116601, -0.5670699205730641568, 0.2299123196654525580 ) ) ;
#37766=CARTESIAN_POINT ( 'NONE',  ( 0.3938123320717736853, -0.9371650893754340794, 0.7866333354397343491 ) ) ;
#37768=CARTESIAN_POINT ( 'NONE',  ( 0.03667004059205163091, -1.157784549275130859, 0.6760954598802072502 ) ) ;
#37771=CARTESIAN_POINT ( 'NONE',  ( 0.1047100132654907034, -0.8222625085212694751, 0.3700008871823666778 ) ) ;
#37773=DIRECTION ( 'NONE',  ( 0.000000000000000000, 1.000000000000000000, 1.566396143878659165E-12 ) ) ;
#37778=FACE_OUTER_BOUND ( 'NONE', #22388, .T. ) ;
#37785=CARTESIAN_POINT ( 'NONE',  ( 0.2592691511196472121, -1.332774616786658761, 0.4676817362816936274 ) ) ;
#37789=CARTESIAN_POINT ( 'NONE',  ( 0.3484262649563198422, -1.078417651898806895, 0.7434214752059845610 ) ) ;
#37793=CARTESIAN_POINT ( 'NONE',  ( 0.4613690144166702201, -1.065390048215762997, 0.6270275320092995042 ) ) ;
#37794=VERTEX_POINT ( 'NONE', #24925 ) ;
#37797=LINE ( 'NONE', #28930, #28321 ) ;
#37799=ORIENTED_EDGE ( 'NONE', *, *, #879, .T. ) ;
#37800=CARTESIAN_POINT ( 'NONE',  ( 0.08048400592800619702, -0.7604391007274543535, 0.6087342011644325535 ) ) ;
#37801=CARTESIAN_POINT ( 'NONE',  ( 0.06534793968408428300, -0.7997581921860751342, 0.04923965712713711251 ) ) ;
#37802=CARTESIAN_POINT ( 'NONE',  ( 0.1756540496027305942, -0.7486115422362458194, -0.07645544523215128119 ) ) ;
#37807=ORIENTED_EDGE ( 'NONE', *, *, #33893, .T. ) ;
#37808=DIRECTION ( 'NONE',  ( 0.4999551463232372317, -0.8660512985181135770, 0.000000000000000000 ) ) ;
#37809=CARTESIAN_POINT ( 'NONE',  ( 0.5678201344545344975, -1.503056767399954863, 0.5929916762886003889 ) ) ;
#37811=CARTESIAN_POINT ( 'NONE',  ( 0.1874213080127691833, -0.6920270397579918464, 0.03916149223782419003 ) ) ;
#37815=CARTESIAN_POINT ( 'NONE',  ( 0.1862096482451259249, -0.7741715863355521643, 0.1916105915568836193 ) ) ;
#37823=FACE_OUTER_BOUND ( 'NONE', #15789, .T. ) ;
#37825=CARTESIAN_POINT ( 'NONE',  ( 0.2135559776035426960, -1.241076878514266513, 0.5839068764539582235 ) ) ;
#37827=CARTESIAN_POINT ( 'NONE',  ( 0.1070962762476720537, -1.392980070899417111, 0.6530324985320268283 ) ) ;
#37830=CARTESIAN_POINT ( 'NONE',  ( 0.2296032268162506162, -0.9382281285954664485, 0.4302797228108481420 ) ) ;
#37832=CARTESIAN_POINT ( 'NONE',  ( 0.5535339714453306748, -1.186249370383523294, 0.6057417262809816627 ) ) ;
#37834=CARTESIAN_POINT ( 'NONE',  ( 0.2640734557584212272, -1.686333136531013466, 0.5670960282305730349 ) ) ;
#37835=EDGE_CURVE ( 'NONE', #12308, #13132, #5511, .T. ) ;
#37837=CARTESIAN_POINT ( 'NONE',  ( 0.04206944528682795420, -1.152159445897246393, 0.6964886360393780507 ) ) ;
#37838=CARTESIAN_POINT ( 'NONE',  ( -0.0002424173180945032727, -0.8751502303707813235, -0.01887031899818753314 ) ) ;
#37841=ORIENTED_EDGE ( 'NONE', *, *, #11565, .F. ) ;
#37847=CARTESIAN_POINT ( 'NONE',  ( 0.4367679725710939542, -1.201179855909204397, 0.8157569126575382468 ) ) ;
#37850=CIRCLE ( 'NONE', #25349, 0.09249999999977555343 ) ;
#37853=CARTESIAN_POINT ( 'NONE',  ( 0.1966708302945472664, -0.7872448539783969412, 0.3093500942271054099 ) ) ;
#37855=CARTESIAN_POINT ( 'NONE',  ( 0.01624379798718045970, -0.5940688689955531121, 0.3554331757638558020 ) ) ;
#37856=CARTESIAN_POINT ( 'NONE',  ( 0.1757454679492159444, -0.9123123364095576671, 0.6095604877834991386 ) ) ;
#37857=CARTESIAN_POINT ( 'NONE',  ( 0.6290530482886385055, -1.474716711548147874, 0.5182417262812423209 ) ) ;
#37860=CARTESIAN_POINT ( 'NONE',  ( 0.1876953789110183679, -0.9196856789278203825, 0.1479976049341028554 ) ) ;
#37866=CARTESIAN_POINT ( 'NONE',  ( 0.1642579856227123214, -0.9583868220818564376, 0.4613279698008625473 ) ) ;
#37869=CARTESIAN_POINT ( 'NONE',  ( 0.5816238657360307540, -1.478355207367950674, 0.6788288349111909481 ) ) ;
#37871=CARTESIAN_POINT ( 'NONE',  ( 0.1805882081786515381, -1.310474468103578038, 0.9369546008279981963 ) ) ;
#37873=CARTESIAN_POINT ( 'NONE',  ( 0.3080248481530759586, -1.647059832894722131, 0.9156036115443938472 ) ) ;
#37881=CARTESIAN_POINT ( 'NONE',  ( 0.3122857990831161556, -1.766572940467653785, 0.5980579735034173838 ) ) ;
#37884=EDGE_CURVE ( 'NONE', #27710, #34692, #16466, .T. ) ;
#37886=B_SPLINE_CURVE_WITH_KNOTS ( 'NONE', 3,
 ( #9045, #38, #9229, #24479 ),
 .UNSPECIFIED., .F., .F.,
 ( 4, 4 ),
 ( 0.000000000000000000, 0.0001096403195332056003 ),
 .UNSPECIFIED. ) ;
#37888=CARTESIAN_POINT ( 'NONE',  ( 0.7053833034112568789, -1.492524922043918734, 0.5185182801802852293 ) ) ;
#37889=CIRCLE ( 'NONE', #20166, 0.04749999999977558285 ) ;
#37890=VERTEX_POINT ( 'NONE', #13591 ) ;
#37894=CARTESIAN_POINT ( 'NONE',  ( 0.1854879680645313555, -1.345035247216854302, 0.9498699178978792235 ) ) ;
#37895=CARTESIAN_POINT ( 'NONE',  ( 0.1327162649517526216, -0.5774347627937225225, 0.2565431035860060716 ) ) ;
#37896=CARTESIAN_POINT ( 'NONE',  ( 0.3725959361440046025, -1.740293560479224011, 0.4320537422923894089 ) ) ;
#37898=ORIENTED_EDGE ( 'NONE', *, *, #26598, .F. ) ;
#37904=CARTESIAN_POINT ( 'NONE',  ( 0.3047942498816851864, -1.756876866921070146, 0.5683792054161904694 ) ) ;
#37907=CARTESIAN_POINT ( 'NONE',  ( 0.08584567903155965185, -0.7460567843300380808, 0.1457185332388686860 ) ) ;
#37910=CARTESIAN_POINT ( 'NONE',  ( 0.5253282373615071332, -1.526886051446876280, 0.5751798715530015427 ) ) ;
#37916=CARTESIAN_POINT ( 'NONE',  ( 0.4574846914228954953, -1.692033587742871381, 0.5885383685939118426 ) ) ;
#37917=CARTESIAN_POINT ( 'NONE',  ( 0.6560342951817995649, -1.361138816048402145, 0.7673092742682359191 ) ) ;
#37919=CARTESIAN_POINT ( 'NONE',  ( 0.6086752090503105839, -1.478944523047028392, 0.5656203117916941414 ) ) ;
#37922=CARTESIAN_POINT ( 'NONE',  ( 0.4093611158985690501, -1.131941421409890403, 0.5197417262808780025 ) ) ;
#37924=CARTESIAN_POINT ( 'NONE',  ( 0.05889106705834949718, -1.326084810051836982, 0.5931655932887337501 ) ) ;
#37925=CARTESIAN_POINT ( 'NONE',  ( 0.5055437690763310288, -1.106959495255247505, 0.6108412925465283028 ) ) ;
#37931=CARTESIAN_POINT ( 'NONE',  ( 0.5377610847061485844, -1.519774373043595972, 0.5731039079555608762 ) ) ;
#37938=CARTESIAN_POINT ( 'NONE',  ( 0.3407574567498363183, -1.752395144162200546, 0.4551695278380876730 ) ) ;
#37939=CARTESIAN_POINT ( 'NONE',  ( 0.0008401815153994757679, -0.9312571135744077688, 0.5924458961409151403 ) ) ;
#37946=CARTESIAN_POINT ( 'NONE',  ( 0.5997906010433834423, -1.596574738763893109, 0.4303942190982675831 ) ) ;
#37951=CARTESIAN_POINT ( 'NONE',  ( 0.01025536129965940943, -0.5346927715679482551, 0.1046735957568519643 ) ) ;
#37953=CARTESIAN_POINT ( 'NONE',  ( 0.1000121428524311934, -0.6364596608959190993, 0.3289196408185624532 ) ) ;
#37955=CARTESIAN_POINT ( 'NONE',  ( 0.0004750028870838371897, -0.4386152171684600254, 0.1457185332388682975 ) ) ;
#37956=CARTESIAN_POINT ( 'NONE',  ( 0.3607945552467097805, -1.331973876078468955, 0.8646488368460186758 ) ) ;
#37965=CARTESIAN_POINT ( 'NONE',  ( 0.3026669703120153376, -1.007674124269388294, 0.7664178669992703918 ) ) ;
#37971=CARTESIAN_POINT ( 'NONE',  ( 0.5154728982652437841, -1.185177693224150008, 0.4436066727502508411 ) ) ;
#37972=CARTESIAN_POINT ( 'NONE',  ( 0.5586414499496984432, -1.205790344466990627, 0.8068181458027993136 ) ) ;
#37973=CARTESIAN_POINT ( 'NONE',  ( 0.5099280420869274355, -1.114989880839767578, 0.5367823920641713320 ) ) ;
#37974=CARTESIAN_POINT ( 'NONE',  ( 0.05800524771820539383, -1.293462930650507214, 0.6434660951334953971 ) ) ;
#37977=CARTESIAN_POINT ( 'NONE',  ( 0.1939270537251513438, -0.9059543765946825866, 0.6046208699968631528 ) ) ;
#37979=CARTESIAN_POINT ( 'NONE',  ( 0.6862067491206771397, -1.510281502546922949, 0.4567439642065846406 ) ) ;
#37982=CARTESIAN_POINT ( 'NONE',  ( 0.1977209903153200055, -0.8506692363503495224, 0.6350317236410694122 ) ) ;
#37983=CARTESIAN_POINT ( 'NONE',  ( 0.6584301049649089466, -1.489287037793245227, 0.4182417262808776903 ) ) ;
#37986=CARTESIAN_POINT ( 'NONE',  ( 0.3874608430265089609, -1.108326039081300785, 0.6051049422084413543 ) ) ;
#37989=CARTESIAN_POINT ( 'NONE',  ( 0.3315018707368336259, -1.291415966887107247, 0.5178325263893220898 ) ) ;
#37992=CARTESIAN_POINT ( 'NONE',  ( 0.4258910459772873858, -1.183759126590261168, 0.7367376598851150815 ) ) ;
#37995=CARTESIAN_POINT ( 'NONE',  ( 0.4083208966368579995, -1.036284369767852764, 0.6331064141399478373 ) ) ;
#37999=CARTESIAN_POINT ( 'NONE',  ( 0.09498762465003944555, -1.342648412413370407, 0.6966705301549200868 ) ) ;
#38001=EDGE_LOOP ( 'NONE', ( #35320, #29042, #14733, #33613 ) ) ;
#38002=CARTESIAN_POINT ( 'NONE',  ( 0.3036885249178302715, -1.390984769928044651, 0.8913742401028124096 ) ) ;
#38004=CARTESIAN_POINT ( 'NONE',  ( 0.1996428621479708065, -0.6036337479795305105, 0.3287165209465360283 ) ) ;
#38005=CARTESIAN_POINT ( 'NONE',  ( 0.6001884367015531963, -1.607799423540326567, 0.4311405334566375536 ) ) ;
#38007=VERTEX_POINT ( 'NONE', #5524 ) ;
#38010=CARTESIAN_POINT ( 'NONE',  ( 0.1181822409742579877, -0.5775493957728874417, 0.2649829690098590707 ) ) ;
#38012=CARTESIAN_POINT ( 'NONE',  ( 0.07556315841227323471, -1.331191507351497716, 0.4849083929475445087 ) ) ;
#38019=CARTESIAN_POINT ( 'NONE',  ( 0.08750309474107365038, -0.6863091869244348775, 0.02122045413186614618 ) ) ;
#38020=CARTESIAN_POINT ( 'NONE',  ( 0.7371735653322752935, -1.498976209023650696, 0.6847608182276055944 ) ) ;
#38024=CARTESIAN_POINT ( 'NONE',  ( 0.1117854919768572763, -1.404504638728010679, 0.6272293575327468895 ) ) ;
#38026=DIRECTION ( 'NONE',  ( 0.4999551463232372317, -0.8660512985181134660, -0.000000000000000000 ) ) ;
#38028=FACE_OUTER_BOUND ( 'NONE', #14783, .T. ) ;
#38030=CARTESIAN_POINT ( 'NONE',  ( 0.03762609415277568675, -1.032875954121303508, 0.6996461994120862782 ) ) ;
#38031=CARTESIAN_POINT ( 'NONE',  ( 0.0003774071935349580386, -0.4512940697347599950, 0.06537198606400290712 ) ) ;
#38040=CARTESIAN_POINT ( 'NONE',  ( 0.6252342874366797476, -1.468101632537779366, 0.5255929057819803685 ) ) ;
#38043=EDGE_CURVE ( 'NONE', #16451, #4940, #39393, .T. ) ;
#38045=CARTESIAN_POINT ( 'NONE',  ( 0.5574173260714455624, -1.620431899042181545, 0.4862486760544370568 ) ) ;
#38047=CARTESIAN_POINT ( 'NONE',  ( 0.04452036461275030166, -0.7338017871114075330, 0.5870408077749112996 ) ) ;
#38049=CARTESIAN_POINT ( 'NONE',  ( 0.2158254279709804768, -1.357966257267858134, 0.4182417262808779679 ) ) ;
#38050=CARTESIAN_POINT ( 'NONE',  ( 0.01180287247555067420, -0.6200342144150551293, -0.1048702747917058531 ) ) ;
#38055=CARTESIAN_POINT ( 'NONE',  ( 0.2165169723861147255, -0.9316405093292169370, 0.3921959536928056322 ) ) ;
#38062=CARTESIAN_POINT ( 'NONE',  ( 0.4768212070748857889, -1.161171340586348411, 0.4226408848665243467 ) ) ;
#38065=DIRECTION ( 'NONE',  ( -0.9117016142544763779, -0.4108529743908177490, -1.183049357217560165E-13 ) ) ;
#38070=CARTESIAN_POINT ( 'NONE',  ( 0.1186213546926599971, -1.414144755877529969, 0.5682417269582831221 ) ) ;
#38075=EDGE_CURVE ( 'NONE', #38007, #24330, #35459, .T. ) ;
#38080=CARTESIAN_POINT ( 'NONE',  ( 0.2721694418667137683, -1.673780725527275415, 0.6241958521473389698 ) ) ;
#38082=CARTESIAN_POINT ( 'NONE',  ( 0.5945617714832603928, -1.487100328519615378, 0.5656869075730865948 ) ) ;
#38084=CARTESIAN_POINT ( 'NONE',  ( 0.5511291867232482877, -1.181973051624798376, 0.6053111933194494920 ) ) ;
#38086=EDGE_CURVE ( 'NONE', #23555, #2251, #16832, .T. ) ;
#38093=CARTESIAN_POINT ( 'NONE',  ( 0.1937211450672182700, -1.200652605839983345, 0.5182417262812423209 ) ) ;
#38094=ORIENTED_EDGE ( 'NONE', *, *, #38178, .T. ) ;
#38095=CARTESIAN_POINT ( 'NONE',  ( 0.1790044836746327306, -0.8586862843173230786, 0.5897763735302309351 ) ) ;
#38096=CARTESIAN_POINT ( 'NONE',  ( 0.06924657340767528813, -0.5400045880099110240, 0.1446695161202853908 ) ) ;
#38097=CARTESIAN_POINT ( 'NONE',  ( 0.3019806439885205362, -1.080587002428585075, 0.8099453515258236980 ) ) ;
#38104=CARTESIAN_POINT ( 'NONE',  ( 0.4191100986681001173, -1.701672718972385701, 0.4233639548768205474 ) ) ;
#38105=CARTESIAN_POINT ( 'NONE',  ( 0.7437942939300432599, -1.516352026067812497, 0.5793574310342267664 ) ) ;
#38106=CARTESIAN_POINT ( 'NONE',  ( 0.5382321766149029685, -1.161161941655082241, 0.5682417262808779901 ) ) ;
#38108=CARTESIAN_POINT ( 'NONE',  ( 0.1373265930037192717, -0.5877730220021950558, 0.2830141842532937768 ) ) ;
#38111=CARTESIAN_POINT ( 'NONE',  ( 0.3211756810167746834, -1.183199798883805887, 0.5707417262808780478 ) ) ;
#38113=CARTESIAN_POINT ( 'NONE',  ( 0.001991602493628476505, -0.9268535620581923595, 0.4078208622452191290 ) ) ;
#38114=CARTESIAN_POINT ( 'NONE',  ( 0.5108734140540642787, -1.113869616463002643, 0.5959577563698095215 ) ) ;
#38121=CARTESIAN_POINT ( 'NONE',  ( 0.4355462401912356674, -1.577933922365856612, 0.5993494760761562956 ) ) ;
#38126=ORIENTED_EDGE ( 'NONE', *, *, #15745, .F. ) ;
#38127=CARTESIAN_POINT ( 'NONE',  ( 0.05573493074139709846, -1.335442843293342063, 0.4177417262808780229 ) ) ;
#38129=CARTESIAN_POINT ( 'NONE',  ( 0.06979003654356794040, -1.061296314535375540, 0.7344295544536164622 ) ) ;
#38131=VERTEX_POINT ( 'NONE', #9218 ) ;
#38134=FACE_OUTER_BOUND ( 'NONE', #15992, .T. ) ;
#38140=CARTESIAN_POINT ( 'NONE',  ( 0.01562499999999999827, -0.4290069966815236446, 0.1935973392073239430 ) ) ;
#38143=CARTESIAN_POINT ( 'NONE',  ( 0.1880902979351556092, -0.8183675832216642521, 0.6251957213044665451 ) ) ;
#38145=CARTESIAN_POINT ( 'NONE',  ( 0.02567193737592736447, -0.6182554903973285221, 0.6062124708192494493 ) ) ;
#38146=CARTESIAN_POINT ( 'NONE',  ( 0.4390231747115009853, -1.490295986258741046, 0.7935392936339821235 ) ) ;
#38148=CARTESIAN_POINT ( 'NONE',  ( 0.02587840337265700716, -0.7241365927453635720, 0.5953219528653882486 ) ) ;
#38150=CARTESIAN_POINT ( 'NONE',  ( 0.008896642862326420084, -0.8607682488963684930, 0.3771998872101971489 ) ) ;
#38155=CARTESIAN_POINT ( 'NONE',  ( 0.1897112079047663935, -0.5340520988485703002, 0.1436109887884086111 ) ) ;
#38160=DIRECTION ( 'NONE',  ( 0.4999551463232372317, -0.8660512985181135770, 0.000000000000000000 ) ) ;
#38161=CARTESIAN_POINT ( 'NONE',  ( 0.4504239474101026652, -1.039103266886249655, 0.7909361398939754872 ) ) ;
#38162=VECTOR ( 'NONE', #30003, 39.37007874015748143 ) ;
#38163=CARTESIAN_POINT ( 'NONE',  ( 0.5093734679828535450, -1.177557262684492123, 0.4426697169515769748 ) ) ;
#38164=CARTESIAN_POINT ( 'NONE',  ( 0.04237657096039100513, -1.193514938088262589, 0.6790371710685850770 ) ) ;
#38169=CARTESIAN_POINT ( 'NONE',  ( 0.3172624056207399290, -1.074258392339833668, 0.7402716440859538061 ) ) ;
#38171=CARTESIAN_POINT ( 'NONE',  ( 0.7052223925351273071, -1.496651798270721478, 0.5101712127052632217 ) ) ;
#38172=ORIENTED_EDGE ( 'NONE', *, *, #14031, .F. ) ;
#38174=CARTESIAN_POINT ( 'NONE',  ( 0.5074983293434512932, -1.310930700276065286, 0.7866430700807623966 ) ) ;
#38175=EDGE_CURVE ( 'NONE', #1496, #15591, #2859, .T. ) ;
#38178=EDGE_CURVE ( 'NONE', #24330, #24709, #31575, .T. ) ;
#38179=VERTEX_POINT ( 'NONE', #35528 ) ;
#38181=CARTESIAN_POINT ( 'NONE',  ( 0.1810371303969632861, -0.5115429810441346481, 0.2061669964520652931 ) ) ;
#38184=CARTESIAN_POINT ( 'NONE',  ( 0.4300745628493823358, -1.186155211153737232, 0.6976739215592587806 ) ) ;
#38187=CARTESIAN_POINT ( 'NONE',  ( 0.3105521454072050491, -1.758467560521084883, 0.5220235835725158813 ) ) ;
#38188=CARTESIAN_POINT ( 'NONE',  ( 0.4925986438152862856, -1.082524672201789828, 0.5763763218629267548 ) ) ;
#38192=CARTESIAN_POINT ( 'NONE',  ( 0.03435895639558289583, -1.001604871562542964, 0.6814382083780546884 ) ) ;
#38195=( BOUNDED_SURFACE ( )  B_SPLINE_SURFACE ( 3, 2, ( 
 ( #15919, #340, #3577 ),
 ( #9551, #3782, #16532 ),
 ( #28875, #21911, #34644 ),
 ( #6254, #25404, #31368 ),
 ( #25807, #22127, #25185 ),
 ( #16336, #6444, #38329 ) ),
 .UNSPECIFIED., .F., .F., .T. ) 
 B_SPLINE_SURFACE_WITH_KNOTS ( ( 4, 2, 4 ),
 ( 3, 3 ),
 ( 0.001871265718127418636, 0.003264854125545280095, 0.004658442532963141987 ),
 ( 0.000000000000000000, 1.000000000000000000 ),
 .UNSPECIFIED. ) 
 GEOMETRIC_REPRESENTATION_ITEM ( )  RATIONAL_B_SPLINE_SURFACE ( (
 ( 1.000000000000000000, 0.9912868421517995188, 1.000000000000000000),
 ( 1.000000000000000000, 0.9874999437985944040, 1.000000000000000000),
 ( 1.000000000000000000, 0.9809055010152987197, 1.000000000000000000),
 ( 1.000000000000000000, 0.9631198196773240738, 1.000000000000000000),
 ( 1.000000000000000000, 0.9523038229114263453, 1.000000000000000000),
 ( 1.000000000000000000, 0.9405852554627024409, 1.000000000000000000) ) ) 
 REPRESENTATION_ITEM ( '' )  SURFACE ( )  );
#38196=CARTESIAN_POINT ( 'NONE',  ( 0.3853488629557857981, -1.605649824104631307, 0.5756816568910164689 ) ) ;
#38197=CARTESIAN_POINT ( 'NONE',  ( 0.08691621476508532007, -0.7276673773931944256, 0.02918323030706625534 ) ) ;
#38198=CARTESIAN_POINT ( 'NONE',  ( 0.1988841153628475300, -0.6078592671934165415, 0.3205631666503918620 ) ) ;
#38201=ORIENTED_EDGE ( 'NONE', *, *, #16465, .F. ) ;
#38206=CARTESIAN_POINT ( 'NONE',  ( 0.1307094081766367877, -0.6333278402568883747, 0.3902961089287821927 ) ) ;
#38213=CARTESIAN_POINT ( 'NONE',  ( 0.7409681548321257472, -1.515722218252784748, 0.5271419462256154986 ) ) ;
#38219=CARTESIAN_POINT ( 'NONE',  ( 0.3297668774377428558, -1.165569269438828215, 0.4615993935216395894 ) ) ;
#38220=CARTESIAN_POINT ( 'NONE',  ( 0.6565177652365870031, -1.363219716956428407, 0.8083140950016142190 ) ) ;
#38221=CARTESIAN_POINT ( 'NONE',  ( 0.6960413307267936389, -1.427205786779416785, 0.4634944759858370955 ) ) ;
#38222=CARTESIAN_POINT ( 'NONE',  ( 0.2644966038856382817, -1.687071023141420545, 0.5682417262808783232 ) ) ;
#38225=CARTESIAN_POINT ( 'NONE',  ( 0.1835308262027276760, -1.352961526709849149, 0.9396307682827382823 ) ) ;
#38226=CARTESIAN_POINT ( 'NONE',  ( 0.0001527010945176735684, -0.5560399355413865319, -0.06596982925828048794 ) ) ;
#38228=CARTESIAN_POINT ( 'NONE',  ( 0.3509251431255968057, -1.165375537921118143, 0.4182417262808918457 ) ) ;
#38229=VERTEX_POINT ( 'NONE', #16619 ) ;
#38235=CARTESIAN_POINT ( 'NONE',  ( 0.4980693604982071032, -1.296659755426072147, 0.8022866093385110364 ) ) ;
#38237=ORIENTED_EDGE ( 'NONE', *, *, #2997, .F. ) ;
#38239=CARTESIAN_POINT ( 'NONE',  ( 0.5558873460704856218, -1.622947742269525095, 0.5440989928495453265 ) ) ;
#38241=CARTESIAN_POINT ( 'NONE',  ( 0.2968959581392767166, -1.656557492789272779, 0.5695608020044338193 ) ) ;
#38242=CARTESIAN_POINT ( 'NONE',  ( 0.6468566800937594063, -1.553424414166365564, 0.4209516853548616599 ) ) ;
#38245=CARTESIAN_POINT ( 'NONE',  ( 0.1837169918685102876, -0.8266995537623093027, 0.1015045423513593059 ) ) ;
#38251=CARTESIAN_POINT ( 'NONE',  ( 0.1454380568973649701, -0.9477385833960229045, 0.4092464228063885101 ) ) ;
#38254=CARTESIAN_POINT ( 'NONE',  ( 0.5706732878214085813, -1.412446763865061294, 0.7287409280026274638 ) ) ;
#38257=CARTESIAN_POINT ( 'NONE',  ( 0.1351628486807437135, -0.8647813875850353105, 0.4853538377376631630 ) ) ;
#38262=CARTESIAN_POINT ( 'NONE',  ( 0.6465835049539362389, -1.539613817736340318, 0.4182417262808776903 ) ) ;
#38263=CARTESIAN_POINT ( 'NONE',  ( 0.3174184176267951796, -1.762933076790987874, 0.5319023928053561168 ) ) ;
#38266=CARTESIAN_POINT ( 'NONE',  ( 0.2292082634166116850, -1.390808673668628259, 1.038138609612698327 ) ) ;
#38271=AXIS2_PLACEMENT_3D ( 'NONE', #27415, #39938, #9476 ) ;
#38277=CARTESIAN_POINT ( 'NONE',  ( 0.4009272606926310711, -1.137264901707352172, 0.4308458577267786915 ) ) ;
#38282=CARTESIAN_POINT ( 'NONE',  ( 0.5957392760757502792, -1.486251830005147712, 0.6051716374586044722 ) ) ;
#38285=ORIENTED_EDGE ( 'NONE', *, *, #8618, .F. ) ;
#38290=FACE_OUTER_BOUND ( 'NONE', #10114, .T. ) ;
#38294=CARTESIAN_POINT ( 'NONE',  ( 0.08584567903155949919, -0.7460567843300386359, 0.1584740188193046739 ) ) ;
#38295=CARTESIAN_POINT ( 'NONE',  ( 0.08990536851188075940, -0.5646295468557095409, 0.1389823447417319335 ) ) ;
#38296=CARTESIAN_POINT ( 'NONE',  ( 0.1100377367245384957, -0.5478698975639066937, 0.1620895514292355621 ) ) ;
#38303=CARTESIAN_POINT ( 'NONE',  ( 0.7432279256316001170, -1.516441678994711051, 0.5660936748573839328 ) ) ;
#38307=CARTESIAN_POINT ( 'NONE',  ( 0.2044722610693382459, -0.7754815171928667317, 0.5837216336432284880 ) ) ;
#38311=CARTESIAN_POINT ( 'NONE',  ( 0.3208715077212234701, -1.182672892261233732, 0.4687417262808780127 ) ) ;
#38312=EDGE_CURVE ( 'NONE', #1588, #15168, #23207, .T. ) ;
#38315=EDGE_CURVE ( 'NONE', #1394, #13751, #36397, .T. ) ;
#38316=CARTESIAN_POINT ( 'NONE',  ( 0.08042334443895514384, -1.362032735465325661, 0.6028738014108521170 ) ) ;
#38318=CARTESIAN_POINT ( 'NONE',  ( 0.5078487756305317680, -1.109832367716456325, 0.6054007957810670915 ) ) ;
#38322=CARTESIAN_POINT ( 'NONE',  ( 0.4688957988796484400, -1.165393138958765729, 0.4182417262808778013 ) ) ;
#38327=CARTESIAN_POINT ( 'NONE',  ( 0.01055999354154976179, -0.5296565605740110039, 0.1431176680404075141 ) ) ;
#38329=CARTESIAN_POINT ( 'NONE',  ( 0.1927077495703349297, -0.8180328145591141409, 0.2791508387892265297 ) ) ;
#38332=CARTESIAN_POINT ( 'NONE',  ( 0.1969702849860160421, -0.5469408226469265610, 0.3272831088336244365 ) ) ;
#38335=DIRECTION ( 'NONE',  ( -0.007367783058131798131, -0.4999457213560382085, 0.8660253988599866393 ) ) ;
#38338=PLANE ( 'NONE',  #14479 ) ;
#38339=FACE_OUTER_BOUND ( 'NONE', #7623, .T. ) ;
#38342=CARTESIAN_POINT ( 'NONE',  ( 0.008458849636713906481, -0.6664941812440515756, -0.01118885721624096607 ) ) ;
#38343=CARTESIAN_POINT ( 'NONE',  ( 0.09450633965359066246, -0.6214005085407516837, 0.2730725926996435127 ) ) ;
#38344=CARTESIAN_POINT ( 'NONE',  ( 0.4640678500019702057, -1.188919783037170275, 0.5182417262812423209 ) ) ;
#38345=CARTESIAN_POINT ( 'NONE',  ( 0.1277384056562314574, -0.7278354053324652684, 0.5494589346582330336 ) ) ;
#38346=CARTESIAN_POINT ( 'NONE',  ( 0.002290818369124609372, -0.5198888459286679087, 0.1457185332388686583 ) ) ;
#38348=CARTESIAN_POINT ( 'NONE',  ( 0.06709112777885012369, -1.107863570390577479, 0.7528161107794053564 ) ) ;
#38349=CARTESIAN_POINT ( 'NONE',  ( 0.3938498138106606428, -1.064849829384627800, 0.6374776580343812782 ) ) ;
#38352=CARTESIAN_POINT ( 'NONE',  ( 0.3827397780245204162, -1.608088820898147864, 0.5231971522552248954 ) ) ;
#38353=CARTESIAN_POINT ( 'NONE',  ( 0.1887413233215596287, -0.4595325217136330131, 0.1463014889510880212 ) ) ;
#38359=CARTESIAN_POINT ( 'NONE',  ( 0.5022839945508311699, -1.192782407697791980, 0.4224083929475445642 ) ) ;
#38361=CARTESIAN_POINT ( 'NONE',  ( 0.6761418372287171241, -1.395094899906518471, 0.6557117145240808354 ) ) ;
#38365=CARTESIAN_POINT ( 'NONE',  ( 0.01888917602804259660, -1.051501505208036313, 0.6153358008999590956 ) ) ;
#38369=CARTESIAN_POINT ( 'NONE',  ( 0.3291361082742700339, -1.091304683942979858, 0.7409066756199927939 ) ) ;
#38375=VERTEX_POINT ( 'NONE', #1029 ) ;
#38377=CARTESIAN_POINT ( 'NONE',  ( 0.5448400828272464969, -1.370358474244389502, 0.7639071756578307282 ) ) ;
#38378=CARTESIAN_POINT ( 'NONE',  ( 0.6498387395261646660, -1.464631408770378673, 0.4182417262808778013 ) ) ;
#38382=CARTESIAN_POINT ( 'NONE',  ( 0.2231482617632921661, -1.353434846386320611, 0.5181482079951671427 ) ) ;
#38383=CARTESIAN_POINT ( 'NONE',  ( 0.4778170654558047126, -1.668016138613298560, 0.5682417262808788783 ) ) ;
#38385=AXIS2_PLACEMENT_3D ( 'NONE', #21664, #6219, #11785 ) ;
#38386=CARTESIAN_POINT ( 'NONE',  ( 0.4900744151468222065, -1.275953078071682789, 0.5997076496587170347 ) ) ;
#38389=CARTESIAN_POINT ( 'NONE',  ( 0.3238203105384647174, -0.9899218032796638367, 0.5856430185708639824 ) ) ;
#38393=CARTESIAN_POINT ( 'NONE',  ( 0.05668208346063462189, -1.107411393821966072, 0.7455345429973143645 ) ) ;
#38394=VERTEX_POINT ( 'NONE', #4267 ) ;
#38398=CARTESIAN_POINT ( 'NONE',  ( 0.4133974373207104369, -1.589464046522193419, 0.5703553845707169945 ) ) ;
#38399=CARTESIAN_POINT ( 'NONE',  ( 0.06591376428800177489, -0.7622139198468362853, 0.01798093938639453923 ) ) ;
#38400=CARTESIAN_POINT ( 'NONE',  ( 0.2012013697609311147, -0.6235265729459525952, 0.3370440851636130053 ) ) ;
#38403=VERTEX_POINT ( 'NONE', #629 ) ;
#38404=CARTESIAN_POINT ( 'NONE',  ( 0.4155048779794340841, -1.128001391588047353, 0.5745684004788098598 ) ) ;
#38405=CARTESIAN_POINT ( 'NONE',  ( 0.4522227720718606792, -1.319557941469291729, 0.8277251512335837003 ) ) ;
#38408=CARTESIAN_POINT ( 'NONE',  ( 0.1874572521746671327, -0.6893911860354969834, 0.06179796301327929176 ) ) ;
#38414=CARTESIAN_POINT ( 'NONE',  ( 0.4158404862163792015, -1.704211426646492944, 0.6192745419747571756 ) ) ;
#38416=CARTESIAN_POINT ( 'NONE',  ( 0.08511258892558128120, -0.8122055842375904833, 0.1451433120779370700 ) ) ;
#38417=CARTESIAN_POINT ( 'NONE',  ( 0.4676789493019616883, -1.559177855287317005, 0.5735223705611400824 ) ) ;
#38419=CARTESIAN_POINT ( 'NONE',  ( 0.3207732826076518662, -1.759136744920719808, 0.5682417262808786562 ) ) ;
#38426=CARTESIAN_POINT ( 'NONE',  ( 0.1846093570424984787, -0.6365630712797759605, -0.02370498549722033915 ) ) ;
#38427=CARTESIAN_POINT ( 'NONE',  ( 0.2592104087477605789, -1.679801881415013964, 0.6057417262800831592 ) ) ;
#38431=CARTESIAN_POINT ( 'NONE',  ( 0.2039603895705197623, -1.429414345016513765, 0.9236325154956378514 ) ) ;
#38432=CARTESIAN_POINT ( 'NONE',  ( -0.0004431470427073231017, -0.9367128829938298207, 0.1457185332388704069 ) ) ;
#38441=ORIENTED_EDGE ( 'NONE', *, *, #31414, .F. ) ;
#38443=( BOUNDED_SURFACE ( )  B_SPLINE_SURFACE ( 3, 2, ( 
 ( #36285, #22403, #5022 ),
 ( #20464, #8103, #1353 ),
 ( #16777, #1960, #23381 ),
 ( #36091, #26235, #29516 ) ),
 .UNSPECIFIED., .F., .F., .T. ) 
 B_SPLINE_SURFACE_WITH_KNOTS ( ( 4, 4 ),
 ( 3, 3 ),
 ( 0.007078665261326035942, 0.008688923783415654703 ),
 ( 0.000000000000000000, 1.000000000000000000 ),
 .UNSPECIFIED. ) 
 GEOMETRIC_REPRESENTATION_ITEM ( )  RATIONAL_B_SPLINE_SURFACE ( (
 ( 1.000000000000000000, 0.7038424801053242419, 1.000000000000000000),
 ( 1.000000000000000000, 0.7026662720910222815, 1.000000000000000000),
 ( 1.000000000000000000, 0.7015046397803297307, 1.000000000000000000),
 ( 1.000000000000000000, 0.7003330442032725811, 1.000000000000000000) ) ) 
 REPRESENTATION_ITEM ( '' )  SURFACE ( )  );
#38448=CARTESIAN_POINT ( 'NONE',  ( 0.5632287240488592639, -1.399421096049667579, 0.6902502155986122157 ) ) ;
#38449=CARTESIAN_POINT ( 'NONE',  ( 0.5841409287570923370, -1.616576648741850253, 0.4600417456556253892 ) ) ;
#38451=CARTESIAN_POINT ( 'NONE',  ( 0.5520143099787153673, -1.183365530476261585, 0.6129298035784942478 ) ) ;
#38454=CARTESIAN_POINT ( 'NONE',  ( 0.5538245623271985663, -1.622806740292896510, 0.5052194400116507556 ) ) ;
#38455=ORIENTED_EDGE ( 'NONE', *, *, #16976, .T. ) ;
#38456=CARTESIAN_POINT ( 'NONE',  ( 0.09652487719191069071, -0.9245692721911921153, 0.7742711943059148449 ) ) ;
#38458=CARTESIAN_POINT ( 'NONE',  ( 0.1111680786003024363, -0.9208225436044804590, 0.08298286711937687132 ) ) ;
#38464=B_SPLINE_CURVE_WITH_KNOTS ( 'NONE', 3,
 ( #40106, #6166, #5761, #37031, #34754, #31475, #5955, #22240, #15030, #34352, #12351, #25100, #24713, #18515, #24499, #40531, #34563, #15441, #8851, #27580, #9060, #6372, #3282, #9671, #18940, #30861, #31070, #6561, #21430, #37244, #37856, #30671, #18729, #2490, #15837, #24909, #31286, #40321, #2890, #11934, #25316, #33961, #18319, #21622 ),
 .UNSPECIFIED., .F., .F.,
 ( 4, 2, 2, 2, 2, 2, 2, 2, 2, 2, 2, 2, 2, 2, 2, 2, 2, 2, 2, 2, 2, 4 ),
 ( 4.382894615908098410E-08, 0.0008319673269041918387, 0.001663890824862219444, 0.002495814322820246942, 0.003327737820778274656, 0.004159661318736302370, 0.004991584816694329650, 0.005823508314652356931, 0.006655431812610384211, 0.007487355310568412359, 0.008319278808526441374, 0.009983125804442492465, 0.01081504930240051801, 0.01164697280035854356, 0.01331081979627459812, 0.01414274329423262540, 0.01497466679219065094, 0.01663851378810670203, 0.01830236078402274619, 0.01996620777993879381, 0.02329390177177089599, 0.02662159576360300164 ),
 .UNSPECIFIED. ) ;
#38466=FACE_BOUND ( 'NONE', #19540, .T. ) ;
#38467=CARTESIAN_POINT ( 'NONE',  ( 0.1402207406671886758, -0.9448101387227968440, 0.3912908471735270233 ) ) ;
#38468=B_SPLINE_CURVE_WITH_KNOTS ( 'NONE', 3,
 ( #19747, #23262, #35788, #25533, #3720, #35388 ),
 .UNSPECIFIED., .F., .F.,
 ( 4, 2, 4 ),
 ( 0.000000000000000000, 0.0006454259618566229222, 0.001290851923713245844 ),
 .UNSPECIFIED. ) ;
#38470=CARTESIAN_POINT ( 'NONE',  ( 0.5862218696159900988, -1.490016463657622525, 0.6275474636321008992 ) ) ;
#38471=CARTESIAN_POINT ( 'NONE',  ( 0.4299965955316200072, -1.218712715363120980, 0.6395725852502865960 ) ) ;
#38476=CARTESIAN_POINT ( 'NONE',  ( 0.4604079122430825288, -1.154977203505554773, 0.4182417262808743597 ) ) ;
#38478=CARTESIAN_POINT ( 'NONE',  ( -0.001474785693551563560, -0.8508472180491982728, 0.1457185332388710453 ) ) ;
#38484=CARTESIAN_POINT ( 'NONE',  ( 0.1821586897988819453, -0.5033064891650144146, 0.1063490580930545742 ) ) ;
#38485=CARTESIAN_POINT ( 'NONE',  ( 0.1102650794266757106, -1.419061346167812099, 0.5811333943417352765 ) ) ;
#38488=CARTESIAN_POINT ( 'NONE',  ( 0.3048570497350418518, -1.756853555320991189, 0.5694442476137144826 ) ) ;
#38491=CARTESIAN_POINT ( 'NONE',  ( 0.6933708823975106572, -1.493733918961976714, 0.4749053888396611578 ) ) ;
#38493=CARTESIAN_POINT ( 'NONE',  ( 0.3504057387187116679, -1.153664717295437070, 0.4422128889498895266 ) ) ;
#38496=CARTESIAN_POINT ( 'NONE',  ( 0.2656260279857282081, -1.687710829545293834, 0.5802884372567370663 ) ) ;
#38497=CARTESIAN_POINT ( 'NONE',  ( 0.5191802974051609176, -1.366849940342511172, 0.7967361778819540552 ) ) ;
#38503=ORIENTED_EDGE ( 'NONE', *, *, #28025, .T. ) ;
#38504=ORIENTED_EDGE ( 'NONE', *, *, #29215, .T. ) ;
#38505=CARTESIAN_POINT ( 'NONE',  ( 0.6094085419975362461, -1.415843169154349379, 0.8536811844606672084 ) ) ;
#38506=ORIENTED_EDGE ( 'NONE', *, *, #9735, .T. ) ;
#38510=CARTESIAN_POINT ( 'NONE',  ( 0.003741017115097356686, -0.5275076572294760124, 0.09509064842808913343 ) ) ;
#38512=CARTESIAN_POINT ( 'NONE',  ( 0.08797380359565291907, -0.7919620400412524797, 0.2352302520415841813 ) ) ;
#38513=CARTESIAN_POINT ( 'NONE',  ( 0.06924657340766490754, -0.5400045880099092477, 0.1437216542238689831 ) ) ;
#38514=CARTESIAN_POINT ( 'NONE',  ( 0.2162141278466277738, -0.8955401101134577990, 0.7086684481727526519 ) ) ;
#38516=CARTESIAN_POINT ( 'NONE',  ( 0.06318324162253809162, -1.280059889144033347, 0.6358524534319103250 ) ) ;
#38517=CARTESIAN_POINT ( 'NONE',  ( 0.6984034912018327601, -1.438197739948913867, 0.5391927685615289789 ) ) ;
#38518=CARTESIAN_POINT ( 'NONE',  ( 0.3216131088691095985, -1.758533047554937223, 0.5670923938871434977 ) ) ;
#38519=CARTESIAN_POINT ( 'NONE',  ( 0.6980269330248262127, -1.438763980271349441, 0.5584498293197519558 ) ) ;
#38521=CARTESIAN_POINT ( 'NONE',  ( 0.4865408785632933664, -1.302845980766627054, 0.8126564211098294965 ) ) ;
#38522=CARTESIAN_POINT ( 'NONE',  ( 0.01172020176831022747, -0.7044715892658922618, -0.1131725940245311424 ) ) ;
#38524=CARTESIAN_POINT ( 'NONE',  ( 0.006049231046327587132, -0.8455795405855527358, 0.1352646710980445199 ) ) ;
#38527=CARTESIAN_POINT ( 'NONE',  ( 0.1224152969000399382, -1.440949543414774547, 0.5682417262808782121 ) ) ;
#38528=CARTESIAN_POINT ( 'NONE',  ( 0.4829770732687932999, -1.083865320555347678, 0.6394302686688468906 ) ) ;
#38532=B_SPLINE_CURVE_WITH_KNOTS ( 'NONE', 3,
 ( #24429, #33464, #27517, #36963, #34078, #37177 ),
 .UNSPECIFIED., .F., .F.,
 ( 4, 2, 4 ),
 ( 0.001438281905272879684, 0.002932816318273989611, 0.004427350731275099538 ),
 .UNSPECIFIED. ) ;
#38533=VERTEX_POINT ( 'NONE', #39843 ) ;
#38534=CARTESIAN_POINT ( 'NONE',  ( 0.4343951858081425144, -1.578589645844999279, 0.5985257411299329533 ) ) ;
#38535=CARTESIAN_POINT ( 'NONE',  ( 0.002367394983748904915, -0.5282119844061563541, 0.1394354128953861627 ) ) ;
#38539=FACE_OUTER_BOUND ( 'NONE', #3, .T. ) ;
#38541=ADVANCED_FACE ( 'NONE', ( #10859 ), #39281, .T. ) ;
#38542=CARTESIAN_POINT ( 'NONE',  ( 0.1905506861939139096, -0.5145941129025596306, 0.2257199139534598609 ) ) ;
#38553=CARTESIAN_POINT ( 'NONE',  ( 0.3739525536434556985, -1.751444307789024046, 0.9007940926418832595 ) ) ;
#38556=CARTESIAN_POINT ( 'NONE',  ( 0.1369077038689281156, -0.7638282256189674602, 0.4971742401558476576 ) ) ;
#38557=CARTESIAN_POINT ( 'NONE',  ( 0.001081227941644962018, -0.4583518364089779196, 0.2957653468694024790 ) ) ;
#38558=CARTESIAN_POINT ( 'NONE',  ( 0.4710354801145309467, -1.557935119788602663, 0.5965418981594908798 ) ) ;
#38561=CARTESIAN_POINT ( 'NONE',  ( 0.2251673531641388559, -1.129950269915442451, 0.6482802119689150544 ) ) ;
#38564=CARTESIAN_POINT ( 'NONE',  ( 0.2649422998572272814, -0.6790022894220869576, 0.6063299226072803583 ) ) ;
#38571=CARTESIAN_POINT ( 'NONE',  ( 0.6027116599735458102, -1.274749097762014616, 0.7879118535713135474 ) ) ;
#38573=CARTESIAN_POINT ( 'NONE',  ( -0.0008089698081453983516, -0.8558335556528616772, 0.3273597777360900962 ) ) ;
#38575=B_SPLINE_CURVE_WITH_KNOTS ( 'NONE', 3,
 ( #23062, #11110, #13778, #4109, #10316, #19965, #877, #7805, #35203, #3913, #20181, #32706, #20375, #13595, #16471, #29013, #13382, #35591, #38484, #4513, #22880 ),
 .UNSPECIFIED., .F., .F.,
 ( 4, 2, 2, 2, 2, 2, 2, 1, 2, 2, 4 ),
 ( 0.000000000000000000, 0.1250000000000031641, 0.1875000000000039690, 0.2500000000000047740, 0.3125000000000055511, 0.3750000000000063838, 0.4375000000000071609, 0.4687500000000072164, 0.4843750000000069389, 0.5000000000000066613, 1.000000000000000000 ),
 .UNSPECIFIED. ) ;
#38578=CARTESIAN_POINT ( 'NONE',  ( 0.3764860865686396330, -1.114925686102496760, 0.7584753650261379931 ) ) ;
#38580=CARTESIAN_POINT ( 'NONE',  ( 0.5529638661199859362, -1.384232351104116132, 0.6057417262806752412 ) ) ;
#38584=CARTESIAN_POINT ( 'NONE',  ( 0.3066637369260901691, -1.757170009578179259, 0.5393777584040966300 ) ) ;
#38586=CARTESIAN_POINT ( 'NONE',  ( 0.1343100678673626591, -1.002698383554990080, 0.7034404322865410730 ) ) ;
#38594=CARTESIAN_POINT ( 'NONE',  ( 0.4837475926090684109, -1.264528724657570935, 0.6352410761543320072 ) ) ;
#38596=CARTESIAN_POINT ( 'NONE',  ( 0.3844223753957967671, -1.715130776584119277, 0.4199023193696783673 ) ) ;
#38603=CARTESIAN_POINT ( 'NONE',  ( 0.07888544339681141659, -0.7040216271993084973, 0.5309320636121914738 ) ) ;
#38604=CARTESIAN_POINT ( 'NONE',  ( 0.08562435543972576890, -0.8179388245747207797, 0.08379651577411588448 ) ) ;
#38605=CARTESIAN_POINT ( 'NONE',  ( 0.2031749929763018991, -0.6988986647121863127, 0.3457752107024871790 ) ) ;
#38608=CARTESIAN_POINT ( 'NONE',  ( 0.3280207512787571833, -1.293371038683761354, 0.5714539138005585439 ) ) ;
#38609=CARTESIAN_POINT ( 'NONE',  ( 0.4829257366551612529, -1.359094011964862014, 0.8132530520444929412 ) ) ;
#38615=LINE ( 'NONE', #3850, #8665 ) ;
#38620=CARTESIAN_POINT ( 'NONE',  ( 0.6473156011871936677, -1.349322671506162141, 0.8501878200258047302 ) ) ;
#38628=CARTESIAN_POINT ( 'NONE',  ( 0.4386021513105624603, -1.229571196490931717, 0.4807399952002933685 ) ) ;
#38630=CARTESIAN_POINT ( 'NONE',  ( 0.01517484414490882783, -0.7999702980829028753, 0.5364596547344525623 ) ) ;
#38644=CARTESIAN_POINT ( 'NONE',  ( 0.5515672481317782649, -1.380278329912550284, 0.6412555363875834802 ) ) ;
#38645=CARTESIAN_POINT ( 'NONE',  ( 0.6590705178848084156, -1.601721441849921268, 0.5182417262812423209 ) ) ;
#38646=ORIENTED_EDGE ( 'NONE', *, *, #1442, .F. ) ;
#38647=CARTESIAN_POINT ( 'NONE',  ( 0.2618294899476097393, -0.7990503781373888836, 0.5447687035333291794 ) ) ;
#38651=CARTESIAN_POINT ( 'NONE',  ( 0.3242406000204350880, -1.171967933293699637, 0.5631067911264762138 ) ) ;
#38653=CARTESIAN_POINT ( 'NONE',  ( 0.3306735325123419944, -1.633537559201160061, 0.6703962882651552935 ) ) ;
#38654=FACE_OUTER_BOUND ( 'NONE', #22514, .T. ) ;
#38659=CARTESIAN_POINT ( 'NONE',  ( 0.3211494819420748215, -1.297383677212298636, 0.5148643787740219135 ) ) ;
#38660=CARTESIAN_POINT ( 'NONE',  ( 0.1852744361557795982, -0.8388916875311454024, 0.1498968110020814648 ) ) ;
#38664=CARTESIAN_POINT ( 'NONE',  ( 0.1748016489742494628, -0.9194174328440815058, 0.6210426057618604334 ) ) ;
#38668=CARTESIAN_POINT ( 'NONE',  ( 0.4065932041851609835, -1.147918556006405577, 0.4182417262808777458 ) ) ;
#38669=ADVANCED_FACE ( 'NONE', ( #25442 ), #2758, .T. ) ;
#38675=CARTESIAN_POINT ( 'NONE',  ( 0.04566385930017818201, -1.214514029449272892, 0.6761745275914542441 ) ) ;
#38680=CARTESIAN_POINT ( 'NONE',  ( 0.4610032414159208614, -1.686334621966218306, 0.4527853876349565709 ) ) ;
#38682=CARTESIAN_POINT ( 'NONE',  ( 0.2665932999777489432, -1.539397319814852949, 0.9862784934333517217 ) ) ;
#38683=CARTESIAN_POINT ( 'NONE',  ( 0.6714407672615939626, -1.521867659483790547, 0.4359222191939696733 ) ) ;
#38685=ORIENTED_EDGE ( 'NONE', *, *, #19527, .T. ) ;
#38687=ORIENTED_EDGE ( 'NONE', *, *, #13427, .F. ) ;
#38690=CARTESIAN_POINT ( 'NONE',  ( 0.5943265527529638659, -1.468666372280408972, 0.6816657076235226320 ) ) ;
#38691=CARTESIAN_POINT ( 'NONE',  ( 0.1539501873670340859, -1.278399339615925667, 0.4182417262808778013 ) ) ;
#38699=CARTESIAN_POINT ( 'NONE',  ( 0.1801302324021237800, -1.378194537208108361, 0.5482363894879486166 ) ) ;
#38704=EDGE_LOOP ( 'NONE', ( #469, #613, #3371, #5454, #30312, #1015, #7110 ) ) ;
#38705=CARTESIAN_POINT ( 'NONE',  ( 0.2439697435047648300, -0.9572542734378898244, 0.6693538292162648506 ) ) ;
#38707=CARTESIAN_POINT ( 'NONE',  ( 0.5388164341061177920, -1.518966147603598049, 0.5683445443996597568 ) ) ;
#38709=CARTESIAN_POINT ( 'NONE',  ( 0.04171458440977070942, -1.134361221218466609, 0.6577934201144993720 ) ) ;
#38712=CARTESIAN_POINT ( 'NONE',  ( 0.3510995257679918602, -1.742526243202041192, 0.6036984576181094742 ) ) ;
#38717=CARTESIAN_POINT ( 'NONE',  ( -0.0001129244011828491533, -0.7912893389636214136, -0.08081660452504497993 ) ) ;
#38718=CARTESIAN_POINT ( 'NONE',  ( 0.3688024341757283331, -1.123809055325019735, 0.8060765054549502429 ) ) ;
#38720=CARTESIAN_POINT ( 'NONE',  ( 0.4971324743577882899, -1.079965756743124006, 0.4177417262808780229 ) ) ;
#38722=CARTESIAN_POINT ( 'NONE',  ( -0.003124719664520056797, -0.8057675726412014683, 0.1627348865840318737 ) ) ;
#38723=CARTESIAN_POINT ( 'NONE',  ( 0.4430687885351943245, -1.051147784193108281, 0.6535119922057798236 ) ) ;
#38731=VERTEX_POINT ( 'NONE', #13489 ) ;
#38733=CARTESIAN_POINT ( 'NONE',  ( 0.6807551469422991053, -1.407487954066357183, 0.5751647024762112093 ) ) ;
#38738=DIRECTION ( 'NONE',  ( 0.8660512985181134660, 0.4999551463232372317, 0.000000000000000000 ) ) ;
#38742=CARTESIAN_POINT ( 'NONE',  ( 0.1875000000000003331, -0.4593131964907913867, 0.1457185332388697407 ) ) ;
#38743=CARTESIAN_POINT ( 'NONE',  ( 0.1930736954529370941, -0.8449126200218157745, 0.6255041996076380340 ) ) ;
#38744=DIRECTION ( 'NONE',  ( -0.4999551463232372317, 0.8660512985181134660, -0.000000000000000000 ) ) ;
#38745=CARTESIAN_POINT ( 'NONE',  ( 0.08524078840219746767, -0.5428247996486973426, 0.1457185332388697407 ) ) ;
#38746=CARTESIAN_POINT ( 'NONE',  ( 0.2654443876445621298, -1.687660951001132004, 0.5779630316034871651 ) ) ;
#38747=DIRECTION ( 'NONE',  ( 0.000000000000000000, 0.000000000000000000, -1.000000000000000000 ) ) ;
#38748=CARTESIAN_POINT ( 'NONE',  ( 0.1627198989308838994, -1.029848727310650469, 0.5977245216963805730 ) ) ;
#38749=ORIENTED_EDGE ( 'NONE', *, *, #30892, .F. ) ;
#38751=CARTESIAN_POINT ( 'NONE',  ( 0.3588042674141814214, -1.621950415644044963, 0.5547558322257422070 ) ) ;
#38752=CARTESIAN_POINT ( 'NONE',  ( 0.2214772573562845126, -0.6571296826234386268, 0.4491444447770453485 ) ) ;
#38757=CARTESIAN_POINT ( 'NONE',  ( 0.4936113061342744524, -1.107001320208115036, 0.7496827700887727097 ) ) ;
#38758=CARTESIAN_POINT ( 'NONE',  ( 0.5271543187458650470, -1.167382716756260042, 0.4878339827211743973 ) ) ;
#38759=FACE_OUTER_BOUND ( 'NONE', #6101, .T. ) ;
#38760=VECTOR ( 'NONE', #16638, 39.37007874015748143 ) ;
#38762=CARTESIAN_POINT ( 'NONE',  ( 0.3289274145732573040, -1.292879115135177059, 0.4679791452570866150 ) ) ;
#38763=ORIENTED_EDGE ( 'NONE', *, *, #30619, .T. ) ;
#38764=CARTESIAN_POINT ( 'NONE',  ( 0.2270139475256796879, -0.9339256942224501978, 0.6530035840272132575 ) ) ;
#38769=CARTESIAN_POINT ( 'NONE',  ( 0.4315909263077353786, -1.207668101024179430, 0.5182417262812423209 ) ) ;
#38770=ORIENTED_EDGE ( 'NONE', *, *, #4454, .F. ) ;
#38771=CARTESIAN_POINT ( 'NONE',  ( 0.08990536850430516647, -0.5646295866045974998, 0.1496696842286166784 ) ) ;
#38773=CARTESIAN_POINT ( 'NONE',  ( 0.2219638282378538774, -1.211848774759766600, 0.7364796804151579890 ) ) ;
#38779=PRODUCT_DEFINITION ( 'UNKNOWN', '', #5625, #32707 ) ;
#38781=CARTESIAN_POINT ( 'NONE',  ( 0.3773743308125420692, -1.120461712655230091, 0.7152730075388841202 ) ) ;
#38782=CARTESIAN_POINT ( 'NONE',  ( 0.4027068045633697690, -1.135255088841635729, 0.5012202440948826387 ) ) ;
#38784=CARTESIAN_POINT ( 'NONE',  ( 0.3026114960654325836, -0.9782852559307895213, 0.5634791713200563157 ) ) ;
#38788=CARTESIAN_POINT ( 'NONE',  ( 0.06044531019120238241, -0.6298155687119810775, 0.4117843844938999243 ) ) ;
#38789=CARTESIAN_POINT ( 'NONE',  ( 0.08828494613019574611, -0.6323668545420986220, 0.03541928192839603751 ) ) ;
#38790=CARTESIAN_POINT ( 'NONE',  ( 0.1744097386003500560, -0.9176933794257766674, 0.1353190812260986475 ) ) ;
#38794=B_SPLINE_CURVE_WITH_KNOTS ( 'NONE', 3,
 ( #2565, #28078, #24971, #21691 ),
 .UNSPECIFIED., .F., .F.,
 ( 4, 4 ),
 ( 0.000000000000000000, 4.801453139129629977E-05 ),
 .UNSPECIFIED. ) ;
#38797=CARTESIAN_POINT ( 'NONE',  ( 0.5748884503991072981, -1.498777740968299188, 0.5996797115467191741 ) ) ;
#38805=CARTESIAN_POINT ( 'NONE',  ( 0.1689017270382413005, -1.269576038341752700, 0.4229621067556875169 ) ) ;
#38807=CARTESIAN_POINT ( 'NONE',  ( 0.4778170654558047126, -1.668016138613298560, 0.5682417262808788783 ) ) ;
#38809=EDGE_CURVE ( 'NONE', #34759, #16750, #10907, .T. ) ;
#38810=CARTESIAN_POINT ( 'NONE',  ( 0.5698123312952257935, -1.224001199585974087, 0.8774075775261976906 ) ) ;
#38818=CARTESIAN_POINT ( 'NONE',  ( 0.1849146134180273127, -0.6975931602019068700, -0.02773678677584009988 ) ) ;
#38822=CARTESIAN_POINT ( 'NONE',  ( 0.003441938119505853853, -0.5826794048688673788, 0.2512083064573837898 ) ) ;
#38835=CARTESIAN_POINT ( 'NONE',  ( 0.01220508677664999299, -0.4284039737085656996, 0.1457185332388702959 ) ) ;
#38837=CARTESIAN_POINT ( 'NONE',  ( 0.4924747549555801851, -1.284741442926763400, 0.7473512348121129634 ) ) ;
#38840=CARTESIAN_POINT ( 'NONE',  ( 0.4556718857535577705, -1.059138143784118302, 0.6919068033735837897 ) ) ;
#38845=CARTESIAN_POINT ( 'NONE',  ( 0.02473703078937821917, -0.5631418136270044394, 0.2740291547039533926 ) ) ;
#38846=CARTESIAN_POINT ( 'NONE',  ( 0.6047538891612445067, -1.605163873594934065, 0.4396382108053981663 ) ) ;
#38847=CARTESIAN_POINT ( 'NONE',  ( 0.1113805825442736736, -0.9071550240875194682, 0.04606443103390334137 ) ) ;
#38848=CARTESIAN_POINT ( 'NONE',  ( 0.05583995664670776682, -1.335624775257321817, 0.3157417262808777658 ) ) ;
#38853=CARTESIAN_POINT ( 'NONE',  ( 0.1826249073287988522, -1.261667980084789420, 0.4182417262808778569 ) ) ;
#38855=CARTESIAN_POINT ( 'NONE',  ( 0.1524423687509998404, -0.8872256037779822080, 0.5537346710474807532 ) ) ;
#38858=CARTESIAN_POINT ( 'NONE',  ( 0.1462308410358738320, -0.9164545692843373281, 0.1457042957556350660 ) ) ;
#38866=CARTESIAN_POINT ( 'NONE',  ( 0.2737252524196370218, -1.671010326955969960, 0.4800311348041322868 ) ) ;
#38869=CARTESIAN_POINT ( 'NONE',  ( 0.3834349357971629790, -1.149375767803377135, 0.4315005731421182600 ) ) ;
#38873=CARTESIAN_POINT ( 'NONE',  ( 0.1153471662232078698, -0.4465907064269051263, 0.1457432652200511269 ) ) ;
#38877=B_SPLINE_CURVE_WITH_KNOTS ( 'NONE', 3,
 ( #31627, #18896, #31434, #22806, #6720, #3240, #35329, #19088, #7118, #207, #15786, #13, #12495, #6929, #12699, #28936, #3442, #16000 ),
 .UNSPECIFIED., .F., .F.,
 ( 4, 2, 2, 2, 2, 2, 2, 2, 4 ),
 ( 0.005943923758767621912, 0.006685218669166347917, 0.007426513579565073922, 0.008167808489963800794, 0.008909103400362525932, 0.009650398310761251069, 0.01039169322115997794, 0.01113298813155870481, 0.01187428304195742995 ),
 .UNSPECIFIED. ) ;
#38879=EDGE_LOOP ( 'NONE', ( #39251, #31243, #31780, #38896, #25240 ) ) ;
#38881=CARTESIAN_POINT ( 'NONE',  ( 0.1886928464339920619, -0.5387472362569383222, 0.2832338156061069423 ) ) ;
#38885=B_SPLINE_CURVE_WITH_KNOTS ( 'NONE', 3,
 ( #12488, #31013, #2834, #27943, #40481, #12306, #37382, #21764, #34905, #37999, #22589, #31831, #13305, #6714, #19288, #31429, #13100, #607, #7112, #16597, #25660, #3648, #38393, #28328, #3436, #202, #19495, #19082, #6318, #38192, #16209, #3233, #18891, #28745, #15780, #3833, #21978, #10018, #34706, #35116, #25878, #15995, #28540, #9808 ),
 .UNSPECIFIED., .F., .F.,
 ( 4, 2, 2, 2, 2, 2, 2, 2, 2, 2, 2, 2, 2, 2, 2, 2, 2, 2, 2, 2, 2, 4 ),
 ( 7.720987835474815629E-06, 0.0008870064552703168593, 0.001766291922705158935, 0.002645577390140001553, 0.003524862857574843304, 0.004404148325009685054, 0.005283433792444528106, 0.006162719259879370290, 0.007042004727314211607, 0.008800575662183894241, 0.009679861129618742496, 0.01055914659705358728, 0.01143843206448843554, 0.01231771753192328206, 0.01319700299935812858, 0.01407628846679297684, 0.01583485940166267161, 0.01671414486909751987, 0.01759343033653236812, 0.02111057220627177503, 0.02462771407601118540, 0.02814485594575059230 ),
 .UNSPECIFIED. ) ;
#38886=CIRCLE ( 'NONE', #11968, 0.07749999999977555398 ) ;
#38887=CARTESIAN_POINT ( 'NONE',  ( 0.6018806508000521527, -1.483118007491554646, 0.5713872269410379401 ) ) ;
#38888=LINE ( 'NONE', #38691, #19161 ) ;
#38893=CARTESIAN_POINT ( 'NONE',  ( 0.1320833403089577973, -0.5364814942693221234, 0.4244164861031392566 ) ) ;
#38896=ORIENTED_EDGE ( 'NONE', *, *, #10763, .F. ) ;
#38897=CARTESIAN_POINT ( 'NONE',  ( -0.01313218671590571027, -0.5535711118707772327, 0.2673923889699659218 ) ) ;
#38903=CARTESIAN_POINT ( 'NONE',  ( 0.004891213885548088142, -0.6339827964191876442, 0.1483282180229320291 ) ) ;
#38904=ORIENTED_EDGE ( 'NONE', *, *, #20852, .T. ) ;
#38906=CARTESIAN_POINT ( 'NONE',  ( 0.1548341679632025680, -0.8596504379563697507, 0.5333057515477647170 ) ) ;
#38907=CARTESIAN_POINT ( 'NONE',  ( 0.06944579691897743989, -0.5431860149686560391, 0.1791531423689709523 ) ) ;
#38908=CARTESIAN_POINT ( 'NONE',  ( 0.5390157067140883829, -1.519029365507106988, 0.5719888029048197930 ) ) ;
#38910=LINE ( 'NONE', #10738, #35610 ) ;
#38911=CARTESIAN_POINT ( 'NONE',  ( 0.6413355266909854802, -1.469255435513146413, 0.4003763534992342832 ) ) ;
#38912=CARTESIAN_POINT ( 'NONE',  ( 0.3478054713553065946, -1.744458529272713498, 0.6010704396163429886 ) ) ;
#38914=CARTESIAN_POINT ( 'NONE',  ( 0.06690744896826546217, -1.340115430975673316, 0.5315786376783453449 ) ) ;
#38917=CARTESIAN_POINT ( 'NONE',  ( -0.0002454585711109004810, -0.8766763345964988519, -0.01713775608600108177 ) ) ;
#38918=CARTESIAN_POINT ( 'NONE',  ( 0.2509773515924360043, -0.9519638977167713678, 0.7406622671168548999 ) ) ;
#38919=( LENGTH_UNIT ( ) NAMED_UNIT ( * ) SI_UNIT ( $, .METRE. ) );
#38925=CARTESIAN_POINT ( 'NONE',  ( 0.007928552535923857544, -0.8847668029847218785, 0.5082548692313750838 ) ) ;
#38926=CARTESIAN_POINT ( 'NONE',  ( 0.1854168535569867549, -0.8697360073808747538, 0.1457185332388700738 ) ) ;
#38928=AXIS2_PLACEMENT_3D ( 'NONE', #39094, #20182, #11310 ) ;
#38929=CARTESIAN_POINT ( 'NONE',  ( 0.5961566725213064410, -1.266700452128206367, 0.8733730542187856383 ) ) ;
#38933=CARTESIAN_POINT ( 'NONE',  ( 0.3136505104175751346, -1.762210813257952147, 0.5687094762557387551 ) ) ;
#38937=CARTESIAN_POINT ( 'NONE',  ( 0.01058516978236496812, -0.5329851777183867156, 0.1813778425092805180 ) ) ;
#38942=EDGE_CURVE ( 'NONE', #20946, #17780, #5971, .T. ) ;
#38944=CARTESIAN_POINT ( 'NONE',  ( 0.5969179818652998737, -1.265625243575819514, 0.7915741918176316672 ) ) ;
#38952=CIRCLE ( 'NONE', #2170, 0.009999999999999981126 ) ;
#38955=CARTESIAN_POINT ( 'NONE',  ( 0.7429241260303106609, -1.515741207197444984, 0.5682417262808784342 ) ) ;
#38956=CARTESIAN_POINT ( 'NONE',  ( 0.2162507585142164346, -0.8790159608897792909, 0.6620781576653871348 ) ) ;
#38958=CARTESIAN_POINT ( 'NONE',  ( 0.2326140044019894271, -1.416031621593191181, 1.021274582455189428 ) ) ;
#38960=CARTESIAN_POINT ( 'NONE',  ( 0.4696795125927291092, -1.557974007221949453, 0.5725897366691788948 ) ) ;
#38961=CARTESIAN_POINT ( 'NONE',  ( 0.1157284135122316898, -1.105864713636613317, 0.8979452765864521790 ) ) ;
#38962=CARTESIAN_POINT ( 'NONE',  ( 0.2779095291147324343, -1.668760755457822986, 0.5790662758146200018 ) ) ;
#38963=CARTESIAN_POINT ( 'NONE',  ( 0.05024437483578383934, -0.9472498927431809435, 0.3056578206038833012 ) ) ;
#38968=CARTESIAN_POINT ( 'NONE',  ( 0.1903103077163704193, -0.5412354413273032794, 0.1986930158102075406 ) ) ;
#38974=DIRECTION ( 'NONE',  ( 0.8660512985181135770, 0.4999551463232368431, 0.000000000000000000 ) ) ;
#38975=CARTESIAN_POINT ( 'NONE',  ( 0.5468032192656866464, -1.183383020191767443, 0.7376474321803302425 ) ) ;
#38977=CARTESIAN_POINT ( 'NONE',  ( 0.01301404012986586214, -0.8779095112082120345, 0.4619222818525974272 ) ) ;
#38978=B_SPLINE_CURVE_WITH_KNOTS ( 'NONE', 3,
 ( #36958, #20940, #5877, #8563 ),
 .UNSPECIFIED., .F., .F.,
 ( 4, 4 ),
 ( 0.006562375122924405529, 0.006754369985014277260 ),
 .UNSPECIFIED. ) ;
#38981=CARTESIAN_POINT ( 'NONE',  ( 0.3889638052529856282, -1.132903526660985705, 0.7528812961574173901 ) ) ;
#38984=CIRCLE ( 'NONE', #22604, 0.1762268159172233339 ) ;
#38987=CARTESIAN_POINT ( 'NONE',  ( 0.5095252007787752779, -1.122954523980121744, 0.6801752979809041477 ) ) ;
#38988=CARTESIAN_POINT ( 'NONE',  ( 0.08996836131725784169, -0.5655380582595669336, 0.1615303154345441861 ) ) ;
#38991=CIRCLE ( 'NONE', #36350, 0.01000000000000004184 ) ;
#38992=CARTESIAN_POINT ( 'NONE',  ( 0.2656213591975871147, -1.296266830651302993, 0.6616968573301059697 ) ) ;
#38993=ORIENTED_EDGE ( 'NONE', *, *, #30119, .T. ) ;
#38999=CARTESIAN_POINT ( 'NONE',  ( 0.4198966019305932496, -1.174027997756919239, 0.7144634253752220054 ) ) ;
#39001=CARTESIAN_POINT ( 'NONE',  ( 0.4759292920945783489, -1.117238247451545874, 0.5687629415736369376 ) ) ;
#39004=LINE ( 'NONE', #8135, #22447 ) ;
#39006=CARTESIAN_POINT ( 'NONE',  ( 0.2937365356607388733, -1.300204286310561175, 0.8910421725200852183 ) ) ;
#39007=CARTESIAN_POINT ( 'NONE',  ( 0.08738472799975360861, -0.6969953448697594478, 0.001717529511606559391 ) ) ;
#39008=CARTESIAN_POINT ( 'NONE',  ( 0.1966785637937622788, -0.7882153485089888889, 0.3097641500712802198 ) ) ;
#39009=CARTESIAN_POINT ( 'NONE',  ( 0.1176733790823393522, -1.298938889880303371, 0.5182417262812425429 ) ) ;
#39013=CARTESIAN_POINT ( 'NONE',  ( 0.1396989859084467323, -0.6541046724775327892, 0.4283214651078913748 ) ) ;
#39019=CARTESIAN_POINT ( 'NONE',  ( 0.6404849885218004690, -1.549707582885980761, 0.4182417262808776903 ) ) ;
#39021=CARTESIAN_POINT ( 'NONE',  ( 0.2228277390803876379, -1.238373433379782229, 0.4925787018828454711 ) ) ;
#39025=CARTESIAN_POINT ( 'NONE',  ( 0.2020777887685438201, -0.5385241820806814239, 0.3979124043150588097 ) ) ;
#39033=CARTESIAN_POINT ( 'NONE',  ( 0.4103535367438664871, -1.245886191849670421, 0.5133467982331404444 ) ) ;
#39034=CARTESIAN_POINT ( 'NONE',  ( 0.1581650021276234941, -1.285700486175304746, 0.4182417262808776903 ) ) ;
#39036=CARTESIAN_POINT ( 'NONE',  ( 0.002392376194700432737, -0.7211561054371403712, 0.3442605867753443794 ) ) ;
#39046=CARTESIAN_POINT ( 'NONE',  ( 0.4646907997295934845, -1.115905291537239830, 0.5753588453296760719 ) ) ;
#39048=CARTESIAN_POINT ( 'NONE',  ( 0.05573493074139709846, -1.335442843293342063, 0.4177417262808780229 ) ) ;
#39053=CARTESIAN_POINT ( 'NONE',  ( 0.4814929157054633202, -1.267930000418878045, 0.7540278765520666004 ) ) ;
#39056=CARTESIAN_POINT ( 'NONE',  ( 0.5083828713348212958, -1.120917766412646177, 0.6786323191735850191 ) ) ;
#39065=CARTESIAN_POINT ( 'NONE',  ( 0.3297717883327160870, -1.638642138455859376, 0.6197557731930207758 ) ) ;
#39066=CARTESIAN_POINT ( 'NONE',  ( 0.6621646329316274171, -1.547049793389352557, 0.4306066971441852020 ) ) ;
#39067=CARTESIAN_POINT ( 'NONE',  ( 0.1140740010698196444, -0.5454507455871950850, -0.04915391599425626701 ) ) ;
#39068=CARTESIAN_POINT ( 'NONE',  ( 0.3210085668004670767, -1.182910313946810010, 0.5197417262808780025 ) ) ;
#39069=EDGE_CURVE ( 'NONE', #34794, #40356, #21686, .T. ) ;
#39071=ORIENTED_EDGE ( 'NONE', *, *, #7687, .F. ) ;
#39076=CARTESIAN_POINT ( 'NONE',  ( 0.2995545230446825524, -1.131849367291001274, 0.7413806071029465095 ) ) ;
#39077=CARTESIAN_POINT ( 'NONE',  ( 0.5848508152300195828, -1.486263022089187036, 0.6467108361231791447 ) ) ;
#39081=AXIS2_PLACEMENT_3D ( 'NONE', #10912, #23479, #33106 ) ;
#39084=CARTESIAN_POINT ( 'NONE',  ( 0.6295207451518218811, -1.563610154300691502, 0.4182417262808778013 ) ) ;
#39085=EDGE_CURVE ( 'NONE', #37238, #20093, #40380, .T. ) ;
#39087=CARTESIAN_POINT ( 'NONE',  ( 0.1581650021276240492, -1.285700486175305635, 0.4182417262808778013 ) ) ;
#39091=CARTESIAN_POINT ( 'NONE',  ( 0.3983340929409861508, -1.147351698812145049, 0.4237746715961450694 ) ) ;
#39094=CARTESIAN_POINT ( 'NONE',  ( 0.4315909263077353786, -1.207668101024179430, 0.5182417262812423209 ) ) ;
#39097=CARTESIAN_POINT ( 'NONE',  ( 0.2330432091865630995, -1.417564937792536117, 1.021065090758958238 ) ) ;
#39098=B_SPLINE_CURVE_WITH_KNOTS ( 'NONE', 3,
 ( #26294, #35533, #28960, #13126, #4467, #10268, #1415, #26498, #13547, #38628, #17227, #16419, #7143, #10648, #35748, #7560, #39033, #824 ),
 .UNSPECIFIED., .F., .F.,
 ( 4, 2, 2, 2, 2, 2, 2, 2, 4 ),
 ( 0.000000000000000000, 0.0003722438250988956946, 0.0007444876501977913891, 0.001116731475296687138, 0.001488975300395582778, 0.001861219125494478419, 0.002233462950593374276, 0.002605706775692269699, 0.002977950600791165556 ),
 .UNSPECIFIED. ) ;
#39100=EDGE_LOOP ( 'NONE', ( #13240, #20536, #18938, #13805 ) ) ;
#39102=CARTESIAN_POINT ( 'NONE',  ( 0.1744808239353030921, -0.5220121294792338107, 0.1088806183924514309 ) ) ;
#39106=CARTESIAN_POINT ( 'NONE',  ( 0.6027238554419750427, -1.482183870088574773, 0.6047563465127264726 ) ) ;
#39107=CARTESIAN_POINT ( 'NONE',  ( 0.006827740514596677447, -0.8142735967992830171, 0.05084675703196275820 ) ) ;
#39108=EDGE_LOOP ( 'NONE', ( #30568, #5187, #2343, #23082 ) ) ;
#39111=CARTESIAN_POINT ( 'NONE',  ( 0.3204479958614548929, -1.182666560659948907, 0.5682417262808776570 ) ) ;
#39114=CARTESIAN_POINT ( 'NONE',  ( 0.2298583264429857054, -1.515562747760924145, 0.9092735558684903463 ) ) ;
#39121=CARTESIAN_POINT ( 'NONE',  ( -0.0003981105962839171755, -0.8469330747986117958, -0.1178596299512797430 ) ) ;
#39125=CARTESIAN_POINT ( 'NONE',  ( 0.08591970961800117490, -0.7898962715215620545, 0.1943287141640972771 ) ) ;
#39127=CARTESIAN_POINT ( 'NONE',  ( 0.06088048528104925139, -1.075208222708675887, 0.7418958488900205817 ) ) ;
#39128=CARTESIAN_POINT ( 'NONE',  ( 0.1312574532462938703, -0.6907975637544085945, 0.4921479965689204983 ) ) ;
#39129=CARTESIAN_POINT ( 'NONE',  ( 0.1758720408525228374, -0.7793959872790835464, 0.5981583825683202127 ) ) ;
#39130=CARTESIAN_POINT ( 'NONE',  ( 0.06841984176915458238, -1.324714172852429650, 0.5852474161806638930 ) ) ;
#39132=CARTESIAN_POINT ( 'NONE',  ( 0.6508782539171524828, -1.549424043532367179, 0.4232305864574226750 ) ) ;
#39136=DIRECTION ( 'NONE',  ( 0.02743089364023493237, 0.02297375779311301713, -0.9993596712530287141 ) ) ;
#39138=CARTESIAN_POINT ( 'NONE',  ( 0.01159392866623401054, -0.8181752906802141068, -0.07781262754897533274 ) ) ;
#39141=CARTESIAN_POINT ( 'NONE',  ( 0.007159747793320437280, -0.7917788012823626653, 0.02659789922158702774 ) ) ;
#39145=CARTESIAN_POINT ( 'NONE',  ( 0.03167879690716527558, -0.8799939210571326997, 0.6541495583543271986 ) ) ;
#39146=CARTESIAN_POINT ( 'NONE',  ( 0.2317493251130877951, -0.9016848682509819302, 0.4453502113744062241 ) ) ;
#39148=CARTESIAN_POINT ( 'NONE',  ( 0.6320591615222423965, -1.324690328322339239, 0.8595101463142521547 ) ) ;
#39151=AXIS2_PLACEMENT_3D ( 'NONE', #17171, #36288, #20467 ) ;
#39152=CARTESIAN_POINT ( 'NONE',  ( 0.3110204894824479260, -1.761578038038337235, 0.5680195786030766136 ) ) ;
#39155=CARTESIAN_POINT ( 'NONE',  ( 0.04534555968120922154, -0.8363173250083066890, 0.7068803008767403639 ) ) ;
#39160=CARTESIAN_POINT ( 'NONE',  ( 0.5799898087634006716, -1.239070881731211049, 0.8001874111395332889 ) ) ;
#39164=ADVANCED_FACE ( 'NONE', ( #3961 ), #31318, .T. ) ;
#39168=CARTESIAN_POINT ( 'NONE',  ( 0.4389213214516935468, -1.229316516391377956, 0.5870219547771845514 ) ) ;
#39169=EDGE_CURVE ( 'NONE', #799, #13526, #39820, .T. ) ;
#39171=ORIENTED_EDGE ( 'NONE', *, *, #22553, .F. ) ;
#39172=CARTESIAN_POINT ( 'NONE',  ( 0.1260557303073279456, -1.253941604664451592, 0.6054858248391781217 ) ) ;
#39174=CARTESIAN_POINT ( 'NONE',  ( 0.08875147084456939950, -0.6445117467991265947, 0.1457185332388690746 ) ) ;
#39175=CARTESIAN_POINT ( 'NONE',  ( 0.2149123625260831172, -1.353071881634811735, 1.025762950587601807 ) ) ;
#39176=CARTESIAN_POINT ( 'NONE',  ( 0.4696012870462846767, -1.557946535618014661, 0.5713013830897200052 ) ) ;
#39177=CARTESIAN_POINT ( 'NONE',  ( 0.2646723247128293655, -1.687375416948911244, 0.5682417262808783232 ) ) ;
#39178=CARTESIAN_POINT ( 'NONE',  ( 0.3222894045021684195, -1.758215778056678724, 0.5682417262808792113 ) ) ;
#39179=CARTESIAN_POINT ( 'NONE',  ( 0.04687500000000017347, -0.9399235171994243521, 0.1457185332388702959 ) ) ;
#39184=CARTESIAN_POINT ( 'NONE',  ( 0.1919946538045175233, -0.5556448844311334678, 0.2441157438994971951 ) ) ;
#39192=CARTESIAN_POINT ( 'NONE',  ( 0.5847200959167868639, -1.241056950120674518, 0.7055318339491533086 ) ) ;
#39204=CARTESIAN_POINT ( 'NONE',  ( 0.4804449940050610768, -1.088495069837083662, 0.7089115947332130796 ) ) ;
#39208=CARTESIAN_POINT ( 'NONE',  ( 0.1854929114990819528, -1.130708035657951305, 0.7521778099971917486 ) ) ;
#39209=EDGE_LOOP ( 'NONE', ( #20814, #5999, #18671, #4451, #36913, #27542, #34486 ) ) ;
#39214=CARTESIAN_POINT ( 'NONE',  ( 0.4639714015768776623, -1.230980424943016516, 0.6209263965717269906 ) ) ;
#39218=CARTESIAN_POINT ( 'NONE',  ( 0.2448569360945407336, -0.9465973144586597998, 0.4687868266098103587 ) ) ;
#39224=CARTESIAN_POINT ( 'NONE',  ( 0.4045308282536131950, -1.554303138208902757, 0.7579804941832600784 ) ) ;
#39225=CARTESIAN_POINT ( 'NONE',  ( 0.08904850043071313448, -0.5718714707336374214, 0.05944887859078885201 ) ) ;
#39227=CARTESIAN_POINT ( 'NONE',  ( 0.1185312037127926460, -1.298473412180007669, 0.5084237371918658432 ) ) ;
#39231=CARTESIAN_POINT ( 'NONE',  ( 0.4167025260715199186, -1.244396403474990809, 0.8329684759543855010 ) ) ;
#39233=CARTESIAN_POINT ( 'NONE',  ( 0.6342910143488530439, -1.590277009563203503, 0.6099924316480835884 ) ) ;
#39236=CARTESIAN_POINT ( 'NONE',  ( 0.1521839796440336845, -1.267694068221620896, 0.4309206314624388079 ) ) ;
#39238=CARTESIAN_POINT ( 'NONE',  ( 0.6998761188508713094, -1.434392152549301747, 0.7385670194571644087 ) ) ;
#39243=CARTESIAN_POINT ( 'NONE',  ( 0.1842078230746693746, -0.5805659298032126436, 0.0009058688700998594528 ) ) ;
#39246=CARTESIAN_POINT ( 'NONE',  ( 0.09104835764951833832, -0.9296025949902090302, 0.8700335549320106221 ) ) ;
#39251=ORIENTED_EDGE ( 'NONE', *, *, #7418, .F. ) ;
#39253=CARTESIAN_POINT ( 'NONE',  ( 0.6179330812053925870, -1.625469311300162811, 0.5182417262812423209 ) ) ;
#39254=CARTESIAN_POINT ( 'NONE',  ( 0.3210085668004670767, -1.182910313946810010, 0.5197417262808780025 ) ) ;
#39258=CARTESIAN_POINT ( 'NONE',  ( 0.5269365913707252380, -1.338824413986121842, 0.7108823065707898792 ) ) ;
#39261=CARTESIAN_POINT ( 'NONE',  ( 0.2858575041057334065, -0.8891697324286316206, 0.5691962326423758434 ) ) ;
#39262=VECTOR ( 'NONE', #25517, 39.37007874015748143 ) ;
#39266=CARTESIAN_POINT ( 'NONE',  ( 0.3270478934205144350, -1.639199132634546086, 0.5744591934003364653 ) ) ;
#39267=CARTESIAN_POINT ( 'NONE',  ( 0.7067742920676829410, -1.507341406312437293, 0.5470997294487818241 ) ) ;
#39273=CARTESIAN_POINT ( 'NONE',  ( 0.1548759089261008415, -1.279768374172244316, 0.4182417262808777458 ) ) ;
#39275=CARTESIAN_POINT ( 'NONE',  ( 0.3303989628691124114, -1.288507568649391866, 0.5994241297422728820 ) ) ;
#39278=ADVANCED_BREP_SHAPE_REPRESENTATION ( '', ( #18583, #27819 ), #21247 ) ;
#39279=CARTESIAN_POINT ( 'NONE',  ( 0.3422841821767727000, -1.070812901706339693, 0.6386172016438887988 ) ) ;
#39281=( BOUNDED_SURFACE ( )  B_SPLINE_SURFACE ( 3, 2, ( 
 ( #17821, #36558, #32844 ),
 ( #4861, #8365, #36137 ),
 ( #5263, #33656, #5469 ),
 ( #24223, #21129, #20934 ) ),
 .UNSPECIFIED., .F., .F., .F. ) 
 B_SPLINE_SURFACE_WITH_KNOTS ( ( 4, 4 ),
 ( 3, 3 ),
 ( -8.890457814381136359E-18, 0.0004170061191612176076 ),
 ( 0.000000000000000000, 1.000000000000000000 ),
 .UNSPECIFIED. ) 
 GEOMETRIC_REPRESENTATION_ITEM ( )  RATIONAL_B_SPLINE_SURFACE ( (
 ( 1.000000000000000000, 0.8864945003983012439, 1.000000000000000000),
 ( 1.000000000000000000, 0.8852517754806471517, 1.000000000000000000),
 ( 1.000000000000000000, 0.8837135633426822512, 1.000000000000000000),
 ( 1.000000000000000000, 0.8817574585067771142, 1.000000000000000000) ) ) 
 REPRESENTATION_ITEM ( '' )  SURFACE ( )  );
#39283=CARTESIAN_POINT ( 'NONE',  ( 0.6499222637756963961, -1.534002237024607584, 0.4182417262808776903 ) ) ;
#39284=CARTESIAN_POINT ( 'NONE',  ( 0.2821932362258575688, -1.666110558802125441, 0.4618966104728081667 ) ) ;
#39286=CARTESIAN_POINT ( 'NONE',  ( 0.4108854627016636507, -1.135744711144478503, 0.4324876386359573499 ) ) ;
#39290=CYLINDRICAL_SURFACE ( 'NONE', #38928, 0.03749999999977551152 ) ;
#39292=CARTESIAN_POINT ( 'NONE',  ( 0.4578538094500779754, -1.109988817041876352, 0.5689675956757063169 ) ) ;
#39293=CARTESIAN_POINT ( 'NONE',  ( 0.2153927220196321379, -1.354775012865835349, 1.025737857953066712 ) ) ;
#39302=CARTESIAN_POINT ( 'NONE',  ( 0.1344514937509518615, -0.5566420558580671418, 0.1875615093596288141 ) ) ;
#39303=CARTESIAN_POINT ( 'NONE',  ( -0.0008048508911302323975, -0.7725538104732808664, 0.0005696801228754680814 ) ) ;
#39306=CARTESIAN_POINT ( 'NONE',  ( 0.3382129488829186403, -0.9467566114000368627, 0.8359658843758493996 ) ) ;
#39308=CARTESIAN_POINT ( 'NONE',  ( -0.01330129037024533299, -0.5512292143768563468, 0.2608376860888254600 ) ) ;
#39310=CARTESIAN_POINT ( 'NONE',  ( 0.1723747331277147021, -1.257869073915691915, 0.6009879486010095695 ) ) ;
#39317=CARTESIAN_POINT ( 'NONE',  ( 0.2071075748763558100, -0.9148240409056219713, 0.6263237739596859699 ) ) ;
#39319=CARTESIAN_POINT ( 'NONE',  ( 0.1134335511682827979, -0.6991477288424914338, 0.5114506147767768907 ) ) ;
#39320=CARTESIAN_POINT ( 'NONE',  ( 0.4972768597348715680, -1.421470149658270898, 0.7931024745911073870 ) ) ;
#39321=CARTESIAN_POINT ( 'NONE',  ( 0.02122736906704300250, -1.007833681744604748, 0.5273104902783299908 ) ) ;
#39323=CARTESIAN_POINT ( 'NONE',  ( 0.1849096901904443147, -1.549205955729533235, 0.5682417262808779901 ) ) ;
#39326=DIRECTION ( 'NONE',  ( 0.01455087615875037474, 0.9998941303973200023, 0.000000000000000000 ) ) ;
#39329=CARTESIAN_POINT ( 'NONE',  ( 0.4690998592273773471, -1.116607765959707343, 0.5684169780556365126 ) ) ;
#39333=ADVANCED_FACE ( 'NONE', ( #3775 ), #32154, .F. ) ;
#39334=CARTESIAN_POINT ( 'NONE',  ( 0.006982617232424345385, -0.7536834681452820872, 0.4384055362127323718 ) ) ;
#39335=CARTESIAN_POINT ( 'NONE',  ( 0.4216623502531439693, -1.034931331451964143, 0.6525378447207771382 ) ) ;
#39338=CARTESIAN_POINT ( 'NONE',  ( 0.3173647091058168779, -0.7919842589448738979, 0.7159411547141941723 ) ) ;
#39346=CARTESIAN_POINT ( 'NONE',  ( 0.1514923887095717958, -1.230592969833345540, 0.9376751449580931208 ) ) ;
#39347=CARTESIAN_POINT ( 'NONE',  ( 0.1577606996786170002, -1.264465854478742157, 0.4314197961377732038 ) ) ;
#39351=CARTESIAN_POINT ( 'NONE',  ( 0.2019795930595086331, -0.6216091269244319317, 0.3384082674912240463 ) ) ;
#39357=ADVANCED_FACE ( 'NONE', ( #24722 ), #11162, .T. ) ;
#39358=PRODUCT ( 'Top Pivot Bracket', 'Top Pivot Bracket', '', ( #31427 ) ) ;
#39363=CARTESIAN_POINT ( 'NONE',  ( 0.1396326186464584285, -1.245954038625972871, 0.6057265985168657219 ) ) ;
#39364=CARTESIAN_POINT ( 'NONE',  ( 0.2446503497336322552, -0.9283727152547225359, 0.6908355059567328205 ) ) ;
#39365=CARTESIAN_POINT ( 'NONE',  ( 0.1472436744124528685, -1.061356063222618218, 0.9705180032994723538 ) ) ;
#39366=CARTESIAN_POINT ( 'NONE',  ( 0.4991955362234085647, -1.540752879515209450, 0.6255465156695737550 ) ) ;
#39367=CARTESIAN_POINT ( 'NONE',  ( 0.1131241454731939100, -0.6872203660140440151, -0.09530310615070609892 ) ) ;
#39368=CARTESIAN_POINT ( 'NONE',  ( 0.3051615010899081382, -1.653119291639537636, 0.5908386205647984113 ) ) ;
#39369=CARTESIAN_POINT ( 'NONE',  ( 0.2487198563054835165, -1.164593893902498234, 0.6393759972551884552 ) ) ;
#39373=CARTESIAN_POINT ( 'NONE',  ( 0.1402999466524724737, -0.5606445496649763438, 0.4675943975877205894 ) ) ;
#39374=LINE ( 'NONE', #4589, #30503 ) ;
#39376=CARTESIAN_POINT ( 'NONE',  ( 0.07620027864266576412, -1.321376928151553498, 0.4820378534147667371 ) ) ;
#39379=CARTESIAN_POINT ( 'NONE',  ( 0.3677026761718887315, -0.9383931188863808837, 0.6934371584156296953 ) ) ;
#39380=EDGE_CURVE ( 'NONE', #26668, #1874, #9602, .T. ) ;
#39391=CARTESIAN_POINT ( 'NONE',  ( 0.5136072266423519217, -1.127739116876707470, 0.6738619914697276947 ) ) ;
#39393=B_SPLINE_CURVE_WITH_KNOTS ( 'NONE', 3,
 ( #30035, #30436, #2263, #36607 ),
 .UNSPECIFIED., .F., .F.,
 ( 4, 4 ),
 ( 0.000000000000000000, 1.000000000000000000 ),
 .UNSPECIFIED. ) ;
#39394=CARTESIAN_POINT ( 'NONE',  ( 0.1803246710466453739, -1.251562748998523489, 0.7307791269380327082 ) ) ;
#39395=ORIENTED_EDGE ( 'NONE', *, *, #36047, .T. ) ;
#39396=LINE ( 'NONE', #8336, #8674 ) ;
#39402=CARTESIAN_POINT ( 'NONE',  ( 0.4358268961743849146, -1.190236072996399441, 0.6640218714533226985 ) ) ;
#39411=CARTESIAN_POINT ( 'NONE',  ( 0.08491816545164443397, -0.6773013968507372029, 0.4888687927153864132 ) ) ;
#39412=CARTESIAN_POINT ( 'NONE',  ( 0.08805611400531067334, -0.6473513853021811704, 0.02913009454904720227 ) ) ;
#39414=CARTESIAN_POINT ( 'NONE',  ( 0.1761392914182259850, -1.265181628236080824, 0.4952186049836316828 ) ) ;
#39415=ORIENTED_EDGE ( 'NONE', *, *, #22567, .F. ) ;
#39418=CARTESIAN_POINT ( 'NONE',  ( 0.2649443680508836718, -0.9506954219886920576, 0.7345657905482877448 ) ) ;
#39423=CARTESIAN_POINT ( 'NONE',  ( 0.2257601701386385828, -1.236660534205411333, 0.5094317095389198080 ) ) ;
#39427=CARTESIAN_POINT ( 'NONE',  ( 0.7110913793137424443, -1.453804679565707803, 0.7028629728786995878 ) ) ;
#39435=ADVANCED_FACE ( 'NONE', ( #22048 ), #19591, .T. ) ;
#39438=CARTESIAN_POINT ( 'NONE',  ( -3.276078897458520021E-17, -0.4262518876079541830, 0.1281883534109924672 ) ) ;
#39441=FACE_OUTER_BOUND ( 'NONE', #30206, .T. ) ;
#39445=CARTESIAN_POINT ( 'NONE',  ( 0.2322138788700108258, -1.233113307957229177, 0.3157417262808777658 ) ) ;
#39446=CARTESIAN_POINT ( 'NONE',  ( 0.08030483728411769162, -0.5440987430357651089, 0.1459341340629038419 ) ) ;
#39448=CARTESIAN_POINT ( 'NONE',  ( 0.3633940536647746189, -1.097306544473756640, 0.7529995174779674505 ) ) ;
#39451=CARTESIAN_POINT ( 'NONE',  ( 0.4504611332311936889, -1.053473412190887304, 0.6915920958210214353 ) ) ;
#39452=EDGE_CURVE ( 'NONE', #38533, #17741, #37889, .T. ) ;
#39456=ORIENTED_EDGE ( 'NONE', *, *, #12267, .F. ) ;
#39458=CARTESIAN_POINT ( 'NONE',  ( 0.3583310641576757938, -1.622257436576277190, 0.6094965212440786040 ) ) ;
#39459=CARTESIAN_POINT ( 'NONE',  ( 0.6778803828687806066, -1.516512415086665344, 0.4467122667541399972 ) ) ;
#39464=ORIENTED_EDGE ( 'NONE', *, *, #4503, .F. ) ;
#39467=CARTESIAN_POINT ( 'NONE',  ( 0.09580522634512994573, -0.8544855528359687202, 0.4211259006973531172 ) ) ;
#39468=CARTESIAN_POINT ( 'NONE',  ( 0.3405242896115074913, -1.744906522954273731, 0.4484829386636806081 ) ) ;
#39474=DIRECTION ( 'NONE',  ( 0.8660512985181134660, 0.4999551463232371762, 0.000000000000000000 ) ) ;
#39477=CARTESIAN_POINT ( 'NONE',  ( 0.06056337598226081698, -1.309773928473624505, 0.6311107274231992914 ) ) ;
#39478=CARTESIAN_POINT ( 'NONE',  ( 0.4510273968575216341, -1.245587961952838718, 0.6057417262809815517 ) ) ;
#39479=CARTESIAN_POINT ( 'NONE',  ( 0.3249483201304784741, -1.768002432019315728, 0.5182417262812728520 ) ) ;
#39482=CARTESIAN_POINT ( 'NONE',  ( 2.290505790419000988E-05, -0.4780051411654945848, -0.01121176583438007919 ) ) ;
#39488=EDGE_LOOP ( 'NONE', ( #17131, #4953, #30355, #12849 ) ) ;
#39490=ORIENTED_EDGE ( 'NONE', *, *, #14535, .T. ) ;
#39493=CARTESIAN_POINT ( 'NONE',  ( 0.008656601633535388959, -0.6460992163107364128, -0.007090344436191942101 ) ) ;
#39496=CARTESIAN_POINT ( 'NONE',  ( 0.1519284701276231164, -0.5919472871766352506, 0.5183721702484739291 ) ) ;
#39497=VERTEX_POINT ( 'NONE', #29152 ) ;
#39506=ORIENTED_EDGE ( 'NONE', *, *, #24256, .F. ) ;
#39508=CARTESIAN_POINT ( 'NONE',  ( 0.1059350862884271965, -1.337751531233084545, 0.7070564584916527728 ) ) ;
#39509=CARTESIAN_POINT ( 'NONE',  ( 0.09365314453647033410, -0.5743219976380223857, 0.2688796733879867951 ) ) ;
#39512=CARTESIAN_POINT ( 'NONE',  ( 0.1870925830679437130, -0.7146760840282513350, 0.03103855360005942920 ) ) ;
#39513=CARTESIAN_POINT ( 'NONE',  ( 0.4757310988838256427, -1.669109449190596228, 0.5669542959959941175 ) ) ;
#39516=CARTESIAN_POINT ( 'NONE',  ( 0.3461189067787796558, -1.156139424848509956, 0.4335238789691411299 ) ) ;
#39518=CARTESIAN_POINT ( 'NONE',  ( 0.1876053338355621880, -0.6785855078148245179, 0.1477569985384105666 ) ) ;
#39520=CARTESIAN_POINT ( 'NONE',  ( 0.01135805250241819081, -0.9385525037653906777, 0.08271764842014434072 ) ) ;
#39521=CARTESIAN_POINT ( 'NONE',  ( 0.4115766028365042128, -1.733048369835246794, 0.5182417262812423209 ) ) ;
#39524=CARTESIAN_POINT ( 'NONE',  ( 0.0003293075040918708759, -0.6974492147978401668, 0.2474296275395909961 ) ) ;
#39525=CARTESIAN_POINT ( 'NONE',  ( 0.4718294406633598559, -1.074170765704426822, 0.6461978756939577018 ) ) ;
#39527=CARTESIAN_POINT ( 'NONE',  ( 0.5225354986670117663, -1.146792065252953297, 0.8742509268737332917 ) ) ;
#39534=CARTESIAN_POINT ( 'NONE',  ( 0.1406468284892466447, -1.193466478313442991, 0.9284149979398328423 ) ) ;
#39536=CARTESIAN_POINT ( 'NONE',  ( 0.3538719729184752749, -1.624715450675502160, 0.4182417262808775238 ) ) ;
#39540=CARTESIAN_POINT ( 'NONE',  ( 0.5387674647098039671, -1.171534441891039169, 0.7413454372389880476 ) ) ;
#39549=ORIENTED_EDGE ( 'NONE', *, *, #875, .T. ) ;
#39550=CARTESIAN_POINT ( 'NONE',  ( 0.1897001248997009504, -1.237817139529930222, 0.5863507469836753971 ) ) ;
#39552=CARTESIAN_POINT ( 'NONE',  ( 0.2609408554674475522, -0.9584677431853507734, 0.7004531198503530787 ) ) ;
#39554=CARTESIAN_POINT ( 'NONE',  ( 0.2692473483777980126, -1.497112465990877439, 1.008263284785997804 ) ) ;
#39555=CARTESIAN_POINT ( 'NONE',  ( 0.4975907999090993794, -1.542531306350466869, 0.5755255995287604787 ) ) ;
#39556=CARTESIAN_POINT ( 'NONE',  ( 0.1149968254612746543, -0.4588679775494129975, 0.06802948968277178210 ) ) ;
#39558=CARTESIAN_POINT ( 'NONE',  ( 0.02367353041037730671, -0.9777710647417211520, 0.4475088345234511933 ) ) ;
#39564=CARTESIAN_POINT ( 'NONE',  ( 0.4977951372335264746, -1.107966894584811790, 0.8692732641236018409 ) ) ;
#39573=CARTESIAN_POINT ( 'NONE',  ( 0.3540817610093318635, -1.633452470505663667, 0.5182417262812423209 ) ) ;
#39574=CARTESIAN_POINT ( 'NONE',  ( 0.1906247196645202702, -0.5843772811062371009, 0.1457185332388696020 ) ) ;
#39578=EDGE_CURVE ( 'NONE', #8227, #8719, #10323, .T. ) ;
#39582=CARTESIAN_POINT ( 'NONE',  ( 0.4692656535582095945, -1.239599139632956426, 0.6019514904091477492 ) ) ;
#39584=CARTESIAN_POINT ( 'NONE',  ( 0.6068869525525029118, -1.480059939399680280, 0.5671080680285526254 ) ) ;
#39588=CARTESIAN_POINT ( 'NONE',  ( 0.1876053338355621880, -0.6785855078148245179, 0.1477569985384105666 ) ) ;
#39590=CARTESIAN_POINT ( 'NONE',  ( 0.1204589479551298192, -1.085572435350046216, 0.7460617499609929482 ) ) ;
#39591=ORIENTED_EDGE ( 'NONE', *, *, #18209, .F. ) ;
#39596=CARTESIAN_POINT ( 'NONE',  ( 0.1574750639814709308, -1.391761509719479761, 0.4336789700803105330 ) ) ;
#39599=CARTESIAN_POINT ( 'NONE',  ( 0.4787510807856267259, -1.256362448863320269, 0.6027525166291474168 ) ) ;
#39603=EDGE_LOOP ( 'NONE', ( #11644, #5961 ) ) ;
#39604=ORIENTED_EDGE ( 'NONE', *, *, #15191, .F. ) ;
#39605=CARTESIAN_POINT ( 'NONE',  ( 0.07006815180908300411, -1.315301596572415299, 0.5080907171456733318 ) ) ;
#39608=CARTESIAN_POINT ( 'NONE',  ( 0.1860373355776311632, -0.4547550531002670371, 0.008518417185872215538 ) ) ;
#39609=CARTESIAN_POINT ( 'NONE',  ( 0.06201235461866828891, -0.5659405159657984186, 0.2619933746457878687 ) ) ;
#39611=CARTESIAN_POINT ( 'NONE',  ( 0.6889402512469305906, -1.555172295161277196, 0.5968700266842814628 ) ) ;
#39615=EDGE_CURVE ( 'NONE', #12702, #40154, #20209, .T. ) ;
#39617=CARTESIAN_POINT ( 'NONE',  ( 0.5640895105453352931, -1.503407492374277510, 0.5358556994421860287 ) ) ;
#39619=CARTESIAN_POINT ( 'NONE',  ( 0.5121199761860573130, -1.393593559852499109, 0.7948695422178503334 ) ) ;
#39621=CARTESIAN_POINT ( 'NONE',  ( 0.3252720331744159421, -1.756211604028340423, 0.5534074152425280113 ) ) ;
#39624=CARTESIAN_POINT ( 'NONE',  ( 0.1981403273678030152, -1.252645933650147425, 0.4502181074018651308 ) ) ;
#39628=CARTESIAN_POINT ( 'NONE',  ( 0.7145247768745858208, -1.460049439684881323, 0.6872404240164239342 ) ) ;
#39633=CARTESIAN_POINT ( 'NONE',  ( 0.0001243953464272101240, -0.9491217415751835862, 0.2153467644550133564 ) ) ;
#39641=CARTESIAN_POINT ( 'NONE',  ( 0.09580854502948936424, -0.9100554415251292939, 0.8942175666832257175 ) ) ;
#39645=ORIENTED_EDGE ( 'NONE', *, *, #18433, .T. ) ;
#39648=CARTESIAN_POINT ( 'NONE',  ( 0.3414116791095713754, -1.169548512706389154, 0.5830580198056709573 ) ) ;
#39652=CARTESIAN_POINT ( 'NONE',  ( 0.4204492835407447893, -1.176608965458264322, 0.7497476517331604917 ) ) ;
#39655=CARTESIAN_POINT ( 'NONE',  ( 0.2247355409086003175, -0.8309010600190726015, 0.4364284219733364223 ) ) ;
#39661=AXIS2_PLACEMENT_3D ( 'NONE', #38645, #28791, #650 ) ;
#39662=CARTESIAN_POINT ( 'NONE',  ( 0.2981414330301035975, -1.451159418586606797, 0.8869886242261938447 ) ) ;
#39663=CARTESIAN_POINT ( 'NONE',  ( 0.6752983665511703704, -1.520205868421071971, 0.4435471312318282622 ) ) ;
#39664=CARTESIAN_POINT ( 'NONE',  ( 0.1869923964628150137, -0.6032852809087916324, 0.0007069082392771173411 ) ) ;
#39668=VERTEX_POINT ( 'NONE', #29975 ) ;
#39673=CARTESIAN_POINT ( 'NONE',  ( 0.2556509140510369038, -1.160232112247506109, 0.7428221499324000332 ) ) ;
#39677=CARTESIAN_POINT ( 'NONE',  ( 0.1109092093543055241, -0.9286325583098424818, 0.1457252011008478843 ) ) ;
#39679=CARTESIAN_POINT ( 'NONE',  ( 0.3571473637288121172, -1.161317952103357865, 0.4288090205490824314 ) ) ;
#39686=CARTESIAN_POINT ( 'NONE',  ( 0.4797714183061499438, -1.117321928803942654, 0.5295840580642868778 ) ) ;
#39693=CARTESIAN_POINT ( 'NONE',  ( 0.0002084515527543570027, -0.5213305055289283452, -0.04052408320813689208 ) ) ;
#39695=CARTESIAN_POINT ( 'NONE',  ( 0.002064972446937151339, -0.4784520794224960683, 0.3149028691301604121 ) ) ;
#39706=CARTESIAN_POINT ( 'NONE',  ( -0.001920489672809163684, -0.8476932489793732595, 0.09397500963053398437 ) ) ;
#39710=CARTESIAN_POINT ( 'NONE',  ( 0.2660823795547838655, -1.675198854444863716, 0.5696963268675777625 ) ) ;
#39712=CARTESIAN_POINT ( 'NONE',  ( 0.1323828673530924871, -1.257873181764345816, 0.6230388128859498664 ) ) ;
#39713=CARTESIAN_POINT ( 'NONE',  ( 0.3645392532257850093, -1.157254380035450447, 0.4995441290596880912 ) ) ;
#39716=EDGE_CURVE ( 'NONE', #31635, #21929, #7425, .T. ) ;
#39718=EDGE_LOOP ( 'NONE', ( #35255, #27937, #21094, #39604, #22587 ) ) ;
#39720=AXIS2_PLACEMENT_3D ( 'NONE', #12062, #8969, #30374 ) ;
#39721=CARTESIAN_POINT ( 'NONE',  ( 0.01167029684184067023, -0.7543104828189726163, -0.1044922862589389156 ) ) ;
#39724=CARTESIAN_POINT ( 'NONE',  ( 0.07028185168205175470, -0.5531160948379537645, 0.2188760460452662537 ) ) ;
#39726=CARTESIAN_POINT ( 'NONE',  ( 0.1873654698603020585, -0.6959066354592325920, 0.03335868142391257979 ) ) ;
#39732=AXIS2_PLACEMENT_3D ( 'NONE', #27362, #33304, #5110 ) ;
#39734=CARTESIAN_POINT ( 'NONE',  ( 0.4820730268389710194, -1.120100422993975275, 0.5182417262812748504 ) ) ;
#39736=CARTESIAN_POINT ( 'NONE',  ( 0.01135114394058200742, -0.9404934803143812916, 0.09104275933669267462 ) ) ;
#39737=CARTESIAN_POINT ( 'NONE',  ( 0.4363412383469720268, -1.230814285733859315, 0.5836505495634819463 ) ) ;
#39740=CARTESIAN_POINT ( 'NONE',  ( 0.2949739106045629056, -1.710307911171992323, 0.7406796427396996618 ) ) ;
#39741=CARTESIAN_POINT ( 'NONE',  ( 0.4319471385618090520, -1.049247276449186916, 0.6348846931381728620 ) ) ;
#39742=CARTESIAN_POINT ( 'NONE',  ( -0.0007814672454587524896, -0.8642386026234205598, 0.3264423145784848268 ) ) ;
#39744=CARTESIAN_POINT ( 'NONE',  ( 0.6630438016670622270, -1.374754038922163080, 0.8377997132616019638 ) ) ;
#39754=CARTESIAN_POINT ( 'NONE',  ( 0.008711396254904512151, -0.6169322991267630618, 0.4321200063933361424 ) ) ;
#39755=CARTESIAN_POINT ( 'NONE',  ( 0.5879381176784390650, -1.491229467720181390, 0.5734525147726333705 ) ) ;
#39761=CARTESIAN_POINT ( 'NONE',  ( 0.2674444507101633728, -0.7485333398656358606, 0.5795413912256205391 ) ) ;
#39765=( BOUNDED_SURFACE ( )  B_SPLINE_SURFACE ( 3, 2, ( 
 ( #11711, #36790, #8211 ),
 ( #17668, #39679, #20977 ),
 ( #17273, #21399, #1669 ),
 ( #36187, #11303, #2047 ) ),
 .UNSPECIFIED., .F., .F., .F. ) 
 B_SPLINE_SURFACE_WITH_KNOTS ( ( 4, 4 ),
 ( 3, 3 ),
 ( 0.01563290161724498195, 0.01614380785394589277 ),
 ( 0.8846791454767857221, 1.000000000000000000 ),
 .UNSPECIFIED. ) 
 GEOMETRIC_REPRESENTATION_ITEM ( )  RATIONAL_B_SPLINE_SURFACE ( (
 ( 0.9401556194672928690, 0.9661773532027507772, 1.000000000000000000),
 ( 0.9401609085802409282, 0.9661803424859135569, 1.000000000000000000),
 ( 0.9401662911497292718, 0.9661833845885311467, 1.000000000000000000),
 ( 0.9401715974566158263, 0.9661863835893065300, 1.000000000000000000) ) ) 
 REPRESENTATION_ITEM ( '' )  SURFACE ( )  );
#39770=VERTEX_POINT ( 'NONE', #17620 ) ;
#39772=CARTESIAN_POINT ( 'NONE',  ( 0.08909969736564220255, -0.7080461655569163515, 0.2259464132569931061 ) ) ;
#39773=CARTESIAN_POINT ( 'NONE',  ( 0.3012310081014870078, -1.678279676007319310, 0.8715374191053447683 ) ) ;
#39774=CARTESIAN_POINT ( 'NONE',  ( 0.4975585306863050117, -1.542526060902300822, 0.5750136511568909592 ) ) ;
#39777=CARTESIAN_POINT ( 'NONE',  ( 0.03992535094069216833, -1.048059102012378840, 0.5962256563898924444 ) ) ;
#39780=CARTESIAN_POINT ( 'NONE',  ( 0.3169571484440001363, -1.762177905942989398, 0.5412171649221120262 ) ) ;
#39781=CARTESIAN_POINT ( 'NONE',  ( 0.3565767535945514877, -0.9039810230172339311, 0.7062321383356453541 ) ) ;
#39786=CARTESIAN_POINT ( 'NONE',  ( 0.06838828474556885029, -1.327737673307782806, 0.5330404844705093348 ) ) ;
#39789=CARTESIAN_POINT ( 'NONE',  ( 0.3178934152576730621, -1.184108536564375314, 0.5634386359574784509 ) ) ;
#39790=CARTESIAN_POINT ( 'NONE',  ( 0.5539006188405288800, -1.190957016459229800, 0.5326915342634773731 ) ) ;
#39796=CARTESIAN_POINT ( 'NONE',  ( 0.4542841342992246512, -1.218320695817829202, 0.6688155487934264176 ) ) ;
#39801=CARTESIAN_POINT ( 'NONE',  ( 0.1892549258828873926, -0.8411929458066104148, 0.2428197129412378030 ) ) ;
#39808=CARTESIAN_POINT ( 'NONE',  ( 0.2263037797473778368, -1.351310894833297915, 0.5807374671911091912 ) ) ;
#39815=CARTESIAN_POINT ( 'NONE',  ( 0.4653576118663421690, -1.234380357178559651, 0.6478506215840158511 ) ) ;
#39820=CIRCLE ( 'NONE', #23440, 0.03749999999977557397 ) ;
#39822=ORIENTED_EDGE ( 'NONE', *, *, #38075, .F. ) ;
#39824=CARTESIAN_POINT ( 'NONE',  ( 0.3896793708141981227, -1.455733931370364553, 0.8396294446493801633 ) ) ;
#39827=CARTESIAN_POINT ( 'NONE',  ( 0.1876235411046664192, -0.7934053227479342940, 0.2850852003878450169 ) ) ;
#39828=CARTESIAN_POINT ( 'NONE',  ( 0.4952252789729119642, -1.180554010857031599, 0.4224090057976987445 ) ) ;
#39831=ORIENTED_EDGE ( 'NONE', *, *, #7422, .F. ) ;
#39833=CARTESIAN_POINT ( 'NONE',  ( 0.5811665336899081158, -1.491966016390690708, 0.6316321043910979594 ) ) ;
#39834=CARTESIAN_POINT ( 'NONE',  ( 0.5825649363837883676, -1.621069190649260694, 0.5720958814438571460 ) ) ;
#39837=CARTESIAN_POINT ( 'NONE',  ( 0.4910727179654820196, -1.657301623184578077, 0.4283731996474700598 ) ) ;
#39842=CARTESIAN_POINT ( 'NONE',  ( 0.3632211645871377126, -0.8757803013682723403, 0.7750855204132592879 ) ) ;
#39843=CARTESIAN_POINT ( 'NONE',  ( 0.1677396061116748216, -1.215651260229680286, 0.5182417262812423209 ) ) ;
#39844=CARTESIAN_POINT ( 'NONE',  ( 0.003727000072687845170, -0.9627618936687203366, 0.4240455811949819243 ) ) ;
#39849=CARTESIAN_POINT ( 'NONE',  ( 0.6292630781544163998, -1.582461550746711909, 0.6099326772577570166 ) ) ;
#39854=CARTESIAN_POINT ( 'NONE',  ( 0.1818238028002573947, -0.5066057096094660483, 0.1075624334068491922 ) ) ;
#39856=ADVANCED_FACE ( 'NONE', ( #28712 ), #29322, .T. ) ;
#39862=CARTESIAN_POINT ( 'NONE',  ( 0.3445304142628009547, -1.145137055011931748, 0.5942808790109807004 ) ) ;
#39863=CARTESIAN_POINT ( 'NONE',  ( 0.1859142959171137532, -0.8501877694175364875, 0.2020740118391618767 ) ) ;
#39865=CARTESIAN_POINT ( 'NONE',  ( 0.5221384440520447923, -1.330831645065488456, 0.6091261937352400180 ) ) ;
#39868=CARTESIAN_POINT ( 'NONE',  ( 0.5137183020217809259, -1.118314259765692764, 0.5770968910244165251 ) ) ;
#39875=CARTESIAN_POINT ( 'NONE',  ( 0.3562241851712061314, -1.622432527926769064, 0.5753824526387549820 ) ) ;
#39877=CARTESIAN_POINT ( 'NONE',  ( 0.7051250147666914270, -1.492378199219462465, 0.5174013405292774426 ) ) ;
#39878=CARTESIAN_POINT ( 'NONE',  ( 0.1764858099340315956, -0.5346581714635332272, -0.02636846031365289167 ) ) ;
#39880=B_SPLINE_CURVE_WITH_KNOTS ( 'NONE', 3,
 ( #7232, #10355, #14032, #4160, #29886, #13630, #20019, #26607, #39141, #32951, #10968, #16727, #14242, #36045, #926, #26002, #38524, #26196 ),
 .UNSPECIFIED., .F., .F.,
 ( 4, 2, 2, 2, 2, 2, 2, 2, 4 ),
 ( 0.006341682393953856911, 0.007137201732907770199, 0.007932721071861683487, 0.008728240410815596775, 0.009523759749769510063, 0.01031927908872342335, 0.01111479842767733664, 0.01191031776663124993, 0.01270583710558516495 ),
 .UNSPECIFIED. ) ;
#39883=CARTESIAN_POINT ( 'NONE',  ( 0.3578131408655606527, -1.083403370911659946, 0.6388820969571129549 ) ) ;
#39884=ORIENTED_EDGE ( 'NONE', *, *, #33368, .F. ) ;
#39887=CARTESIAN_POINT ( 'NONE',  ( 0.3843371407211305657, -1.261522862150258772, 0.5682417262808739933 ) ) ;
#39888=DIRECTION ( 'NONE',  ( 0.4999551463232371762, -0.8660512985181134660, 0.000000000000000000 ) ) ;
#39890=CARTESIAN_POINT ( 'NONE',  ( 0.1316017208954911588, -1.248059642665102942, 0.5182417262812423209 ) ) ;
#39893=CARTESIAN_POINT ( 'NONE',  ( 0.4134740292144571949, -1.130738711115819140, 0.4880408775256062093 ) ) ;
#39896=CARTESIAN_POINT ( 'NONE',  ( 0.4819606849173208030, -1.119673669223240520, 0.5199609940792718765 ) ) ;
#39899=EDGE_CURVE ( 'NONE', #13346, #3151, #4002, .T. ) ;
#39900=FACE_OUTER_BOUND ( 'NONE', #4538, .T. ) ;
#39903=CARTESIAN_POINT ( 'NONE',  ( 0.08577121655192940231, -0.8846912944720071170, 0.8606152429655203884 ) ) ;
#39904=CARTESIAN_POINT ( 'NONE',  ( 0.3702085959188072817, -1.615317497076966813, 0.4882469897972006589 ) ) ;
#39913=CARTESIAN_POINT ( 'NONE',  ( 0.006342365902731740036, -0.8382430779231306861, 0.09710106263402516757 ) ) ;
#39918=ORIENTED_EDGE ( 'NONE', *, *, #15969, .T. ) ;
#39920=CARTESIAN_POINT ( 'NONE',  ( -0.0005976636740459253172, -0.5552437863504529059, 0.2653367056401107482 ) ) ;
#39922=CARTESIAN_POINT ( 'NONE',  ( 0.1617803284656291196, -1.239972288448516702, 0.6007116129271903304 ) ) ;
#39930=CARTESIAN_POINT ( 'NONE',  ( 0.3648817522660376400, -1.130029036334877279, 0.6215301754536329826 ) ) ;
#39932=CARTESIAN_POINT ( 'NONE',  ( 0.2654586657438877673, -0.9403158806777288659, 0.7264623116330005681 ) ) ;
#39933=CARTESIAN_POINT ( 'NONE',  ( 0.1853458231138309653, -0.8340042177779849464, 0.1270555878011652151 ) ) ;
#39934=DIRECTION ( 'NONE',  ( 0.8660512985181134660, 0.4999551463232372317, 0.000000000000000000 ) ) ;
#39937=CARTESIAN_POINT ( 'NONE',  ( 0.3954090057121530388, -1.720129112149186845, 0.4259808212722830389 ) ) ;
#39938=DIRECTION ( 'NONE',  ( -0.4999551463232333459, 0.8660512985181156864, 0.000000000000000000 ) ) ;
#39940=CARTESIAN_POINT ( 'NONE',  ( 0.4190882504452823620, -1.118891637760769830, 0.5995514612943967370 ) ) ;
#39943=CARTESIAN_POINT ( 'NONE',  ( 0.03474859143381433396, -0.6982915424597320175, 0.6540940360414806420 ) ) ;
#39944=CARTESIAN_POINT ( 'NONE',  ( 0.05991778417293673609, -1.332687696286689594, 0.5682717497416263086 ) ) ;
#39946=CARTESIAN_POINT ( 'NONE',  ( 0.7224934542336318710, -1.479659627397842403, 0.5766931279523788145 ) ) ;
#39947=ADVANCED_FACE ( 'NONE', ( #27801 ), #10697, .F. ) ;
#39954=CARTESIAN_POINT ( 'NONE',  ( 0.01685698302946367702, -0.6256804056397152758, 0.4269450335313899059 ) ) ;
#39955=CARTESIAN_POINT ( 'NONE',  ( 0.1285611044470676978, -0.5511077305290806860, 0.1614518025332021822 ) ) ;
#39959=CARTESIAN_POINT ( 'NONE',  ( 0.1943341254738605584, -0.5992045414336306663, 0.2618067726929366734 ) ) ;
#39962=CARTESIAN_POINT ( 'NONE',  ( 0.6927131938946141654, -1.422842782059151157, 0.6785767152737546271 ) ) ;
#39968=CARTESIAN_POINT ( 'NONE',  ( 0.1645055737317709932, -0.8154898342693455149, 0.5663631941838773720 ) ) ;
#39969=CARTESIAN_POINT ( 'NONE',  ( 0.3201253347856640175, -1.704124430139120072, 0.8372518665352793876 ) ) ;
#39970=CARTESIAN_POINT ( 'NONE',  ( 0.09934153309614388028, -0.5690506854145357396, 0.2508956654826926536 ) ) ;
#39971=CARTESIAN_POINT ( 'NONE',  ( 0.3352399569063156393, -1.753319872000470792, 0.4596133135264604541 ) ) ;
#39972=CARTESIAN_POINT ( 'NONE',  ( 0.001312449538768875905, -0.5612271264025527895, 0.03476213731316191852 ) ) ;
#39973=CARTESIAN_POINT ( 'NONE',  ( 0.03908111062118940771, -1.198967014588472102, 0.6667909696853414614 ) ) ;
#39977=CARTESIAN_POINT ( 'NONE',  ( 0.3967191919388743382, -0.9324009735222377193, 0.8071385964775494859 ) ) ;
#39979=CARTESIAN_POINT ( 'NONE',  ( 0.4687631324631791330, -1.116557084650701359, 0.5688798658794104179 ) ) ;
#39980=CARTESIAN_POINT ( 'NONE',  ( 0.6841302653033145553, -1.411212316466117223, 0.6057417262805112612 ) ) ;
#39982=CARTESIAN_POINT ( 'NONE',  ( 0.3246143735900494653, -1.168538765758894371, 0.4697788401231595690 ) ) ;
#39983=B_SPLINE_CURVE_WITH_KNOTS ( 'NONE', 3,
 ( #15738, #38352, #10190, #7077, #22758, #1555, #35683, #38751, #13266, #10796, #4204, #7483, #23565, #32182, #29317, #16769, #20062, #35283 ),
 .UNSPECIFIED., .F., .F.,
 ( 4, 2, 2, 2, 2, 2, 2, 2, 4 ),
 ( 0.000000000000000000, 0.0003722439366697991980, 0.0007444878733395983959, 0.001116731810009397594, 0.001488975746679196792, 0.001861219683348995990, 0.002233463620018795188, 0.002605707556688594169, 0.002977951493358393584 ),
 .UNSPECIFIED. ) ;
#39984=CARTESIAN_POINT ( 'NONE',  ( 0.5505100836374232642, -1.180854739677868359, 0.6191363254822006557 ) ) ;
#39986=CARTESIAN_POINT ( 'NONE',  ( 0.6184971854324693430, -1.588153737519645281, 0.6167571325555825101 ) ) ;
#39987=B_SPLINE_CURVE_WITH_KNOTS ( 'NONE', 5,
 ( #8677, #17345, #30286, #29902, #20645, #2119 ),
 .UNSPECIFIED., .F., .F.,
 ( 6, 6 ),
 ( 4.822244625248871763, 7.710395699062019936 ),
 .UNSPECIFIED. ) ;
#39989=DIRECTION ( 'NONE',  ( -0.4999551463232372317, 0.8660512985181135770, -0.000000000000000000 ) ) ;
#39991=( BOUNDED_SURFACE ( )  B_SPLINE_SURFACE ( 3, 2, ( 
 ( #34490, #37368, #27926 ),
 ( #18444, #19067, #37178 ),
 ( #15764, #182, #15977 ),
 ( #30995, #15368, #37983 ),
 ( #9793, #28312, #40465 ),
 ( #37560, #5883, #6303 ),
 ( #18657, #24847, #31603 ),
 ( #12290, #9179, #21747 ),
 ( #34279, #8995, #6088 ),
 ( #9599, #12675, #31216 ) ),
 .UNSPECIFIED., .F., .F., .T. ) 
 B_SPLINE_SURFACE_WITH_KNOTS ( ( 4, 2, 2, 2, 4 ),
 ( 3, 3 ),
 ( -9.757819552369539906E-18, 0.0004973432167690072835, 0.0009946864335380243248, 0.001492029650307041475, 0.001989372867076058624 ),
 ( 0.000000000000000000, 1.000000000000000000 ),
 .UNSPECIFIED. ) 
 GEOMETRIC_REPRESENTATION_ITEM ( )  RATIONAL_B_SPLINE_SURFACE ( (
 ( 1.000000000000000000, 0.8897565210026132654, 1.000000000000000000),
 ( 1.000000000000000000, 0.8899231130074136686, 1.000000000000000000),
 ( 1.000000000000000000, 0.8890122559934640067, 1.000000000000000000),
 ( 1.000000000000000000, 0.8849579905325665186, 1.000000000000000000),
 ( 1.000000000000000000, 0.8818374620091549154, 1.000000000000000000),
 ( 1.000000000000000000, 0.8735256406124205508, 1.000000000000000000),
 ( 1.000000000000000000, 0.8682786441878931338, 1.000000000000000000),
 ( 1.000000000000000000, 0.8559483198610358112, 1.000000000000000000),
 ( 1.000000000000000000, 0.8487295818195398356, 1.000000000000000000),
 ( 1.000000000000000000, 0.8407181564550617603, 1.000000000000000000) ) ) 
 REPRESENTATION_ITEM ( '' )  SURFACE ( )  );
#39994=CARTESIAN_POINT ( 'NONE',  ( 0.08510361377861434817, -0.8106636051554854117, 0.1454306519311501233 ) ) ;
#39997=CARTESIAN_POINT ( 'NONE',  ( 0.1533772736604412101, -1.181689746394253726, 0.7533906142735892209 ) ) ;
#39998=ORIENTED_EDGE ( 'NONE', *, *, #14433, .F. ) ;
#40004=CARTESIAN_POINT ( 'NONE',  ( 0.4711122148191352887, -1.243347910189986916, 0.6355297091942355703 ) ) ;
#40006=CARTESIAN_POINT ( 'NONE',  ( -0.0004431470427073231017, -0.9367128829938298207, 0.1457185332388704069 ) ) ;
#40008=VERTEX_POINT ( 'NONE', #26981 ) ;
#40010=CARTESIAN_POINT ( 'NONE',  ( 0.06545186104482746126, -1.329499349160038868, 0.5176190731536282064 ) ) ;
#40012=CARTESIAN_POINT ( 'NONE',  ( 0.1861675601333642183, -0.7337134285967986669, -0.03797464539687132185 ) ) ;
#40013=CARTESIAN_POINT ( 'NONE',  ( 0.3382961071825119070, -1.342601817737219205, 0.8746150539162650395 ) ) ;
#40014=DIRECTION ( 'NONE',  ( 0.9966814372958092694, 0.000000000000000000, 0.08140093703367154432 ) ) ;
#40019=ORIENTED_EDGE ( 'NONE', *, *, #13923, .F. ) ;
#40021=CARTESIAN_POINT ( 'NONE',  ( 0.1311121416671343076, -0.6135371899443636812, 0.3487476746206483735 ) ) ;
#40022=CARTESIAN_POINT ( 'NONE',  ( 0.4696177048947446919, -1.669690955150979095, 0.4747328526538268645 ) ) ;
#40025=CARTESIAN_POINT ( 'NONE',  ( 0.2147974912797966929, -1.231358751133227347, 0.5546678855025314325 ) ) ;
#40026=CARTESIAN_POINT ( 'NONE',  ( 0.2135845999631697523, -1.238000303071007613, 0.5636751376830327898 ) ) ;
#40029=CARTESIAN_POINT ( 'NONE',  ( 0.1969702849860160421, -0.5469408226469265610, 0.3272831088336244365 ) ) ;
#40034=CARTESIAN_POINT ( 'NONE',  ( 0.5996218235215466930, -1.599608852905763712, 0.6078077878447281091 ) ) ;
#40035=CARTESIAN_POINT ( 'NONE',  ( 0.6568730927750874304, -1.460570608776338597, 0.4224083929475443977 ) ) ;
#40045=CARTESIAN_POINT ( 'NONE',  ( 0.4145109374026955673, -1.110466390532955927, 0.6153597435504403190 ) ) ;
#40046=CARTESIAN_POINT ( 'NONE',  ( 0.3332542364016487513, -1.159914367434109694, 0.5808425792736833237 ) ) ;
#40047=CARTESIAN_POINT ( 'NONE',  ( 0.07414957964017190872, -1.324282773101342459, 0.5611483367411455037 ) ) ;
#40049=CARTESIAN_POINT ( 'NONE',  ( 0.4819304095161658363, -1.265165726648666666, 0.7071056013453563827 ) ) ;
#40052=CARTESIAN_POINT ( 'NONE',  ( 0.5055437690763310288, -1.106959495255247505, 0.6108412925465283028 ) ) ;
#40058=CARTESIAN_POINT ( 'NONE',  ( 0.03564512600577746798, -0.5402024432579285440, 0.1944966300737278331 ) ) ;
#40060=CARTESIAN_POINT ( 'NONE',  ( 0.1754821060578101444, -0.7911127963077850822, -0.05965230147901675467 ) ) ;
#40063=ORIENTED_EDGE ( 'NONE', *, *, #2201, .T. ) ;
#40064=CARTESIAN_POINT ( 'NONE',  ( 0.4532541167939423410, -1.052918095400384502, 0.6353596524208835472 ) ) ;
#40065=CARTESIAN_POINT ( 'NONE',  ( 0.5530491884521703261, -1.511199273475291704, 0.5743520122765221059 ) ) ;
#40072=EDGE_CURVE ( 'NONE', #10513, #2583, #6093, .T. ) ;
#40074=ADVANCED_FACE ( 'NONE', ( #11564 ), #13797, .F. ) ;
#40076=DIRECTION ( 'NONE',  ( -0.7451425084519979203, 0.000000000000000000, -0.6669052722072786876 ) ) ;
#40077=CARTESIAN_POINT ( 'NONE',  ( 0.5698035129313328007, -1.613887348078733019, 0.3667417262808780887 ) ) ;
#40081=CARTESIAN_POINT ( 'NONE',  ( 0.4254375920900159702, -1.133939855871281654, 0.4364855428459707976 ) ) ;
#40086=CARTESIAN_POINT ( 'NONE',  ( 0.01185072000139549518, -0.5792930532549652733, -0.08974618506422621378 ) ) ;
#40088=CARTESIAN_POINT ( 'NONE',  ( 0.003526303896849130280, -0.4943637263100597035, 0.3555042333582821845 ) ) ;
#40091=ORIENTED_EDGE ( 'NONE', *, *, #27560, .T. ) ;
#40097=CARTESIAN_POINT ( 'NONE',  ( 0.002240231740626892794, -0.5288788276447421444, 0.1275514325127009851 ) ) ;
#40105=CARTESIAN_POINT ( 'NONE',  ( 0.002070590758578906478, -0.5820978177397124753, 0.3347319319685872485 ) ) ;
#40106=CARTESIAN_POINT ( 'NONE',  ( 0.4351293263873937667, -1.231514889939106849, 0.5832342842089121016 ) ) ;
#40107=CARTESIAN_POINT ( 'NONE',  ( 0.1519872515161661553, -1.248741164724253894, 0.6214439643266400637 ) ) ;
#40110=CARTESIAN_POINT ( 'NONE',  ( 0.4778170654558047126, -1.668016138613298560, 0.5682417262808788783 ) ) ;
#40111=VERTEX_POINT ( 'NONE', #29160 ) ;
#40113=CARTESIAN_POINT ( 'NONE',  ( 0.3289569715009816875, -1.175130748077982012, 0.5862253151572544008 ) ) ;
#40114=CARTESIAN_POINT ( 'NONE',  ( 0.3681699996139363162, -1.734736572097494323, 0.4293946410173364869 ) ) ;
#40116=EDGE_CURVE ( 'NONE', #13190, #37440, #35005, .T. ) ;
#40117=CARTESIAN_POINT ( 'NONE',  ( 0.5267604045959165537, -1.342330622345534685, 0.7955128641744203533 ) ) ;
#40118=CARTESIAN_POINT ( 'NONE',  ( 0.1871516419350925109, -0.7106192216159855635, 0.03078494767255909870 ) ) ;
#40120=CARTESIAN_POINT ( 'NONE',  ( 0.2435586465554056279, -1.522308288314433655, 0.8982978177552802812 ) ) ;
#40123=CARTESIAN_POINT ( 'NONE',  ( 0.2534765463136028352, -1.439939349519022693, 1.023019129304256758 ) ) ;
#40135=CARTESIAN_POINT ( 'NONE',  ( 0.1835387414513457993, -1.269102812158692473, 1.002600033288329140 ) ) ;
#40136=CARTESIAN_POINT ( 'NONE',  ( 0.09673638787972767272, -1.284069476777787822, 0.7393371349209389987 ) ) ;
#40138=CARTESIAN_POINT ( 'NONE',  ( 0.7188893830798498419, -1.468416639873279861, 0.6609592937859087858 ) ) ;
#40140=EDGE_CURVE ( 'NONE', #11376, #35222, #19101, .T. ) ;
#40141=CARTESIAN_POINT ( 'NONE',  ( 0.7063157497510277327, -1.525259356795145127, 0.5664836816230577332 ) ) ;
#40146=CARTESIAN_POINT ( 'NONE',  ( 0.2051436026844577765, -1.420721181919286646, 0.9359180069770434152 ) ) ;
#40148=CARTESIAN_POINT ( 'NONE',  ( 0.5887033537614668743, -1.489407499613006003, 0.6187394134856357697 ) ) ;
#40149=FACE_OUTER_BOUND ( 'NONE', #34398, .T. ) ;
#40150=EDGE_LOOP ( 'NONE', ( #844, #33737, #35507, #10605, #25804, #15383, #32763 ) ) ;
#40152=CARTESIAN_POINT ( 'NONE',  ( 0.1927699586607699855, -0.5931527414817471255, 0.2350819919684725701 ) ) ;
#40153=VERTEX_POINT ( 'NONE', #25275 ) ;
#40154=VERTEX_POINT ( 'NONE', #31640 ) ;
#40155=CARTESIAN_POINT ( 'NONE',  ( 0.3676236827432866061, -0.9197762930895730937, 0.7185230970922997784 ) ) ;
#40158=CARTESIAN_POINT ( 'NONE',  ( 0.3186313696869653711, -1.760405484422319367, 0.5654039123650882459 ) ) ;
#40163=CARTESIAN_POINT ( 'NONE',  ( 0.08755603795678691681, -0.7055197249887150690, 0.1887500319921082692 ) ) ;
#40164=CARTESIAN_POINT ( 'NONE',  ( 0.3100815786102045224, -1.704140726556199192, 0.8491805645699977978 ) ) ;
#40165=CARTESIAN_POINT ( 'NONE',  ( 0.1062697735069367821, -0.5760192370515179183, 0.2670765053398264643 ) ) ;
#40166=CARTESIAN_POINT ( 'NONE',  ( 0.3246612779430983475, -1.768063379345279795, 0.5167178742723262941 ) ) ;
#40167=CARTESIAN_POINT ( 'NONE',  ( 0.08016251834805442067, -1.309203902574839207, 0.5631135398343307674 ) ) ;
#40169=EDGE_LOOP ( 'NONE', ( #39506, #17461, #24979, #25778 ) ) ;
#40170=ORIENTED_EDGE ( 'NONE', *, *, #35400, .T. ) ;
#40172=CARTESIAN_POINT ( 'NONE',  ( 0.3467295405477267001, -1.741324348151121360, 0.4554588174254002308 ) ) ;
#40173=CARTESIAN_POINT ( 'NONE',  ( 0.6552418622445979057, -1.362413096819954594, 0.8455477964343599551 ) ) ;
#40178=CARTESIAN_POINT ( 'NONE',  ( 0.2719170612657579311, -1.671617796861691874, 0.5389836619028499642 ) ) ;
#40179=CARTESIAN_POINT ( 'NONE',  ( 0.3387784160096277142, -1.171947433235863700, 0.4559352600701537805 ) ) ;
#40180=CARTESIAN_POINT ( 'NONE',  ( 0.5367554652047751285, -1.159747519872984300, 0.6504567231333411303 ) ) ;
#40198=CARTESIAN_POINT ( 'NONE',  ( 0.04446389708692845971, -0.9676817186006311244, 0.6578482448476006272 ) ) ;
#40202=CARTESIAN_POINT ( 'NONE',  ( 0.1857430203655688061, -0.8056635886342108366, 0.2698372336795828996 ) ) ;
#40206=VECTOR ( 'NONE', #3068, 39.37007874015748143 ) ;
#40216=CARTESIAN_POINT ( 'NONE',  ( 0.4418554096259977859, -1.573809027168237229, 0.5761839767669477697 ) ) ;
#40218=CARTESIAN_POINT ( 'NONE',  ( 0.5911745308593184811, -1.601329302922394060, 0.4457227088930317827 ) ) ;
#40221=VERTEX_POINT ( 'NONE', #19900 ) ;
#40222=EDGE_CURVE ( 'NONE', #31015, #37794, #10877, .T. ) ;
#40223=CARTESIAN_POINT ( 'NONE',  ( 0.06444297064315794576, -0.8352831487901670737, 0.1457185332388703236 ) ) ;
#40225=CARTESIAN_POINT ( 'NONE',  ( 0.1237348556611498201, -0.5762697135983080310, 0.2583543961155602697 ) ) ;
#40226=CARTESIAN_POINT ( 'NONE',  ( 0.4325092394784135763, -1.691959258954059964, 0.4228211183897995218 ) ) ;
#40227=CARTESIAN_POINT ( 'NONE',  ( 0.5264113014007820723, -1.640729993778254014, 0.5682417262808777680 ) ) ;
#40228=ORIENTED_EDGE ( 'NONE', *, *, #39578, .F. ) ;
#40233=CARTESIAN_POINT ( 'NONE',  ( 0.6809224168725948045, -1.405736369044236378, 0.6042223006942389896 ) ) ;
#40236=DIRECTION ( 'NONE',  ( 0.4999551463232372317, -0.8660512985181135770, 0.000000000000000000 ) ) ;
#40240=CARTESIAN_POINT ( 'NONE',  ( 0.6038480862555802853, -1.597583055984439504, 0.5993263282456581242 ) ) ;
#40249=ADVANCED_FACE ( 'NONE', ( #22398 ), #18008, .F. ) ;
#40251=B_SPLINE_SURFACE_WITH_KNOTS ( 'NONE', 3, 3, ( 
 ( #22941, #10378, #10175, #3795, #20050, #13253, #25610 ),
 ( #35059, #38140, #28696, #23358, #9964, #38553, #13654 ),
 ( #16350, #955, #19445, #13466, #3984, #35457, #28886 ),
 ( #22744, #6868, #35669, #35272, #31981, #10568, #747 ),
 ( #26031, #7259, #7691, #7068, #7472, #19833, #25821 ),
 ( #32582, #19639, #31775, #16159, #29306, #1153, #26220 ),
 ( #38742, #4398, #16954, #26420, #29499, #1339, #38955 ) ),
 .UNSPECIFIED., .F., .F., .F.,
 ( 4, 1, 1, 1, 4 ),
 ( 4, 1, 1, 1, 4 ),
 ( 0.000000000000000000, 0.2500000000000000000, 0.5000000000000000000, 0.7500000000000000000, 1.000000000000000000 ),
 ( 0.000000000000000000, 0.05000000000000037748, 0.1666666666666666574, 0.5555555555555555802, 1.000000000000000000 ),
 .UNSPECIFIED. ) ;
#40256=CARTESIAN_POINT ( 'NONE',  ( 0.3267351042122170202, -1.764838374829281742, 0.4935885800319553263 ) ) ;
#40258=CARTESIAN_POINT ( 'NONE',  ( 0.5271251199429588530, -1.338340238819080819, 0.6479144337828351974 ) ) ;
#40261=CARTESIAN_POINT ( 'NONE',  ( 0.2392493758066867593, -0.9067917679836680067, 0.4646394045636887959 ) ) ;
#40262=ORIENTED_EDGE ( 'NONE', *, *, #26595, .T. ) ;
#40266=CARTESIAN_POINT ( 'NONE',  ( 0.009983477080391305741, -0.5455653694289525069, 0.07572401711799378599 ) ) ;
#40267=CARTESIAN_POINT ( 'NONE',  ( 0.03656494915825564407, -0.5581536149038067718, 0.2534570078657710224 ) ) ;
#40269=CARTESIAN_POINT ( 'NONE',  ( 0.1759098769117282413, -0.6728151866080555044, -0.08429024728173926950 ) ) ;
#40274=ORIENTED_EDGE ( 'NONE', *, *, #25629, .F. ) ;
#40275=CARTESIAN_POINT ( 'NONE',  ( 0.3144151427965208301, -1.049253354087126500, 0.6307772725301707961 ) ) ;
#40276=CARTESIAN_POINT ( 'NONE',  ( 0.5541385590046753462, -1.509386730049579572, 0.6214236857019725946 ) ) ;
#40285=DIRECTION ( 'NONE',  ( 0.8660512985181133550, 0.4999551463232373982, 0.000000000000000000 ) ) ;
#40286=CARTESIAN_POINT ( 'NONE',  ( 0.3912168351225406848, -1.712565751828606153, 0.4687417262808791230 ) ) ;
#40290=CARTESIAN_POINT ( 'NONE',  ( 0.08096179802327445330, -1.367098532309424685, 0.5880770290185818316 ) ) ;
#40292=CARTESIAN_POINT ( 'NONE',  ( 0.4561653094204668468, -1.131358138958592718, 0.4538444256416698241 ) ) ;
#40293=CARTESIAN_POINT ( 'NONE',  ( 0.4670621156540841756, -1.236494891586305211, 0.6057417262809811076 ) ) ;
#40295=CARTESIAN_POINT ( 'NONE',  ( 0.01926973937230214845, -1.027504089262102349, 0.6199911605063174180 ) ) ;
#40296=CARTESIAN_POINT ( 'NONE',  ( 0.3369441150334460677, -1.754019818956965127, 0.4603468005407844177 ) ) ;
#40298=CARTESIAN_POINT ( 'NONE',  ( 0.3161418316428721287, -1.757545499489290286, 0.4995718330220786374 ) ) ;
#40299=B_SPLINE_CURVE_WITH_KNOTS ( 'NONE', 3,
 ( #19524, #29778, #20133, #4466, #17226, #10446, #16418, #823, #39243, #7335, #23625, #32661, #38426, #13546, #4273, #13334, #38818, #26293, #10647, #10267, #22830, #29383, #23438, #35349, #1037, #35532, #23222, #35747, #3865, #7559, #29573, #7761, #7141, #1619 ),
 .UNSPECIFIED., .F., .F.,
 ( 4, 2, 2, 2, 2, 2, 2, 2, 2, 2, 2, 2, 2, 2, 2, 2, 4 ),
 ( 0.001574216056284313391, 0.002349730643885267114, 0.003125245231486220836, 0.003900759819087174559, 0.004676274406688128715, 0.005451788994289081570, 0.006227303581890041365, 0.007002818169491000291, 0.007778332757091959218, 0.008553847344692918145, 0.009329361932293877072, 0.01010487651989483773, 0.01088039110749579666, 0.01165590569509675559, 0.01243142028269771451, 0.01320693487029867517, 0.01398244945789963410 ),
 .UNSPECIFIED. ) ;
#40300=CARTESIAN_POINT ( 'NONE',  ( 0.3827388732655720438, -1.608087253622227042, 0.5083331137473884320 ) ) ;
#40313=CARTESIAN_POINT ( 'NONE',  ( 0.001331136673900325858, -0.5599312581362586583, 0.03624264176424291106 ) ) ;
#40320=CARTESIAN_POINT ( 'NONE',  ( 0.005043818368537927865, -0.6038779608865681992, 0.3826815526081347452 ) ) ;
#40321=CARTESIAN_POINT ( 'NONE',  ( 0.1021712152378831950, -0.8583302296959987032, 0.4405693860677040719 ) ) ;
#40322=CARTESIAN_POINT ( 'NONE',  ( 0.09680642637387373850, -1.309618686966848466, 0.5813006354277100440 ) ) ;
#40330=CARTESIAN_POINT ( 'NONE',  ( 0.2258291083026367774, -0.8976967229642250912, 0.6721174698541964032 ) ) ;
#40331=ADVANCED_FACE ( 'NONE', ( #8972 ), #5140, .T. ) ;
#40339=CARTESIAN_POINT ( 'NONE',  ( 0.5698035129313328007, -1.613887348078733019, 0.3667417262808780887 ) ) ;
#40344=CARTESIAN_POINT ( 'NONE',  ( 0.02242113575389428556, -0.7151737931810984161, 0.5646644402375310401 ) ) ;
#40347=CARTESIAN_POINT ( 'NONE',  ( 0.06590158485999333959, -1.101506299248170118, 0.7509233284053542512 ) ) ;
#40349=CARTESIAN_POINT ( 'NONE',  ( 0.5877184641988779656, -1.252861897328551022, 0.8491679911058225283 ) ) ;
#40351=CARTESIAN_POINT ( 'NONE',  ( 0.6834792670387838109, -1.548921872613369777, 0.5978341875930145433 ) ) ;
#40356=VERTEX_POINT ( 'NONE', #28110 ) ;
#40358=CARTESIAN_POINT ( 'NONE',  ( 0.2492448580361798227, -1.564264300073486602, 0.8870779812646237827 ) ) ;
#40361=CARTESIAN_POINT ( 'NONE',  ( 0.5881849326769416075, -1.491250579143394317, 0.5780151184862688529 ) ) ;
#40366=CARTESIAN_POINT ( 'NONE',  ( 0.5530797604979859061, -1.185210387710321944, 0.6074893116751658440 ) ) ;
#40378=CARTESIAN_POINT ( 'NONE',  ( 0.09783940332773917448, -0.7228957342152418919, 0.3200629931280229434 ) ) ;
#40380=B_SPLINE_CURVE_WITH_KNOTS ( 'NONE', 3,
 ( #2365, #33832, #18188, #6244 ),
 .UNSPECIFIED., .F., .F.,
 ( 4, 4 ),
 ( 2.016909803241189850E-16, 0.0003300623014047657277 ),
 .UNSPECIFIED. ) ;
#40382=CARTESIAN_POINT ( 'NONE',  ( 0.1397249117745774649, -0.7016623770517458336, 0.5057382675813436590 ) ) ;
#40386=CARTESIAN_POINT ( 'NONE',  ( 0.05670245286071558255, -1.312040770489931729, 0.6142165760128855956 ) ) ;
#40388=CARTESIAN_POINT ( 'NONE',  ( 0.4611826087952243247, -1.678346039424960523, 0.5931467301849101537 ) ) ;
#40389=CARTESIAN_POINT ( 'NONE',  ( 0.4821892592075923134, -1.087465116796244802, 0.8049660430408165368 ) ) ;
#40397=CARTESIAN_POINT ( 'NONE',  ( 0.3088330115105235030, -1.189194436044654912, 0.5067259279166422825 ) ) ;
#40398=CARTESIAN_POINT ( 'NONE',  ( 0.4714567382560805875, -1.076664716445512093, 0.6912835816774075548 ) ) ;
#40411=CARTESIAN_POINT ( 'NONE',  ( 0.08978320868449755909, -0.5653313875429684110, 0.1301661300597059812 ) ) ;
#40414=CARTESIAN_POINT ( 'NONE',  ( -0.01435986368806844819, -0.8524412751134723409, 0.2543499331468145330 ) ) ;
#40419=FACE_OUTER_BOUND ( 'NONE', #34925, .T. ) ;
#40428=CARTESIAN_POINT ( 'NONE',  ( 0.08031759231403769184, -1.309115413162167396, 0.5634110904151367061 ) ) ;
#40431=CARTESIAN_POINT ( 'NONE',  ( 0.09166549204113492999, -0.6531214586304496805, 0.4451350988387396401 ) ) ;
#40433=CARTESIAN_POINT ( 'NONE',  ( 0.1876095839365585771, -1.270310460104812744, 0.4282417262808775882 ) ) ;
#40434=CARTESIAN_POINT ( 'NONE',  ( 0.5534895568977906688, -1.623564024766104508, 0.5247869855815567863 ) ) ;
#40443=CARTESIAN_POINT ( 'NONE',  ( 0.5736464802932748075, -1.499188840390029975, 0.5681326666576531625 ) ) ;
#40445=CARTESIAN_POINT ( 'NONE',  ( 0.4776203807509608046, -1.679318457215359883, 0.5575138488100176426 ) ) ;
#40450=CARTESIAN_POINT ( 'NONE',  ( 0.1840567930975518796, -0.8547793429265486687, 0.1477568935609660794 ) ) ;
#40451=CARTESIAN_POINT ( 'NONE',  ( 0.3560095073596968307, -0.8726986411092064744, 0.7484988241699506162 ) ) ;
#40454=VECTOR ( 'NONE', #21707, 39.37007874015748143 ) ;
#40459=CARTESIAN_POINT ( 'NONE',  ( 0.3993723638686003108, -1.146829347344676453, 0.4244434305191919776 ) ) ;
#40465=CARTESIAN_POINT ( 'NONE',  ( 0.6589248908660086945, -1.495897505468516853, 0.4182417262808776903 ) ) ;
#40473=CARTESIAN_POINT ( 'NONE',  ( 0.3327923242355236289, -1.761774052064265295, 0.4761320618463714127 ) ) ;
#40475=CARTESIAN_POINT ( 'NONE',  ( 0.5035873862616617735, -1.298196369232728076, 0.6491550123535173578 ) ) ;
#40478=CARTESIAN_POINT ( 'NONE',  ( 0.2117717001728993131, -0.8880493388543053701, 0.3804667941236127282 ) ) ;
#40481=CARTESIAN_POINT ( 'NONE',  ( 0.1041180756838251814, -1.398163384010766785, 0.6248096187470618679 ) ) ;
#40484=CARTESIAN_POINT ( 'NONE',  ( 0.04822329218285972136, -0.5481102735168966733, 0.2156808200189340163 ) ) ;
#40486=CARTESIAN_POINT ( 'NONE',  ( 0.1121164433129688554, -0.8360957577110439409, -0.04471693353407518723 ) ) ;
#40487=PLANE ( 'NONE',  #2412 ) ;
#40491=CARTESIAN_POINT ( 'NONE',  ( 0.3927997951677614785, -1.109372561784171873, 0.6250621135928259298 ) ) ;
#40492=CARTESIAN_POINT ( 'NONE',  ( 0.5532976880032102196, -1.511228520888749927, 0.5786546175993648733 ) ) ;
#40500=CARTESIAN_POINT ( 'NONE',  ( 0.3538719729184750529, -1.624715450675502826, 0.4182417262808776903 ) ) ;
#40501=CARTESIAN_POINT ( 'NONE',  ( 0.4790130493689879199, -1.660633143797948241, 0.5197417262808792238 ) ) ;
#40504=CARTESIAN_POINT ( 'NONE',  ( 0.07539036843641495900, -1.329185100875404313, 0.6514330093269139477 ) ) ;
#40507=CARTESIAN_POINT ( 'NONE',  ( 0.2098534808732534784, -0.9273921219866952947, 0.3620977009047463002 ) ) ;
#40508=CARTESIAN_POINT ( 'NONE',  ( 0.4726093400148664303, -1.113121474480951889, 0.5480980819454659425 ) ) ;
#40509=CARTESIAN_POINT ( 'NONE',  ( 0.5594238137014129197, -1.182849275086621521, 0.6057417262809816627 ) ) ;
#40511=CARTESIAN_POINT ( 'NONE',  ( 0.004566372195762857279, -0.8656213538948328567, 0.4622093217984943880 ) ) ;
#40513=CARTESIAN_POINT ( 'NONE',  ( 0.6928668329258086400, -1.429029060959297937, 0.5420566053040769550 ) ) ;
#40514=AXIS2_PLACEMENT_3D ( 'NONE', #14863, #27424, #7671 ) ;
#40519=ORIENTED_EDGE ( 'NONE', *, *, #27792, .T. ) ;
#40523=CARTESIAN_POINT ( 'NONE',  ( 0.5969700620808515712, -1.458905189709731154, 0.6310679806792612867 ) ) ;
#40524=CARTESIAN_POINT ( 'NONE',  ( 0.6054889487767985967, -1.479703267939684874, 0.5856070495615782745 ) ) ;
#40530=CARTESIAN_POINT ( 'NONE',  ( 0.1847070558194194301, -1.276978442851412154, 0.9301116397864819252 ) ) ;
#40531=CARTESIAN_POINT ( 'NONE',  ( 0.3416240168993061044, -1.109164787499526961, 0.7393468023686904367 ) ) ;
#40533=CARTESIAN_POINT ( 'NONE',  ( 0.3663975874019590462, -1.157438136726378408, 0.4269148889825721827 ) ) ;
#40540=CARTESIAN_POINT ( 'NONE',  ( 0.2098138332575895104, -0.8876503706691467599, 0.7004616250147996936 ) ) ;
#40541=CARTESIAN_POINT ( 'NONE',  ( 0.1383678021865805130, -0.8347292794016092365, 0.3450883820417707804 ) ) ;
#40546=CARTESIAN_POINT ( 'NONE',  ( 0.4168539117269804417, -1.242125193379584935, 0.5412798315864792986 ) ) ;
#40548=CARTESIAN_POINT ( 'NONE',  ( 0.3476487115878558187, -1.071941005786004819, 0.7622982368131399067 ) ) ;
#40552=CARTESIAN_POINT ( 'NONE',  ( 0.03506116283237684095, -0.6633195576212149724, 0.6677130251333698308 ) ) ;
#40553=CARTESIAN_POINT ( 'NONE',  ( 0.05525033686093953900, -1.048202366712872147, 0.7271762683524501947 ) ) ;
#40555=CARTESIAN_POINT ( 'NONE',  ( 0.6859459673519229250, -1.411154268469613227, 0.7682993476293730195 ) ) ;
#40556=CARTESIAN_POINT ( 'NONE',  ( 0.3222894045021684195, -1.758215778056678724, 0.5682417262808792113 ) ) ;
#40564=CARTESIAN_POINT ( 'NONE',  ( 0.2128671618955360612, -1.417862351214104200, 0.9322687174078309047 ) ) ;
#40565=CARTESIAN_POINT ( 'NONE',  ( 0.4825082729884774269, -1.333409512969114141, 0.8153832532642322217 ) ) ;
#40568=CARTESIAN_POINT ( 'NONE',  ( 0.2495280903959155583, -0.7823963870098056272, 0.5160991521645093005 ) ) ;
#40570=ORIENTED_EDGE ( 'NONE', *, *, #10752, .F. ) ;
#40571=DIRECTION ( 'NONE',  ( 0.4999551463232372317, -0.8660512985181134660, -6.869252350113302335E-17 ) ) ;
#40577=CARTESIAN_POINT ( 'NONE',  ( 0.1281083501185726337, -0.8152981500214998567, 0.4630848436273822810 ) ) ;
#40579=CARTESIAN_POINT ( 'NONE',  ( 0.3164777849907467466, -1.747345822248904668, 0.7454006856945649684 ) ) ;
#40580=CARTESIAN_POINT ( 'NONE',  ( 0.5043263792969816528, -1.486040407161054233, 0.7488984814174186599 ) ) ;
#40584=CARTESIAN_POINT ( 'NONE',  ( 0.4439201956396305326, -1.688295707146957758, 0.5959241158817605299 ) ) ;
#40585=CARTESIAN_POINT ( 'NONE',  ( 0.7052107660210322759, -1.443684245437774294, 0.7850599799250342903 ) ) ;
#40597=CARTESIAN_POINT ( 'NONE',  ( 0.4100600194349330319, -1.011029760475403494, 0.6817144834752139060 ) ) ;
#40602=CARTESIAN_POINT ( 'NONE',  ( 0.3959951078739687436, -1.707197240620605738, 0.4182417262808776903 ) ) ;
#40612=CARTESIAN_POINT ( 'NONE',  ( 0.1363060833980020425, -1.291389234375735384, 0.7246493219598814095 ) ) ;
#40613=ORIENTED_EDGE ( 'NONE', *, *, #3635, .F. ) ;
#40618=CARTESIAN_POINT ( 'NONE',  ( 0.3539619486986738672, -1.095399617261031411, 0.7051293634830863022 ) ) ;
#40620=CARTESIAN_POINT ( 'NONE',  ( 0.01220508677664999299, -0.4284039737085656996, 0.1457185332388702959 ) ) ;
#40623=CARTESIAN_POINT ( 'NONE',  ( 0.08996436532983868861, -0.5633779834408316756, 0.1624145888708820040 ) ) ;
#40624=ORIENTED_EDGE ( 'NONE', *, *, #12408, .T. ) ;
#40627=CARTESIAN_POINT ( 'NONE',  ( 0.4415431555067652059, -1.573721655358518268, 0.5715020639883481302 ) ) ;
#40634=CARTESIAN_POINT ( 'NONE',  ( 0.1253475045672584887, -0.5634446532171664135, 0.2188656290601465049 ) ) ;
#40635=CARTESIAN_POINT ( 'NONE',  ( 0.4798443520715884869, -1.677655393100440318, 0.5509470553349121724 ) ) ;
#40638=DIRECTION ( 'NONE',  ( 0.9998941247116546194, -0.01455087607601020412, 0.0001066420868422379362 ) ) ;
#40639=CARTESIAN_POINT ( 'NONE',  ( 0.2316897038216818305, -1.233203694889816404, 0.5465952261361649578 ) ) ;
#40641=CARTESIAN_POINT ( 'NONE',  ( 0.2114942970145866630, -1.236211323811057694, 0.5631196975457352094 ) ) ;
#40644=CARTESIAN_POINT ( 'NONE',  ( 0.6775446752225827707, -1.407456786189307696, 0.5068639979343774193 ) ) ;
#40646=CARTESIAN_POINT ( 'NONE',  ( 0.02238204800581933274, -1.092291325666332469, 0.6350144242741103673 ) ) ;
#40667=COLOUR_RGB('Dark Blue',0.08,0.2,0.34);
#40668=FILL_AREA_STYLE_COLOUR('',#40667);
#40669=FILL_AREA_STYLE('',(#40668));
#40670=SURFACE_STYLE_FILL_AREA(#40669);
#40671=SURFACE_SIDE_STYLE('',(#40670));
#40672=SURFACE_STYLE_USAGE(.BOTH.,#40671);
#40673=PRESENTATION_STYLE_ASSIGNMENT((#40672));
#40717=STYLED_ITEM('',(#40673),#18583);
#40721=MECHANICAL_DESIGN_GEOMETRIC_PRESENTATION_REPRESENTATION('',(#40717),#11399);
ENDSEC;
END-ISO-10303-21;
